ISO-10303-21;
HEADER;
FILE_DESCRIPTION (('STEP AP214'),
    '1' );
FILE_NAME ('Height Adjustment Lead Screw.step',
    '2026-10-09T12:05:53',
    ( '' ),
    ( '' ),
    'SwSTEP 2.0',
    'SolidWorks 2026',
    '' );
FILE_SCHEMA (( 'AUTOMOTIVE_DESIGN' ));
ENDSEC;

DATA;
#1=CARTESIAN_POINT ( 'NONE',  ( 24.04473007462266310, -15.61618926727986789, -75.50766188105974663 ) ) ;
#12=CARTESIAN_POINT ( 'NONE',  ( 9.221498779823216196, -11.63191302842313313, -56.67433499279778175 ) ) ;
#15=CARTESIAN_POINT ( 'NONE',  ( 20.62196618598149911, -8.699519395578539260, -73.47554475576539801 ) ) ;
#16=CYLINDRICAL_SURFACE ( 'NONE', #33863, 6.766999999999998572 ) ;
#22=CARTESIAN_POINT ( 'NONE',  ( 9.962852259819479528, -19.79044361182920042, -65.04335028194189761 ) ) ;
#26=CARTESIAN_POINT ( 'NONE',  ( 9.625247127302518635, -19.52582424083449908, -32.14999999999999858 ) ) ;
#31=CARTESIAN_POINT ( 'NONE',  ( 11.75558472888330108, -8.629576846066969509, -76.82947711988130379 ) ) ;
#42=CARTESIAN_POINT ( 'NONE',  ( 20.99557441488136078, -21.94238693200700041, -72.08401915777523072 ) ) ;
#44=CARTESIAN_POINT ( 'NONE',  ( 22.19687809394159927, -11.28635708649630054, -78.03525497637551211 ) ) ;
#50=ORIENTED_EDGE ( 'NONE', *, *, #39346, .T. ) ;
#54=CARTESIAN_POINT ( 'NONE',  ( 22.50468263344456687, -12.72456034819510151, -68.71118389017816241 ) ) ;
#56=CARTESIAN_POINT ( 'NONE',  ( 10.72262792443331492, -19.77487285394900951, -71.24448753608163543 ) ) ;
#63=CARTESIAN_POINT ( 'NONE',  ( 22.90087412606865058, -16.66897304226082710, -40.89671642115739303 ) ) ;
#65=ORIENTED_EDGE ( 'NONE', *, *, #51526, .T. ) ;
#66=ORIENTED_EDGE ( 'NONE', *, *, #10007, .T. ) ;
#67=LINE ( 'NONE', #19711, #13704 ) ;
#68=CARTESIAN_POINT ( 'NONE',  ( 22.04686178097117732, -19.02415631444728561, -58.61948664697574429 ) ) ;
#70=CARTESIAN_POINT ( 'NONE',  ( 14.06316349757885042, -7.911113466102105640, -58.92429889998866344 ) ) ;
#75=CARTESIAN_POINT ( 'NONE',  ( 23.84711268294356046, -17.41670964262949894, -65.58063247732249579 ) ) ;
#77=CARTESIAN_POINT ( 'NONE',  ( 21.74894416331870062, -9.578439440273777805, -43.53078881371720144 ) ) ;
#82=CARTESIAN_POINT ( 'NONE',  ( 9.221484299827681141, -19.60044010530257097, -42.62566474563559638 ) ) ;
#83=CARTESIAN_POINT ( 'NONE',  ( 9.878977750625089982, -11.56869915257929904, -35.41547006414829468 ) ) ;
#91=CARTESIAN_POINT ( 'NONE',  ( 8.278517517462621100, -18.12120375785029935, -46.40940759145149741 ) ) ;
#92=ORIENTED_EDGE ( 'NONE', *, *, #43426, .F. ) ;
#95=CARTESIAN_POINT ( 'NONE',  ( 19.30039974071021902, -22.89444622034352861, -39.87698757616706757 ) ) ;
#97=CARTESIAN_POINT ( 'NONE',  ( 22.90093739844393284, -15.61845303799943174, -56.45293168557734020 ) ) ;
#101=CARTESIAN_POINT ( 'NONE',  ( 18.20467283260814639, -23.32127324669528434, -38.20900000048465017 ) ) ;
#106=CARTESIAN_POINT ( 'NONE',  ( 22.72481333909230017, -17.38742284364922597, -64.53615558299642885 ) ) ;
#109=CARTESIAN_POINT ( 'NONE',  ( 9.221334957865163773, -11.63219308205320957, -74.95902792597172493 ) ) ;
#111=CARTESIAN_POINT ( 'NONE',  ( 12.72590726626352975, -21.52907858405782449, -63.11948344771946040 ) ) ;
#118=CARTESIAN_POINT ( 'NONE',  ( 11.66207609259309841, -9.394545466821320190, -81.23899999999999011 ) ) ;
#124=CARTESIAN_POINT ( 'NONE',  ( 23.50285504017600147, -13.84387210050659966, -81.23899999999999011 ) ) ;
#133=ORIENTED_EDGE ( 'NONE', *, *, #22274, .F. ) ;
#137=CARTESIAN_POINT ( 'NONE',  ( 22.18886536826886768, -12.48613193644987263, -40.30080353194567522 ) ) ;
#142=CARTESIAN_POINT ( 'NONE',  ( 23.87684719361660157, -16.89450661858629843, -59.33958724536129381 ) ) ;
#157=EDGE_CURVE ( 'NONE', #32127, #27118, #5412, .T. ) ;
#160=CARTESIAN_POINT ( 'NONE',  ( 20.11809687624943521, -22.52869528883066153, -54.12566693902919468 ) ) ;
#162=CARTESIAN_POINT ( 'NONE',  ( 8.696784336233250201, -15.17409326420679960, -34.08624212660659936 ) ) ;
#174=ORIENTED_EDGE ( 'NONE', *, *, #31789, .F. ) ;
#177=LINE ( 'NONE', #11984, #16918 ) ;
#183=CARTESIAN_POINT ( 'NONE',  ( 18.20454837585587526, -23.32130853119455693, -55.92427167932272170 ) ) ;
#189=CARTESIAN_POINT ( 'NONE',  ( 9.367050196127319595, -15.61601677469269944, -55.84717978380999881 ) ) ;
#197=CARTESIAN_POINT ( 'NONE',  ( 18.24071347613679706, -23.17583458100989802, -56.42598068654729104 ) ) ;
#204=CARTESIAN_POINT ( 'NONE',  ( 12.63580666350229897, -21.74037383255939915, -53.51237412773319591 ) ) ;
#205=ORIENTED_EDGE ( 'NONE', *, *, #35909, .F. ) ;
#209=CARTESIAN_POINT ( 'NONE',  ( 9.807775352051226747, -10.75450683567505550, -36.71600244428209692 ) ) ;
#211=CARTESIAN_POINT ( 'NONE',  ( 24.04447781939626338, -15.52406317847051120, -55.50396621545129250 ) ) ;
#212=CARTESIAN_POINT ( 'NONE',  ( 10.72251451727398397, -11.45765055134171284, -75.66113898378057456 ) ) ;
#228=CARTESIAN_POINT ( 'NONE',  ( 18.41697451332290214, -22.28929168817850126, -66.84789180586540169 ) ) ;
#234=CARTESIAN_POINT ( 'NONE',  ( 15.51400525636760008, -23.43938728828090134, -43.81267675689189645 ) ) ;
#243=CARTESIAN_POINT ( 'NONE',  ( 24.04493741881096014, -14.58063984321919015, -75.46599062978197026 ) ) ;
#248=CARTESIAN_POINT ( 'NONE',  ( 24.04493739085331683, -15.62301657200399418, -43.79259974408412859 ) ) ;
#250=CARTESIAN_POINT ( 'NONE',  ( 22.88637251419359941, -11.47525136018554370, -49.33255534741104498 ) ) ;
#253=CARTESIAN_POINT ( 'NONE',  ( 23.83903514183533190, -17.68687693202930333, -35.59099905439017419 ) ) ;
#256=CARTESIAN_POINT ( 'NONE',  ( 22.51916824768339609, -10.39972011525970075, -71.57429041023848981 ) ) ;
#262=CARTESIAN_POINT ( 'NONE',  ( 13.95200227718980024, -8.492576593136959673, -69.63804828363188903 ) ) ;
#271=EDGE_CURVE ( 'NONE', #20377, #35517, #9367, .T. ) ;
#274=CARTESIAN_POINT ( 'NONE',  ( 23.75374426366189695, -12.46638513581170038, -69.38289759990109928 ) ) ;
#277=CARTESIAN_POINT ( 'NONE',  ( 16.13393739769620083, -15.61618894467929941, -28.45282021618999835 ) ) ;
#278=DIRECTION ( 'NONE',  ( 0.000000000000000000, 0.000000000000000000, -1.000000000000000000 ) ) ;
#281=CARTESIAN_POINT ( 'NONE',  ( 12.14986981628316620, -8.703629658544938863, -78.84100245546133579 ) ) ;
#288=CARTESIAN_POINT ( 'NONE',  ( 10.21452801543910027, -20.14026745531459994, -75.02493559595789918 ) ) ;
#295=AXIS2_PLACEMENT_3D ( 'NONE', #26378, #18789, #37943 ) ;
#296=DIRECTION ( 'NONE',  ( 0.000000000000000000, 0.000000000000000000, 1.000000000000000000 ) ) ;
#311=CARTESIAN_POINT ( 'NONE',  ( 22.90093739248998972, -16.50198092149558349, -58.49448661159359375 ) ) ;
#317=CARTESIAN_POINT ( 'NONE',  ( 10.20899662427918564, -12.23061640146900686, -71.61833297012245225 ) ) ;
#318=CARTESIAN_POINT ( 'NONE',  ( 23.83903770539513900, -13.54551362709085538, -35.42433238772350279 ) ) ;
#319=CARTESIAN_POINT ( 'NONE',  ( 17.19215044318390184, -7.439214858484909598, -47.33329750477089704 ) ) ;
#320=CIRCLE ( 'NONE', #22077, 7.910999999999997812 ) ;
#321=CARTESIAN_POINT ( 'NONE',  ( 8.428846698934018278, -17.68690243860981681, -68.42433492461131550 ) ) ;
#323=SHAPE_REPRESENTATION_RELATIONSHIP ( 'NONE' , 'NONE' ,  #19070, #24050 ) ;
#326=CARTESIAN_POINT ( 'NONE',  ( 21.51457940895319965, -10.46299709236900100, -33.98952930500309577 ) ) ;
#334=DIRECTION ( 'NONE',  ( 1.000000000000000000, 0.000000000000000000, 0.000000000000000000 ) ) ;
#335=CARTESIAN_POINT ( 'NONE',  ( 8.883252294883678957, -19.54178268943019958, -44.34971538379739542 ) ) ;
#345=CARTESIAN_POINT ( 'NONE',  ( 21.54530417723247737, -19.77479742635252080, -48.66115513169237516 ) ) ;
#350=DIRECTION ( 'NONE',  ( 1.000000000000000000, 2.460964292799963328E-14, 0.000000000000000000 ) ) ;
#353=CARTESIAN_POINT ( 'NONE',  ( 16.13393739769620083, -15.61618894467929941, -22.14999999999999858 ) ) ;
#355=CYLINDRICAL_SURFACE ( 'NONE', #16437, 7.910999999999997812 ) ;
#360=CARTESIAN_POINT ( 'NONE',  ( 22.46012642958591599, -10.75454366414201246, -73.29933459694514397 ) ) ;
#363=FACE_OUTER_BOUND ( 'NONE', #31062, .T. ) ;
#365=CARTESIAN_POINT ( 'NONE',  ( 22.90093635944459649, -15.62053987609991701, -34.45302314068787553 ) ) ;
#366=CARTESIAN_POINT ( 'NONE',  ( 11.41959527949359909, -9.607686208987979981, -81.23899999999999011 ) ) ;
#367=VERTEX_POINT ( 'NONE', #1612 ) ;
#370=ORIENTED_EDGE ( 'NONE', *, *, #29740, .F. ) ;
#374=CARTESIAN_POINT ( 'NONE',  ( 9.807832152388833435, -10.75443395529458535, -62.71600216802090699 ) ) ;
#379=ORIENTED_EDGE ( 'NONE', *, *, #9836, .T. ) ;
#394=CARTESIAN_POINT ( 'NONE',  ( 10.01583490929099973, -20.53102059231009946, -58.07208434834350186 ) ) ;
#409=CARTESIAN_POINT ( 'NONE',  ( 16.13393739769620083, -15.61618894467929941, -23.15000000000000213 ) ) ;
#411=CARTESIAN_POINT ( 'NONE',  ( 19.99250983278150073, -9.242954828350208984, -40.74063233595069988 ) ) ;
#427=B_SPLINE_CURVE_WITH_KNOTS ( 'NONE', 3,
 ( #29954, #1422, #45970, #5870, #21837, #29447, #49652, #1939, #10063, #37844, #38104, #33890, #29696, #26023, #9030, #1680, #49901, #42035, #13995, #40993, #6136, #49137, #13234, #22092, #25758, #34143, #2201, #28925, #37572, #13489, #17407, #41510, #24977, #9299, #5107 ),
 .UNSPECIFIED., .F., .F.,
 ( 4, 2, 2, 2, 2, 2, 2, 2, 2, 2, 2, 2, 2, 1, 1, 1, 1, 1, 2, 4 ),
 ( 0.000000000000000000, 0.03125022957391215134, 0.06250045914782430267, 0.09375068872173646095, 0.1250009182956486053, 0.1562511478695607636, 0.1875013774434729219, 0.2500018365912970997, 0.3125022957391213607, 0.3750027548869455107, 0.4375032140347697718, 0.4687534436086817080, 0.4843785583956377039, 0.4921911157891156186, 0.4960973944858545481, 0.4980505338342237631, 0.4990271035084085649, 0.4995153883455007993, 0.4997595307640467777, 0.5000036731825925340 ),
 .UNSPECIFIED. ) ;
#430=CARTESIAN_POINT ( 'NONE',  ( 8.428856344205472695, -13.54544038257251160, -78.87566503557303577 ) ) ;
#436=CARTESIAN_POINT ( 'NONE',  ( 22.14946380439831941, -18.71488146266838370, -32.99858898373786076 ) ) ;
#438=CARTESIAN_POINT ( 'NONE',  ( 20.29260916630788714, -10.20487065087579026, -36.16115160781710358 ) ) ;
#439=CARTESIAN_POINT ( 'NONE',  ( 24.04493740220357978, -15.60985432249296423, -59.79207070245149680 ) ) ;
#445=CARTESIAN_POINT ( 'NONE',  ( 19.92217479402680169, -8.743343462593710314, -51.67284482273019819 ) ) ;
#455=CARTESIAN_POINT ( 'NONE',  ( 9.307192117435908685, -13.84471835421079966, -51.92799550646089557 ) ) ;
#464=CARTESIAN_POINT ( 'NONE',  ( 24.02795760665879854, -15.08725952809635373, -55.48638191674730535 ) ) ;
#479=CARTESIAN_POINT ( 'NONE',  ( 22.10083642963680006, -11.85604604323910038, -68.27383256501039455 ) ) ;
#492=AXIS2_PLACEMENT_3D ( 'NONE', #43225, #42968, #30365 ) ;
#497=CARTESIAN_POINT ( 'NONE',  ( 15.09837707772988225, -23.52718739147557869, -60.04936120705558977 ) ) ;
#506=CARTESIAN_POINT ( 'NONE',  ( 8.766479793714031743, -11.91439363571640087, -70.94053896172950147 ) ) ;
#514=CARTESIAN_POINT ( 'NONE',  ( 23.21317868976809606, -13.29432836881139934, -60.13177655599749727 ) ) ;
#525=CARTESIAN_POINT ( 'NONE',  ( 19.12205772217659927, -7.931538163062599622, -71.12571408330079237 ) ) ;
#531=ADVANCED_FACE ( 'NONE', ( #39580 ), #38821, .T. ) ;
#533=ORIENTED_EDGE ( 'NONE', *, *, #7118, .T. ) ;
#539=CARTESIAN_POINT ( 'NONE',  ( 19.49523065122039966, -9.415844892879128736, -36.11094655318100166 ) ) ;
#545=ORIENTED_EDGE ( 'NONE', *, *, #34037, .F. ) ;
#547=CARTESIAN_POINT ( 'NONE',  ( 22.90007318524572000, -14.73211321227309512, -68.80558412982628624 ) ) ;
#555=CARTESIAN_POINT ( 'NONE',  ( 9.221329868776839689, -19.60017621584825775, -72.34096665405537863 ) ) ;
#567=CARTESIAN_POINT ( 'NONE',  ( 9.366937397696199596, -15.61618894467949836, -28.45282021618999835 ) ) ;
#570=CARTESIAN_POINT ( 'NONE',  ( 20.11810930412978138, -8.703690030208671047, -35.17433314337063877 ) ) ;
#571=CARTESIAN_POINT ( 'NONE',  ( 9.848987560566159871, -10.27932417210969973, -47.01642178051639576 ) ) ;
#572=CARTESIAN_POINT ( 'NONE',  ( 22.46010534431878369, -20.47786315848903271, -67.71599960382185657 ) ) ;
#575=EDGE_CURVE ( 'NONE', #14719, #11008, #2482, .T. ) ;
#576=CARTESIAN_POINT ( 'NONE',  ( 18.20469237649928118, -23.32126772162391148, -42.20899783913211678 ) ) ;
#577=CARTESIAN_POINT ( 'NONE',  ( 9.430654476343230286, -12.36462134097749832, -39.37641661732919829 ) ) ;
#585=CARTESIAN_POINT ( 'NONE',  ( 16.51850286063059770, -7.379998677711620658, -41.02252027912539489 ) ) ;
#586=VERTEX_POINT ( 'NONE', #35117 ) ;
#590=CARTESIAN_POINT ( 'NONE',  ( 14.06336117282463150, -23.32131560580253193, -64.37566576587414602 ) ) ;
#593=ORIENTED_EDGE ( 'NONE', *, *, #39989, .T. ) ;
#602=CARTESIAN_POINT ( 'NONE',  ( 20.11808726905815803, -8.703676856905904202, -61.45899610695946791 ) ) ;
#609=CARTESIAN_POINT ( 'NONE',  ( 10.26456537522289914, -19.52689034815859870, -81.26573725944388116 ) ) ;
#610=CARTESIAN_POINT ( 'NONE',  ( 9.366948553292196777, -14.73030905516724509, -47.49448696612870435 ) ) ;
#612=FACE_BOUND ( 'NONE', #38097, .T. ) ;
#615=ADVANCED_FACE ( 'NONE', ( #51634 ), #29332, .F. ) ;
#616=CARTESIAN_POINT ( 'NONE',  ( 13.72573378235179931, -8.165455470583809827, -81.23899999999999011 ) ) ;
#626=CARTESIAN_POINT ( 'NONE',  ( 23.04658433577699839, -17.87353418447250064, -81.23899999999999011 ) ) ;
#628=CARTESIAN_POINT ( 'NONE',  ( 9.221464511544803955, -11.63197161253809675, -62.67433543276930408 ) ) ;
#630=VERTEX_POINT ( 'NONE', #47964 ) ;
#632=CARTESIAN_POINT ( 'NONE',  ( 9.367521945652839577, -16.18213243797932677, -35.82056437903438706 ) ) ;
#637=VERTEX_POINT ( 'NONE', #4185 ) ;
#651=CARTESIAN_POINT ( 'NONE',  ( 19.27421804432820096, -22.80822521013089954, -59.65646296961579509 ) ) ;
#660=DIRECTION ( 'NONE',  ( 0.000000000000000000, 0.000000000000000000, -1.000000000000000000 ) ) ;
#661=CARTESIAN_POINT ( 'NONE',  ( 9.993740982288887409, -20.62509161583232142, -34.28983011217102472 ) ) ;
#662=LINE ( 'NONE', #32351, #47229 ) ;
#663=CARTESIAN_POINT ( 'NONE',  ( 9.367097141674031846, -15.61601956221279863, -71.84717978381000592 ) ) ;
#665=CARTESIAN_POINT ( 'NONE',  ( 16.48142850091230116, -8.174015587955670625, -40.58219447382339951 ) ) ;
#667=VERTEX_POINT ( 'NONE', #32194 ) ;
#674=CARTESIAN_POINT ( 'NONE',  ( 8.222928424025267802, -16.65167072501185075, -78.75066471084360842 ) ) ;
#676=CARTESIAN_POINT ( 'NONE',  ( 11.27226524438746047, -21.94235859059851634, -52.21600097131449303 ) ) ;
#684=CARTESIAN_POINT ( 'NONE',  ( 9.221442382393673753, -11.63200944172679385, -78.95899856290910179 ) ) ;
#691=CARTESIAN_POINT ( 'NONE',  ( 22.84901343360919768, -14.12476282708878372, -66.77701941837864297 ) ) ;
#699=DIRECTION ( 'NONE',  ( -1.000000000000000000, 9.391392475159538137E-33, -1.071169953407190059E-15 ) ) ;
#701=CARTESIAN_POINT ( 'NONE',  ( 23.59082625508080255, -13.17046693263549884, -59.91161365334649958 ) ) ;
#716=CARTESIAN_POINT ( 'NONE',  ( 14.06325258520262267, -7.911090401242016235, -36.92433639680130142 ) ) ;
#718=CARTESIAN_POINT ( 'NONE',  ( 9.366937397696199596, -15.61618894467949836, -28.45282021618999835 ) ) ;
#719=CARTESIAN_POINT ( 'NONE',  ( 23.19722557037290045, -14.28277357378349954, -32.14999999999999858 ) ) ;
#726=CARTESIAN_POINT ( 'NONE',  ( 10.90011346693460048, -20.34373019106079994, -67.61334385705760042 ) ) ;
#730=CYLINDRICAL_SURFACE ( 'NONE', #6163, 6.766999999999998572 ) ;
#733=CARTESIAN_POINT ( 'NONE',  ( 12.44997199531479914, -9.601959350568199270, -61.77788021779369387 ) ) ;
#736=CARTESIAN_POINT ( 'NONE',  ( 24.04493742152532576, -16.65172855544441788, -79.83400040593491553 ) ) ;
#744=CARTESIAN_POINT ( 'NONE',  ( 24.04493742238449627, -16.65172779011892601, -63.54933673588272569 ) ) ;
#762=CARTESIAN_POINT ( 'NONE',  ( 7.893181483431141565, -15.34663001334440047, -76.80273986043728485 ) ) ;
#764=CARTESIAN_POINT ( 'NONE',  ( 22.90093739769620029, -15.61618894467913243, -28.45282021618999835 ) ) ;
#769=CARTESIAN_POINT ( 'NONE',  ( 23.36054005697790004, -17.42806857920490060, -66.31085317895978903 ) ) ;
#771=CARTESIAN_POINT ( 'NONE',  ( 9.366937397696199596, -15.61618894467949836, -28.45282021618999835 ) ) ;
#780=DIRECTION ( 'NONE',  ( 1.000000000000000000, 2.460964292799963328E-14, 0.000000000000000000 ) ) ;
#790=CARTESIAN_POINT ( 'NONE',  ( 24.01815955786813461, -16.28851273216530871, -65.81940510519697796 ) ) ;
#792=CARTESIAN_POINT ( 'NONE',  ( 13.77087701533600139, -22.26137549781239855, -37.06157372594439181 ) ) ;
#800=CARTESIAN_POINT ( 'NONE',  ( 22.90090027005575379, -15.64040245347762870, -40.45396332187905131 ) ) ;
#801=CARTESIAN_POINT ( 'NONE',  ( 10.94036863195580089, -20.95786825121460240, -61.81286799887340067 ) ) ;
#811=CARTESIAN_POINT ( 'NONE',  ( 24.04492190258993389, -15.63236072556031075, -71.50832317379786218 ) ) ;
#812=EDGE_CURVE ( 'NONE', #15276, #40924, #12511, .T. ) ;
#817=DIRECTION ( 'NONE',  ( 0.000000000000000000, 0.000000000000000000, -1.000000000000000000 ) ) ;
#819=CARTESIAN_POINT ( 'NONE',  ( 9.464122031033584292, -13.86995827888586419, -71.92931663830769651 ) ) ;
#820=DIRECTION ( 'NONE',  ( 0.000000000000000000, -1.000000000000000000, 0.000000000000000000 ) ) ;
#821=DIRECTION ( 'NONE',  ( 0.000000000000000000, 0.000000000000000000, -1.000000000000000000 ) ) ;
#832=CARTESIAN_POINT ( 'NONE',  ( 22.58857181005839720, -20.74653149256879914, -44.00610240009889651 ) ) ;
#833=CARTESIAN_POINT ( 'NONE',  ( 22.82184556707856871, -14.56300605882913324, -56.40312229056203819 ) ) ;
#837=ORIENTED_EDGE ( 'NONE', *, *, #30668, .T. ) ;
#839=CARTESIAN_POINT ( 'NONE',  ( 23.56125590958530225, -15.03169469483670007, -36.20765937478449814 ) ) ;
#842=CARTESIAN_POINT ( 'NONE',  ( 24.04470022272198193, -15.61619473591594698, -59.79232576333501470 ) ) ;
#846=CARTESIAN_POINT ( 'NONE',  ( 8.679101862113558497, -12.09366884588789937, -54.64817642206789827 ) ) ;
#852=CARTESIAN_POINT ( 'NONE',  ( 9.458115080269156039, -13.90150626531904976, -55.92783392174342794 ) ) ;
#868=CARTESIAN_POINT ( 'NONE',  ( 24.04493739769619864, -15.61618894467929941, -32.14999999999999858 ) ) ;
#869=CARTESIAN_POINT ( 'NONE',  ( 25.83723722998072247, -15.61618894467929941, -22.14999999999999858 ) ) ;
#871=CARTESIAN_POINT ( 'NONE',  ( 14.33494800996290586, -22.21088556678449422, -67.03786065450826470 ) ) ;
#875=CARTESIAN_POINT ( 'NONE',  ( 19.54190971727932791, -21.52911178881554477, -60.78616782307490496 ) ) ;
#882=EDGE_CURVE ( 'NONE', #6987, #19003, #21862, .T. ) ;
#890=CARTESIAN_POINT ( 'NONE',  ( 20.73418997509670092, -20.86103424430950071, -81.23899999999999011 ) ) ;
#891=CARTESIAN_POINT ( 'NONE',  ( 14.06331861277063666, -7.911073306414944994, -62.92433584427882209 ) ) ;
#894=ORIENTED_EDGE ( 'NONE', *, *, #30363, .F. ) ;
#897=FACE_OUTER_BOUND ( 'NONE', #2547, .T. ) ;
#903=ORIENTED_EDGE ( 'NONE', *, *, #44355, .T. ) ;
#910=CARTESIAN_POINT ( 'NONE',  ( 9.807807230283941635, -20.47791195640980533, -68.58399767422770310 ) ) ;
#913=EDGE_CURVE ( 'NONE', #35517, #36938, #13355, .T. ) ;
#914=CARTESIAN_POINT ( 'NONE',  ( 20.13079160575060200, -22.36984755485060106, -63.61740952279680528 ) ) ;
#924=CARTESIAN_POINT ( 'NONE',  ( 8.389157129729829521, -13.77808729393154685, -64.58170620237746107 ) ) ;
#928=CARTESIAN_POINT ( 'NONE',  ( 24.04493440204280574, -15.62413989401176373, -33.50798514483673785 ) ) ;
#933=CARTESIAN_POINT ( 'NONE',  ( 12.08985222827440076, -9.359027489130609112, -44.38470316487709511 ) ) ;
#935=ORIENTED_EDGE ( 'NONE', *, *, #38697, .F. ) ;
#949=ORIENTED_EDGE ( 'NONE', *, *, #24161, .T. ) ;
#952=CARTESIAN_POINT ( 'NONE',  ( 8.222946371911650232, -14.58057577448233033, -78.83399827190503117 ) ) ;
#958=CARTESIAN_POINT ( 'NONE',  ( 22.47159906988888878, -10.82927912022386252, -77.30170387646415975 ) ) ;
#963=CARTESIAN_POINT ( 'NONE',  ( 9.366931398960248956, -14.73043463447693213, -53.49448701394783967 ) ) ;
#964=ORIENTED_EDGE ( 'NONE', *, *, #11171, .T. ) ;
#967=CARTESIAN_POINT ( 'NONE',  ( 16.14243133923272566, -22.38318395068864675, -46.95242411700758112 ) ) ;
#969=CARTESIAN_POINT ( 'NONE',  ( 8.323089174469110674, -16.37605579175999893, -64.98162524141820029 ) ) ;
#970=DIRECTION ( 'NONE',  ( 0.000000000000000000, 0.000000000000000000, -1.000000000000000000 ) ) ;
#986=CARTESIAN_POINT ( 'NONE',  ( 22.89998285337925310, -16.42400860516817573, -76.88518437983843512 ) ) ;
#987=CARTESIAN_POINT ( 'NONE',  ( 20.98660220077443839, -9.290834596779705024, -55.21623050661466436 ) ) ;
#988=CARTESIAN_POINT ( 'NONE',  ( 22.44491825635649818, -19.88650245843829723, -32.14999999999999858 ) ) ;
#992=CARTESIAN_POINT ( 'NONE',  ( 9.807852707146459181, -20.47797030866249912, -74.29933501067056056 ) ) ;
#997=CARTESIAN_POINT ( 'NONE',  ( 21.69971205180370077, -19.94801438831689921, -59.05769930218669828 ) ) ;
#1004=CARTESIAN_POINT ( 'NONE',  ( 14.06839928245249993, -8.872591166704909327, -69.85821118628280146 ) ) ;
#1008=CARTESIAN_POINT ( 'NONE',  ( 12.14991563812279907, -22.52877415440609354, -80.45899895091454823 ) ) ;
#1019=DIRECTION ( 'NONE',  ( -1.000000000000000000, -5.367253113454777116E-16, 0.000000000000000000 ) ) ;
#1027=EDGE_CURVE ( 'NONE', #630, #27600, #34293, .T. ) ;
#1030=CARTESIAN_POINT ( 'NONE',  ( 22.72481326017360104, -13.84495465653436774, -68.36948467987761546 ) ) ;
#1035=CARTESIAN_POINT ( 'NONE',  ( 23.97401567591719740, -15.96280768448609955, -32.02654991895260395 ) ) ;
#1042=CARTESIAN_POINT ( 'NONE',  ( 22.90571047178250197, -13.64498330036649953, -32.75701418906499640 ) ) ;
#1057=ORIENTED_EDGE ( 'NONE', *, *, #16426, .F. ) ;
#1062=CARTESIAN_POINT ( 'NONE',  ( 15.91222836016400066, -22.66554379454339951, -38.96282807147130001 ) ) ;
#1067=ORIENTED_EDGE ( 'NONE', *, *, #20321, .T. ) ;
#1068=CARTESIAN_POINT ( 'NONE',  ( 9.533333296005068291, -19.07143420819970103, -75.91383772819759201 ) ) ;
#1081=VERTEX_POINT ( 'NONE', #51317 ) ;
#1086=CARTESIAN_POINT ( 'NONE',  ( 22.27312146484720046, -12.14444901143390076, -72.68335544512909507 ) ) ;
#1088=CARTESIAN_POINT ( 'NONE',  ( 14.04940779400430984, -9.151428043508968102, -49.85362723947532970 ) ) ;
#1096=CARTESIAN_POINT ( 'NONE',  ( 13.31717580901180042, -23.36529045443169750, -52.40330909284259775 ) ) ;
#1097=CARTESIAN_POINT ( 'NONE',  ( 22.90039887029312737, -15.52396765975452908, -56.44848823407438232 ) ) ;
#1101=CARTESIAN_POINT ( 'NONE',  ( 22.83083802998899969, -12.35110237284849966, -32.08827495947629416 ) ) ;
#1107=CARTESIAN_POINT ( 'NONE',  ( 23.97380802304540737, -16.70946919957393106, -59.83642518982571090 ) ) ;
#1110=EDGE_CURVE ( 'NONE', #11008, #14401, #41834, .T. ) ;
#1111=CARTESIAN_POINT ( 'NONE',  ( 9.466508518632270608, -10.76561033469889850, -56.70786862972200026 ) ) ;
#1116=CARTESIAN_POINT ( 'NONE',  ( 9.852065557373178351, -12.47056568813226107, -69.99514707462319052 ) ) ;
#1134=CARTESIAN_POINT ( 'NONE',  ( 22.90093737924810569, -16.50198979217266171, -60.49448455657499579 ) ) ;
#1135=CARTESIAN_POINT ( 'NONE',  ( 21.54529342003797154, -11.45756571115651745, -48.24448846502571087 ) ) ;
#1136=VERTEX_POINT ( 'NONE', #44213 ) ;
#1149=CARTESIAN_POINT ( 'NONE',  ( 19.95187633256550086, -21.36878654213050055, -81.23899999999999011 ) ) ;
#1153=EDGE_CURVE ( 'NONE', #21674, #36323, #43957, .T. ) ;
#1162=VERTEX_POINT ( 'NONE', #4379 ) ;
#1169=CARTESIAN_POINT ( 'NONE',  ( 22.90080846266944548, -15.61618871746016879, -44.84718732428002852 ) ) ;
#1170=CARTESIAN_POINT ( 'NONE',  ( 23.04646694808121410, -19.60030851528551210, -67.95899617219959055 ) ) ;
#1172=CARTESIAN_POINT ( 'NONE',  ( 22.90117443638819239, -15.61618876209028528, -62.84717844892357164 ) ) ;
#1175=CARTESIAN_POINT ( 'NONE',  ( 10.99779310440810143, -21.54971824701760497, -72.01461621554039993 ) ) ;
#1176=ORIENTED_EDGE ( 'NONE', *, *, #35132, .T. ) ;
#1183=ADVANCED_FACE ( 'NONE', ( #23758 ), #7621, .F. ) ;
#1189=CARTESIAN_POINT ( 'NONE',  ( 23.98466744169371978, -16.62257527342094576, -33.54825124114566393 ) ) ;
#1190=DIRECTION ( 'NONE',  ( 0.000000000000000000, 0.000000000000000000, -1.000000000000000000 ) ) ;
#1191=CARTESIAN_POINT ( 'NONE',  ( 22.90068744318051586, -15.61618870719606278, -70.84718393407784731 ) ) ;
#1194=CARTESIAN_POINT ( 'NONE',  ( 20.37871476403569915, -21.73897911326690036, -41.37438378445959586 ) ) ;
#1204=FACE_OUTER_BOUND ( 'NONE', #46556, .T. ) ;
#1207=ORIENTED_EDGE ( 'NONE', *, *, #7215, .T. ) ;
#1209=VERTEX_POINT ( 'NONE', #46762 ) ;
#1214=ORIENTED_EDGE ( 'NONE', *, *, #2608, .T. ) ;
#1216=VERTEX_POINT ( 'NONE', #13042 ) ;
#1217=DIRECTION ( 'NONE',  ( -0.8090169943749487835, -0.5877852522924713607, 0.000000000000000000 ) ) ;
#1221=EDGE_CURVE ( 'NONE', #4288, #13029, #8048, .T. ) ;
#1223=VECTOR ( 'NONE', #46761, 1000.000000000000000 ) ;
#1229=CARTESIAN_POINT ( 'NONE',  ( 22.90086341797264780, -15.61618933298137790, -46.45282805145726002 ) ) ;
#1231=CARTESIAN_POINT ( 'NONE',  ( 17.24545617948280096, -23.38479715910980161, -68.46725820821738751 ) ) ;
#1249=CARTESIAN_POINT ( 'NONE',  ( 24.04482276282174169, -15.57017577287801124, -55.50582115160575825 ) ) ;
#1250=CARTESIAN_POINT ( 'NONE',  ( 22.52893251407120090, -12.64281036005729852, -32.14999999999999858 ) ) ;
#1255=CARTESIAN_POINT ( 'NONE',  ( 9.366602974803960535, -15.61605382581650048, -49.84717978381009118 ) ) ;
#1259=CARTESIAN_POINT ( 'NONE',  ( 9.908454316688080965, -18.93069035251320287, -59.69145075069559425 ) ) ;
#1266=CARTESIAN_POINT ( 'NONE',  ( 11.13117135703519978, -20.58759625438899832, -63.20382097693880041 ) ) ;
#1272=ORIENTED_EDGE ( 'NONE', *, *, #3205, .F. ) ;
#1278=ORIENTED_EDGE ( 'NONE', *, *, #26962, .F. ) ;
#1287=VERTEX_POINT ( 'NONE', #25162 ) ;
#1291=CARTESIAN_POINT ( 'NONE',  ( 9.807746736123759135, -10.75454355271028639, -53.00066549702621899 ) ) ;
#1292=FACE_OUTER_BOUND ( 'NONE', #38022, .T. ) ;
#1294=CARTESIAN_POINT ( 'NONE',  ( 17.58945275769320205, -7.904624730565840807, -37.57187509340590026 ) ) ;
#1304=CARTESIAN_POINT ( 'NONE',  ( 21.99623050575979732, -19.53742327708049942, -37.03483646650040129 ) ) ;
#1305=LINE ( 'NONE', #771, #12830 ) ;
#1313=CARTESIAN_POINT ( 'NONE',  ( 8.058121637015549510, -13.95368465620019904, -78.57229360328089740 ) ) ;
#1315=CARTESIAN_POINT ( 'NONE',  ( 24.04462826173309153, -15.61618628916268392, -33.50766512250601181 ) ) ;
#1316=CARTESIAN_POINT ( 'NONE',  ( 16.13393739769620083, -15.61618894467929941, -28.45282021618999835 ) ) ;
#1318=CARTESIAN_POINT ( 'NONE',  ( 8.428832403331353973, -13.54552742703515911, -68.59100208448060698 ) ) ;
#1327=CARTESIAN_POINT ( 'NONE',  ( 14.81228562542739979, -8.688288820165540827, -33.89281648339969166 ) ) ;
#1335=CARTESIAN_POINT ( 'NONE',  ( 10.29322140962580079, -20.24141662394440289, -73.85414552054359660 ) ) ;
#1338=CARTESIAN_POINT ( 'NONE',  ( 14.81467456660999993, -7.815966731016759539, -81.23899999999999011 ) ) ;
#1346=EDGE_LOOP ( 'NONE', ( #33772, #30629, #30206, #50001 ) ) ;
#1351=CARTESIAN_POINT ( 'NONE',  ( 14.36265541187617956, -9.025324658394913158, -69.86948818930653715 ) ) ;
#1352=DIRECTION ( 'NONE',  ( 0.000000000000000000, 0.000000000000000000, 1.000000000000000000 ) ) ;
#1358=CARTESIAN_POINT ( 'NONE',  ( 23.04645231909379888, -11.63204132127529888, -43.62568514326029856 ) ) ;
#1359=CARTESIAN_POINT ( 'NONE',  ( 8.099657082704819544, -17.46904076716189991, -52.72018481709709903 ) ) ;
#1364=CARTESIAN_POINT ( 'NONE',  ( 23.58352022967059725, -15.51416230748120029, -42.22829813561959611 ) ) ;
#1367=CARTESIAN_POINT ( 'NONE',  ( 11.01954162827919959, -11.00411938779079968, -32.14999999999999858 ) ) ;
#1374=CARTESIAN_POINT ( 'NONE',  ( 17.58032879468959919, -7.498881962947089974, -53.06379780079550557 ) ) ;
#1401=CARTESIAN_POINT ( 'NONE',  ( 14.47161711077219870, -7.905140794172798024, -81.23899999999999011 ) ) ;
#1402=ORIENTED_EDGE ( 'NONE', *, *, #47573, .T. ) ;
#1407=CARTESIAN_POINT ( 'NONE',  ( 9.807871516326736483, -20.47799444578012285, -80.29933555240771170 ) ) ;
#1408=EDGE_CURVE ( 'NONE', #8663, #31302, #31927, .T. ) ;
#1412=CARTESIAN_POINT ( 'NONE',  ( 19.28358208762359993, -21.69091679252559857, -81.23899999999999011 ) ) ;
#1417=ORIENTED_EDGE ( 'NONE', *, *, #33330, .T. ) ;
#1422=CARTESIAN_POINT ( 'NONE',  ( 8.222921933280828100, -16.32121750950448558, -34.76395294823650772 ) ) ;
#1438=CARTESIAN_POINT ( 'NONE',  ( 9.431647741891751480, -19.69859773764449784, -70.11336187001349174 ) ) ;
#1440=CARTESIAN_POINT ( 'NONE',  ( 22.90066504558609850, -15.61618132107965984, -48.84717678326153845 ) ) ;
#1445=CARTESIAN_POINT ( 'NONE',  ( 24.04493700328880479, -15.41104471036569024, -65.49941472047517266 ) ) ;
#1448=CARTESIAN_POINT ( 'NONE',  ( 9.221332323800828235, -19.60018030228138741, -56.62567467500329599 ) ) ;
#1449=CARTESIAN_POINT ( 'NONE',  ( 8.222936770565050679, -15.65019028997524586, -34.50629429565288575 ) ) ;
#1451=ORIENTED_EDGE ( 'NONE', *, *, #25769, .T. ) ;
#1452=CARTESIAN_POINT ( 'NONE',  ( 22.05896741169510022, -11.09947402434689856, -44.86001675125889676 ) ) ;
#1457=CARTESIAN_POINT ( 'NONE',  ( 9.366426063424411197, -15.61626247110940113, -71.45282021618990598 ) ) ;
#1460=FACE_OUTER_BOUND ( 'NONE', #45509, .T. ) ;
#1463=ORIENTED_EDGE ( 'NONE', *, *, #6459, .F. ) ;
#1464=B_SPLINE_CURVE_WITH_KNOTS ( 'NONE', 3,
 ( #15475, #31173, #253, #44023, #23301, #47202, #11808, #31426, #47962, #4440, #32192, #51119, #7870, #19653, #39578, #27770, #20407, #47455 ),
 .UNSPECIFIED., .F., .F.,
 ( 4, 2, 2, 2, 2, 2, 2, 2, 4 ),
 ( 0.4999984887057566940, 0.5624986776175371350, 0.6249988665293175760, 0.6874990554410981280, 0.7499992443528785691, 0.8124994332646588990, 0.8749996221764393400, 0.9374998110882196700, 1.000000000000000000 ),
 .UNSPECIFIED. ) ;
#1467=EDGE_CURVE ( 'NONE', #7417, #30849, #38039, .T. ) ;
#1479=CARTESIAN_POINT ( 'NONE',  ( 17.90512215027165155, -22.20707991068925935, -72.86943705533576576 ) ) ;
#1482=AXIS2_PLACEMENT_3D ( 'NONE', #21995, #42200, #6298 ) ;
#1483=CARTESIAN_POINT ( 'NONE',  ( 22.90093737893454318, -16.50198540115231083, -52.49448440678582273 ) ) ;
#1491=CARTESIAN_POINT ( 'NONE',  ( 19.15004480972399747, -22.86117643056869753, -60.38692723972829413 ) ) ;
#1499=CARTESIAN_POINT ( 'NONE',  ( 8.633937397696200833, -15.61618894467929941, -81.65000000000000568 ) ) ;
#1501=ORIENTED_EDGE ( 'NONE', *, *, #1027, .F. ) ;
#1507=CARTESIAN_POINT ( 'NONE',  ( 23.29272054552549776, -14.67821866136879905, -32.14999999999999858 ) ) ;
#1511=CARTESIAN_POINT ( 'NONE',  ( 10.17382535698764912, -11.84529732105606570, -50.02674116095206358 ) ) ;
#1515=CARTESIAN_POINT ( 'NONE',  ( 11.21742354769409999, -20.67291226489259870, -61.59270509622239587 ) ) ;
#1519=CARTESIAN_POINT ( 'NONE',  ( 9.366956123961729830, -16.50212425713979414, -43.41115352553956086 ) ) ;
#1522=CARTESIAN_POINT ( 'NONE',  ( 22.84952155313539990, -17.77106438141320055, -72.55165484244589891 ) ) ;
#1526=VERTEX_POINT ( 'NONE', #9411 ) ;
#1532=CARTESIAN_POINT ( 'NONE',  ( 11.97534989113796478, -21.02757240557042806, -55.16115446716158033 ) ) ;
#1542=CARTESIAN_POINT ( 'NONE',  ( 23.04646112206593145, -19.60031942610110178, -43.67434694693088915 ) ) ;
#1546=CARTESIAN_POINT ( 'NONE',  ( 24.04493741605278956, -14.58064998728431583, -57.46600087271308865 ) ) ;
#1549=CARTESIAN_POINT ( 'NONE',  ( 9.272314511663010350, -20.18801675654929895, -80.60524855149100176 ) ) ;
#1553=ORIENTED_EDGE ( 'NONE', *, *, #3853, .T. ) ;
#1565=EDGE_CURVE ( 'NONE', #48357, #10825, #38099, .T. ) ;
#1566=CARTESIAN_POINT ( 'NONE',  ( 24.15168607019749913, -17.53938432383520052, -81.58261298369829717 ) ) ;
#1569=CARTESIAN_POINT ( 'NONE',  ( 22.90114886013774864, -15.61618877916400017, -48.45281860778688809 ) ) ;
#1572=CARTESIAN_POINT ( 'NONE',  ( 15.09837409447361978, -7.705190857215417743, -68.96600325170983581 ) ) ;
#1575=ORIENTED_EDGE ( 'NONE', *, *, #48319, .F. ) ;
#1577=VERTEX_POINT ( 'NONE', #25868 ) ;
#1580=CARTESIAN_POINT ( 'NONE',  ( 24.04483683623963941, -15.65738770392476020, -65.79398883384345709 ) ) ;
#1582=CARTESIAN_POINT ( 'NONE',  ( 11.85511828107729926, -21.22281588510560013, -35.16031938041760441 ) ) ;
#1588=ORIENTED_EDGE ( 'NONE', *, *, #14854, .F. ) ;
#1590=CARTESIAN_POINT ( 'NONE',  ( 9.160088560685300862, -18.23766309806380193, -71.95289117501670262 ) ) ;
#1593=CARTESIAN_POINT ( 'NONE',  ( 18.02367597830500756, -7.913804971115164122, -49.36890451167464278 ) ) ;
#1597=CARTESIAN_POINT ( 'NONE',  ( 20.09906114624694951, -22.53978528867605036, -76.12648450854941018 ) ) ;
#1598=CARTESIAN_POINT ( 'NONE',  ( 22.67257700126428333, -13.83859173790965258, -62.36835213070619233 ) ) ;
#1599=CARTESIAN_POINT ( 'NONE',  ( 13.79739187203479744, -23.21386632249247839, -46.10279150706872997 ) ) ;
#1607=CARTESIAN_POINT ( 'NONE',  ( 10.13629284140139930, -19.32709435317449831, -53.67081198986049628 ) ) ;
#1610=VERTEX_POINT ( 'NONE', #10955 ) ;
#1612=CARTESIAN_POINT ( 'NONE',  ( 9.366560669795820360, -15.61606439180730099, -33.84717978380999881 ) ) ;
#1613=CARTESIAN_POINT ( 'NONE',  ( 8.313605784523671716, -16.98482869512226401, -66.45256872909452284 ) ) ;
#1614=CARTESIAN_POINT ( 'NONE',  ( 15.81717235992440074, -23.85526534721260106, -54.30456343836939936 ) ) ;
#1620=CARTESIAN_POINT ( 'NONE',  ( 11.79648058786079901, -9.558700832602001540, -39.53485447945649867 ) ) ;
#1623=CARTESIAN_POINT ( 'NONE',  ( 8.222919265141586109, -14.58077434080222545, -32.54933488526609153 ) ) ;
#1630=CARTESIAN_POINT ( 'NONE',  ( 18.48369898198360062, -23.51943772008690203, -55.91567931908580391 ) ) ;
#1633=EDGE_CURVE ( 'NONE', #1136, #48851, #35566, .T. ) ;
#1635=CARTESIAN_POINT ( 'NONE',  ( 12.98154199631053274, -22.91985500418327248, -40.13723907971733951 ) ) ;
#1637=CARTESIAN_POINT ( 'NONE',  ( 12.00938018391108919, -9.895123749747092745, -70.14834965109328380 ) ) ;
#1639=EDGE_CURVE ( 'NONE', #21944, #32127, #11212, .T. ) ;
#1650=DIRECTION ( 'NONE',  ( 0.000000000000000000, 0.000000000000000000, -1.000000000000000000 ) ) ;
#1656=ORIENTED_EDGE ( 'NONE', *, *, #8046, .F. ) ;
#1659=DIRECTION ( 'NONE',  ( 0.000000000000000000, 0.000000000000000000, -1.000000000000000000 ) ) ;
#1661=CARTESIAN_POINT ( 'NONE',  ( 14.81467456660999993, -7.815966731016759539, -81.23899999999999011 ) ) ;
#1662=EDGE_CURVE ( 'NONE', #48498, #12296, #21120, .T. ) ;
#1663=CARTESIAN_POINT ( 'NONE',  ( 11.55666008087221641, -9.119572623996059946, -80.81238995496710231 ) ) ;
#1665=VERTEX_POINT ( 'NONE', #31350 ) ;
#1672=CARTESIAN_POINT ( 'NONE',  ( 23.99259192901511284, -16.66193452127228625, -77.54972237907269061 ) ) ;
#1676=ORIENTED_EDGE ( 'NONE', *, *, #48105, .F. ) ;
#1678=ORIENTED_EDGE ( 'NONE', *, *, #32314, .F. ) ;
#1680=CARTESIAN_POINT ( 'NONE',  ( 19.34678433693689215, -22.91919624005971556, -34.16012075487866895 ) ) ;
#1681=CARTESIAN_POINT ( 'NONE',  ( 22.90092006877790709, -15.63200709851992443, -50.45356305415408826 ) ) ;
#1691=CARTESIAN_POINT ( 'NONE',  ( 22.90147442980407888, -15.70852189567019330, -62.85151964813176306 ) ) ;
#1695=CARTESIAN_POINT ( 'NONE',  ( 21.65169865715700226, -21.19660639024510118, -71.53930262915869775 ) ) ;
#1697=EDGE_LOOP ( 'NONE', ( #38223, #35096, #38212, #11603 ) ) ;
#1698=CARTESIAN_POINT ( 'NONE',  ( 18.21162691092218111, -8.876325039443173637, -48.44236253966248995 ) ) ;
#1713=CARTESIAN_POINT ( 'NONE',  ( 11.29738606970870052, -21.28315158705520105, -55.79222923803829559 ) ) ;
#1716=CARTESIAN_POINT ( 'NONE',  ( 10.14762331803407669, -11.88703313963010189, -34.02451708608307968 ) ) ;
#1726=EDGE_LOOP ( 'NONE', ( #15779, #17354, #33318, #39302 ) ) ;
#1734=EDGE_LOOP ( 'NONE', ( #45147, #20798, #48731, #3768 ) ) ;
#1736=ORIENTED_EDGE ( 'NONE', *, *, #35169, .F. ) ;
#1743=CARTESIAN_POINT ( 'NONE',  ( 15.32497155414790058, -23.42210476894710425, -60.54536510185550213 ) ) ;
#1748=CARTESIAN_POINT ( 'NONE',  ( 16.13393739769620083, -15.61618894467929941, -32.14999999999999858 ) ) ;
#1761=CARTESIAN_POINT ( 'NONE',  ( 23.40110066171819980, -15.35420991546000025, -32.14999999999999858 ) ) ;
#1766=CARTESIAN_POINT ( 'NONE',  ( 13.22040357262759791, -8.188698541349817006, -44.88848981900320467 ) ) ;
#1768=CARTESIAN_POINT ( 'NONE',  ( 15.09833599464489140, -23.52718242961558914, -46.33404756934790214 ) ) ;
#1771=CARTESIAN_POINT ( 'NONE',  ( 13.52272076457530048, -9.064539772954379515, -62.22645654473139842 ) ) ;
#1775=CARTESIAN_POINT ( 'NONE',  ( 21.54530064538955614, -19.77480226385806716, -42.66115309383150134 ) ) ;
#1778=CARTESIAN_POINT ( 'NONE',  ( 11.42698330956450015, -20.86853526883250254, -73.18540629095488725 ) ) ;
#1787=CARTESIAN_POINT ( 'NONE',  ( 24.04493700143699186, -15.61325609016573779, -39.50755344202253383 ) ) ;
#1799=CARTESIAN_POINT ( 'NONE',  ( 10.90918837189948754, -9.627391034007024118, -33.06390794336576988 ) ) ;
#1803=CARTESIAN_POINT ( 'NONE',  ( 20.11812543827117494, -8.703699676690527909, -57.17433449590220107 ) ) ;
#1805=EDGE_CURVE ( 'NONE', #20360, #49314, #10568, .T. ) ;
#1807=CARTESIAN_POINT ( 'NONE',  ( 8.558321896845489718, -13.56758030102569990, -37.09656150702419808 ) ) ;
#1808=CARTESIAN_POINT ( 'NONE',  ( 9.813195994592092575, -18.65377965825830486, -65.70430698158793348 ) ) ;
#1813=CARTESIAN_POINT ( 'NONE',  ( 9.366947176629301097, -14.73031912718973047, -77.49448675212997273 ) ) ;
#1815=CARTESIAN_POINT ( 'NONE',  ( 14.69332040448139942, -8.712069350285601033, -32.28170060268329422 ) ) ;
#1818=B_SPLINE_CURVE_WITH_KNOTS ( 'NONE', 3,
 ( #24431, #48580, #12681, #44636, #18852, #6300, #19112, #7331, #14671 ),
 .UNSPECIFIED., .F., .F.,
 ( 4, 1, 1, 1, 1, 1, 4 ),
 ( 0.000000000000000000, 0.08931995506724747791, 0.2031549606839579136, 0.3169899663004408508, 0.4308249719171447500, 0.5446599775336212756, 0.6416644417609895790 ),
 .UNSPECIFIED. ) ;
#1825=CARTESIAN_POINT ( 'NONE',  ( 18.67273062756910207, -7.771648177471909946, -81.10729939731677973 ) ) ;
#1842=CARTESIAN_POINT ( 'NONE',  ( 22.37652147218269860, -18.89836852075259799, -42.60689890039769523 ) ) ;
#1849=CARTESIAN_POINT ( 'NONE',  ( 20.48230527184779959, -9.566528533608519069, -78.76571924648798984 ) ) ;
#1853=CARTESIAN_POINT ( 'NONE',  ( 10.13549572879737148, -10.40084719372432254, -49.02025583064260417 ) ) ;
#1858=CARTESIAN_POINT ( 'NONE',  ( 22.89447552609475878, -15.29690831320359656, -62.43780689980356868 ) ) ;
#1859=CARTESIAN_POINT ( 'NONE',  ( 9.367163129351689932, -15.61602587752549809, -57.45282021618999835 ) ) ;
#1863=CARTESIAN_POINT ( 'NONE',  ( 17.16953043169627691, -7.705195452461492067, -47.33399925743757564 ) ) ;
#1874=CARTESIAN_POINT ( 'NONE',  ( 7.979399327260850328, -14.39707905883819983, -56.83956923240529591 ) ) ;
#1876=CARTESIAN_POINT ( 'NONE',  ( 18.14582764655064651, -9.096175230596063699, -56.04792584441368319 ) ) ;
#1878=ADVANCED_FACE ( 'NONE', ( #29375 ), #17083, .T. ) ;
#1882=CARTESIAN_POINT ( 'NONE',  ( 21.35513134223840126, -20.93086933004790140, -40.48548165221990303 ) ) ;
#1885=CARTESIAN_POINT ( 'NONE',  ( 9.706165438393730582, -12.70257730181489997, -32.14999999999999858 ) ) ;
#1890=CYLINDRICAL_SURFACE ( 'NONE', #7233, 6.766999999999998572 ) ;
#1891=CARTESIAN_POINT ( 'NONE',  ( 19.91591662378250049, -22.94280848184829935, -53.85598711143169481 ) ) ;
#1893=ORIENTED_EDGE ( 'NONE', *, *, #28364, .T. ) ;
#1898=CARTESIAN_POINT ( 'NONE',  ( 22.49413451099558614, -12.69308235403424590, -52.70970122521629975 ) ) ;
#1922=EDGE_LOOP ( 'NONE', ( #50683, #28575, #11412, #1656 ) ) ;
#1927=ORIENTED_EDGE ( 'NONE', *, *, #5665, .T. ) ;
#1931=CARTESIAN_POINT ( 'NONE',  ( 22.72480972994501869, -17.38744065826488239, -44.53615520578274101 ) ) ;
#1939=CARTESIAN_POINT ( 'NONE',  ( 10.85063640367556204, -21.53850039894781432, -34.52410773689097567 ) ) ;
#1941=CARTESIAN_POINT ( 'NONE',  ( 22.90093740079596429, -15.61855648616878689, -50.45293054938055377 ) ) ;
#1942=EDGE_CURVE ( 'NONE', #30218, #26995, #5027, .T. ) ;
#1954=CARTESIAN_POINT ( 'NONE',  ( 23.86772648130780183, -16.94857574789820021, -75.34181132021238625 ) ) ;
#1955=ADVANCED_FACE ( 'NONE', ( #37251 ), #40400, .T. ) ;
#1957=CARTESIAN_POINT ( 'NONE',  ( 24.04461175216078317, -15.61617380819018663, -65.50766589912049653 ) ) ;
#1963=CARTESIAN_POINT ( 'NONE',  ( 24.04508668034977248, -15.61618904219531778, -35.79233368253564862 ) ) ;
#1964=CARTESIAN_POINT ( 'NONE',  ( 15.09831437461540915, -7.705198071712128005, -42.96596090275411939 ) ) ;
#1972=CARTESIAN_POINT ( 'NONE',  ( 17.44088820494859959, -8.281437829217798807, -52.62347199549359544 ) ) ;
#1980=CARTESIAN_POINT ( 'NONE',  ( 11.96950732185187327, -9.924082013335068453, -54.14612557624229794 ) ) ;
#1983=ORIENTED_EDGE ( 'NONE', *, *, #32786, .F. ) ;
#1985=EDGE_LOOP ( 'NONE', ( #14919, #4355, #20268, #30721, #27509 ) ) ;
#1993=ORIENTED_EDGE ( 'NONE', *, *, #16301, .F. ) ;
#1994=CARTESIAN_POINT ( 'NONE',  ( 24.04484245248367458, -15.57431735484160384, -77.50599178999226524 ) ) ;
#1998=CARTESIAN_POINT ( 'NONE',  ( 23.90266814002770346, -17.16108999061242102, -49.57014705178468716 ) ) ;
#2001=CARTESIAN_POINT ( 'NONE',  ( 23.98165953727020039, -15.61838248587350009, -74.01258338267071224 ) ) ;
#2009=LINE ( 'NONE', #1499, #42841 ) ;
#2012=ORIENTED_EDGE ( 'NONE', *, *, #5435, .T. ) ;
#2025=CARTESIAN_POINT ( 'NONE',  ( 8.222262383277058717, -15.61618471288229948, -44.50766849176299900 ) ) ;
#2029=CARTESIAN_POINT ( 'NONE',  ( 22.73929038217119825, -18.08840882263159955, -76.96117772256469891 ) ) ;
#2030=ORIENTED_EDGE ( 'NONE', *, *, #39129, .T. ) ;
#2033=CARTESIAN_POINT ( 'NONE',  ( 12.14992638744813824, -8.703597654584235954, -40.84100140184820305 ) ) ;
#2036=CARTESIAN_POINT ( 'NONE',  ( 20.66515000696679749, -21.02087866656289705, -78.73073146540821199 ) ) ;
#2043=ORIENTED_EDGE ( 'NONE', *, *, #23955, .F. ) ;
#2047=CARTESIAN_POINT ( 'NONE',  ( 22.90093381512099668, -15.61618921778096336, -54.45281771551935890 ) ) ;
#2049=ORIENTED_EDGE ( 'NONE', *, *, #271, .F. ) ;
#2064=CARTESIAN_POINT ( 'NONE',  ( 20.97397396333849784, -9.337171417351125768, -33.50141378971362371 ) ) ;
#2070=CARTESIAN_POINT ( 'NONE',  ( 14.22007994406810027, -8.005413869907048507, -43.43407599211369075 ) ) ;
#2076=CARTESIAN_POINT ( 'NONE',  ( 11.97534233955078165, -10.20481119701443262, -77.74448596776977638 ) ) ;
#2078=CARTESIAN_POINT ( 'NONE',  ( 15.59821405493169877, -8.583724250529140676, -44.32297812435340489 ) ) ;
#2084=CARTESIAN_POINT ( 'NONE',  ( 15.09849320450292431, -7.705176464883582099, -57.25066471183642136 ) ) ;
#2092=LINE ( 'NONE', #8930, #22623 ) ;
#2093=CARTESIAN_POINT ( 'NONE',  ( 8.222845792583640900, -15.61638830267690103, -48.79233150823699816 ) ) ;
#2102=CARTESIAN_POINT ( 'NONE',  ( 17.88832476977960084, -8.785033577883739397, -44.03283965954289414 ) ) ;
#2107=CARTESIAN_POINT ( 'NONE',  ( 19.88348325370240133, -22.05417008143080082, -79.39947069499689292 ) ) ;
#2109=FACE_OUTER_BOUND ( 'NONE', #17396, .T. ) ;
#2114=CARTESIAN_POINT ( 'NONE',  ( 22.90083777812701982, -15.57647135431740004, -62.45096014559136677 ) ) ;
#2115=CARTESIAN_POINT ( 'NONE',  ( 21.32685934670647043, -21.60664595198382898, -45.78044139066837204 ) ) ;
#2125=CARTESIAN_POINT ( 'NONE',  ( 20.99564533579582104, -21.94233031744103002, -69.79933736319598836 ) ) ;
#2132=CARTESIAN_POINT ( 'NONE',  ( 22.90071998467804804, -15.61618839864605057, -72.45282571548244732 ) ) ;
#2135=CARTESIAN_POINT ( 'NONE',  ( 23.78551980429849877, -12.54438056346319996, -53.67081198986049628 ) ) ;
#2140=CARTESIAN_POINT ( 'NONE',  ( 16.33068269661450245, -23.06387214769610239, -48.72425048283629678 ) ) ;
#2142=CARTESIAN_POINT ( 'NONE',  ( 9.524248426565812053, -13.05564950212349906, -32.14999999999999858 ) ) ;
#2144=EDGE_CURVE ( 'NONE', #28912, #14719, #3039, .T. ) ;
#2147=CARTESIAN_POINT ( 'NONE',  ( 23.57883367829501609, -12.85227554272108463, -61.39446357243666341 ) ) ;
#2149=CARTESIAN_POINT ( 'NONE',  ( 18.93672734906450117, -23.37035487000509804, -65.89726463310188365 ) ) ;
#2152=VECTOR ( 'NONE', #27858, 1000.000000000000000 ) ;
#2175=CARTESIAN_POINT ( 'NONE',  ( 9.807752066895531584, -20.47784117495694645, -76.29935098731050402 ) ) ;
#2190=CARTESIAN_POINT ( 'NONE',  ( 20.11810193263714552, -8.703685627498805033, -63.17433625578833301 ) ) ;
#2191=EDGE_CURVE ( 'NONE', #48341, #7094, #21775, .T. ) ;
#2201=CARTESIAN_POINT ( 'NONE',  ( 24.04034479754921705, -15.90769644645291159, -33.80405724268722167 ) ) ;
#2203=CARTESIAN_POINT ( 'NONE',  ( 21.43993832425762847, -20.26257607252427206, -49.07611398817140724 ) ) ;
#2204=CARTESIAN_POINT ( 'NONE',  ( 29.99034385824719706, -15.61618894467929941, -24.14999999999999858 ) ) ;
#2212=CARTESIAN_POINT ( 'NONE',  ( 15.98404599893290090, -7.372388041690080662, -35.00188151829029692 ) ) ;
#2213=VERTEX_POINT ( 'NONE', #37770 ) ;
#2215=LINE ( 'NONE', #21588, #48947 ) ;
#2217=LINE ( 'NONE', #50174, #35402 ) ;
#2230=CARTESIAN_POINT ( 'NONE',  ( 22.81411437884488791, -16.71916889329374811, -62.50490964971036334 ) ) ;
#2232=ADVANCED_FACE ( 'NONE', ( #27242 ), #15719, .T. ) ;
#2233=VERTEX_POINT ( 'NONE', #23556 ) ;
#2234=CARTESIAN_POINT ( 'NONE',  ( 18.78540261209650097, -8.653687486498709447, -54.68316420314759796 ) ) ;
#2237=CARTESIAN_POINT ( 'NONE',  ( 19.54194422072443516, -21.52909115720838429, -68.78615194735675686 ) ) ;
#2240=CARTESIAN_POINT ( 'NONE',  ( 16.14559401701608365, -23.52718254156647149, -62.00720200095474155 ) ) ;
#2242=CARTESIAN_POINT ( 'NONE',  ( 11.27235727644277929, -9.289949671220924188, -35.08399737537874330 ) ) ;
#2250=FACE_OUTER_BOUND ( 'NONE', #33222, .T. ) ;
#2253=ADVANCED_FACE ( 'NONE', ( #43259 ), #39316, .T. ) ;
#2262=CARTESIAN_POINT ( 'NONE',  ( 22.20860492341360271, -20.58460539698850056, -76.23071345245209329 ) ) ;
#2276=CARTESIAN_POINT ( 'NONE',  ( 16.13393739769620083, -15.61618894467929941, -32.14999999999999858 ) ) ;
#2280=CARTESIAN_POINT ( 'NONE',  ( 22.00814659180725386, -11.71282814676025730, -50.66049260946093824 ) ) ;
#2283=CARTESIAN_POINT ( 'NONE',  ( 12.14974942666175828, -22.52868013065419461, -46.45904183493432527 ) ) ;
#2286=CARTESIAN_POINT ( 'NONE',  ( 9.148329271428000453, -14.64467554761950119, -71.89116613449289162 ) ) ;
#2287=ORIENTED_EDGE ( 'NONE', *, *, #49546, .F. ) ;
#2292=CARTESIAN_POINT ( 'NONE',  ( 18.20470697638991808, -7.911114290554745132, -41.09100108441210608 ) ) ;
#2295=CARTESIAN_POINT ( 'NONE',  ( 9.350953455536869185, -17.54846419477570052, -79.36448291391718612 ) ) ;
#2297=CARTESIAN_POINT ( 'NONE',  ( 17.16957190133613054, -7.705201370156754770, -67.33399687314600612 ) ) ;
#2304=CARTESIAN_POINT ( 'NONE',  ( 8.602773590722975428, -13.11400814803269732, -38.60984802764800605 ) ) ;
#2318=CARTESIAN_POINT ( 'NONE',  ( 24.02155121257710846, -14.98319770599232470, -33.76684429329586123 ) ) ;
#2323=CARTESIAN_POINT ( 'NONE',  ( 8.452546488159928373, -14.00902333825419888, -47.07814682104019255 ) ) ;
#2331=CARTESIAN_POINT ( 'NONE',  ( 9.414480144562521247, -17.75895664038510091, -45.74891888349859670 ) ) ;
#2352=CARTESIAN_POINT ( 'NONE',  ( 12.72604580451289813, -9.703220991147921026, -41.78615335765307037 ) ) ;
#2355=CARTESIAN_POINT ( 'NONE',  ( 15.45594426927969955, -22.63636586655560023, -44.98346683230629850 ) ) ;
#2361=CARTESIAN_POINT ( 'NONE',  ( 18.42797611233919852, -8.527907785417399467, -80.66697359201479856 ) ) ;
#2367=CARTESIAN_POINT ( 'NONE',  ( 24.04521450903870061, -15.61618868716203501, -63.50766715510244609 ) ) ;
#2368=CARTESIAN_POINT ( 'NONE',  ( 22.86433249997304884, -14.89035933162552539, -62.41863209491601339 ) ) ;
#2370=CARTESIAN_POINT ( 'NONE',  ( 16.13393739769620083, -15.61618894467929941, -32.14999999999999858 ) ) ;
#2375=ORIENTED_EDGE ( 'NONE', *, *, #11059, .T. ) ;
#2385=CARTESIAN_POINT ( 'NONE',  ( 20.16438269627179736, -8.423259725569389289, -67.45490599493020056 ) ) ;
#2390=CARTESIAN_POINT ( 'NONE',  ( 15.41773806569820060, -23.03196620144690243, -44.76330392965540028 ) ) ;
#2393=CARTESIAN_POINT ( 'NONE',  ( 8.222961267541252894, -14.58046671945546002, -50.83399806724860071 ) ) ;
#2395=CARTESIAN_POINT ( 'NONE',  ( 24.04493710079389146, -15.61360612403737314, -61.50757231037331962 ) ) ;
#2397=CARTESIAN_POINT ( 'NONE',  ( 19.43325479052089833, -23.17245954930830010, -59.87662587226670041 ) ) ;
#2406=CYLINDRICAL_SURFACE ( 'NONE', #28182, 7.910999999999997812 ) ;
#2408=FACE_OUTER_BOUND ( 'NONE', #1734, .T. ) ;
#2411=CARTESIAN_POINT ( 'NONE',  ( 11.65531868176484487, -9.064193434896999690, -65.10144457859644262 ) ) ;
#2425=CARTESIAN_POINT ( 'NONE',  ( 9.367299438200719308, -15.61632798465739924, -73.84717978381010539 ) ) ;
#2428=EDGE_CURVE ( 'NONE', #32624, #4643, #25526, .T. ) ;
#2440=CARTESIAN_POINT ( 'NONE',  ( 23.61408947799745661, -18.30540000354351449, -77.61739823543270234 ) ) ;
#2441=CARTESIAN_POINT ( 'NONE',  ( 16.13393739769620083, -15.61618894467929941, -23.15000000000000213 ) ) ;
#2442=ORIENTED_EDGE ( 'NONE', *, *, #1408, .T. ) ;
#2446=CARTESIAN_POINT ( 'NONE',  ( 16.13393739769620083, -27.61618894467930474, -22.14999999999999858 ) ) ;
#2450=CARTESIAN_POINT ( 'NONE',  ( 8.174661525294158793, -13.46383032146310121, -36.87639860437320038 ) ) ;
#2454=CARTESIAN_POINT ( 'NONE',  ( 16.59010301012261834, -22.43865132935006201, -50.93120400185586050 ) ) ;
#2455=CARTESIAN_POINT ( 'NONE',  ( 14.36263005250068758, -22.20704640813376685, -47.03613900106096679 ) ) ;
#2459=EDGE_CURVE ( 'NONE', #50858, #4288, #18686, .T. ) ;
#2463=CARTESIAN_POINT ( 'NONE',  ( 8.447399571967670440, -14.03382222439730143, -78.35213070062989971 ) ) ;
#2482=B_SPLINE_CURVE_WITH_KNOTS ( 'NONE', 3,
 ( #11034, #2910, #6581, #27512, #11291, #31174, #27252, #3686, #14696, #3168, #31428, #46949, #43266, #43514, #14955, #7618, #46690, #42492 ),
 .UNSPECIFIED., .F., .F.,
 ( 4, 2, 2, 2, 2, 2, 2, 2, 4 ),
 ( 0.3486532883837264452, 0.4300716273357606534, 0.5114899662877948616, 0.5929083052398289588, 0.6743266441918631671, 0.7557449831438973753, 0.8371633220959315835, 0.9185816610479657918, 1.000000000000000000 ),
 .UNSPECIFIED. ) ;
#2486=CARTESIAN_POINT ( 'NONE',  ( 22.55531972313694666, -17.79662447378222367, -62.55699137843335933 ) ) ;
#2488=B_SPLINE_CURVE_WITH_KNOTS ( 'NONE', 3,
 ( #34929, #47272, #15026, #30993, #11106, #28086, #51450, #19723, #39649, #19965, #43331, #44091, #43836, #35963, #39141, #47520, #11359, #7937, #3755, #7424, #8192, #27070, #43076, #24135, #23373, #40160, #31754, #39395, #11616, #27581, #43584, #35715, #51699, #15792, #47774, #11880, #8974 ),
 .UNSPECIFIED., .F., .F.,
 ( 4, 2, 2, 2, 2, 2, 2, 2, 2, 2, 2, 2, 2, 2, 1, 1, 1, 1, 1, 2, 4 ),
 ( 0.000000000000000000, 0.03125019491472925265, 0.06250038982945850530, 0.09375058474418775101, 0.1250007796589170106, 0.1562509745736462563, 0.1875011694883755020, 0.2187513644031047477, 0.2500015593178340212, 0.3125019491472925681, 0.3750023389767511151, 0.4375027288062096620, 0.4687529237209391297, 0.4843780211783040301, 0.4921905699069865081, 0.4960968442713278859, 0.4980499814534985470, 0.4990265500445839053, 0.4995148343401266122, 0.4997589764878979657, 0.5000031186356694857 ),
 .UNSPECIFIED. ) ;
#2491=CARTESIAN_POINT ( 'NONE',  ( 12.43868033672440099, -22.08548331050309699, -53.73253703038420070 ) ) ;
#2497=CARTESIAN_POINT ( 'NONE',  ( 23.78344371453452410, -17.69876028378456922, -61.59227590569546607 ) ) ;
#2499=CARTESIAN_POINT ( 'NONE',  ( 9.788743069423331278, -18.35763646220170031, -81.23899999999999011 ) ) ;
#2508=ORIENTED_EDGE ( 'NONE', *, *, #9627, .T. ) ;
#2511=CARTESIAN_POINT ( 'NONE',  ( 19.54191378771778531, -9.703268531717034406, -54.11948898031546662 ) ) ;
#2513=CIRCLE ( 'NONE', #38504, 12.00000000000000000 ) ;
#2515=CARTESIAN_POINT ( 'NONE',  ( 16.79377243150814536, -23.56734767625158256, -49.98149220073255350 ) ) ;
#2521=CARTESIAN_POINT ( 'NONE',  ( 22.21138144903229872, -10.65116916682739934, -71.79445331288948751 ) ) ;
#2523=EDGE_CURVE ( 'NONE', #26915, #43399, #47386, .T. ) ;
#2524=CARTESIAN_POINT ( 'NONE',  ( 23.13393739769620083, -15.61618894467929941, -82.15000000000000568 ) ) ;
#2530=LINE ( 'NONE', #22936, #6989 ) ;
#2533=CARTESIAN_POINT ( 'NONE',  ( 13.65479182716389950, -8.170345444894159925, -52.68519703601729987 ) ) ;
#2539=CARTESIAN_POINT ( 'NONE',  ( 21.88969301003089996, -11.69594164191370034, -32.14999999999999858 ) ) ;
#2547=EDGE_LOOP ( 'NONE', ( #23653, #6453, #1676 ) ) ;
#2549=CARTESIAN_POINT ( 'NONE',  ( 23.17868282713410011, -15.95400683938519926, -78.86243206809150763 ) ) ;
#2556=CARTESIAN_POINT ( 'NONE',  ( 20.99563651348813664, -9.290040531262853563, -77.50066261921593025 ) ) ;
#2559=CARTESIAN_POINT ( 'NONE',  ( 21.87115360135859987, -19.71825049090939785, -70.65040049691899071 ) ) ;
#2562=CARTESIAN_POINT ( 'NONE',  ( 24.04493737600856207, -16.65173076576985878, -41.54933394159128568 ) ) ;
#2563=CARTESIAN_POINT ( 'NONE',  ( 20.29254098389584726, -21.02756184446683463, -40.74443803683676890 ) ) ;
#2570=CARTESIAN_POINT ( 'NONE',  ( 19.60730040409203667, -8.442301474033923725, -39.15105660710381130 ) ) ;
#2571=CARTESIAN_POINT ( 'NONE',  ( 12.72599916435775214, -21.52913051451223225, -55.11948793158605753 ) ) ;
#2574=ORIENTED_EDGE ( 'NONE', *, *, #40111, .F. ) ;
#2582=CARTESIAN_POINT ( 'NONE',  ( 16.13393739769620083, -15.61618894467929941, -28.45282021618999835 ) ) ;
#2585=CARTESIAN_POINT ( 'NONE',  ( 17.01980719008272658, -8.849199162639587612, -51.99448548333836584 ) ) ;
#2587=CARTESIAN_POINT ( 'NONE',  ( 12.83474630336350053, -8.495649237981627522, -41.37438378445959586 ) ) ;
#2597=CARTESIAN_POINT ( 'NONE',  ( 9.202753043728490567, -16.92050586389959932, -41.78797233031760072 ) ) ;
#2608=EDGE_CURVE ( 'NONE', #50703, #22911, #42457, .T. ) ;
#2615=CARTESIAN_POINT ( 'NONE',  ( 24.04493739244504624, -14.58064021191867887, -69.46600480801545530 ) ) ;
#2624=CARTESIAN_POINT ( 'NONE',  ( 16.77661224428939590, -22.63968719969309973, -42.92377462465219651 ) ) ;
#2629=ORIENTED_EDGE ( 'NONE', *, *, #51660, .T. ) ;
#2630=CARTESIAN_POINT ( 'NONE',  ( 18.51684932252259941, -22.35565481394259990, -81.45916290265100201 ) ) ;
#2637=CARTESIAN_POINT ( 'NONE',  ( 23.79010008140480892, -17.67459298788599398, -75.87594074650500886 ) ) ;
#2638=CARTESIAN_POINT ( 'NONE',  ( 24.04493738655059687, -14.58064352360674043, -45.75066538883495326 ) ) ;
#2639=VECTOR ( 'NONE', #19715, 1000.000000000000000 ) ;
#2641=CARTESIAN_POINT ( 'NONE',  ( 9.653816277033588023, -20.24304174429426340, -46.31047858425840502 ) ) ;
#2646=CARTESIAN_POINT ( 'NONE',  ( 21.28881342178227243, -11.15893607458650294, -32.22570542542457162 ) ) ;
#2654=CARTESIAN_POINT ( 'NONE',  ( 16.13393739769620083, -15.61618894467929941, -41.53556505950739819 ) ) ;
#2656=CARTESIAN_POINT ( 'NONE',  ( 8.562943635882170668, -18.88157919922900163, -66.66271668429418185 ) ) ;
#2658=CARTESIAN_POINT ( 'NONE',  ( 22.90068744318051586, -15.61618870719606278, -70.84718393407784731 ) ) ;
#2662=CARTESIAN_POINT ( 'NONE',  ( 8.689358087320488977, -15.90762109230819910, -55.22020283005320351 ) ) ;
#2663=CARTESIAN_POINT ( 'NONE',  ( 9.375062053639432236, -18.97670595503450031, -32.14999999999999858 ) ) ;
#2664=CARTESIAN_POINT ( 'NONE',  ( 10.13166960481762757, -12.43500837955161309, -61.60803830279134274 ) ) ;
#2669=CARTESIAN_POINT ( 'NONE',  ( 8.974883818595877472, -12.14812015699499526, -60.65116565854415143 ) ) ;
#2671=CARTESIAN_POINT ( 'NONE',  ( 24.35155753959719860, -14.94280947335750120, -67.48164325437410582 ) ) ;
#2673=CARTESIAN_POINT ( 'NONE',  ( 20.61518557697189991, -22.02660557262029783, -32.14999999999999858 ) ) ;
#2687=CARTESIAN_POINT ( 'NONE',  ( 13.41159479355771467, -22.12244823249002224, -57.47332068091731827 ) ) ;
#2695=CARTESIAN_POINT ( 'NONE',  ( 11.27223392903683497, -21.94233489862524067, -76.21602140441011386 ) ) ;
#2703=LINE ( 'NONE', #11345, #48828 ) ;
#2711=DIRECTION ( 'NONE',  ( 0.000000000000000000, 0.000000000000000000, -1.000000000000000000 ) ) ;
#2721=CARTESIAN_POINT ( 'NONE',  ( 12.23243695589036761, -21.17135045914907820, -51.14773272228742940 ) ) ;
#2725=CARTESIAN_POINT ( 'NONE',  ( 10.22105554918047865, -12.20814692505701160, -63.61948725257905579 ) ) ;
#2732=CARTESIAN_POINT ( 'NONE',  ( 9.135602731787439978, -11.25659805155929938, -34.68500579403580275 ) ) ;
#2749=CARTESIAN_POINT ( 'NONE',  ( 20.29256185465771267, -21.02754514162187860, -62.74448681189702626 ) ) ;
#2752=ORIENTED_EDGE ( 'NONE', *, *, #32037, .F. ) ;
#2753=CARTESIAN_POINT ( 'NONE',  ( 17.36723456227180051, -22.96368324152579987, -51.51440696060289781 ) ) ;
#2761=CARTESIAN_POINT ( 'NONE',  ( 9.042768892828480176, -16.06693453323889997, -81.23899999999999011 ) ) ;
#2766=ORIENTED_EDGE ( 'NONE', *, *, #812, .F. ) ;
#2772=ORIENTED_EDGE ( 'NONE', *, *, #6864, .T. ) ;
#2773=CARTESIAN_POINT ( 'NONE',  ( 14.06329792164433101, -7.911078663674788736, -63.20899909920748883 ) ) ;
#2779=CARTESIAN_POINT ( 'NONE',  ( 10.83684432477319959, -19.82762902495380075, -81.23899999999999011 ) ) ;
#2792=CARTESIAN_POINT ( 'NONE',  ( 23.66220021668120310, -17.83249377738399843, -55.37864069218029073 ) ) ;
#2797=UNCERTAINTY_MEASURE_WITH_UNIT (LENGTH_MEASURE( 1.000000000000000082E-05 ), #44346, 'distance_accuracy_value', 'NONE');
#2803=CARTESIAN_POINT ( 'NONE',  ( 8.222911085862994796, -16.64130829724042115, -40.46641358909141672 ) ) ;
#2808=CARTESIAN_POINT ( 'NONE',  ( 20.49757756391890240, -10.07532225487519284, -36.55952288011872042 ) ) ;
#2809=CARTESIAN_POINT ( 'NONE',  ( 22.46008945880927499, -20.47788497429293031, -46.00070147826757250 ) ) ;
#2812=VECTOR ( 'NONE', #44702, 1000.000000000000000 ) ;
#2813=CARTESIAN_POINT ( 'NONE',  ( 20.07088694243709881, -21.46793974735500043, -73.15866903151078304 ) ) ;
#2820=CARTESIAN_POINT ( 'NONE',  ( 9.366881967297588929, -15.61636073738300112, -79.84717978380999170 ) ) ;
#2823=LINE ( 'NONE', #42395, #32065 ) ;
#2824=CARTESIAN_POINT ( 'NONE',  ( 20.99564842327679415, -21.94232784797836544, -41.79933425902736843 ) ) ;
#2825=CARTESIAN_POINT ( 'NONE',  ( 10.72251060975740877, -19.77472240810697102, -41.24444634761481154 ) ) ;
#2826=ORIENTED_EDGE ( 'NONE', *, *, #35749, .F. ) ;
#2827=CARTESIAN_POINT ( 'NONE',  ( 16.13393739769620083, -15.61618894467929941, -22.14999999999999858 ) ) ;
#2829=ORIENTED_EDGE ( 'NONE', *, *, #51342, .T. ) ;
#2846=CARTESIAN_POINT ( 'NONE',  ( 23.80355599767301555, -13.57222019766435039, -33.70949676018119590 ) ) ;
#2850=CARTESIAN_POINT ( 'NONE',  ( 24.04493740689873960, -16.65173053041055695, -53.54933808698535103 ) ) ;
#2852=CARTESIAN_POINT ( 'NONE',  ( 11.56509562211340025, -9.235559475632230786, -39.31469157680550097 ) ) ;
#2856=CARTESIAN_POINT ( 'NONE',  ( 10.72262850419906677, -11.45750429148510996, -77.66115289588985604 ) ) ;
#2858=CARTESIAN_POINT ( 'NONE',  ( 9.135435583350210109, -14.74238603266360137, -39.88671798479069963 ) ) ;
#2859=CARTESIAN_POINT ( 'NONE',  ( 22.90075166721855737, -15.61618922411645727, -44.45281379938008115 ) ) ;
#2863=CARTESIAN_POINT ( 'NONE',  ( 20.11811289261132885, -8.703692175439130096, -51.17433320692831700 ) ) ;
#2872=CARTESIAN_POINT ( 'NONE',  ( 18.20469613467166425, -23.32126666006107030, -58.20899800978780547 ) ) ;
#2873=CARTESIAN_POINT ( 'NONE',  ( 20.73040871625291715, -9.100038570834694696, -71.20348830954932851 ) ) ;
#2879=CARTESIAN_POINT ( 'NONE',  ( 9.543105373624433341, -13.84479165416296809, -41.53615350155577346 ) ) ;
#2882=CARTESIAN_POINT ( 'NONE',  ( 20.74023174533219915, -20.95703261207519930, -46.72628331570599869 ) ) ;
#2889=CARTESIAN_POINT ( 'NONE',  ( 9.244676780691371221, -12.77985576054640049, -80.19166000563309638 ) ) ;
#2891=EDGE_CURVE ( 'NONE', #27600, #14302, #17390, .T. ) ;
#2897=CARTESIAN_POINT ( 'NONE',  ( 9.366937397696199596, -15.61618894467949836, -28.45282021618999835 ) ) ;
#2909=CARTESIAN_POINT ( 'NONE',  ( 16.13393739769620083, -15.61618894467929941, -28.45282021618999835 ) ) ;
#2910=CARTESIAN_POINT ( 'NONE',  ( 21.80550130585419311, -19.38323868333978695, -32.63959037186587864 ) ) ;
#2913=CARTESIAN_POINT ( 'NONE',  ( 19.30279291186920076, -23.22809243764550047, -60.16676433707729643 ) ) ;
#2916=FACE_OUTER_BOUND ( 'NONE', #48205, .T. ) ;
#2920=CARTESIAN_POINT ( 'NONE',  ( 20.88369410565369932, -9.876284326973658878, -53.95269993303519840 ) ) ;
#2921=CARTESIAN_POINT ( 'NONE',  ( 9.015406492218581036, -14.49019859173800029, -32.14999999999999858 ) ) ;
#2927=CARTESIAN_POINT ( 'NONE',  ( 8.304045112041299248, -13.03248859362910039, -58.60912297524879477 ) ) ;
#2938=CARTESIAN_POINT ( 'NONE',  ( 16.23169237103991236, -7.684835125088456564, -65.29632762180530392 ) ) ;
#2946=LINE ( 'NONE', #19695, #33441 ) ;
#2949=CYLINDRICAL_SURFACE ( 'NONE', #22126, 6.766999999999998572 ) ;
#2962=ORIENTED_EDGE ( 'NONE', *, *, #35366, .T. ) ;
#2965=CARTESIAN_POINT ( 'NONE',  ( 13.58486031666897098, -23.12313378403861819, -78.11181520993953598 ) ) ;
#2968=ORIENTED_EDGE ( 'NONE', *, *, #2608, .F. ) ;
#2974=FACE_OUTER_BOUND ( 'NONE', #13672, .T. ) ;
#2978=CARTESIAN_POINT ( 'NONE',  ( 22.88218496723100159, -16.13676012226024170, -50.47731942806621674 ) ) ;
#2984=VECTOR ( 'NONE', #43778, 1000.000000000000000 ) ;
#2987=CARTESIAN_POINT ( 'NONE',  ( 10.09313298742930165, -21.22790907185699893, -36.26938441530820256 ) ) ;
#2989=ORIENTED_EDGE ( 'NONE', *, *, #47820, .F. ) ;
#3006=ADVANCED_FACE ( 'NONE', ( #24426 ), #9001, .T. ) ;
#3010=CARTESIAN_POINT ( 'NONE',  ( 23.39063669964830083, -17.30349732769349913, -65.14006310354538698 ) ) ;
#3017=DIRECTION ( 'NONE',  ( 0.8660254037844387076, 0.4999999999999998890, 0.000000000000000000 ) ) ;
#3021=ORIENTED_EDGE ( 'NONE', *, *, #3116, .F. ) ;
#3026=CARTESIAN_POINT ( 'NONE',  ( 22.62424293246530382, -11.35212744648809924, -81.23899999999999011 ) ) ;
#3031=VERTEX_POINT ( 'NONE', #17122 ) ;
#3035=VERTEX_POINT ( 'NONE', #29153 ) ;
#3036=CARTESIAN_POINT ( 'NONE',  ( 9.781452946156626638, -20.36976900595904283, -50.30319433359476733 ) ) ;
#3039=B_SPLINE_CURVE_WITH_KNOTS ( 'NONE', 3,
 ( #34854, #29875, #2646, #13919, #45895, #10249, #46422, #30401, #34328, #10510 ),
 .UNSPECIFIED., .F., .F.,
 ( 4, 2, 2, 2, 4 ),
 ( 0.000000000000000000, 0.08716332209593161129, 0.1743266441918632226, 0.2614899662877948616, 0.3486532883837264452 ),
 .UNSPECIFIED. ) ;
#3041=DIRECTION ( 'NONE',  ( 0.000000000000000000, 0.000000000000000000, -1.000000000000000000 ) ) ;
#3050=CARTESIAN_POINT ( 'NONE',  ( 12.31011725209880048, -8.763076682552949137, -50.62550482836309840 ) ) ;
#3059=CARTESIAN_POINT ( 'NONE',  ( 17.74966129736979781, -22.48146355349690140, -45.27360529711679504 ) ) ;
#3062=CARTESIAN_POINT ( 'NONE',  ( 24.04493711684570201, -15.61369914127065428, -45.50757579690004206 ) ) ;
#3066=CARTESIAN_POINT ( 'NONE',  ( 20.11811137678875738, -22.52868662009152700, -37.84100380649100970 ) ) ;
#3069=ADVANCED_FACE ( 'NONE', ( #49358 ), #28630, .T. ) ;
#3070=CARTESIAN_POINT ( 'NONE',  ( 17.86626912417429836, -8.779407102036641319, -74.42617192852868868 ) ) ;
#3106=CARTESIAN_POINT ( 'NONE',  ( 18.20470550922528119, -23.32126401386723202, -48.20899934070940418 ) ) ;
#3108=CARTESIAN_POINT ( 'NONE',  ( 18.20468139625259596, -23.32127082703616949, -53.92433694102878405 ) ) ;
#3109=CARTESIAN_POINT ( 'NONE',  ( 16.84904414660969962, -23.43126219636669916, -42.48344881935029349 ) ) ;
#3116=EDGE_CURVE ( 'NONE', #11348, #17454, #51187, .T. ) ;
#3117=CARTESIAN_POINT ( 'NONE',  ( 21.16241148139290118, -20.56159161423429893, -39.09452867415449617 ) ) ;
#3118=DIRECTION ( 'NONE',  ( 0.000000000000000000, 0.000000000000000000, -1.000000000000000000 ) ) ;
#3119=ORIENTED_EDGE ( 'NONE', *, *, #32389, .F. ) ;
#3128=CARTESIAN_POINT ( 'NONE',  ( 12.32273708341836915, -8.640312908610901843, -64.84861858487673203 ) ) ;
#3130=CARTESIAN_POINT ( 'NONE',  ( 23.83903819154209458, -17.68686180718279743, -57.87566458210246623 ) ) ;
#3131=CARTESIAN_POINT ( 'NONE',  ( 18.96081146330753597, -8.159879717317295444, -71.12286597728768811 ) ) ;
#3132=B_SPLINE_CURVE_WITH_KNOTS ( 'NONE', 3,
 ( #37543, #7394, #3721, #3467, #14737, #51420, #47743, #35418, #51164, #15514, #23852, #50899, #23600, #34900, #14991, #15257, #31468, #47492 ),
 .UNSPECIFIED., .F., .F.,
 ( 4, 2, 2, 2, 2, 2, 2, 2, 4 ),
 ( 0.000000000000000000, 0.06249980403246548771, 0.1249996080649309754, 0.1874994120973964562, 0.2499992161298619509, 0.3124990201623274455, 0.3749988241947929124, 0.4374986282272584348, 0.4999984322597239017 ),
 .UNSPECIFIED. ) ;
#3139=CARTESIAN_POINT ( 'NONE',  ( 9.367118387258660306, -15.61602127472129986, -41.45282021618999835 ) ) ;
#3142=CARTESIAN_POINT ( 'NONE',  ( 14.55382961656019880, -22.48974829167110201, -57.02474435397660102 ) ) ;
#3148=CARTESIAN_POINT ( 'NONE',  ( 14.53095738391709979, -7.933948783221270951, -32.72202640798520434 ) ) ;
#3162=CARTESIAN_POINT ( 'NONE',  ( 19.52320908822511569, -22.84352052172154401, -44.15244030110604712 ) ) ;
#3165=ORIENTED_EDGE ( 'NONE', *, *, #21582, .T. ) ;
#3168=CARTESIAN_POINT ( 'NONE',  ( 13.80921672251139931, -22.01564006803594964, -33.06388420368715941 ) ) ;
#3169=VECTOR ( 'NONE', #37471, 1000.000000000000000 ) ;
#3171=CARTESIAN_POINT ( 'NONE',  ( 9.618119672177739332, -20.66859821390469776, -58.58238571580489662 ) ) ;
#3172=CARTESIAN_POINT ( 'NONE',  ( 24.04523214473702097, -15.61618869705131729, -47.50766735973101618 ) ) ;
#3178=CARTESIAN_POINT ( 'NONE',  ( 23.37302340462380457, -17.37753149780470352, -50.30862910410869659 ) ) ;
#3188=CARTESIAN_POINT ( 'NONE',  ( 23.21148977389540136, -19.84596116917700215, -63.67913456332050259 ) ) ;
#3189=CARTESIAN_POINT ( 'NONE',  ( 22.02707644877200011, -20.53240942572870154, -32.14999999999999858 ) ) ;
#3192=CARTESIAN_POINT ( 'NONE',  ( 23.06214062797170072, -27.61618894467930119, -32.14999999999999858 ) ) ;
#3195=EDGE_LOOP ( 'NONE', ( #1272, #7409, #51083, #35729 ) ) ;
#3202=CARTESIAN_POINT ( 'NONE',  ( 20.58572098376589921, -9.642218563498740735, -79.93650932190229241 ) ) ;
#3205=EDGE_CURVE ( 'NONE', #32305, #6987, #34633, .T. ) ;
#3209=DIRECTION ( 'NONE',  ( 0.000000000000000000, 0.000000000000000000, -1.000000000000000000 ) ) ;
#3219=EDGE_LOOP ( 'NONE', ( #48871, #17949, #41493, #25278 ) ) ;
#3224=CARTESIAN_POINT ( 'NONE',  ( 14.84447007510781980, -23.42568434902701213, -78.05974216284950273 ) ) ;
#3231=CARTESIAN_POINT ( 'NONE',  ( 23.19779881621899875, -19.86867582181319847, -31.96482487842879650 ) ) ;
#3234=CARTESIAN_POINT ( 'NONE',  ( 9.787098110040155063, -18.04122145005927536, -51.33655066882005968 ) ) ;
#3242=EDGE_CURVE ( 'NONE', #16604, #49444, #38596, .T. ) ;
#3243=CARTESIAN_POINT ( 'NONE',  ( 9.366602974803960535, -15.61605382581650048, -49.84717978381009118 ) ) ;
#3247=CARTESIAN_POINT ( 'NONE',  ( 11.52974377330020062, -22.18186745672379701, -32.20281262070909634 ) ) ;
#3255=CARTESIAN_POINT ( 'NONE',  ( 24.04493740109851529, -16.65173145406349775, -37.83400117407241936 ) ) ;
#3259=CARTESIAN_POINT ( 'NONE',  ( 9.205734167420699166, -27.61618894467930119, -32.14999999999999858 ) ) ;
#3263=DIRECTION ( 'NONE',  ( -1.000000000000000000, 0.000000000000000000, 0.000000000000000000 ) ) ;
#3268=CARTESIAN_POINT ( 'NONE',  ( 19.50497178776589990, -22.26019537749590071, -69.41788538098089134 ) ) ;
#3270=ORIENTED_EDGE ( 'NONE', *, *, #33939, .T. ) ;
#3275=CARTESIAN_POINT ( 'NONE',  ( 9.543102826887107426, -13.84480091498138421, -73.53615355050735047 ) ) ;
#3276=VECTOR ( 'NONE', #34005, 1000.000000000000000 ) ;
#3277=CARTESIAN_POINT ( 'NONE',  ( 10.10545813131939852, -11.17681743330739863, -81.23899999999999011 ) ) ;
#3282=EDGE_LOOP ( 'NONE', ( #18547, #37830, #47118, #35387 ) ) ;
#3284=CARTESIAN_POINT ( 'NONE',  ( 23.56919067231890352, -15.75467248557949773, -81.23899999999999011 ) ) ;
#3286=CYLINDRICAL_SURFACE ( 'NONE', #36887, 6.766999999999998572 ) ;
#3288=CARTESIAN_POINT ( 'NONE',  ( 17.16947923318423008, -7.705188139706350192, -53.04933681370027188 ) ) ;
#3295=CARTESIAN_POINT ( 'NONE',  ( 22.85695788854713228, -14.82042754783183547, -40.41532941938547907 ) ) ;
#3296=ADVANCED_FACE ( 'NONE', ( #41938 ), #6038, .T. ) ;
#3297=FACE_OUTER_BOUND ( 'NONE', #27923, .T. ) ;
#3305=CARTESIAN_POINT ( 'NONE',  ( 21.03233565530110027, -9.484921319377349391, -53.00207276027180114 ) ) ;
#3310=UNCERTAINTY_MEASURE_WITH_UNIT (LENGTH_MEASURE( 1.000000000000000082E-05 ), #12066, 'distance_accuracy_value', 'NONE');
#3316=CARTESIAN_POINT ( 'NONE',  ( 22.89998289909242501, -16.39251803772393856, -44.88370135509944703 ) ) ;
#3320=CARTESIAN_POINT ( 'NONE',  ( 23.83903359263120336, -17.68688467594312996, -45.87568617554371286 ) ) ;
#3324=CARTESIAN_POINT ( 'NONE',  ( 21.42514567518789903, -10.37121405310790045, -32.81873922958869372 ) ) ;
#3332=CARTESIAN_POINT ( 'NONE',  ( 22.58711562570864118, -12.98538437038062021, -58.72346069000413848 ) ) ;
#3334=CARTESIAN_POINT ( 'NONE',  ( 8.222955670729223954, -16.65187018699299060, -42.46600177219022498 ) ) ;
#3339=APPLICATION_CONTEXT ( 'automotive_design' ) ;
#3343=CARTESIAN_POINT ( 'NONE',  ( 9.221362871281039375, -11.63214536758718154, -38.95899421604067214 ) ) ;
#3350=VERTEX_POINT ( 'NONE', #43927 ) ;
#3355=CARTESIAN_POINT ( 'NONE',  ( 21.47698520338149564, -11.41770701216577422, -46.24076139810592423 ) ) ;
#3362=CARTESIAN_POINT ( 'NONE',  ( 12.72603898113892917, -9.703224850274590807, -51.78615268828129814 ) ) ;
#3364=CARTESIAN_POINT ( 'NONE',  ( 17.29970893726160241, -23.37684125676760161, -52.46503413336629507 ) ) ;
#3367=CARTESIAN_POINT ( 'NONE',  ( 9.366931599644679807, -15.61636246440640008, -63.84717978381009118 ) ) ;
#3373=CARTESIAN_POINT ( 'NONE',  ( 22.00814659178010047, -11.71282814677829975, -50.66049260944289045 ) ) ;
#3375=EDGE_CURVE ( 'NONE', #27673, #17098, #39949, .T. ) ;
#3376=ORIENTED_EDGE ( 'NONE', *, *, #16874, .F. ) ;
#3383=CARTESIAN_POINT ( 'NONE',  ( 10.30441904797920216, -10.14968042360930056, -54.74717805172168994 ) ) ;
#3393=CARTESIAN_POINT ( 'NONE',  ( 18.95485614926927198, -23.03702254430130836, -32.17677060365137720 ) ) ;
#3398=ORIENTED_EDGE ( 'NONE', *, *, #47916, .F. ) ;
#3400=DIRECTION ( 'NONE',  ( 0.000000000000000000, 0.000000000000000000, -1.000000000000000000 ) ) ;
#3403=CARTESIAN_POINT ( 'NONE',  ( 10.50288950272969934, -11.36955989315870141, -57.65849580248539752 ) ) ;
#3408=CARTESIAN_POINT ( 'NONE',  ( 12.77237362966949874, -22.26499250170639854, -79.71634641925140841 ) ) ;
#3415=CARTESIAN_POINT ( 'NONE',  ( 8.223031589278729570, -15.61632747405269939, -32.50766849176289952 ) ) ;
#3429=CARTESIAN_POINT ( 'NONE',  ( 8.223340741289188571, -15.61635616670070092, -42.79233150823699816 ) ) ;
#3431=CARTESIAN_POINT ( 'NONE',  ( 24.36517369343270190, -16.09521827539409955, -63.81083516600379113 ) ) ;
#3437=B_SPLINE_CURVE_WITH_KNOTS ( 'NONE', 3,
 ( #14956, #34603, #47459, #15222, #27003, #43011, #10519, #39325, #47205, #50606, #6850, #26735, #27513, #46432, #26477, #42494, #6583, #31175 ),
 .UNSPECIFIED., .F., .F.,
 ( 4, 2, 2, 2, 2, 2, 2, 2, 4 ),
 ( 0.4999984322597239017, 0.5624986282272584903, 0.6249988241947930234, 0.6874990201623275565, 0.7499992161298620896, 0.8124994120973966227, 0.8749996080649310448, 0.9374998040324655779, 1.000000000000000000 ),
 .UNSPECIFIED. ) ;
#3439=CARTESIAN_POINT ( 'NONE',  ( 23.53416472175010199, -16.47835444936559668, -54.26957565728959310 ) ) ;
#3442=CARTESIAN_POINT ( 'NONE',  ( 9.718336914000449411, -19.70433485797880380, -32.14999999999999858 ) ) ;
#3448=CARTESIAN_POINT ( 'NONE',  ( 12.64353542633499927, -8.146261583098500125, -72.86853056670030071 ) ) ;
#3449=CARTESIAN_POINT ( 'NONE',  ( 21.21709022629629970, -21.48422859372540117, -32.14999999999999858 ) ) ;
#3461=LINE ( 'NONE', #23594, #41261 ) ;
#3462=CARTESIAN_POINT ( 'NONE',  ( 8.317988017466229067, -17.01659171872782750, -66.73595314439963033 ) ) ;
#3464=CARTESIAN_POINT ( 'NONE',  ( 23.06708755827619939, -12.88889676084650127, -70.11336187001349174 ) ) ;
#3467=CARTESIAN_POINT ( 'NONE',  ( 9.221449781846978055, -19.60038109878267321, -70.62566536415043572 ) ) ;
#3470=CARTESIAN_POINT ( 'NONE',  ( 16.29993763818361430, -23.52570124991906653, -62.00099320790554458 ) ) ;
#3471=CARTESIAN_POINT ( 'NONE',  ( 22.46009718676461375, -10.75450352810032051, -37.58400065247785449 ) ) ;
#3475=FACE_OUTER_BOUND ( 'NONE', #27619, .T. ) ;
#3478=CARTESIAN_POINT ( 'NONE',  ( 16.89732681591289776, -22.62759363779219868, -41.31265874393579907 ) ) ;
#3482=VERTEX_POINT ( 'NONE', #4041 ) ;
#3487=CARTESIAN_POINT ( 'NONE',  ( 14.08272732913061809, -23.27416204732341853, -78.09098556571072436 ) ) ;
#3495=CARTESIAN_POINT ( 'NONE',  ( 12.19021776734980023, -8.375346760609819086, -35.13358212097350020 ) ) ;
#3503=CARTESIAN_POINT ( 'NONE',  ( 9.898752574389790837, -20.38160789906219961, -74.80477269330690149 ) ) ;
#3511=CARTESIAN_POINT ( 'NONE',  ( 18.53886225874440186, -23.50282682920819965, -39.91345524423469726 ) ) ;
#3520=CARTESIAN_POINT ( 'NONE',  ( 14.36278677302630591, -22.20708724394357958, -49.03615438224388612 ) ) ;
#3524=CARTESIAN_POINT ( 'NONE',  ( 22.90093741918837722, -16.50198006501137016, -64.49448900876036816 ) ) ;
#3532=CARTESIAN_POINT ( 'NONE',  ( 23.50430387603210036, -14.52789104733479952, -61.02067868823719721 ) ) ;
#3537=CIRCLE ( 'NONE', #31112, 9.703299832284479010 ) ;
#3541=CARTESIAN_POINT ( 'NONE',  ( 9.072718278985821172, -13.88952453628539985, -81.23899999999999011 ) ) ;
#3544=EDGE_CURVE ( 'NONE', #13029, #17698, #39292, .T. ) ;
#3546=VERTEX_POINT ( 'NONE', #17130 ) ;
#3548=CARTESIAN_POINT ( 'NONE',  ( 23.33198322512879841, -13.07647044784360091, -81.23899999999999011 ) ) ;
#3549=ADVANCED_FACE ( 'NONE', ( #13211 ), #33351, .T. ) ;
#3552=CARTESIAN_POINT ( 'NONE',  ( 24.04493738849360795, -14.58064088933272373, -53.46600475365202954 ) ) ;
#3561=CARTESIAN_POINT ( 'NONE',  ( 22.90093739503438641, -15.61216303397516647, -40.45263532482819357 ) ) ;
#3562=EDGE_CURVE ( 'NONE', #43383, #48498, #39432, .T. ) ;
#3571=CARTESIAN_POINT ( 'NONE',  ( 23.80689242842739972, -13.96921921831510005, -55.22020283005320351 ) ) ;
#3579=CYLINDRICAL_SURFACE ( 'NONE', #18691, 7.910999999999997812 ) ;
#3583=CARTESIAN_POINT ( 'NONE',  ( 23.83903782902317303, -17.68686365390393078, -37.59100454951404657 ) ) ;
#3585=ORIENTED_EDGE ( 'NONE', *, *, #18831, .F. ) ;
#3586=CARTESIAN_POINT ( 'NONE',  ( 23.55010335841370051, -14.90402549293309953, -35.03686929936998951 ) ) ;
#3600=EDGE_CURVE ( 'NONE', #5111, #28199, #28726, .T. ) ;
#3603=CARTESIAN_POINT ( 'NONE',  ( 11.27219059296783854, -9.290075776696600229, -39.08399250801967639 ) ) ;
#3613=CARTESIAN_POINT ( 'NONE',  ( 16.65209534521472889, -8.850437320969684052, -45.97722336490771511 ) ) ;
#3617=ORIENTED_EDGE ( 'NONE', *, *, #17482, .T. ) ;
#3622=CARTESIAN_POINT ( 'NONE',  ( 18.72609985679629929, -23.02344493979749629, -50.40534192571220018 ) ) ;
#3630=CARTESIAN_POINT ( 'NONE',  ( 15.24819415861908212, -22.38319558909093487, -38.99448831724205888 ) ) ;
#3631=CARTESIAN_POINT ( 'NONE',  ( 9.141711747553159739, -14.69350826755799844, -55.88894205964179207 ) ) ;
#3632=CARTESIAN_POINT ( 'NONE',  ( 10.22096416429083554, -12.20830314663815663, -43.61946976819260868 ) ) ;
#3636=CARTESIAN_POINT ( 'NONE',  ( 8.428878250350352985, -13.54536072994490326, -50.59100158115866464 ) ) ;
#3644=FACE_OUTER_BOUND ( 'NONE', #17708, .T. ) ;
#3657=CARTESIAN_POINT ( 'NONE',  ( 20.38450248183900015, -21.24426633950000110, -52.74692207654109666 ) ) ;
#3662=ORIENTED_EDGE ( 'NONE', *, *, #28140, .F. ) ;
#3664=CARTESIAN_POINT ( 'NONE',  ( 21.36084080367719906, -21.46992527011509821, -45.55549324029160374 ) ) ;
#3672=EDGE_CURVE ( 'NONE', #33168, #36842, #26002, .T. ) ;
#3678=VERTEX_POINT ( 'NONE', #14482 ) ;
#3679=CARTESIAN_POINT ( 'NONE',  ( 24.04145801234410129, -15.86957246127301424, -43.80251945200132724 ) ) ;
#3684=CARTESIAN_POINT ( 'NONE',  ( 14.06320179395276071, -23.32127433849228382, -62.37566354910524069 ) ) ;
#3686=CARTESIAN_POINT ( 'NONE',  ( 16.03039053705856887, -22.42402112133541792, -32.95781074573184100 ) ) ;
#3688=CARTESIAN_POINT ( 'NONE',  ( 12.76833210023839982, -23.14316848747460043, -74.42617192852888763 ) ) ;
#3694=EDGE_LOOP ( 'NONE', ( #903, #5641, #2989, #46289 ) ) ;
#3695=CARTESIAN_POINT ( 'NONE',  ( 22.16647721471450083, -11.24410052365730017, -62.03303090152439125 ) ) ;
#3697=CARTESIAN_POINT ( 'NONE',  ( 10.37974942112630039, -20.72019953162940098, -32.14999999999999858 ) ) ;
#3703=CARTESIAN_POINT ( 'NONE',  ( 19.38037798442189796, -23.19532769692779794, -75.87884994711779996 ) ) ;
#3715=CARTESIAN_POINT ( 'NONE',  ( 8.222787824498201559, -15.61638397318239946, -64.79233150823698395 ) ) ;
#3718=CARTESIAN_POINT ( 'NONE',  ( 18.08382399952279940, -22.80678252554330143, -72.64836766404950197 ) ) ;
#3721=CARTESIAN_POINT ( 'NONE',  ( 8.428860607946825567, -17.68695301239758777, -70.70899843619372405 ) ) ;
#3725=CARTESIAN_POINT ( 'NONE',  ( 22.90078883224852291, -15.66462347074845596, -40.45510235809472732 ) ) ;
#3733=DIRECTION ( 'NONE',  ( 0.000000000000000000, 0.000000000000000000, -1.000000000000000000 ) ) ;
#3741=CARTESIAN_POINT ( 'NONE',  ( 24.04466642925503095, -15.61618863334376250, -55.79233649161735542 ) ) ;
#3750=CARTESIAN_POINT ( 'NONE',  ( 8.222496981792570381, -15.61604333543320067, -34.50766849176299900 ) ) ;
#3752=CARTESIAN_POINT ( 'NONE',  ( 11.33371065636610098, -8.912418118662481348, -39.09452867415449617 ) ) ;
#3754=VECTOR ( 'NONE', #30945, 1000.000000000000000 ) ;
#3755=CARTESIAN_POINT ( 'NONE',  ( 20.57778927394911861, -22.22610635818881875, -50.10404926845265550 ) ) ;
#3759=CARTESIAN_POINT ( 'NONE',  ( 15.27045073980099943, -23.41626191762090059, -76.54758917670669405 ) ) ;
#3766=B_SPLINE_CURVE_WITH_KNOTS ( 'NONE', 3,
 ( #47660, #3897, #35854, #7310, #3383, #35335, #11767, #25064, #36886, #36355, #28753, #987, #29017, #32934, #44495, #40559, #16194, #4140, #41080, #464, #5193, #24027, #211, #1249, #21146, #16985, #28231, #32404, #48960 ),
 .UNSPECIFIED., .F., .F.,
 ( 4, 2, 2, 2, 2, 2, 2, 2, 2, 2, 1, 1, 1, 1, 1, 2, 4 ),
 ( 0.000000000000000000, 0.06250045598305266348, 0.1250009119661053270, 0.1875013679491579766, 0.2500018239322106539, 0.3125022799152633035, 0.3750027358983159531, 0.4375031918813686582, 0.4687534198728949830, 0.4843785338686582564, 0.4921910908665399487, 0.4960973693654808225, 0.4980505086149513150, 0.4990270782396864502, 0.4995153630520540733, 0.4997595054582379404, 0.5000036478644217519 ),
 .UNSPECIFIED. ) ;
#3767=CARTESIAN_POINT ( 'NONE',  ( 17.05134355889540032, -7.422222466570630672, -47.04315903996049286 ) ) ;
#3768=ORIENTED_EDGE ( 'NONE', *, *, #20321, .F. ) ;
#3785=CARTESIAN_POINT ( 'NONE',  ( 20.11801398371856919, -8.703633029438034185, -75.45904336070280749 ) ) ;
#3786=CARTESIAN_POINT ( 'NONE',  ( 11.97525993411146139, -21.02750440564567924, -63.16115020960447168 ) ) ;
#3790=CARTESIAN_POINT ( 'NONE',  ( 23.54258513496609950, -16.40272123479050137, -69.10100965672640427 ) ) ;
#3795=CARTESIAN_POINT ( 'NONE',  ( 22.89700924243567570, -15.86553210016712256, -34.46454548921436611 ) ) ;
#3798=CARTESIAN_POINT ( 'NONE',  ( 10.07131628902749831, -11.23148262131390140, -81.23899999999999011 ) ) ;
#3805=CARTESIAN_POINT ( 'NONE',  ( 23.51291121479609814, -16.19875826520710049, -81.23899999999999011 ) ) ;
#3808=CARTESIAN_POINT ( 'NONE',  ( 18.14187589073995710, -9.105712570752443114, -80.04820986649650649 ) ) ;
#3809=EDGE_LOOP ( 'NONE', ( #48930, #11439, #41179, #33989 ) ) ;
#3818=CARTESIAN_POINT ( 'NONE',  ( 9.366488261363459245, -15.61629045172390029, -39.45282021618999835 ) ) ;
#3822=CARTESIAN_POINT ( 'NONE',  ( 15.57679709041789984, -22.64698931536659998, -43.37235095159000053 ) ) ;
#3824=CARTESIAN_POINT ( 'NONE',  ( 8.307315901316570717, -15.04108535784360079, -66.31085317895978903 ) ) ;
#3839=CARTESIAN_POINT ( 'NONE',  ( 11.27234542262131889, -21.94241925001478322, -38.21600269195644017 ) ) ;
#3840=CARTESIAN_POINT ( 'NONE',  ( 23.04645466576749513, -11.63204637672123276, -71.62566002335191229 ) ) ;
#3842=CARTESIAN_POINT ( 'NONE',  ( 21.37438191210599925, -20.33663280004660123, -81.08056213787280342 ) ) ;
#3843=CARTESIAN_POINT ( 'NONE',  ( 17.01970131259685459, -22.38319384293092895, -76.91116700029822084 ) ) ;
#3850=CARTESIAN_POINT ( 'NONE',  ( 22.90077909847273219, -15.61618896438501203, -58.84717277627543552 ) ) ;
#3853=EDGE_CURVE ( 'NONE', #33352, #667, #18974, .T. ) ;
#3856=EDGE_LOOP ( 'NONE', ( #24963, #23173, #26739, #46276 ) ) ;
#3858=DIRECTION ( 'NONE',  ( 0.000000000000000000, 0.000000000000000000, -1.000000000000000000 ) ) ;
#3860=CARTESIAN_POINT ( 'NONE',  ( 13.52272076457530048, -9.064539772954379515, -62.22645654473139842 ) ) ;
#3865=VECTOR ( 'NONE', #26245, 1000.000000000000000 ) ;
#3876=CARTESIAN_POINT ( 'NONE',  ( 20.64167000759333348, -10.49200264909508995, -34.18273036881165439 ) ) ;
#3879=CARTESIAN_POINT ( 'NONE',  ( 20.44785949262530167, -22.17186005833840312, -58.32723503207409976 ) ) ;
#3887=CARTESIAN_POINT ( 'NONE',  ( 22.90093739769620029, -15.61618894467913243, -28.45282021618999835 ) ) ;
#3888=CARTESIAN_POINT ( 'NONE',  ( 21.43993832425640278, -20.26257607252319914, -49.07611398817049775 ) ) ;
#3892=EDGE_CURVE ( 'NONE', #18872, #38732, #21031, .T. ) ;
#3897=CARTESIAN_POINT ( 'NONE',  ( 8.222915678894278102, -14.38730632297055045, -54.55712915330399682 ) ) ;
#3900=AXIS2_PLACEMENT_3D ( 'NONE', #12611, #29097, #28574 ) ;
#3901=CARTESIAN_POINT ( 'NONE',  ( 9.410656861959711961, -11.36542763060938555, -64.68701949937872087 ) ) ;
#3909=ORIENTED_EDGE ( 'NONE', *, *, #15800, .T. ) ;
#3915=CARTESIAN_POINT ( 'NONE',  ( 22.98684880019740362, -17.28357132616680047, -50.52879200675969429 ) ) ;
#3922=CARTESIAN_POINT ( 'NONE',  ( 16.49996568077149917, -7.777007132833650083, -40.80235737647439720 ) ) ;
#3923=EDGE_CURVE ( 'NONE', #41326, #5472, #17124, .T. ) ;
#3924=VERTEX_POINT ( 'NONE', #36499 ) ;
#3937=CARTESIAN_POINT ( 'NONE',  ( 8.277338810346954290, -14.47788413087303638, -76.55341515652921203 ) ) ;
#3939=CARTESIAN_POINT ( 'NONE',  ( 14.96646045001671865, -7.755344280765369191, -48.96083666094899201 ) ) ;
#3947=CARTESIAN_POINT ( 'NONE',  ( 16.77504506022210151, -7.395988155100910788, -73.31710689363809763 ) ) ;
#3949=CARTESIAN_POINT ( 'NONE',  ( 24.04493739769619864, -15.61618894467929941, -32.14999999999999858 ) ) ;
#3951=CARTESIAN_POINT ( 'NONE',  ( 16.27864033302759950, -23.06506502538119818, -64.72647455768748159 ) ) ;
#3955=CARTESIAN_POINT ( 'NONE',  ( 10.35872898856410096, -20.69271781505580066, -32.14999999999999858 ) ) ;
#3959=DIRECTION ( 'NONE',  ( 0.000000000000000000, 0.000000000000000000, -1.000000000000000000 ) ) ;
#3961=CARTESIAN_POINT ( 'NONE',  ( 24.02699963285100182, -17.99994423013719924, -71.60102766968249455 ) ) ;
#3963=CARTESIAN_POINT ( 'NONE',  ( 21.54526424423086439, -11.45752564796633699, -60.24446586214138932 ) ) ;
#3967=ORIENTED_EDGE ( 'NONE', *, *, #18742, .F. ) ;
#3972=CARTESIAN_POINT ( 'NONE',  ( 8.687503549248530632, -15.85559810456780028, -71.22242690490419648 ) ) ;
#3978=VERTEX_POINT ( 'NONE', #869 ) ;
#3983=DIRECTION ( 'NONE',  ( 0.000000000000000000, 0.000000000000000000, 1.000000000000000000 ) ) ;
#3998=ORIENTED_EDGE ( 'NONE', *, *, #51342, .F. ) ;
#4002=CARTESIAN_POINT ( 'NONE',  ( 8.715470921945700056, -12.01770659734159885, -38.93609081202730238 ) ) ;
#4003=CARTESIAN_POINT ( 'NONE',  ( 8.222941217535151281, -16.65176438257585900, -68.46600170818715014 ) ) ;
#4007=CARTESIAN_POINT ( 'NONE',  ( 14.06334520972920288, -23.32131147013534189, -42.37566460173350436 ) ) ;
#4008=CARTESIAN_POINT ( 'NONE',  ( 8.705489043054660314, -15.04623381650379876, -35.25703220202099430 ) ) ;
#4010=EDGE_CURVE ( 'NONE', #19315, #47534, #12437, .T. ) ;
#4017=CARTESIAN_POINT ( 'NONE',  ( 17.02638215719250070, -23.81291164709050179, -41.97314745188879215 ) ) ;
#4021=CARTESIAN_POINT ( 'NONE',  ( 24.01727330109450165, -16.33183074238797872, -39.53649162746054913 ) ) ;
#4023=CARTESIAN_POINT ( 'NONE',  ( 22.90070561427262064, -15.61618657793558818, -56.45282510079097449 ) ) ;
#4037=CARTESIAN_POINT ( 'NONE',  ( 9.367501421782780113, -15.61622054991689978, -37.45282021618999835 ) ) ;
#4041=CARTESIAN_POINT ( 'NONE',  ( 24.04523903120960782, -15.61618918343368101, -41.50766953063602926 ) ) ;
#4045=CARTESIAN_POINT ( 'NONE',  ( 10.05451364342030018, -11.25897035538629964, -81.23899999999999011 ) ) ;
#4051=CARTESIAN_POINT ( 'NONE',  ( 22.65381097660240428, -11.40563906863610022, -81.23899999999999011 ) ) ;
#4064=CARTESIAN_POINT ( 'NONE',  ( 9.581787940992585462, -13.67368164010640186, -39.54428995716352802 ) ) ;
#4072=CARTESIAN_POINT ( 'NONE',  ( 20.92727658674290225, -21.82993560848299808, -67.57835607597769467 ) ) ;
#4074=CARTESIAN_POINT ( 'NONE',  ( 22.80253552484781210, -13.86357800176847199, -76.76474318907416716 ) ) ;
#4084=CARTESIAN_POINT ( 'NONE',  ( 14.06330850377756292, -23.32130196735118588, -54.37566615248211122 ) ) ;
#4086=CARTESIAN_POINT ( 'NONE',  ( 18.76418403170740135, -22.58673428566360286, -33.45249067809769628 ) ) ;
#4087=CARTESIAN_POINT ( 'NONE',  ( 10.22099316920907697, -19.02412432503898287, -77.28616187159222761 ) ) ;
#4088=EDGE_LOOP ( 'NONE', ( #3909, #18481, #33156, #2442 ) ) ;
#4095=CARTESIAN_POINT ( 'NONE',  ( 9.807855859684124766, -10.75440353299834584, -66.71600124055041192 ) ) ;
#4100=DIRECTION ( 'NONE',  ( 0.000000000000000000, 0.000000000000000000, -1.000000000000000000 ) ) ;
#4102=CARTESIAN_POINT ( 'NONE',  ( 23.83903634813313843, -13.54550697675067283, -79.70900030893358235 ) ) ;
#4113=CARTESIAN_POINT ( 'NONE',  ( 21.54530141090581452, -11.45757666743581638, -36.24448471271439587 ) ) ;
#4117=TOROIDAL_SURFACE ( 'NONE', #22626, 7.050000000000200551, 2.999999999999960032 ) ;
#4123=CARTESIAN_POINT ( 'NONE',  ( 2.277530937145189949, -15.61618894467929941, -24.14999999999999858 ) ) ;
#4125=CARTESIAN_POINT ( 'NONE',  ( 23.83408638490000087, -14.10144369664360120, -55.95066710016559597 ) ) ;
#4131=CARTESIAN_POINT ( 'NONE',  ( 11.55539561595339926, -20.98084311128560131, -55.57206633538729790 ) ) ;
#4140=CARTESIAN_POINT ( 'NONE',  ( 23.97633652620590183, -14.55430446190974969, -55.46484585604141415 ) ) ;
#4141=CARTESIAN_POINT ( 'NONE',  ( 22.04683749721616692, -12.20817609659607328, -76.28613765794165147 ) ) ;
#4143=CARTESIAN_POINT ( 'NONE',  ( 18.71043739769620018, -15.61618894467929941, -40.14999999999999858 ) ) ;
#4148=VERTEX_POINT ( 'NONE', #21809 ) ;
#4155=DIRECTION ( 'NONE',  ( 1.060511545910580040E-15, 5.351958659602149705E-17, -1.000000000000000000 ) ) ;
#4158=CARTESIAN_POINT ( 'NONE',  ( 12.80387281675960054, -9.399016871829989128, -51.79629490377769940 ) ) ;
#4163=CARTESIAN_POINT ( 'NONE',  ( 16.98336371009930090, -23.41780564399109821, -41.75298454923780156 ) ) ;
#4170=DIRECTION ( 'NONE',  ( 1.000000000000000000, 0.000000000000000000, 0.000000000000000000 ) ) ;
#4177=CARTESIAN_POINT ( 'NONE',  ( 24.04471994510320343, -15.67954950804986680, -43.79487400242773276 ) ) ;
#4183=CARTESIAN_POINT ( 'NONE',  ( 22.46009133970864369, -20.47788239125953424, -62.00066238588659218 ) ) ;
#4185=CARTESIAN_POINT ( 'NONE',  ( 24.04477596867337041, -15.61618922203197357, -43.50766101656756746 ) ) ;
#4187=CARTESIAN_POINT ( 'NONE',  ( 9.019481128741650977, -19.78359005965110029, -70.62366323747509966 ) ) ;
#4193=CARTESIAN_POINT ( 'NONE',  ( 9.274006477917760449, -12.70963745175619941, -65.36022600619639888 ) ) ;
#4196=CARTESIAN_POINT ( 'NONE',  ( 12.55905327122290061, -22.66178945083330021, -32.14999999999999858 ) ) ;
#4205=CARTESIAN_POINT ( 'NONE',  ( 9.670066446664469240, -20.73488927165520224, -74.29447132584539304 ) ) ;
#4215=CARTESIAN_POINT ( 'NONE',  ( 23.24841639254534087, -19.17784153847612316, -65.93991975907368897 ) ) ;
#4217=CARTESIAN_POINT ( 'NONE',  ( 11.16173748537739918, -21.16451498386290098, -72.96524338830400325 ) ) ;
#4239=ORIENTED_EDGE ( 'NONE', *, *, #13488, .F. ) ;
#4250=CARTESIAN_POINT ( 'NONE',  ( 21.60595093793588006, -21.40777320653291937, -65.76646804696460435 ) ) ;
#4251=CARTESIAN_POINT ( 'NONE',  ( 11.51910120158669848, -22.44890487167439730, -44.48141598648059158 ) ) ;
#4256=DIRECTION ( 'NONE',  ( 0.000000000000000000, 0.000000000000000000, -1.000000000000000000 ) ) ;
#4257=CARTESIAN_POINT ( 'NONE',  ( 23.54000810228229668, -16.42662742094869799, -38.26735158243859303 ) ) ;
#4262=CARTESIAN_POINT ( 'NONE',  ( 24.03244302888166217, -16.09623076095370209, -59.81164409149027250 ) ) ;
#4264=CYLINDRICAL_SURFACE ( 'NONE', #16195, 7.910999999999997812 ) ;
#4265=CARTESIAN_POINT ( 'NONE',  ( 14.97627619889470019, -7.452700642625790017, -38.96282807147130001 ) ) ;
#4270=DIRECTION ( 'NONE',  ( -1.000000000000000000, 0.000000000000000000, 0.000000000000000000 ) ) ;
#4286=CARTESIAN_POINT ( 'NONE',  ( 18.20470492032551846, -7.911113710251287401, -73.09100141137088258 ) ) ;
#4288=VERTEX_POINT ( 'NONE', #34635 ) ;
#4291=CARTESIAN_POINT ( 'NONE',  ( 22.90065656494205726, -15.61616387038935017, -34.45281736178981902 ) ) ;
#4292=CARTESIAN_POINT ( 'NONE',  ( 10.32524240406999994, -10.84237056084089978, -81.23899999999999011 ) ) ;
#4299=CARTESIAN_POINT ( 'NONE',  ( 18.77361538871150159, -21.88214511621840330, -81.23899999999999011 ) ) ;
#4300=EDGE_CURVE ( 'NONE', #40766, #40450, #5593, .T. ) ;
#4302=CARTESIAN_POINT ( 'NONE',  ( 24.04493739743120173, -14.58064912574057992, -73.75066485288634510 ) ) ;
#4303=EDGE_CURVE ( 'NONE', #20658, #37252, #3132, .T. ) ;
#4305=CARTESIAN_POINT ( 'NONE',  ( 10.11051084926620014, -19.28509774568809831, -69.67303606471168109 ) ) ;
#4311=DIRECTION ( 'NONE',  ( 0.000000000000000000, 0.000000000000000000, -1.000000000000000000 ) ) ;
#4325=CARTESIAN_POINT ( 'NONE',  ( 22.00167714248629736, -20.82736716755679751, -65.51866386832359979 ) ) ;
#4329=LINE ( 'NONE', #8787, #43662 ) ;
#4335=CARTESIAN_POINT ( 'NONE',  ( 8.223596773276058869, -15.61622589296290009, -36.79233150823699816 ) ) ;
#4342=LINE ( 'NONE', #43924, #15577 ) ;
#4344=CARTESIAN_POINT ( 'NONE',  ( 18.30559885472430182, -8.906037589390139786, -80.44681068936390034 ) ) ;
#4354=CARTESIAN_POINT ( 'NONE',  ( 8.428842546461108753, -17.68688734103686500, -52.42433491449200034 ) ) ;
#4355=ORIENTED_EDGE ( 'NONE', *, *, #17566, .F. ) ;
#4358=ORIENTED_EDGE ( 'NONE', *, *, #8638, .F. ) ;
#4364=ORIENTED_EDGE ( 'NONE', *, *, #6824, .F. ) ;
#4377=AXIS2_PLACEMENT_3D ( 'NONE', #9647, #26640, #18271 ) ;
#4379=CARTESIAN_POINT ( 'NONE',  ( 19.55461702279360026, -22.74941205225439944, -32.14999999999999858 ) ) ;
#4380=LINE ( 'NONE', #36088, #4452 ) ;
#4381=CARTESIAN_POINT ( 'NONE',  ( 19.61313273130900114, -22.65052952657820029, -54.36628847889309668 ) ) ;
#4385=CARTESIAN_POINT ( 'NONE',  ( 16.13393739769620083, -15.61618894467929941, -28.45282021618999835 ) ) ;
#4389=CARTESIAN_POINT ( 'NONE',  ( 9.096621006920289076, -15.14849546539219993, -49.86830329880680068 ) ) ;
#4397=CARTESIAN_POINT ( 'NONE',  ( 9.367432603602109609, -15.61609789975089946, -77.84717978380999170 ) ) ;
#4404=CARTESIAN_POINT ( 'NONE',  ( 20.99565372478078729, -21.94232361745867621, -73.79933465604877085 ) ) ;
#4417=CARTESIAN_POINT ( 'NONE',  ( 19.17564323794969994, -9.252967725988789027, -62.09475594204819515 ) ) ;
#4420=CARTESIAN_POINT ( 'NONE',  ( 18.20469955901954862, -23.32126569534955962, -80.20899953292267526 ) ) ;
#4429=FACE_OUTER_BOUND ( 'NONE', #6380, .T. ) ;
#4432=CARTESIAN_POINT ( 'NONE',  ( 17.16941045954151690, -7.705178316448852094, -75.04930124495368204 ) ) ;
#4440=CARTESIAN_POINT ( 'NONE',  ( 15.09838727772565647, -23.52718862466428718, -36.04933377307653330 ) ) ;
#4444=CARTESIAN_POINT ( 'NONE',  ( 24.31683970193839883, -16.62753949476709892, -69.83147392683889620 ) ) ;
#4451=CARTESIAN_POINT ( 'NONE',  ( 17.14173437892020146, -8.234384351642349387, -63.77584738492399197 ) ) ;
#4452=VECTOR ( 'NONE', #48150, 1000.000000000000000 ) ;
#4454=CARTESIAN_POINT ( 'NONE',  ( 18.71043739769620018, -15.61618894467929941, -22.64999999999999858 ) ) ;
#4457=FACE_OUTER_BOUND ( 'NONE', #46813, .T. ) ;
#4459=CARTESIAN_POINT ( 'NONE',  ( 23.31098559560239991, -11.55753154673280036, -73.34384415308208816 ) ) ;
#4463=CYLINDRICAL_SURFACE ( 'NONE', #8996, 6.766999999999998572 ) ;
#4464=DIRECTION ( 'NONE',  ( 1.000000000000000000, 2.460964292799963328E-14, 0.000000000000000000 ) ) ;
#4472=CARTESIAN_POINT ( 'NONE',  ( 23.04644707764643741, -19.60034574208615510, -71.95901429853738307 ) ) ;
#4474=CARTESIAN_POINT ( 'NONE',  ( 9.101765327396449834, -15.07663851068110006, -35.47719510467199910 ) ) ;
#4493=VERTEX_POINT ( 'NONE', #19818 ) ;
#4494=ORIENTED_EDGE ( 'NONE', *, *, #17547, .T. ) ;
#4496=ORIENTED_EDGE ( 'NONE', *, *, #12191, .T. ) ;
#4497=CYLINDRICAL_SURFACE ( 'NONE', #50152, 6.766999999999998572 ) ;
#4499=CARTESIAN_POINT ( 'NONE',  ( 18.66275191049972193, -9.321185306396447601, -50.07447558512664187 ) ) ;
#4503=CARTESIAN_POINT ( 'NONE',  ( 24.04493739922218509, -15.61697502474068244, -65.50769812753713950 ) ) ;
#4504=CARTESIAN_POINT ( 'NONE',  ( 16.88526009776989767, -23.82704969470360012, -42.26328591669929580 ) ) ;
#4510=CARTESIAN_POINT ( 'NONE',  ( 23.02829992630010025, -12.79228046009130004, -38.10891372031129976 ) ) ;
#4511=CARTESIAN_POINT ( 'NONE',  ( 11.72631995337559907, -10.41982837502230019, -32.14999999999999858 ) ) ;
#4516=CARTESIAN_POINT ( 'NONE',  ( 8.654671703226251012, -12.14584236537350037, -38.64595234721679162 ) ) ;
#4517=ORIENTED_EDGE ( 'NONE', *, *, #25718, .T. ) ;
#4523=CARTESIAN_POINT ( 'NONE',  ( 22.90093474723966338, -15.62310588710952430, -56.45315049504032601 ) ) ;
#4528=CARTESIAN_POINT ( 'NONE',  ( 22.90114886013774864, -15.61618877916400017, -48.45281860778688809 ) ) ;
#4535=CARTESIAN_POINT ( 'NONE',  ( 24.03381927417788688, -15.16328978430293617, -75.77410088211345851 ) ) ;
#4540=CARTESIAN_POINT ( 'NONE',  ( 8.428888066787989075, -13.54532504059405262, -72.59100176599271492 ) ) ;
#4541=CARTESIAN_POINT ( 'NONE',  ( 19.57810744170729933, -21.77087888895180257, -80.79042367306239214 ) ) ;
#4544=CARTESIAN_POINT ( 'NONE',  ( 16.13393739769620083, -15.61618894467929941, -22.14999999999999858 ) ) ;
#4557=DIRECTION ( 'NONE',  ( 0.000000000000000000, 0.000000000000000000, 1.000000000000000000 ) ) ;
#4558=CARTESIAN_POINT ( 'NONE',  ( 22.59237592338839917, -18.78433718290749965, -81.23899999999999011 ) ) ;
#4560=ORIENTED_EDGE ( 'NONE', *, *, #15196, .T. ) ;
#4573=CARTESIAN_POINT ( 'NONE',  ( 11.27229808032523728, -21.94238343154312076, -68.50066414062398223 ) ) ;
#4577=CARTESIAN_POINT ( 'NONE',  ( 8.411629955056419305, -17.01358507482030191, -58.23052221047058907 ) ) ;
#4582=CARTESIAN_POINT ( 'NONE',  ( 19.11048863820259669, -9.222230711542339421, -76.48586413618289725 ) ) ;
#4590=CARTESIAN_POINT ( 'NONE',  ( 13.03988958525129505, -22.92537339708916022, -34.13518226141717804 ) ) ;
#4591=LINE ( 'NONE', #48369, #38012 ) ;
#4592=CARTESIAN_POINT ( 'NONE',  ( 21.09281434348020667, -20.63137574190061230, -71.09897682385668816 ) ) ;
#4593=ORIENTED_EDGE ( 'NONE', *, *, #26317, .T. ) ;
#4595=CARTESIAN_POINT ( 'NONE',  ( 10.99422185684939812, -10.22267260582209936, -42.32501095722309259 ) ) ;
#4604=CARTESIAN_POINT ( 'NONE',  ( 20.99560079206503360, -21.94236587381720938, -78.08399595254924463 ) ) ;
#4609=AXIS2_PLACEMENT_3D ( 'NONE', #34730, #30537, #37644 ) ;
#4614=CYLINDRICAL_SURFACE ( 'NONE', #30289, 6.766999999999998572 ) ;
#4619=B_SPLINE_CURVE_WITH_KNOTS ( 'NONE', 3,
 ( #46484, #30977, #50656, #34915, #14492, #27311, #39381, #43317, #14752, #7410, #19191 ),
 .UNSPECIFIED., .F., .F.,
 ( 4, 1, 1, 1, 1, 1, 1, 1, 4 ),
 ( 0.4999961688222710476, 0.5146094102817740934, 0.5938283413453584458, 0.6730472724089429093, 0.7522662034725273728, 0.8314851345361116142, 0.9107040655996961886, 0.9899229966632812072, 1.000000000000000000 ),
 .UNSPECIFIED. ) ;
#4628=ORIENTED_EDGE ( 'NONE', *, *, #882, .F. ) ;
#4631=CARTESIAN_POINT ( 'NONE',  ( 10.33236275321031883, -12.06453136622874744, -33.62757847280354895 ) ) ;
#4633=CARTESIAN_POINT ( 'NONE',  ( 10.18757820060029928, -10.49490396035219852, -63.23880875801859958 ) ) ;
#4642=CARTESIAN_POINT ( 'NONE',  ( 24.04526736911255469, -15.61618908158827068, -41.79233198438217300 ) ) ;
#4643=VERTEX_POINT ( 'NONE', #28698 ) ;
#4644=AXIS2_PLACEMENT_3D ( 'NONE', #28363, #48053, #8214 ) ;
#4648=CARTESIAN_POINT ( 'NONE',  ( 10.22101148145273264, -12.20822225728566757, -37.61948740445134831 ) ) ;
#4651=EDGE_CURVE ( 'NONE', #367, #12539, #11308, .T. ) ;
#4653=CARTESIAN_POINT ( 'NONE',  ( 22.89031856386410269, -13.37760718783400193, -32.14999999999999858 ) ) ;
#4658=CARTESIAN_POINT ( 'NONE',  ( 17.16950934076716351, -23.52718544910446496, -52.25066344205447422 ) ) ;
#4664=CARTESIAN_POINT ( 'NONE',  ( 22.58529838043510196, -18.46618905781010156, -66.97959240854848417 ) ) ;
#4672=CARTESIAN_POINT ( 'NONE',  ( 9.352034712855139986, -13.68012214057080023, -69.54133546202830019 ) ) ;
#4675=CARTESIAN_POINT ( 'NONE',  ( 16.13393739769620083, -15.61618894467929941, -28.45282021618999835 ) ) ;
#4702=CARTESIAN_POINT ( 'NONE',  ( 24.23411650087799885, -17.15561044391580126, -75.85211268767397996 ) ) ;
#4704=CARTESIAN_POINT ( 'NONE',  ( 22.90065884458136480, -15.61618680935524317, -64.84717769963093303 ) ) ;
#4707=VERTEX_POINT ( 'NONE', #29220 ) ;
#4708=CARTESIAN_POINT ( 'NONE',  ( 17.01975004494453714, -22.38318688418750213, -36.91115206468915488 ) ) ;
#4709=CARTESIAN_POINT ( 'NONE',  ( 18.99729670757870181, -22.49426042349189814, -60.60709014237919234 ) ) ;
#4719=VECTOR ( 'NONE', #36360, 1000.000000000000000 ) ;
#4723=DIRECTION ( 'NONE',  ( 1.000000000000000000, 0.000000000000000000, 0.000000000000000000 ) ) ;
#4727=CARTESIAN_POINT ( 'NONE',  ( 23.04646983122121284, -11.63207477299024717, -79.34100340100883386 ) ) ;
#4734=CARTESIAN_POINT ( 'NONE',  ( 10.21265337833550113, -11.78461560499999905, -35.63563296679929948 ) ) ;
#4742=CARTESIAN_POINT ( 'NONE',  ( 8.683925679600550396, -15.55278753634380173, -60.07005151547389943 ) ) ;
#4745=CARTESIAN_POINT ( 'NONE',  ( 13.95270971513190084, -8.909117678376349048, -68.24709530556648929 ) ) ;
#4757=CARTESIAN_POINT ( 'NONE',  ( 17.16943767478000638, -7.705182206336107953, -55.33398825597025450 ) ) ;
#4761=CARTESIAN_POINT ( 'NONE',  ( 16.13393739769620083, -15.61618894467929941, -22.14999999999999858 ) ) ;
#4762=CARTESIAN_POINT ( 'NONE',  ( 9.366859039486531202, -15.61635947376150035, -49.45282021618999835 ) ) ;
#4764=VERTEX_POINT ( 'NONE', #18985 ) ;
#4767=VECTOR ( 'NONE', #13403, 1000.000000000000000 ) ;
#4770=CARTESIAN_POINT ( 'NONE',  ( 10.32617582395110034, -21.46876321233829898, -46.54110819413470068 ) ) ;
#4777=CARTESIAN_POINT ( 'NONE',  ( 9.603064799516298322, -19.96764128708570141, -80.82541145414208472 ) ) ;
#4783=CARTESIAN_POINT ( 'NONE',  ( 18.99083791357429973, -23.35058227262370067, -49.89504055825069884 ) ) ;
#4801=CARTESIAN_POINT ( 'NONE',  ( 18.20465301297571159, -7.911099042431281703, -61.37566303211916363 ) ) ;
#4822=CARTESIAN_POINT ( 'NONE',  ( 20.78638485713110029, -20.82189247438619972, -81.23899999999999011 ) ) ;
#4829=CARTESIAN_POINT ( 'NONE',  ( 22.90012820302155205, -16.52286888951047317, -34.88983980414008812 ) ) ;
#4832=EDGE_CURVE ( 'NONE', #21944, #39379, #8754, .T. ) ;
#4834=CARTESIAN_POINT ( 'NONE',  ( 22.90093739769620029, -15.61618894467913243, -28.45282021618999835 ) ) ;
#4847=CARTESIAN_POINT ( 'NONE',  ( 22.32699604808950156, -20.43622761008139932, -59.49802510748859419 ) ) ;
#4857=B_SPLINE_CURVE_WITH_KNOTS ( 'NONE', 3,
 ( #45852, #26163, #46118, #9937, #13622, #10464, #30092, #42697, #33518, #25898, #14387 ),
 .UNSPECIFIED., .F., .F.,
 ( 4, 1, 1, 1, 1, 1, 1, 1, 4 ),
 ( 0.000000000000000000, 0.0002423770808862299518, 0.07946130814449685331, 0.1586802392081063384, 0.2378991702717181134, 0.3171181013353275846, 0.3963370323989381938, 0.4755559634625476928, 0.5000037312039752324 ),
 .UNSPECIFIED. ) ;
#4861=CARTESIAN_POINT ( 'NONE',  ( 23.80906457898844053, -17.59608236765743428, -33.58805050710569873 ) ) ;
#4865=CARTESIAN_POINT ( 'NONE',  ( 10.35842378612870007, -20.32258213489830112, -41.84969737084129093 ) ) ;
#4870=CARTESIAN_POINT ( 'NONE',  ( 8.222919723998259656, -14.85903073721773993, -80.82280372480568076 ) ) ;
#4894=B_SPLINE_CURVE_WITH_KNOTS ( 'NONE', 3,
 ( #21443, #8897, #8633, #1542, #48467, #4958, #33238, #16489, #49255, #12569, #24583, #29056, #37441, #36392, #37189, #28531, #45312, #44532 ),
 .UNSPECIFIED., .F., .F.,
 ( 4, 2, 2, 2, 2, 2, 2, 2, 4 ),
 ( 0.4999961881505365913, 0.5624966646317195451, 0.6249971411129024990, 0.6874976175940853418, 0.7499980940752682956, 0.8124985705564512495, 0.8749990470376340923, 0.9374995235188170462, 1.000000000000000000 ),
 .UNSPECIFIED. ) ;
#4899=CARTESIAN_POINT ( 'NONE',  ( 22.85640968062299194, -16.50885056875128498, -46.49478737242424131 ) ) ;
#4901=CARTESIAN_POINT ( 'NONE',  ( 23.23545949276009992, -12.27625907641840008, -63.87256020652749555 ) ) ;
#4902=CARTESIAN_POINT ( 'NONE',  ( 24.04493739769619864, -15.61618894467929941, -32.14999999999999858 ) ) ;
#4912=ORIENTED_EDGE ( 'NONE', *, *, #21269, .T. ) ;
#4920=CARTESIAN_POINT ( 'NONE',  ( 22.43194022673959864, -19.90881204782320069, -32.14999999999999858 ) ) ;
#4928=CARTESIAN_POINT ( 'NONE',  ( 16.39219225208960040, -22.66429958545629830, -63.33552157962199658 ) ) ;
#4929=ORIENTED_EDGE ( 'NONE', *, *, #2191, .F. ) ;
#4935=CARTESIAN_POINT ( 'NONE',  ( 14.95389657571809927, -22.56960985492850114, -67.00632966799250312 ) ) ;
#4936=DIRECTION ( 'NONE',  ( 4.006994122734829692E-31, -1.000000000000000000, -3.740764114965449782E-16 ) ) ;
#4938=CYLINDRICAL_SURFACE ( 'NONE', #8869, 6.766999999999998572 ) ;
#4939=ORIENTED_EDGE ( 'NONE', *, *, #6666, .T. ) ;
#4946=TOROIDAL_SURFACE ( 'NONE', #7465, 6.949999999999999289, 2.999999999999960032 ) ;
#4958=CARTESIAN_POINT ( 'NONE',  ( 20.99561544827837167, -21.94235417058543547, -43.79935663472948448 ) ) ;
#4961=( NAMED_UNIT ( * ) PLANE_ANGLE_UNIT ( ) SI_UNIT ( $, .RADIAN. ) );
#4962=DIRECTION ( 'NONE',  ( 0.000000000000000000, 0.000000000000000000, -1.000000000000000000 ) ) ;
#4965=PLANE ( 'NONE',  #27012 ) ;
#4967=CARTESIAN_POINT ( 'NONE',  ( 21.06068861467879927, -9.004846484592640365, -79.49618351660039650 ) ) ;
#4975=CARTESIAN_POINT ( 'NONE',  ( 9.557361903038261275, -13.06853739366259859, -31.96482487842879650 ) ) ;
#4983=VECTOR ( 'NONE', #45903, 1000.000000000000000 ) ;
#4987=CARTESIAN_POINT ( 'NONE',  ( 13.13486993893959998, -7.935803858833188507, -78.88916932753539868 ) ) ;
#4989=CARTESIAN_POINT ( 'NONE',  ( 8.222732946675209931, -15.61637358666110131, -80.79233150823698395 ) ) ;
#4995=CARTESIAN_POINT ( 'NONE',  ( 8.222933577955913620, -14.58066943308473995, -68.54933528812181009 ) ) ;
#4998=( BOUNDED_CURVE ( )  B_SPLINE_CURVE ( 2, ( #19943, #39881, #8166 ),
 .UNSPECIFIED., .F., .T. ) 
 B_SPLINE_CURVE_WITH_KNOTS ( ( 3, 3 ),
 ( 2.168627590050199672, 3.232274745523169734 ),
 .UNSPECIFIED. ) 
 CURVE ( )  GEOMETRIC_REPRESENTATION_ITEM ( )  RATIONAL_B_SPLINE_CURVE ( ( 1.425426480542939967, 1.425426480542939967, 1.323085463760209857 ) ) 
 REPRESENTATION_ITEM ( '' )  );
#5001=CARTESIAN_POINT ( 'NONE',  ( 8.222524523195870572, -15.61634168869099959, -38.50766849176289952 ) ) ;
#5004=CARTESIAN_POINT ( 'NONE',  ( 12.02786555360810006, -9.881842189571759860, -39.75501738210749636 ) ) ;
#5011=CARTESIAN_POINT ( 'NONE',  ( 23.57566764420120009, -15.97304352090550239, -79.08259497074239164 ) ) ;
#5027=LINE ( 'NONE', #20464, #33589 ) ;
#5029=CARTESIAN_POINT ( 'NONE',  ( 16.56130706594500168, -8.576308665788749508, -72.36647972087459380 ) ) ;
#5030=CARTESIAN_POINT ( 'NONE',  ( 24.04493741779556260, -14.58064063100057339, -59.46598965420297844 ) ) ;
#5032=AXIS2_PLACEMENT_3D ( 'NONE', #32126, #40537, #44208 ) ;
#5042=CARTESIAN_POINT ( 'NONE',  ( 16.18347776944520078, -7.371174341447729539, -51.29424405795199249 ) ) ;
#5044=CIRCLE ( 'NONE', #36812, 2.999999999999960920 ) ;
#5046=ORIENTED_EDGE ( 'NONE', *, *, #7221, .F. ) ;
#5048=CARTESIAN_POINT ( 'NONE',  ( 16.23152780737629897, -23.46331552995090064, -80.50853572988748397 ) ) ;
#5049=CARTESIAN_POINT ( 'NONE',  ( 10.85080901074660176, -11.16945680538309915, -32.14999999999999858 ) ) ;
#5052=CARTESIAN_POINT ( 'NONE',  ( 9.658618216099990050, -20.27044307813694601, -60.59413031184570997 ) ) ;
#5054=CARTESIAN_POINT ( 'NONE',  ( 22.33694808633480022, -21.04807435451730058, -49.73660269612349794 ) ) ;
#5058=CARTESIAN_POINT ( 'NONE',  ( 18.20470375856487166, -23.32126450859495748, -64.20899946892900800 ) ) ;
#5059=CARTESIAN_POINT ( 'NONE',  ( 15.24805240113982663, -22.38317849424599970, -56.99443076857846791 ) ) ;
#5073=CARTESIAN_POINT ( 'NONE',  ( 9.367491665984019278, -15.61623476897930018, -53.45282021618999124 ) ) ;
#5078=ADVANCED_FACE ( 'NONE', ( #3475 ), #23609, .T. ) ;
#5081=CARTESIAN_POINT ( 'NONE',  ( 11.97526571559677677, -21.02750872198566157, -61.16116878873128115 ) ) ;
#5083=EDGE_LOOP ( 'NONE', ( #10646, #26586, #21157, #15720 ) ) ;
#5088=ORIENTED_EDGE ( 'NONE', *, *, #24618, .F. ) ;
#5093=ORIENTED_EDGE ( 'NONE', *, *, #38340, .F. ) ;
#5096=CARTESIAN_POINT ( 'NONE',  ( 22.12745480022610067, -19.48200407513829902, -81.23899999999999011 ) ) ;
#5107=CARTESIAN_POINT ( 'NONE',  ( 24.04460909154476056, -15.61619055174803172, -33.79232989763376338 ) ) ;
#5111=VERTEX_POINT ( 'NONE', #8954 ) ;
#5120=CARTESIAN_POINT ( 'NONE',  ( 11.55539561595326425, -20.98084311128575763, -55.57206633538740448 ) ) ;
#5122=CARTESIAN_POINT ( 'NONE',  ( 10.31024158113670097, -20.87654209055929755, -68.05366966235949633 ) ) ;
#5132=CARTESIAN_POINT ( 'NONE',  ( 18.20454803119799791, -23.32130851867060173, -56.20901675537331954 ) ) ;
#5136=CARTESIAN_POINT ( 'NONE',  ( 23.83903696605923273, -17.68686790340041526, -53.87566772557626393 ) ) ;
#5140=CARTESIAN_POINT ( 'NONE',  ( 13.30627730215510063, -22.50901367206249759, -41.69125950871409003 ) ) ;
#5151=DIRECTION ( 'NONE',  ( 1.000000000000000000, 0.000000000000000000, 0.000000000000000000 ) ) ;
#5156=EDGE_LOOP ( 'NONE', ( #30866, #5782, #7269, #12914 ) ) ;
#5167=CARTESIAN_POINT ( 'NONE',  ( 8.223585368203801593, -15.61624251583899969, -52.79233150823699816 ) ) ;
#5171=ORIENTED_EDGE ( 'NONE', *, *, #30069, .F. ) ;
#5174=CARTESIAN_POINT ( 'NONE',  ( 20.48510588023628287, -20.83495730151230418, -46.73167619432699382 ) ) ;
#5176=CARTESIAN_POINT ( 'NONE',  ( 22.77332867066339972, -11.43226362077250080, -67.83350675970849863 ) ) ;
#5185=CARTESIAN_POINT ( 'NONE',  ( 11.27237010540747875, -9.289939966437113839, -41.08399800701788962 ) ) ;
#5193=CARTESIAN_POINT ( 'NONE',  ( 24.03754256302241998, -15.24659606640338083, -55.49280163511743780 ) ) ;
#5194=CARTESIAN_POINT ( 'NONE',  ( 22.65097095636950186, -12.86430221781309946, -32.14999999999999858 ) ) ;
#5203=CARTESIAN_POINT ( 'NONE',  ( 9.278031783360169982, -17.27121685434340037, -67.77178171918468763 ) ) ;
#5210=CARTESIAN_POINT ( 'NONE',  ( 21.62437782416010279, -20.04310916307899859, -60.66881518290298914 ) ) ;
#5211=DIRECTION ( 'NONE',  ( 1.000000000000000000, 2.460964292799963328E-14, 0.000000000000000000 ) ) ;
#5221=CARTESIAN_POINT ( 'NONE',  ( 22.46012706948180337, -20.47783335039490993, -63.71600312820974210 ) ) ;
#5227=CARTESIAN_POINT ( 'NONE',  ( 8.222268241235530795, -15.61616536502389962, -60.50766849176299900 ) ) ;
#5233=CARTESIAN_POINT ( 'NONE',  ( 17.01981006685115716, -8.849199573316891332, -67.99448558109631335 ) ) ;
#5236=CARTESIAN_POINT ( 'NONE',  ( 12.14977632440493416, -8.703682543532863747, -53.12566589029975717 ) ) ;
#5237=DIRECTION ( 'NONE',  ( 0.000000000000000000, 0.000000000000000000, -1.000000000000000000 ) ) ;
#5238=CARTESIAN_POINT ( 'NONE',  ( 23.30211932285680021, -18.81054576247569798, -36.14593433426069424 ) ) ;
#5245=CARTESIAN_POINT ( 'NONE',  ( 10.96668629868520028, -20.41640511211859987, -35.60889570735529475 ) ) ;
#5253=CARTESIAN_POINT ( 'NONE',  ( 10.93345605571719936, -9.217934799021591630, -80.79042367306230688 ) ) ;
#5259=CARTESIAN_POINT ( 'NONE',  ( 17.16953355736119136, -7.705195898817367883, -79.04933618277276253 ) ) ;
#5267=CARTESIAN_POINT ( 'NONE',  ( 22.99833165505350152, -17.23564876112759947, -34.52656793190860185 ) ) ;
#5275=CARTESIAN_POINT ( 'NONE',  ( 20.29274154463319846, -21.79769704592460045, -73.37883193416179495 ) ) ;
#5279=CARTESIAN_POINT ( 'NONE',  ( 20.48567924760130055, -8.989398011352820461, -49.47734670041616312 ) ) ;
#5280=DIRECTION ( 'NONE',  ( 0.000000000000000000, 0.000000000000000000, -1.000000000000000000 ) ) ;
#5293=CARTESIAN_POINT ( 'NONE',  ( 16.13393739769620083, -15.61618894467929941, -32.14999999999999858 ) ) ;
#5300=CARTESIAN_POINT ( 'NONE',  ( 22.68113533337184151, -13.84826337360422421, -72.36886283329307901 ) ) ;
#5301=CARTESIAN_POINT ( 'NONE',  ( 24.01953185394659940, -14.96960027129633097, -43.76628852390030744 ) ) ;
#5302=CARTESIAN_POINT ( 'NONE',  ( 24.35800691670550222, -15.02678195249309923, -51.76955764433359519 ) ) ;
#5307=CARTESIAN_POINT ( 'NONE',  ( 23.47193497312810351, -16.90478717069920123, -44.28799034327369100 ) ) ;
#5308=CARTESIAN_POINT ( 'NONE',  ( 24.04500464303940888, -15.61618902416171295, -53.50766607493442706 ) ) ;
#5314=CARTESIAN_POINT ( 'NONE',  ( 24.33890690060549744, -16.42932864073580035, -53.53911138717730012 ) ) ;
#5318=CARTESIAN_POINT ( 'NONE',  ( 12.14992171379115149, -22.52877759129744462, -64.45899891434670792 ) ) ;
#5319=EDGE_CURVE ( 'NONE', #3978, #37534, #5044, .T. ) ;
#5336=DIRECTION ( 'NONE',  ( 0.000000000000000000, 0.000000000000000000, -1.000000000000000000 ) ) ;
#5341=CARTESIAN_POINT ( 'NONE',  ( 15.24818525250952561, -8.849183378239496633, -47.91115446551594914 ) ) ;
#5343=FACE_OUTER_BOUND ( 'NONE', #9257, .T. ) ;
#5346=CARTESIAN_POINT ( 'NONE',  ( 12.79927192150049997, -8.608885486179000068, -81.23899999999999011 ) ) ;
#5352=VERTEX_POINT ( 'NONE', #41425 ) ;
#5353=EDGE_CURVE ( 'NONE', #5352, #23033, #18766, .T. ) ;
#5356=CARTESIAN_POINT ( 'NONE',  ( 22.55493904458150212, -18.84709759249869876, -81.23899999999999011 ) ) ;
#5360=CARTESIAN_POINT ( 'NONE',  ( 21.94086349853619922, -19.61895903973029931, -69.03928461620259327 ) ) ;
#5365=ORIENTED_EDGE ( 'NONE', *, *, #34508, .F. ) ;
#5373=CARTESIAN_POINT ( 'NONE',  ( 9.366931599644679807, -15.61636246440640008, -63.84717978381009118 ) ) ;
#5375=CARTESIAN_POINT ( 'NONE',  ( 8.287157259014669819, -15.49457628754339922, -76.29243849297590430 ) ) ;
#5378=VECTOR ( 'NONE', #35312, 1000.000000000000000 ) ;
#5379=LINE ( 'NONE', #33126, #5993 ) ;
#5383=B_SPLINE_CURVE_WITH_KNOTS ( 'NONE', 3,
 ( #17497, #29534, #9888, #37929, #33971, #22178, #2283, #41596, #1768, #50246, #14336, #30305, #46322, #2809, #46845, #3320, #42905, #7001 ),
 .UNSPECIFIED., .F., .F.,
 ( 4, 2, 2, 2, 2, 2, 2, 2, 4 ),
 ( 0.000000000000000000, 0.06249952337696731974, 0.1249990467539346395, 0.1874985701309019592, 0.2499980935078692790, 0.3124976168848365710, 0.3749971402618039185, 0.4374966636387712660, 0.4999961870157385579 ),
 .UNSPECIFIED. ) ;
#5384=CARTESIAN_POINT ( 'NONE',  ( 20.11802686909307525, -8.703640737107740222, -43.17429654658235449 ) ) ;
#5389=CARTESIAN_POINT ( 'NONE',  ( 8.254536426267019777, -16.37770113429971630, -34.47698882255479447 ) ) ;
#5393=CARTESIAN_POINT ( 'NONE',  ( 23.30168784358699696, -13.58393702039099971, -48.97940116656700127 ) ) ;
#5398=CARTESIAN_POINT ( 'NONE',  ( 22.90119541241246637, -15.61618911972255930, -40.84718082130915207 ) ) ;
#5412=B_SPLINE_CURVE_WITH_KNOTS ( 'NONE', 3,
 ( #28655, #25244, #41248, #5360, #24192, #21316, #40213, #4305, #16614, #20274, #48337 ),
 .UNSPECIFIED., .F., .F.,
 ( 4, 1, 1, 1, 1, 1, 1, 1, 4 ),
 ( 0.4999959824775806472, 0.5168334851326326085, 0.5960524161961817668, 0.6752713472598913524, 0.7544902783234405108, 0.8337092093871478760, 0.9129281404507014752, 0.9921470715144067309, 1.000000000000000000 ),
 .UNSPECIFIED. ) ;
#5413=VERTEX_POINT ( 'NONE', #2367 ) ;
#5414=ORIENTED_EDGE ( 'NONE', *, *, #7620, .T. ) ;
#5416=CARTESIAN_POINT ( 'NONE',  ( 19.54188188357280964, -21.52912844502688117, -72.78610869383017246 ) ) ;
#5421=CARTESIAN_POINT ( 'NONE',  ( 22.72480973293551898, -13.84493719928921784, -54.36948976686252877 ) ) ;
#5425=CARTESIAN_POINT ( 'NONE',  ( 16.25549387145995084, -22.38225831564430734, -46.94710703770110882 ) ) ;
#5429=CARTESIAN_POINT ( 'NONE',  ( 8.288808833082619287, -15.41443316095459792, -61.02067868823729668 ) ) ;
#5433=AXIS2_PLACEMENT_3D ( 'NONE', #16911, #45209, #44426 ) ;
#5435=EDGE_CURVE ( 'NONE', #16752, #3546, #16259, .T. ) ;
#5436=CARTESIAN_POINT ( 'NONE',  ( 16.13393739769620083, -15.61618894467929941, -32.14999999999999858 ) ) ;
#5444=B_SPLINE_CURVE_WITH_KNOTS ( 'NONE', 3,
 ( #37575, #1941, #17921, #1681, #29698, #9811, #33892, #30738, #30480, #2978, #38360, #42821, #34930, #47521, #6917, #22868, #38889, #27326, #18434, #38629, #2454, #34408, #11107, #10848, #14770, #2721, #18952, #50930, #31500, #15027, #3234, #42562, #50422, #6653 ),
 .UNSPECIFIED., .F., .F.,
 ( 4, 2, 1, 1, 1, 1, 2, 2, 2, 2, 2, 2, 2, 2, 2, 2, 2, 2, 4 ),
 ( 0.4999993943104570904, 0.5004876761519508888, 0.5009759579934445206, 0.5019525216764315623, 0.5039056490424062007, 0.5078119037743555886, 0.5156244132382546974, 0.5312494321660528040, 0.5624994700216491283, 0.6249995457328421100, 0.6874996214440350917, 0.7499996971552280733, 0.8124997728664211660, 0.8437498107220176013, 0.8749998485776140367, 0.9062498864332106940, 0.9374999242888071294, 0.9687499621444035647, 1.000000000000000000 ),
 .UNSPECIFIED. ) ;
#5447=CARTESIAN_POINT ( 'NONE',  ( 23.44327699831620038, -15.93920061306999791, -32.14999999999999858 ) ) ;
#5453=CARTESIAN_POINT ( 'NONE',  ( 9.120647901033246185, -11.85279051307570342, -44.66432580115215956 ) ) ;
#5455=B_SPLINE_CURVE_WITH_KNOTS ( 'NONE', 3,
 ( #37782, #13431, #37264, #17351, #25962, #33316, #17608, #21002, #16829, #36999, #1876, #49073, #25442, #41973, #6070, #36727, #49329, #833, #9741, #32776, #25700, #12911, #1097, #17856, #13180, #29127, #28867, #44869 ),
 .UNSPECIFIED., .F., .F.,
 ( 4, 2, 2, 2, 2, 2, 2, 2, 2, 2, 1, 1, 1, 1, 2, 4 ),
 ( 0.000000000000000000, 0.06250046681096792234, 0.1250009336219358447, 0.1875014004329037531, 0.2500018672438716894, 0.3125023340548396256, 0.3750028008658075063, 0.4375032676767754425, 0.4687535010822594383, 0.4843786177850014085, 0.4921911761363723659, 0.4960974553120579555, 0.4980505948999007781, 0.4990271646938223005, 0.4995154495907830339, 0.5000037344877438228 ),
 .UNSPECIFIED. ) ;
#5459=CARTESIAN_POINT ( 'NONE',  ( 19.06574088075160134, -9.201589384987739706, -60.48364006133169823 ) ) ;
#5463=CARTESIAN_POINT ( 'NONE',  ( 12.72603136295543891, -21.52914872767418686, -43.11948669098642029 ) ) ;
#5466=CARTESIAN_POINT ( 'NONE',  ( 19.62102412718670053, -21.74666892895760029, -64.78819959821109364 ) ) ;
#5467=DIRECTION ( 'NONE',  ( 0.000000000000000000, 0.000000000000000000, -1.000000000000000000 ) ) ;
#5471=ORIENTED_EDGE ( 'NONE', *, *, #25109, .T. ) ;
#5472=VERTEX_POINT ( 'NONE', #3415 ) ;
#5476=CARTESIAN_POINT ( 'NONE',  ( 10.22106225561806880, -19.02424243086505129, -55.28615407388804215 ) ) ;
#5490=CARTESIAN_POINT ( 'NONE',  ( 14.06321933549888570, -7.911099009402122739, -53.20899948581546113 ) ) ;
#5493=CARTESIAN_POINT ( 'NONE',  ( 9.545302122914700149, -11.35278270015860080, -35.19530716149729699 ) ) ;
#5499=ORIENTED_EDGE ( 'NONE', *, *, #46177, .F. ) ;
#5503=CARTESIAN_POINT ( 'NONE',  ( 16.03351556195739747, -22.66831448449759989, -37.35171219075489546 ) ) ;
#5511=CARTESIAN_POINT ( 'NONE',  ( 16.37827341743040321, -23.85773112360640269, -79.99823436242610342 ) ) ;
#5513=VECTOR ( 'NONE', #19362, 1000.000000000000000 ) ;
#5519=CARTESIAN_POINT ( 'NONE',  ( 12.14979057282054242, -8.703674483741680845, -68.84100286263340251 ) ) ;
#5521=VERTEX_POINT ( 'NONE', #15714 ) ;
#5528=CARTESIAN_POINT ( 'NONE',  ( 20.42372255482109722, -21.21442991862110006, -36.74469800168989764 ) ) ;
#5535=CARTESIAN_POINT ( 'NONE',  ( 14.07085440528040010, -22.77512621944960003, -77.65665421159729931 ) ) ;
#5538=CARTESIAN_POINT ( 'NONE',  ( 15.62246519096099107, -7.695412796532114186, -49.27188937755772002 ) ) ;
#5544=CARTESIAN_POINT ( 'NONE',  ( 15.09828667837113336, -23.52717655769652083, -72.04927324925495213 ) ) ;
#5551=CARTESIAN_POINT ( 'NONE',  ( 20.99558181260091061, -9.289996862630026442, -59.21596848997750584 ) ) ;
#5552=CARTESIAN_POINT ( 'NONE',  ( 15.09845797924882760, -23.52719716851022724, -70.04933658504315019 ) ) ;
#5558=CARTESIAN_POINT ( 'NONE',  ( 14.06315832308397873, -7.911114717410128172, -43.20903977167234444 ) ) ;
#5559=CARTESIAN_POINT ( 'NONE',  ( 19.78933351317860101, -23.00677750682039857, -54.14612557624229083 ) ) ;
#5564=B_SPLINE_CURVE_WITH_KNOTS ( 'NONE', 3,
 ( #1338, #10238, #29864, #22264 ),
 .UNSPECIFIED., .F., .F.,
 ( 4, 4 ),
 ( 0.000000000000000000, 0.1813467805151689483 ),
 .UNSPECIFIED. ) ;
#5567=CARTESIAN_POINT ( 'NONE',  ( 10.45489348174570132, -10.79382914828800111, -47.45674758581839825 ) ) ;
#5572=CARTESIAN_POINT ( 'NONE',  ( 22.46012451160922652, -10.75454102864662609, -51.58399612945741808 ) ) ;
#5574=CARTESIAN_POINT ( 'NONE',  ( 7.906922477136400396, -15.06942921146810122, -50.52879200675969429 ) ) ;
#5580=CARTESIAN_POINT ( 'NONE',  ( 20.53618552854030099, -10.10594661162980046, -52.56174695496989102 ) ) ;
#5593=LINE ( 'NONE', #9526, #32519 ) ;
#5599=ORIENTED_EDGE ( 'NONE', *, *, #5784, .F. ) ;
#5610=ORIENTED_EDGE ( 'NONE', *, *, #48872, .F. ) ;
#5613=CARTESIAN_POINT ( 'NONE',  ( 24.04470913566636625, -15.68475005675827916, -77.51042278623567938 ) ) ;
#5614=DIRECTION ( 'NONE',  ( 1.000000000000000000, 0.000000000000000000, 0.000000000000000000 ) ) ;
#5628=EDGE_CURVE ( 'NONE', #17098, #1610, #15204, .T. ) ;
#5636=CARTESIAN_POINT ( 'NONE',  ( 9.443963076300310178, -17.25402591980700606, -63.77013741789689050 ) ) ;
#5637=AXIS2_PLACEMENT_3D ( 'NONE', #28579, #37241, #17071 ) ;
#5640=CARTESIAN_POINT ( 'NONE',  ( 15.64724003739100056, -7.783572915366379519, -76.76775207935759227 ) ) ;
#5641=ORIENTED_EDGE ( 'NONE', *, *, #25101, .T. ) ;
#5656=CARTESIAN_POINT ( 'NONE',  ( 12.93294630233359932, -8.888607629990449510, -56.42598068654719157 ) ) ;
#5661=CARTESIAN_POINT ( 'NONE',  ( 21.66930937907060084, -19.98679716348209823, -75.05992337703780493 ) ) ;
#5662=CARTESIAN_POINT ( 'NONE',  ( 21.74730038895833673, -21.19061166947408381, -61.75655418039362132 ) ) ;
#5664=CARTESIAN_POINT ( 'NONE',  ( 15.19249895237996917, -8.626464141217111248, -54.30456343836949884 ) ) ;
#5665=EDGE_CURVE ( 'NONE', #20377, #38000, #7604, .T. ) ;
#5678=CARTESIAN_POINT ( 'NONE',  ( 24.04490354837754396, -15.59228409935874637, -77.50671465413907413 ) ) ;
#5681=CARTESIAN_POINT ( 'NONE',  ( 14.36266333286323338, -9.025322607677731312, -53.86948819376841868 ) ) ;
#5683=CARTESIAN_POINT ( 'NONE',  ( 24.04456899842966067, -15.69869672982768982, -49.51098473570640124 ) ) ;
#5686=CARTESIAN_POINT ( 'NONE',  ( 12.03477506705270095, -8.924132774964691706, -61.33755441249169849 ) ) ;
#5690=FACE_OUTER_BOUND ( 'NONE', #41235, .T. ) ;
#5693=CARTESIAN_POINT ( 'NONE',  ( 22.14946380439831941, -18.71488146266838370, -32.99858898373786076 ) ) ;
#5701=CARTESIAN_POINT ( 'NONE',  ( 23.21588883353000199, -14.35342990756280024, -32.14999999999999858 ) ) ;
#5703=CARTESIAN_POINT ( 'NONE',  ( 21.11091583202307120, -9.437894192877843480, -45.22360369773933542 ) ) ;
#5706=CARTESIAN_POINT ( 'NONE',  ( 11.87323508191540000, -21.23659595402939715, -65.55365164940349132 ) ) ;
#5709=CARTESIAN_POINT ( 'NONE',  ( 14.36277100459635570, -22.20708315903983987, -43.03615330968553820 ) ) ;
#5712=EDGE_CURVE ( 'NONE', #49951, #40988, #35103, .T. ) ;
#5713=CARTESIAN_POINT ( 'NONE',  ( 15.81768230162860078, -8.570442610110308834, -77.93854215477199432 ) ) ;
#5732=B_SPLINE_CURVE_WITH_KNOTS ( 'NONE', 3,
 ( #51339, #35605, #924, #16921, #3901, #35857, #32863, #3128, #31133, #39035, #51846, #35072, #12025, #15950, #31903, #47923, #27977, #47161, #25528, #25783, #25270, #50181, #38126, #41531, #41791, #22115, #1445, #33910 ),
 .UNSPECIFIED., .F., .F.,
 ( 4, 2, 2, 2, 2, 2, 2, 2, 2, 2, 2, 2, 2, 4 ),
 ( 0.000000000000000000, 0.03124990345073212078, 0.06249980690146424156, 0.09374971035219635540, 0.1249996138029284831, 0.1562495172536605970, 0.1874994207043927108, 0.2187493241551248246, 0.2499992276058569662, 0.2812491310565890523, 0.3124990345073211939, 0.3749988414087853106, 0.4374986483102494272, 0.4999984552117135994 ),
 .UNSPECIFIED. ) ;
#5736=CARTESIAN_POINT ( 'NONE',  ( 17.90525091854434692, -9.025334375736962400, -68.03615214762757546 ) ) ;
#5739=CARTESIAN_POINT ( 'NONE',  ( 22.46009513736006369, -10.75450071354899428, -53.58400066563606856 ) ) ;
#5743=CARTESIAN_POINT ( 'NONE',  ( 12.17215262800660014, -22.39047924184240301, -38.68094012829649841 ) ) ;
#5757=CARTESIAN_POINT ( 'NONE',  ( 8.428886257399922144, -13.54533162025536441, -56.87566481798235429 ) ) ;
#5769=VECTOR ( 'NONE', #18751, 1000.000000000000000 ) ;
#5771=CARTESIAN_POINT ( 'NONE',  ( 23.93344121396042823, -16.98588554008669149, -65.84766514592809017 ) ) ;
#5774=CARTESIAN_POINT ( 'NONE',  ( 22.15074124698030289, -19.29594846615139758, -48.62753766123279320 ) ) ;
#5782=ORIENTED_EDGE ( 'NONE', *, *, #28170, .T. ) ;
#5783=CARTESIAN_POINT ( 'NONE',  ( 15.67188839633519848, -8.180248852217671285, -76.54758917670659457 ) ) ;
#5784=EDGE_CURVE ( 'NONE', #5413, #3924, #44991, .T. ) ;
#5792=CARTESIAN_POINT ( 'NONE',  ( 8.222290034161709116, -15.61613760572089937, -44.79233150823699816 ) ) ;
#5796=ORIENTED_EDGE ( 'NONE', *, *, #2459, .T. ) ;
#5799=ORIENTED_EDGE ( 'NONE', *, *, #18962, .T. ) ;
#5801=CARTESIAN_POINT ( 'NONE',  ( 24.04464518807997919, -15.61618401921712618, -71.50767245506341396 ) ) ;
#5802=CARTESIAN_POINT ( 'NONE',  ( 24.04493740294731552, -16.65173115070739840, -69.54933814134879810 ) ) ;
#5808=ADVANCED_FACE ( 'NONE', ( #4429 ), #20398, .T. ) ;
#5809=CARTESIAN_POINT ( 'NONE',  ( 21.39045294677319831, -9.263885084012120075, -53.51237412773329538 ) ) ;
#5812=ADVANCED_FACE ( 'NONE', ( #40078 ), #39343, .T. ) ;
#5816=CARTESIAN_POINT ( 'NONE',  ( 19.86268612959200297, -22.06623752585539933, -48.56581262070909588 ) ) ;
#5819=CARTESIAN_POINT ( 'NONE',  ( 9.071496094108649544, -18.06536394266180068, -32.14999999999999858 ) ) ;
#5824=CARTESIAN_POINT ( 'NONE',  ( 24.04493739770204641, -15.61617025106582446, -61.50767538883729912 ) ) ;
#5825=CARTESIAN_POINT ( 'NONE',  ( 22.95508758428769625, -20.24810332654539735, -53.69754924930440154 ) ) ;
#5828=B_SPLINE_CURVE_WITH_KNOTS ( 'NONE', 3,
 ( #16361, #4829, #24457, #17151, #33104, #48083, #7987, #20797, #632, #23938 ),
 .UNSPECIFIED., .F., .F.,
 ( 4, 1, 1, 1, 1, 1, 1, 4 ),
 ( 0.5000038964883081194, 0.5639822375181338110, 0.6432011685817549118, 0.7224200996453765677, 0.8016390307090128786, 0.8808579617726346456, 0.9600768928362556354, 1.000000000000000000 ),
 .UNSPECIFIED. ) ;
#5832=CARTESIAN_POINT ( 'NONE',  ( 9.367272718592845493, -14.60504838226429314, -69.89475711886211684 ) ) ;
#5845=CARTESIAN_POINT ( 'NONE',  ( 9.975091091254757458, -18.47606888634118150, -67.31448443351787603 ) ) ;
#5860=CARTESIAN_POINT ( 'NONE',  ( 8.222872596472118545, -15.61638977992110000, -80.50766849176289952 ) ) ;
#5865=FACE_OUTER_BOUND ( 'NONE', #12472, .T. ) ;
#5870=CARTESIAN_POINT ( 'NONE',  ( 8.672104946893240296, -18.33092530368449502, -34.68117512106212530 ) ) ;
#5887=CARTESIAN_POINT ( 'NONE',  ( 22.12508014151499935, -10.54736691127049930, -71.06398904277699557 ) ) ;
#5890=CARTESIAN_POINT ( 'NONE',  ( 11.60944838831535897, -10.20586932579674944, -48.12548681540801709 ) ) ;
#5896=CARTESIAN_POINT ( 'NONE',  ( 19.54191009578054050, -21.52911156565832940, -78.78615145789616747 ) ) ;
#5905=CARTESIAN_POINT ( 'NONE',  ( 14.24329851705899941, -8.409790471005749168, -58.48567289420139304 ) ) ;
#5910=CARTESIAN_POINT ( 'NONE',  ( 9.367848958511704183, -14.88152289001418715, -73.88173930325579875 ) ) ;
#5911=CARTESIAN_POINT ( 'NONE',  ( 22.38196252458151037, -20.47457147835186575, -61.71802975325617524 ) ) ;
#5913=CARTESIAN_POINT ( 'NONE',  ( 8.222623404330700936, -15.61601543569009820, -34.79233150823699816 ) ) ;
#5917=ORIENTED_EDGE ( 'NONE', *, *, #35453, .T. ) ;
#5939=CARTESIAN_POINT ( 'NONE',  ( 20.40563007449969746, -9.032923093559031003, -73.69570765841629623 ) ) ;
#5954=DIRECTION ( 'NONE',  ( 0.000000000000000000, 0.000000000000000000, -1.000000000000000000 ) ) ;
#5965=CARTESIAN_POINT ( 'NONE',  ( 21.80209328419340054, -11.41921765328320149, -76.64430199831019763 ) ) ;
#5967=ORIENTED_EDGE ( 'NONE', *, *, #18128, .T. ) ;
#5973=CARTESIAN_POINT ( 'NONE',  ( 9.490404654256218819, -17.98389487732099923, -73.34384415308200289 ) ) ;
#5982=CARTESIAN_POINT ( 'NONE',  ( 23.01789209736645603, -11.61359716709991119, -39.34022659375048647 ) ) ;
#5993=VECTOR ( 'NONE', #25522, 1000.000000000000000 ) ;
#5995=CARTESIAN_POINT ( 'NONE',  ( 24.04488894642461005, -15.58382787379838774, -33.79102812862304006 ) ) ;
#6002=CARTESIAN_POINT ( 'NONE',  ( 21.52278304119420227, -10.21091847863399948, -31.76248681540709384 ) ) ;
#6029=AXIS2_PLACEMENT_3D ( 'NONE', #16155, #4100, #15137 ) ;
#6037=CARTESIAN_POINT ( 'NONE',  ( 9.181343238418110175, -16.80109111490159890, -43.39908821103389869 ) ) ;
#6038=CYLINDRICAL_SURFACE ( 'NONE', #1482, 6.766999999999998572 ) ;
#6045=CARTESIAN_POINT ( 'NONE',  ( 21.37225650031859914, -20.91399106607289937, -71.31913972650760059 ) ) ;
#6047=CARTESIAN_POINT ( 'NONE',  ( 12.42940066044197422, -8.592417990221209223, -49.13779373100693704 ) ) ;
#6052=CARTESIAN_POINT ( 'NONE',  ( 22.89932169800278317, -15.45644993449541715, -62.44531429522186272 ) ) ;
#6053=CARTESIAN_POINT ( 'NONE',  ( 11.56113406461153126, -22.12597267880275353, -46.20275904408111245 ) ) ;
#6057=CARTESIAN_POINT ( 'NONE',  ( 11.27231506636646330, -9.289981607459157686, -47.08399875780654043 ) ) ;
#6061=CARTESIAN_POINT ( 'NONE',  ( 18.20467564891351131, -23.32127245094282131, -69.92433697411958349 ) ) ;
#6069=CARTESIAN_POINT ( 'NONE',  ( 17.35874840962710053, -23.76987265457309917, -52.24487123071529027 ) ) ;
#6070=CARTESIAN_POINT ( 'NONE',  ( 22.11375918210443459, -12.33543082924636280, -56.29291989957688003 ) ) ;
#6073=AXIS2_PLACEMENT_3D ( 'NONE', #36992, #821, #16551 ) ;
#6076=CARTESIAN_POINT ( 'NONE',  ( 17.09013251674910450, -8.227522982582710753, -47.77362331007289953 ) ) ;
#6080=ADVANCED_FACE ( 'NONE', ( #25176 ), #49320, .T. ) ;
#6081=CARTESIAN_POINT ( 'NONE',  ( 8.943693940708850931, -14.83288028135000047, -32.14999999999999858 ) ) ;
#6087=CARTESIAN_POINT ( 'NONE',  ( 8.222268241235530795, -15.61616536502389962, -60.50766849176299900 ) ) ;
#6088=CARTESIAN_POINT ( 'NONE',  ( 10.88887983203600029, -9.254420963851531567, -64.78819959821119312 ) ) ;
#6113=CARTESIAN_POINT ( 'NONE',  ( 15.09836673641149574, -23.52718614182695944, -76.04935793674373201 ) ) ;
#6121=ORIENTED_EDGE ( 'NONE', *, *, #34664, .F. ) ;
#6122=CARTESIAN_POINT ( 'NONE',  ( 20.99566267773841943, -21.94231647796216933, -79.79933649795523820 ) ) ;
#6124=ORIENTED_EDGE ( 'NONE', *, *, #1633, .F. ) ;
#6127=CARTESIAN_POINT ( 'NONE',  ( 11.97527466958848130, -21.02751549615875959, -45.16117179432525575 ) ) ;
#6132=ORIENTED_EDGE ( 'NONE', *, *, #18335, .F. ) ;
#6136=CARTESIAN_POINT ( 'NONE',  ( 23.56187535230263208, -18.44086820948935923, -33.90806464902174611 ) ) ;
#6150=CARTESIAN_POINT ( 'NONE',  ( 8.295765907398179095, -16.00324949790340057, -70.27179973214080633 ) ) ;
#6160=CARTESIAN_POINT ( 'NONE',  ( 15.09829761739486464, -7.705200025808673914, -59.25071220949133988 ) ) ;
#6161=ADVANCED_FACE ( 'NONE', ( #44593 ), #4497, .T. ) ;
#6163=AXIS2_PLACEMENT_3D ( 'NONE', #16726, #32681, #41096 ) ;
#6167=ORIENTED_EDGE ( 'NONE', *, *, #21582, .F. ) ;
#6168=CARTESIAN_POINT ( 'NONE',  ( 9.397791606579609436, -12.43326038450650017, -54.20785061676589578 ) ) ;
#6171=CARTESIAN_POINT ( 'NONE',  ( 22.72481146437324639, -17.38743204429671607, -68.53615134654430108 ) ) ;
#6173=CARTESIAN_POINT ( 'NONE',  ( 17.86626912417429836, -8.779407102036641319, -74.42617192852868868 ) ) ;
#6174=CARTESIAN_POINT ( 'NONE',  ( 16.21641506526469101, -23.52682115103659655, -62.00435319991119343 ) ) ;
#6176=CARTESIAN_POINT ( 'NONE',  ( 21.48628740521284541, -11.02326954940455828, -54.62143916262400012 ) ) ;
#6177=B_SPLINE_CURVE_WITH_KNOTS ( 'NONE', 3,
 ( #27669, #39736, #51785, #3840, #50761, #31331, #51017, #34755, #15115, #47103, #35282, #19813, #15888, #14855, #27154, #31842, #7256, #39225 ),
 .UNSPECIFIED., .F., .F.,
 ( 4, 2, 2, 2, 2, 2, 2, 2, 4 ),
 ( 0.5000000032664997374, 0.5625000028581871314, 0.6250000024498745255, 0.6875000020415620305, 0.7500000016332494246, 0.8125000012249370407, 0.8750000008166247678, 0.9375000004083123839, 1.000000000000000000 ),
 .UNSPECIFIED. ) ;
#6190=VERTEX_POINT ( 'NONE', #40920 ) ;
#6191=CARTESIAN_POINT ( 'NONE',  ( 9.367206039829609310, -15.61603166621950045, -73.45282021618999124 ) ) ;
#6192=B_SPLINE_CURVE_WITH_KNOTS ( 'NONE', 3,
 ( #40773, #28970, #9342, #16664, #21360, #20841, #25019, #48918, #17452, #9071, #33416 ),
 .UNSPECIFIED., .F., .F.,
 ( 4, 1, 1, 1, 1, 1, 1, 1, 4 ),
 ( 0.000000000000000000, 0.001354414506361919807, 0.08057334556998355102, 0.1597922766336074829, 0.2390112076972449318, 0.3182301387608665322, 0.3974490698244904641, 0.4766680008880465058, 0.5000038607551413605 ),
 .UNSPECIFIED. ) ;
#6194=CARTESIAN_POINT ( 'NONE',  ( 12.89365889624202133, -8.399591182479161589, -80.87333339708158064 ) ) ;
#6196=CARTESIAN_POINT ( 'NONE',  ( 24.03121162336080019, -16.09189990580818730, -49.52681125393587536 ) ) ;
#6199=CARTESIAN_POINT ( 'NONE',  ( 19.10341123310410083, -8.351963402172360773, -71.63601545076220134 ) ) ;
#6203=EDGE_CURVE ( 'NONE', #38000, #36938, #21822, .T. ) ;
#6214=DIRECTION ( 'NONE',  ( 0.000000000000000000, 0.000000000000000000, -1.000000000000000000 ) ) ;
#6223=ORIENTED_EDGE ( 'NONE', *, *, #14256, .F. ) ;
#6224=CARTESIAN_POINT ( 'NONE',  ( 12.00938018391109985, -9.895123749747108732, -70.14834965109328380 ) ) ;
#6233=CARTESIAN_POINT ( 'NONE',  ( 9.165464470679451026, -16.70382112609910052, -75.40353636073618304 ) ) ;
#6236=CARTESIAN_POINT ( 'NONE',  ( 22.84664670202137771, -16.49985376298375073, -40.49448084163965689 ) ) ;
#6250=AXIS2_PLACEMENT_3D ( 'NONE', #31381, #32146, #39024 ) ;
#6260=CARTESIAN_POINT ( 'NONE',  ( 11.27222774357445978, -9.290047668763994793, -53.08399909254191584 ) ) ;
#6262=CARTESIAN_POINT ( 'NONE',  ( 23.47482255641189752, -18.39074344551899642, -46.12751964827670292 ) ) ;
#6272=CARTESIAN_POINT ( 'NONE',  ( 21.45406565774140262, -10.98598436268509992, -38.61921508777290057 ) ) ;
#6287=CARTESIAN_POINT ( 'NONE',  ( 19.55461702279360026, -22.74941205225439944, -32.14999999999999858 ) ) ;
#6294=CARTESIAN_POINT ( 'NONE',  ( 23.83903833740709288, -17.68686109898874292, -73.87566485239436531 ) ) ;
#6297=CARTESIAN_POINT ( 'NONE',  ( 22.28429397680109858, -12.16428039338680023, -42.29002317614330053 ) ) ;
#6298=DIRECTION ( 'NONE',  ( 1.000000000000000000, 2.460964292799963328E-14, 0.000000000000000000 ) ) ;
#6300=CARTESIAN_POINT ( 'NONE',  ( 18.30559885472430182, -8.906037589390139786, -80.44681068936390034 ) ) ;
#6303=CARTESIAN_POINT ( 'NONE',  ( 21.01363834691890276, -21.76234764997069959, -35.57390792627550269 ) ) ;
#6311=CARTESIAN_POINT ( 'NONE',  ( 11.41477078611200824, -10.71002323189214778, -61.70916163504242036 ) ) ;
#6313=DIRECTION ( 'NONE',  ( 1.000000000000000000, 0.000000000000000000, 0.000000000000000000 ) ) ;
#6323=ORIENTED_EDGE ( 'NONE', *, *, #16495, .T. ) ;
#6327=CARTESIAN_POINT ( 'NONE',  ( 8.903861523391762844, -18.89162002862403256, -66.37230234641415905 ) ) ;
#6328=CARTESIAN_POINT ( 'NONE',  ( 7.922553350839290687, -14.87060723154609931, -66.82115454642119801 ) ) ;
#6329=CARTESIAN_POINT ( 'NONE',  ( 8.428889365030967085, -17.68705757020854819, -48.42433527398944904 ) ) ;
#6334=CARTESIAN_POINT ( 'NONE',  ( 23.10304989619800153, -18.25022857770899876, -46.34768255092769351 ) ) ;
#6335=CARTESIAN_POINT ( 'NONE',  ( 9.170124594752591562, -18.41179469585090089, -32.14999999999999858 ) ) ;
#6337=LINE ( 'NONE', #38304, #50151 ) ;
#6339=DIRECTION ( 'NONE',  ( 1.000000000000000000, 0.000000000000000000, 0.000000000000000000 ) ) ;
#6344=CARTESIAN_POINT ( 'NONE',  ( 9.794802990449738900, -10.34379900501819982, -62.72850739055710534 ) ) ;
#6374=CARTESIAN_POINT ( 'NONE',  ( 12.89365889624202133, -8.399591182479161589, -80.87333339708158064 ) ) ;
#6380=EDGE_LOOP ( 'NONE', ( #21760, #44150, #26869, #36844 ) ) ;
#6383=CARTESIAN_POINT ( 'NONE',  ( 23.78923512644315608, -17.67736616603236044, -77.59138855168500015 ) ) ;
#6386=( BOUNDED_CURVE ( )  B_SPLINE_CURVE ( 2, ( #18509, #22164, #38176 ),
 .UNSPECIFIED., .F., .T. ) 
 B_SPLINE_CURVE_WITH_KNOTS ( ( 3, 3 ),
 ( 1.104980434577240045, 2.168627590050209886 ),
 .UNSPECIFIED. ) 
 CURVE ( )  GEOMETRIC_REPRESENTATION_ITEM ( )  RATIONAL_B_SPLINE_CURVE ( ( 1.323085463760220071, 1.425426480542949959, 1.425426480542949959 ) ) 
 REPRESENTATION_ITEM ( '' )  );
#6399=CARTESIAN_POINT ( 'NONE',  ( 20.92839437590340879, -20.39170135171949028, -46.70218316016916305 ) ) ;
#6408=CARTESIAN_POINT ( 'NONE',  ( 23.70898548626439961, -12.36021487155560017, -37.37844945019890019 ) ) ;
#6422=CARTESIAN_POINT ( 'NONE',  ( 9.807687359717487396, -10.75461966244250611, -59.00069697328734009 ) ) ;
#6426=CARTESIAN_POINT ( 'NONE',  ( 22.68450600391640393, -17.37075470328159454, -62.53615866583844962 ) ) ;
#6429=CARTESIAN_POINT ( 'NONE',  ( 8.695472295357721038, -16.03563054923700193, -54.04941275463870198 ) ) ;
#6432=CARTESIAN_POINT ( 'NONE',  ( 9.366945217436017046, -16.50204441428810753, -69.41115344938793896 ) ) ;
#6434=CARTESIAN_POINT ( 'NONE',  ( 16.13393739769620083, -15.61618894467929941, -41.53556505950739819 ) ) ;
#6435=CARTESIAN_POINT ( 'NONE',  ( 19.25005220832321129, -22.90603194472208770, -61.87906973423940826 ) ) ;
#6437=CARTESIAN_POINT ( 'NONE',  ( 22.90093381512099668, -15.61618921778096336, -54.45281771551935890 ) ) ;
#6441=ORIENTED_EDGE ( 'NONE', *, *, #48433, .F. ) ;
#6446=EDGE_CURVE ( 'NONE', #37842, #44438, #13666, .T. ) ;
#6452=DIRECTION ( 'NONE',  ( 0.000000000000000000, 0.000000000000000000, -1.000000000000000000 ) ) ;
#6453=ORIENTED_EDGE ( 'NONE', *, *, #27725, .T. ) ;
#6454=CARTESIAN_POINT ( 'NONE',  ( 23.98909829869109700, -16.57502267198761103, -49.54631662027205152 ) ) ;
#6458=CARTESIAN_POINT ( 'NONE',  ( 17.69277123176280142, -23.30753373288560226, -78.44884352223360224 ) ) ;
#6459=EDGE_CURVE ( 'NONE', #20583, #18282, #43508, .T. ) ;
#6469=CARTESIAN_POINT ( 'NONE',  ( 20.97057552888700016, -21.79629248516249973, -51.57613200112659513 ) ) ;
#6476=B_SPLINE_CURVE_WITH_KNOTS ( 'NONE', 3,
 ( #21955, #38752, #5995, #6778, #30850, #50019, #10187, #30597, #2318, #46880, #46618, #2846, #26660, #33754, #10449, #26147, #14109, #2064, #18290, #34262, #10967, #21695, #30339, #50286, #46362, #26402, #26933, #18040, #1799, #42423, #42938, #6513, #22473, #37703, #37965 ),
 .UNSPECIFIED., .F., .F.,
 ( 4, 2, 1, 2, 2, 2, 2, 2, 2, 2, 2, 2, 2, 2, 2, 2, 2, 4 ),
 ( 0.5000036731825925340, 0.5039098944858534379, 0.5078161157891143418, 0.5156285583956361496, 0.5312534436086802092, 0.5625032140347683285, 0.6250027548869443450, 0.6875022957391202505, 0.7187520661652082588, 0.7500018365912961560, 0.7812516070173841642, 0.8125013774434721725, 0.8437511478695601808, 0.8750009182956480780, 0.9062506887217359752, 0.9375004591478239835, 0.9687502295739119917, 1.000000000000000000 ),
 .UNSPECIFIED. ) ;
#6478=CARTESIAN_POINT ( 'NONE',  ( 9.367202679915338948, -15.61634672871210050, -75.45282021618999124 ) ) ;
#6479=B_SPLINE_CURVE_WITH_KNOTS ( 'NONE', 3,
 ( #11352, #23117, #39135, #51442, #19198, #15538, #27831, #7930, #31490, #20218, #47515, #35184, #19718, #23879, #39903, #11610, #11100, #51186 ),
 .UNSPECIFIED., .F., .F.,
 ( 4, 2, 2, 2, 2, 2, 2, 2, 4 ),
 ( 0.4999969675811580805, 0.5624973466335132510, 0.6249977256858685326, 0.6874981047382237032, 0.7499984837905790958, 0.8124988628429342663, 0.8749992418952895479, 0.9374996209476447184, 1.000000000000000000 ),
 .UNSPECIFIED. ) ;
#6482=CARTESIAN_POINT ( 'NONE',  ( 12.38873293430890143, -9.639902246245529938, -76.16898841192839598 ) ) ;
#6485=CARTESIAN_POINT ( 'NONE',  ( 16.13393739769620083, -15.61618894467929941, -28.45282021618999835 ) ) ;
#6491=CARTESIAN_POINT ( 'NONE',  ( 19.21648360630749863, -21.95972640956449951, -70.80883835904629109 ) ) ;
#6493=CARTESIAN_POINT ( 'NONE',  ( 24.04513930477782679, -15.61618913701998146, -67.79233342760500136 ) ) ;
#6494=CARTESIAN_POINT ( 'NONE',  ( 9.366915451059274034, -16.50182680598841500, -41.41114337331676154 ) ) ;
#6500=CARTESIAN_POINT ( 'NONE',  ( 16.13393739769620083, -15.61618894467929941, -32.14999999999999858 ) ) ;
#6502=CARTESIAN_POINT ( 'NONE',  ( 9.366948908879642488, -16.50207144407324478, -55.41115368061451107 ) ) ;
#6513=CARTESIAN_POINT ( 'NONE',  ( 8.944826496811360883, -12.20469241501894331, -32.93351229774626887 ) ) ;
#6516=CARTESIAN_POINT ( 'NONE',  ( 9.543102507195031947, -13.84480207404790342, -51.53615333421284106 ) ) ;
#6518=CARTESIAN_POINT ( 'NONE',  ( 23.21194978661330310, -12.22672169835309930, -47.87033613167638890 ) ) ;
#6526=CARTESIAN_POINT ( 'NONE',  ( 11.60944838831639991, -10.20586932579799821, -48.12548681540710049 ) ) ;
#6532=CARTESIAN_POINT ( 'NONE',  ( 12.14991910881904502, -8.703601772961780725, -57.12566474721839427 ) ) ;
#6537=DIRECTION ( 'NONE',  ( 0.000000000000000000, 0.000000000000000000, -1.000000000000000000 ) ) ;
#6539=CARTESIAN_POINT ( 'NONE',  ( 23.99634207538090891, -14.71164246568921641, -71.47121910958560420 ) ) ;
#6540=CARTESIAN_POINT ( 'NONE',  ( 22.46009814471073440, -10.75450484369422455, -69.29933762258028196 ) ) ;
#6546=CARTESIAN_POINT ( 'NONE',  ( 10.22109612992661098, -12.20807755088076441, -41.61948678692156278 ) ) ;
#6549=CARTESIAN_POINT ( 'NONE',  ( 9.459240049790720306, -13.33781803315300074, -43.55752607316119906 ) ) ;
#6556=CARTESIAN_POINT ( 'NONE',  ( 21.72913965751709853, -21.11895732567419870, -39.53485447945639919 ) ) ;
#6557=EDGE_CURVE ( 'NONE', #3678, #37798, #37656, .T. ) ;
#6565=CARTESIAN_POINT ( 'NONE',  ( 16.57903057602875663, -8.841341571868987614, -61.97366626368047093 ) ) ;
#6567=CARTESIAN_POINT ( 'NONE',  ( 23.78210164868285048, -17.70463183224734038, -45.59262049459194799 ) ) ;
#6574=ORIENTED_EDGE ( 'NONE', *, *, #3892, .F. ) ;
#6581=CARTESIAN_POINT ( 'NONE',  ( 21.34899891482215395, -19.99345227585487095, -32.67494819118432048 ) ) ;
#6583=CARTESIAN_POINT ( 'NONE',  ( 8.222928256549737469, -14.58070839043696409, -68.83399830554878918 ) ) ;
#6584=CARTESIAN_POINT ( 'NONE',  ( 12.33875874437710074, -22.93597986008980172, -64.44458661451268711 ) ) ;
#6590=CARTESIAN_POINT ( 'NONE',  ( 14.93875137453389890, -22.96997872785800254, -50.78394269049049825 ) ) ;
#6591=CARTESIAN_POINT ( 'NONE',  ( 8.946858529655370873, -17.52974850216140013, -32.14999999999999858 ) ) ;
#6599=CARTESIAN_POINT ( 'NONE',  ( 20.04006244057629971, -8.354997041254607737, -67.16476753011970402 ) ) ;
#6600=VECTOR ( 'NONE', #19896, 1000.000000000000000 ) ;
#6601=ORIENTED_EDGE ( 'NONE', *, *, #39218, .F. ) ;
#6611=CARTESIAN_POINT ( 'NONE',  ( 24.04460285965960864, -15.61618860597671876, -65.79233133698019742 ) ) ;
#6644=VECTOR ( 'NONE', #4256, 1000.000000000000000 ) ;
#6646=EDGE_CURVE ( 'NONE', #25231, #14553, #48465, .T. ) ;
#6653=CARTESIAN_POINT ( 'NONE',  ( 9.366715917462860475, -15.61603296970410071, -51.45282021618999835 ) ) ;
#6655=CARTESIAN_POINT ( 'NONE',  ( 22.88143834593734027, -16.17571944551308860, -46.47913774983016566 ) ) ;
#6661=CARTESIAN_POINT ( 'NONE',  ( 24.04465145034966156, -15.61618865458276595, -39.79233592887338489 ) ) ;
#6663=CARTESIAN_POINT ( 'NONE',  ( 10.80048316119169982, -9.328284477191109758, -32.78375144850900114 ) ) ;
#6666=EDGE_CURVE ( 'NONE', #22911, #3350, #28529, .T. ) ;
#6675=CARTESIAN_POINT ( 'NONE',  ( 29.99034385824719706, -15.61618894467929941, -32.14999999999999858 ) ) ;
#6684=CARTESIAN_POINT ( 'NONE',  ( 22.84664696149711105, -16.49985153785048908, -62.49449331979504052 ) ) ;
#6689=CARTESIAN_POINT ( 'NONE',  ( 13.70954523500570055, -22.66097545527179946, -51.67284482273019819 ) ) ;
#6693=CARTESIAN_POINT ( 'NONE',  ( 15.24817145470214719, -22.38319284411442212, -68.99448578136716037 ) ) ;
#6697=CARTESIAN_POINT ( 'NONE',  ( 9.074293494951078287, -16.25319589821559774, -81.23899999999999011 ) ) ;
#6706=ORIENTED_EDGE ( 'NONE', *, *, #1153, .T. ) ;
#6707=CARTESIAN_POINT ( 'NONE',  ( 10.05068326232998288, -12.54826803111968303, -79.60166762876662006 ) ) ;
#6709=CARTESIAN_POINT ( 'NONE',  ( 20.11809143863368377, -8.703679352620326881, -63.45899965378977470 ) ) ;
#6712=AXIS2_PLACEMENT_3D ( 'NONE', #2441, #2711, #8122 ) ;
#6726=CARTESIAN_POINT ( 'NONE',  ( 22.78736197255772922, -17.44565462478292872, -42.93322834753961814 ) ) ;
#6728=CARTESIAN_POINT ( 'NONE',  ( 8.836122779856628640, -12.73024889214359945, -48.40737475858179550 ) ) ;
#6737=CARTESIAN_POINT ( 'NONE',  ( 20.98195727178219983, -10.76281971865039999, -32.14999999999999858 ) ) ;
#6738=CARTESIAN_POINT ( 'NONE',  ( 16.13393739769620083, -15.61618894467929941, -32.14999999999999858 ) ) ;
#6741=DIRECTION ( 'NONE',  ( 0.000000000000000000, 0.000000000000000000, -1.000000000000000000 ) ) ;
#6742=CARTESIAN_POINT ( 'NONE',  ( 17.32262310423930174, -8.664240623128923957, -36.40108501799142005 ) ) ;
#6746=CARTESIAN_POINT ( 'NONE',  ( 23.08438461476639958, -16.81362063674830054, -74.90148551491040507 ) ) ;
#6754=VECTOR ( 'NONE', #41439, 1000.000000000000000 ) ;
#6769=VERTEX_POINT ( 'NONE', #40535 ) ;
#6778=CARTESIAN_POINT ( 'NONE',  ( 24.04468094043696880, -15.55032358031935047, -33.78968039492959718 ) ) ;
#6779=CARTESIAN_POINT ( 'NONE',  ( 15.09849799342586607, -23.52720200456179711, -48.33399909089389723 ) ) ;
#6781=CARTESIAN_POINT ( 'NONE',  ( 17.90524838325329071, -9.025333659381530538, -52.03615204234977654 ) ) ;
#6783=CARTESIAN_POINT ( 'NONE',  ( 21.25937865767100021, -21.55896602969010090, -46.28595751040398909 ) ) ;
#6789=CARTESIAN_POINT ( 'NONE',  ( 10.74314122376619984, -11.06845590621349906, -78.07024275745519049 ) ) ;
#6792=CARTESIAN_POINT ( 'NONE',  ( 14.74159083669250059, -8.702150310963681079, -48.28392467753440087 ) ) ;
#6793=CARTESIAN_POINT ( 'NONE',  ( 12.72586417107244827, -9.703323737910269031, -43.78612585668066970 ) ) ;
#6799=CARTESIAN_POINT ( 'NONE',  ( 14.06334000076352098, -7.911067765953196051, -50.92433393874132008 ) ) ;
#6814=CARTESIAN_POINT ( 'NONE',  ( 22.46012469463212469, -20.47783660219755220, -74.00066485091836910 ) ) ;
#6817=CARTESIAN_POINT ( 'NONE',  ( 9.082333282492209392, -15.48413554993459940, -45.45878041868800068 ) ) ;
#6823=CARTESIAN_POINT ( 'NONE',  ( 23.94862035779809872, -16.33554867129409871, -37.31672440967509630 ) ) ;
#6824=EDGE_CURVE ( 'NONE', #1526, #4493, #21401, .T. ) ;
#6832=DIRECTION ( 'NONE',  ( 0.000000000000000000, 0.000000000000000000, -1.000000000000000000 ) ) ;
#6833=CARTESIAN_POINT ( 'NONE',  ( 22.03288545771612306, -12.23521849110922233, -62.28727064598228935 ) ) ;
#6834=AXIS2_PLACEMENT_3D ( 'NONE', #4761, #31737, #43827 ) ;
#6836=CARTESIAN_POINT ( 'NONE',  ( 20.89950193901299613, -21.95748695813169959, -45.80256656510095326 ) ) ;
#6841=CARTESIAN_POINT ( 'NONE',  ( 9.221455577410790028, -11.63198688526945546, -46.95899850799102637 ) ) ;
#6846=ORIENTED_EDGE ( 'NONE', *, *, #19462, .T. ) ;
#6848=CYLINDRICAL_SURFACE ( 'NONE', #17517, 6.766999999999998572 ) ;
#6850=CARTESIAN_POINT ( 'NONE',  ( 14.06321007543174417, -7.911101406802497849, -69.20899948135398461 ) ) ;
#6851=CARTESIAN_POINT ( 'NONE',  ( 23.82603912714330363, -18.58507611662970049, -61.90958082047689004 ) ) ;
#6857=CARTESIAN_POINT ( 'NONE',  ( 21.31786979423969797, -20.96722050067040399, -56.48770572707099547 ) ) ;
#6860=CARTESIAN_POINT ( 'NONE',  ( 8.912722752349319322, -17.33563004555450249, -32.14999999999999858 ) ) ;
#6861=DIRECTION ( 'NONE',  ( 0.000000000000000000, 0.000000000000000000, 1.000000000000000000 ) ) ;
#6864=EDGE_CURVE ( 'NONE', #50522, #8604, #28270, .T. ) ;
#6869=CARTESIAN_POINT ( 'NONE',  ( 13.39647449081169839, -23.39365752657710473, -68.11539470288319364 ) ) ;
#6891=CARTESIAN_POINT ( 'NONE',  ( 24.04493739769620930, -15.61618894467930119, -81.23899999999999011 ) ) ;
#6897=CARTESIAN_POINT ( 'NONE',  ( 22.90093729192429350, -15.13018493110448759, -66.42996439909107664 ) ) ;
#6914=CARTESIAN_POINT ( 'NONE',  ( 24.33017316509850048, -16.51309434721139979, -37.82702577713659764 ) ) ;
#6917=CARTESIAN_POINT ( 'NONE',  ( 22.31602583494875702, -18.45493576387408652, -50.58969767961466601 ) ) ;
#6923=DIRECTION ( 'NONE',  ( 1.000000000000000000, 0.000000000000000000, 0.000000000000000000 ) ) ;
#6928=CARTESIAN_POINT ( 'NONE',  ( 10.62413350085140173, -21.20446320448329658, -78.03525497637551211 ) ) ;
#6938=CARTESIAN_POINT ( 'NONE',  ( 8.222952931006085819, -16.65185013945336223, -38.75066497196897330 ) ) ;
#6943=CARTESIAN_POINT ( 'NONE',  ( 24.04493320937934442, -15.61618918076996110, -53.79232900421944663 ) ) ;
#6951=CARTESIAN_POINT ( 'NONE',  ( 10.60517752403560010, -20.61013614081009848, -67.83350675970849863 ) ) ;
#6957=CARTESIAN_POINT ( 'NONE',  ( 9.176796790077460741, -16.74902148356379783, -81.23899999999999011 ) ) ;
#6964=CARTESIAN_POINT ( 'NONE',  ( 23.39056959072010144, -13.30350361608390131, -81.23899999999999011 ) ) ;
#6979=DIRECTION ( 'NONE',  ( 0.000000000000000000, 0.000000000000000000, 1.000000000000000000 ) ) ;
#6981=EDGE_CURVE ( 'NONE', #9856, #21614, #27609, .T. ) ;
#6986=CARTESIAN_POINT ( 'NONE',  ( 22.62628819889769716, -20.02483150870289919, -53.47738634665349622 ) ) ;
#6987=VERTEX_POINT ( 'NONE', #6943 ) ;
#6989=VECTOR ( 'NONE', #38955, 1000.000000000000000 ) ;
#7000=CARTESIAN_POINT ( 'NONE',  ( 22.48345733077898245, -12.66161032470672332, -36.70821858127289516 ) ) ;
#7001=CARTESIAN_POINT ( 'NONE',  ( 24.04485091158800003, -15.61618876680915236, -45.79233931912149558 ) ) ;
#7005=CARTESIAN_POINT ( 'NONE',  ( 18.68994930968700174, -9.042806080414319325, -70.46522537534779929 ) ) ;
#7009=CARTESIAN_POINT ( 'NONE',  ( 22.46012054408591752, -20.47784229346886065, -57.71600103834494178 ) ) ;
#7015=CARTESIAN_POINT ( 'NONE',  ( 18.20470158624356927, -7.911112766937162810, -67.37566343967748139 ) ) ;
#7018=CARTESIAN_POINT ( 'NONE',  ( 16.13393739769620083, -15.61618894467929941, -32.14999999999999858 ) ) ;
#7028=CARTESIAN_POINT ( 'NONE',  ( 24.04463300525956981, -15.61618495692933273, -55.50767188603018809 ) ) ;
#7039=CARTESIAN_POINT ( 'NONE',  ( 20.29261090969894354, -10.20487204212595245, -52.16115171938402995 ) ) ;
#7041=CARTESIAN_POINT ( 'NONE',  ( 21.63365994436270157, -21.21438503817850219, -40.26531874956899770 ) ) ;
#7050=CARTESIAN_POINT ( 'NONE',  ( 23.01920207597069634, -14.08789267609899909, -38.77765294989999489 ) ) ;
#7066=CARTESIAN_POINT ( 'NONE',  ( 18.31867110002825427, -23.24857340604850364, -32.20353412124205761 ) ) ;
#7073=CARTESIAN_POINT ( 'NONE',  ( 16.46289132105319908, -8.571024043077699162, -40.36203157117240181 ) ) ;
#7076=CARTESIAN_POINT ( 'NONE',  ( 9.338672804374079206, -13.72755509891449854, -53.53911138717720064 ) ) ;
#7082=CARTESIAN_POINT ( 'NONE',  ( 15.03207885390800058, -7.846204650443991291, -38.74266516882029521 ) ) ;
#7090=CARTESIAN_POINT ( 'NONE',  ( 10.90011346691389171, -20.34373019107950498, -67.61334385707304762 ) ) ;
#7094=VERTEX_POINT ( 'NONE', #47043 ) ;
#7102=EDGE_CURVE ( 'NONE', #32691, #19523, #43358, .T. ) ;
#7106=FACE_OUTER_BOUND ( 'NONE', #8494, .T. ) ;
#7109=CARTESIAN_POINT ( 'NONE',  ( 14.17907360716779941, -7.606118556947649267, -59.21613716431379260 ) ) ;
#7115=CARTESIAN_POINT ( 'NONE',  ( 20.62402991675640251, -21.56141921569700060, -52.52675917389010607 ) ) ;
#7118=EDGE_CURVE ( 'NONE', #34659, #33336, #33288, .T. ) ;
#7119=LINE ( 'NONE', #39090, #21645 ) ;
#7125=CARTESIAN_POINT ( 'NONE',  ( 22.72588359820849746, -10.66351633299509949, -61.30256663141189932 ) ) ;
#7129=CARTESIAN_POINT ( 'NONE',  ( 19.54188346692635037, -9.703250399025609596, -60.11946100766459722 ) ) ;
#7138=CARTESIAN_POINT ( 'NONE',  ( 13.54377112832909980, -8.630651498136270305, -79.61963359764780535 ) ) ;
#7154=CARTESIAN_POINT ( 'NONE',  ( 9.366921553120977961, -14.97355191961400500, -65.48305900605150498 ) ) ;
#7163=CARTESIAN_POINT ( 'NONE',  ( 21.28925556178230494, -21.62091513535972709, -77.78184806566041232 ) ) ;
#7167=ORIENTED_EDGE ( 'NONE', *, *, #9190, .T. ) ;
#7170=CARTESIAN_POINT ( 'NONE',  ( 9.133937397696382021, -15.61618894467929763, -23.74958330439410048 ) ) ;
#7174=CARTESIAN_POINT ( 'NONE',  ( 22.90093738118858013, -16.50198597715758808, -36.49448425584234457 ) ) ;
#7176=EDGE_CURVE ( 'NONE', #22439, #1287, #42692, .T. ) ;
#7180=CARTESIAN_POINT ( 'NONE',  ( 8.445554253283772184, -12.63784234794610128, -32.62531358638169365 ) ) ;
#7189=CARTESIAN_POINT ( 'NONE',  ( 17.16953927579633898, -23.52718117654557872, -38.25066653675266792 ) ) ;
#7201=CARTESIAN_POINT ( 'NONE',  ( 8.826359436922910362, -14.16498300286340140, -62.12974372312799431 ) ) ;
#7207=PLANE ( 'NONE',  #37416 ) ;
#7209=CARTESIAN_POINT ( 'NONE',  ( 9.006752130201981288, -14.38476595312559958, -81.23899999999999011 ) ) ;
#7214=ORIENTED_EDGE ( 'NONE', *, *, #35453, .F. ) ;
#7215=EDGE_CURVE ( 'NONE', #40924, #43673, #35743, .T. ) ;
#7218=CARTESIAN_POINT ( 'NONE',  ( 23.37200753273739906, -13.22834593274319914, -81.23899999999999011 ) ) ;
#7221=EDGE_CURVE ( 'NONE', #11267, #16071, #32809, .T. ) ;
#7224=CARTESIAN_POINT ( 'NONE',  ( 9.807767002083743080, -10.75451754946909944, -52.71600246173886717 ) ) ;
#7225=ORIENTED_EDGE ( 'NONE', *, *, #48943, .T. ) ;
#7233=AXIS2_PLACEMENT_3D ( 'NONE', #17868, #29902, #46450 ) ;
#7234=VECTOR ( 'NONE', #46665, 1000.000000000000000 ) ;
#7241=CARTESIAN_POINT ( 'NONE',  ( 8.298661659914731814, -16.05800598386570144, -54.26957565728969257 ) ) ;
#7244=CYLINDRICAL_SURFACE ( 'NONE', #8757, 6.766999999999998572 ) ;
#7250=CARTESIAN_POINT ( 'NONE',  ( 16.13393739769620083, -15.61618894467929941, -28.45282021618999835 ) ) ;
#7253=CARTESIAN_POINT ( 'NONE',  ( 24.04525281611314824, -15.61618915252426376, -57.50766930885080086 ) ) ;
#7256=CARTESIAN_POINT ( 'NONE',  ( 8.222926147295824606, -14.58072384180595549, -70.83399561464088379 ) ) ;
#7258=CARTESIAN_POINT ( 'NONE',  ( 20.74347699498930098, -9.763083867941830363, -36.77968578276969680 ) ) ;
#7261=CARTESIAN_POINT ( 'NONE',  ( 20.99565119372854483, -21.94232563707941353, -57.79933445449422891 ) ) ;
#7262=AXIS2_PLACEMENT_3D ( 'NONE', #40049, #47919, #40306 ) ;
#7265=CYLINDRICAL_SURFACE ( 'NONE', #13940, 6.766999999999998572 ) ;
#7267=CARTESIAN_POINT ( 'NONE',  ( 12.14991857309165368, -8.703602074731387361, -67.12566404048868662 ) ) ;
#7269=ORIENTED_EDGE ( 'NONE', *, *, #9567, .F. ) ;
#7273=DIRECTION ( 'NONE',  ( 0.000000000000000000, 0.000000000000000000, 1.000000000000000000 ) ) ;
#7275=CARTESIAN_POINT ( 'NONE',  ( 8.222937397696199469, -15.61618894467929941, -32.14999999999999858 ) ) ;
#7279=B_SPLINE_CURVE_WITH_KNOTS ( 'NONE', 3,
 ( #30517, #34450, #13527, #5661, #49941, #17702, #9587, #42071, #9843, #29990 ),
 .UNSPECIFIED., .F., .F.,
 ( 4, 1, 1, 1, 1, 1, 1, 4 ),
 ( 0.4999968673859223056, 0.5271528655503062710, 0.6063717966138713056, 0.6855907276774317882, 0.7648096587411550296, 0.8440285898047201751, 0.9232475208684389756, 1.000000000000000000 ),
 .UNSPECIFIED. ) ;
#7280=ORIENTED_EDGE ( 'NONE', *, *, #44073, .T. ) ;
#7282=CARTESIAN_POINT ( 'NONE',  ( 24.04489399084747703, -15.64449660401445996, -55.50881072821707818 ) ) ;
#7285=CARTESIAN_POINT ( 'NONE',  ( 10.81595853043058675, -11.36155942741024560, -45.66747770548867891 ) ) ;
#7291=CARTESIAN_POINT ( 'NONE',  ( 20.48068097650709873, -21.17032068915356646, -51.13580619584276832 ) ) ;
#7293=CARTESIAN_POINT ( 'NONE',  ( 14.06332963686348059, -23.32130743969031172, -54.09100309838140674 ) ) ;
#7294=CARTESIAN_POINT ( 'NONE',  ( 8.617266676947521020, -17.87149576802320183, -46.91970895891299165 ) ) ;
#7302=CARTESIAN_POINT ( 'NONE',  ( 9.942021269482310686, -12.23939551960640060, -44.00610240009889651 ) ) ;
#7303=CARTESIAN_POINT ( 'NONE',  ( 22.72480813554982149, -13.84492922675662463, -44.36947208136891163 ) ) ;
#7310=CARTESIAN_POINT ( 'NONE',  ( 9.555189432054399745, -11.06668960550747727, -54.70064004558554416 ) ) ;
#7329=CARTESIAN_POINT ( 'NONE',  ( 9.677450050134419612, -18.45455640281440068, -51.32098131739589775 ) ) ;
#7331=CARTESIAN_POINT ( 'NONE',  ( 22.20691379552689426, -12.48290680228687322, -80.69525706773917761 ) ) ;
#7334=CARTESIAN_POINT ( 'NONE',  ( 23.37872820719320188, -17.35397704167489863, -81.14228717839650074 ) ) ;
#7340=CARTESIAN_POINT ( 'NONE',  ( 24.04493741668374440, -16.65174122825144920, -39.83400417788456593 ) ) ;
#7350=CARTESIAN_POINT ( 'NONE',  ( 10.09028208944064353, -10.43082494342464450, -76.73325434315464122 ) ) ;
#7352=ORIENTED_EDGE ( 'NONE', *, *, #21820, .T. ) ;
#7358=CARTESIAN_POINT ( 'NONE',  ( 22.16775957127159913, -9.996962126548099903, -65.55365164940339184 ) ) ;
#7364=ORIENTED_EDGE ( 'NONE', *, *, #48986, .F. ) ;
#7366=CARTESIAN_POINT ( 'NONE',  ( 20.14552668288030191, -9.338144248108390499, -57.91364648621609490 ) ) ;
#7369=CARTESIAN_POINT ( 'NONE',  ( 10.11873436104249890, -20.36210433234809969, -32.14999999999999858 ) ) ;
#7372=B_SPLINE_CURVE_WITH_KNOTS ( 'NONE', 3,
 ( #6611, #38591, #45934, #46203, #10023, #42000, #22055, #39106, #26507, #26766, #35150, #26251, #2938, #30440, #18142, #34107, #38322, #2411, #14214, #18393, #34371, #50384, #43549, #47233, #23336, #3715 ),
 .UNSPECIFIED., .F., .F.,
 ( 4, 2, 2, 2, 2, 2, 2, 2, 2, 2, 2, 2, 4 ),
 ( 0.5000000130881896432, 0.5625000114521658823, 0.6250000098161422324, 0.6875000081801185825, 0.7500000065440948216, 0.7812500057260829411, 0.8125000049080710607, 0.8437500040900592913, 0.8750000032720474108, 0.9062500024540355303, 0.9375000016360237609, 0.9687500008180118805, 1.000000000000000000 ),
 .UNSPECIFIED. ) ;
#7374=CARTESIAN_POINT ( 'NONE',  ( 19.86463262639870209, -22.96905463225390065, -69.85821118628290094 ) ) ;
#7375=CARTESIAN_POINT ( 'NONE',  ( 21.17364772268240003, -21.52724977567429931, -32.14999999999999858 ) ) ;
#7385=CARTESIAN_POINT ( 'NONE',  ( 15.82102960914879830, -7.675182713834671766, -80.99522283173863002 ) ) ;
#7391=CARTESIAN_POINT ( 'NONE',  ( 21.28336590497879754, -10.23194527880280091, -75.97556276872150249 ) ) ;
#7394=CARTESIAN_POINT ( 'NONE',  ( 8.222948648952634443, -16.65181879039660018, -70.75066497221537531 ) ) ;
#7396=B_SPLINE_CURVE_WITH_KNOTS ( 'NONE', 3,
 ( #1859, #17838, #30394, #49822, #22270, #46417, #13914, #29870, #10504, #45891, #9977, #41956, #38280, #10244, #34324, #50339, #22530, #16418 ),
 .UNSPECIFIED., .F., .F.,
 ( 4, 2, 2, 2, 2, 2, 2, 2, 4 ),
 ( 0.000000000000000000, 0.06249998230893073076, 0.1249999646178614615, 0.1874999469267921992, 0.2499999292357229230, 0.3124999115446535636, 0.3749998938535841764, 0.4374998761625147892, 0.4999998584714454020 ),
 .UNSPECIFIED. ) ;
#7398=CARTESIAN_POINT ( 'NONE',  ( 15.09829607975676957, -23.52717697970637190, -62.04932902358816449 ) ) ;
#7407=CARTESIAN_POINT ( 'NONE',  ( 11.03453497164934838, -11.13167925635793942, -65.68238587149497221 ) ) ;
#7409=ORIENTED_EDGE ( 'NONE', *, *, #22875, .T. ) ;
#7410=CARTESIAN_POINT ( 'NONE',  ( 9.366458663215507130, -15.75911442933090889, -37.84046178158559570 ) ) ;
#7417=VERTEX_POINT ( 'NONE', #35870 ) ;
#7422=CARTESIAN_POINT ( 'NONE',  ( 18.64322687137160273, -7.762133735154519876, -33.39076563757389948 ) ) ;
#7424=CARTESIAN_POINT ( 'NONE',  ( 21.98228690486360648, -21.02318771973998324, -50.02964728310828235 ) ) ;
#7426=CARTESIAN_POINT ( 'NONE',  ( 22.04685551236088870, -12.20820984684314681, -64.28615539813523583 ) ) ;
#7428=CARTESIAN_POINT ( 'NONE',  ( 23.84448207147010024, -14.15528223125809859, -71.95289117501670262 ) ) ;
#7437=CARTESIAN_POINT ( 'NONE',  ( 21.98967281619519909, -9.811619623081579533, -33.25906503489069621 ) ) ;
#7446=CARTESIAN_POINT ( 'NONE',  ( 23.04647088892617646, -19.60030115133175599, -37.95900078287649393 ) ) ;
#7447=CARTESIAN_POINT ( 'NONE',  ( 15.24823161472325772, -22.38320011598096926, -48.99448779884927774 ) ) ;
#7451=CARTESIAN_POINT ( 'NONE',  ( 22.90112932213407149, -15.61618880384378905, -64.45281843961751633 ) ) ;
#7458=CARTESIAN_POINT ( 'NONE',  ( 9.344596190075201037, -18.68401232695549652, -65.93225241418160465 ) ) ;
#7463=CARTESIAN_POINT ( 'NONE',  ( 21.43037387198247856, -19.89010587847297984, -34.66902735005525216 ) ) ;
#7465=AXIS2_PLACEMENT_3D ( 'NONE', #11944, #35523, #15613 ) ;
#7468=CARTESIAN_POINT ( 'NONE',  ( 11.84380770541370076, -9.249706252957370367, -81.23899999999999011 ) ) ;
#7477=CARTESIAN_POINT ( 'NONE',  ( 23.01036527161310019, -12.13836321956489783, -81.23899999999999011 ) ) ;
#7480=CARTESIAN_POINT ( 'NONE',  ( 23.04646052128485323, -11.63205733350218551, -53.34100437166649300 ) ) ;
#7488=CARTESIAN_POINT ( 'NONE',  ( 22.88339355091036964, -15.11907872941729991, -40.42942904639821222 ) ) ;
#7497=CARTESIAN_POINT ( 'NONE',  ( 15.08639525488320032, -7.838695541132539191, -54.74488924367149423 ) ) ;
#7498=ORIENTED_EDGE ( 'NONE', *, *, #22640, .T. ) ;
#7499=DIRECTION ( 'NONE',  ( 0.000000000000000000, 0.000000000000000000, -1.000000000000000000 ) ) ;
#7506=ADVANCED_FACE ( 'NONE', ( #29791 ), #25601, .T. ) ;
#7514=CARTESIAN_POINT ( 'NONE',  ( 17.16955493387669307, -23.52717894132403842, -37.96600343497949126 ) ) ;
#7516=VERTEX_POINT ( 'NONE', #13331 ) ;
#7517=CARTESIAN_POINT ( 'NONE',  ( 8.698584540071550464, -16.08759346412580271, -38.04718867978759533 ) ) ;
#7527=CARTESIAN_POINT ( 'NONE',  ( 16.13393739769620083, -15.61618894467929941, -28.45282021618999835 ) ) ;
#7531=EDGE_CURVE ( 'NONE', #31864, #50665, #23400, .T. ) ;
#7533=CARTESIAN_POINT ( 'NONE',  ( 9.921778078347148977, -18.94533778500921173, -59.69054780769135249 ) ) ;
#7540=VECTOR ( 'NONE', #30516, 1000.000000000000000 ) ;
#7542=CARTESIAN_POINT ( 'NONE',  ( 22.46008086064721354, -20.47789713743962281, -55.71595987601556743 ) ) ;
#7545=CARTESIAN_POINT ( 'NONE',  ( 22.90091625179776358, -15.59788028122024350, -46.45196706549376842 ) ) ;
#7551=CARTESIAN_POINT ( 'NONE',  ( 12.14992424677891947, -22.52877902415496081, -48.45899884107838318 ) ) ;
#7552=CARTESIAN_POINT ( 'NONE',  ( 22.72481315194836782, -13.84495412362821831, -52.36948451444106212 ) ) ;
#7555=CARTESIAN_POINT ( 'NONE',  ( 23.05439743991649948, -19.31672679688609762, -58.16879716994689886 ) ) ;
#7560=CARTESIAN_POINT ( 'NONE',  ( 14.36274735259626567, -22.20707703622060336, -39.03615485351005532 ) ) ;
#7561=CARTESIAN_POINT ( 'NONE',  ( 13.41159479355990136, -22.12244823248479975, -57.47332068091419188 ) ) ;
#7576=ADVANCED_FACE ( 'NONE', ( #33219 ), #25350, .T. ) ;
#7580=CARTESIAN_POINT ( 'NONE',  ( 8.428882786094106905, -17.68703364650084353, -58.70899815131578237 ) ) ;
#7587=CARTESIAN_POINT ( 'NONE',  ( 9.367202679915338948, -15.61634672871210050, -75.45282021618999124 ) ) ;
#7590=CARTESIAN_POINT ( 'NONE',  ( 10.56036407591849979, -19.93797551083379815, -59.24287442375789681 ) ) ;
#7595=CARTESIAN_POINT ( 'NONE',  ( 10.70276100678979958, -21.28091057897379912, -46.03080682667329881 ) ) ;
#7604=LINE ( 'NONE', #2897, #28424 ) ;
#7606=CARTESIAN_POINT ( 'NONE',  ( 8.222916120934886663, -14.58079724080996264, -74.54932982785270212 ) ) ;
#7611=CARTESIAN_POINT ( 'NONE',  ( 17.01696881212998136, -7.733254499902739276, -77.04325171109016424 ) ) ;
#7616=FILL_AREA_STYLE ('',( #11548 ) ) ;
#7618=CARTESIAN_POINT ( 'NONE',  ( 9.493364934882555062, -17.11955126427607965, -33.38210457755312177 ) ) ;
#7620=EDGE_CURVE ( 'NONE', #20658, #31407, #2823, .T. ) ;
#7621=TOROIDAL_SURFACE ( 'NONE', #31856, 6.949999999999999289, 2.999999999999960032 ) ;
#7622=CARTESIAN_POINT ( 'NONE',  ( 21.43117737877189910, -21.93457233315599808, -78.07024275745530417 ) ) ;
#7623=EDGE_CURVE ( 'NONE', #22194, #42604, #25105, .T. ) ;
#7625=DIRECTION ( 'NONE',  ( 0.000000000000000000, 0.000000000000000000, -1.000000000000000000 ) ) ;
#7628=CARTESIAN_POINT ( 'NONE',  ( 13.14039184046809972, -22.43860631698549923, -58.86427365897949926 ) ) ;
#7630=CARTESIAN_POINT ( 'NONE',  ( 11.76305550340469885, -22.11297765233079815, -32.14999999999999858 ) ) ;
#7636=CARTESIAN_POINT ( 'NONE',  ( 23.94181861929380162, -12.96671512174780005, -75.40353636073618304 ) ) ;
#7638=CARTESIAN_POINT ( 'NONE',  ( 22.14137220198069755, -20.37380969475220027, -32.14999999999999858 ) ) ;
#7647=CIRCLE ( 'NONE', #26027, 2.999999999999960920 ) ;
#7650=DIRECTION ( 'NONE',  ( 0.5000000000000003331, 0.8660254037844383745, 0.000000000000000000 ) ) ;
#7654=CARTESIAN_POINT ( 'NONE',  ( 23.45398833085310031, -14.22926856443589827, -72.17305407766770031 ) ) ;
#7659=ORIENTED_EDGE ( 'NONE', *, *, #45538, .F. ) ;
#7660=LINE ( 'NONE', #40644, #21265 ) ;
#7676=CARTESIAN_POINT ( 'NONE',  ( 21.70064287550836113, -21.23721361656830453, -77.75920763157944293 ) ) ;
#7683=CARTESIAN_POINT ( 'NONE',  ( 13.37138816098100058, -23.38478223887699770, -36.40108501799149820 ) ) ;
#7684=ADVANCED_FACE ( 'NONE', ( #31086, #47114 ), #18017, .T. ) ;
#7685=CARTESIAN_POINT ( 'NONE',  ( 16.13393739769620083, -15.61618894467929941, -28.45282021618999835 ) ) ;
#7693=CARTESIAN_POINT ( 'NONE',  ( 23.60773268908170053, -13.22262851426480168, -75.91383772819759201 ) ) ;
#7701=CARTESIAN_POINT ( 'NONE',  ( 22.01250374557920253, -21.39764018139420187, -39.75501738210738978 ) ) ;
#7707=CARTESIAN_POINT ( 'NONE',  ( 9.367479537931210132, -15.61613030728229923, -79.45282021618999124 ) ) ;
#7720=CARTESIAN_POINT ( 'NONE',  ( 24.04489396232973064, -15.58787332083394617, -75.79118696779985953 ) ) ;
#7721=CARTESIAN_POINT ( 'NONE',  ( 15.24810277342973031, -22.38318460617302819, -62.99448372488342329 ) ) ;
#7724=CARTESIAN_POINT ( 'NONE',  ( 9.020183826706210439, -17.83005535202389780, -61.97130586100059446 ) ) ;
#7730=CARTESIAN_POINT ( 'NONE',  ( 9.973190895944735956, -18.47182041587143431, -35.31469777396277010 ) ) ;
#7733=CARTESIAN_POINT ( 'NONE',  ( 9.374784576662598568, -12.69651527581430095, -81.23899999999999011 ) ) ;
#7739=CARTESIAN_POINT ( 'NONE',  ( 23.51964986281049974, -16.15416379988030116, -81.23899999999999011 ) ) ;
#7742=CARTESIAN_POINT ( 'NONE',  ( 20.25644374842187645, -10.19188613274733157, -80.15984542592896389 ) ) ;
#7744=CARTESIAN_POINT ( 'NONE',  ( 9.221449101009920213, -11.63199795648596258, -62.95899854462519585 ) ) ;
#7752=CARTESIAN_POINT ( 'NONE',  ( 16.13393739769620083, -3.616188944679339823, -22.14999999999999858 ) ) ;
#7757=CARTESIAN_POINT ( 'NONE',  ( 9.934167556912912644, -18.97671188063486980, -43.68906509112390779 ) ) ;
#7758=CARTESIAN_POINT ( 'NONE',  ( 11.14170694428959862, -9.561076783599030904, -64.56803669556019543 ) ) ;
#7774=CARTESIAN_POINT ( 'NONE',  ( 11.68549127948460153, -10.14317847777680015, -80.12993496510929958 ) ) ;
#7775=CARTESIAN_POINT ( 'NONE',  ( 11.97525711002020898, -21.02750221141963394, -77.16116563337958212 ) ) ;
#7776=ORIENTED_EDGE ( 'NONE', *, *, #29136, .F. ) ;
#7792=CARTESIAN_POINT ( 'NONE',  ( 22.90117443638819239, -15.61618876209028528, -62.84717844892357164 ) ) ;
#7796=CARTESIAN_POINT ( 'NONE',  ( 20.11801379417378755, -22.52874512401025342, -55.84094417680480404 ) ) ;
#7797=CARTESIAN_POINT ( 'NONE',  ( 12.20479792536879948, -10.10644435241950134, -32.14999999999999858 ) ) ;
#7800=CARTESIAN_POINT ( 'NONE',  ( 22.90093709110179887, -15.61375976151432532, -46.45271396509134831 ) ) ;
#7809=CARTESIAN_POINT ( 'NONE',  ( 18.57444516463139905, -8.157591929750100945, -49.61315261507609620 ) ) ;
#7817=CARTESIAN_POINT ( 'NONE',  ( 14.34415610061919821, -8.794221333858748935, -58.26550999155039534 ) ) ;
#7830=CARTESIAN_POINT ( 'NONE',  ( 9.366916744691108576, -14.73054192615060032, -75.49448329847818684 ) ) ;
#7836=EDGE_LOOP ( 'NONE', ( #34578, #14099, #19479, #7659 ) ) ;
#7842=DIRECTION ( 'NONE',  ( 0.000000000000000000, 0.000000000000000000, -1.000000000000000000 ) ) ;
#7843=CARTESIAN_POINT ( 'NONE',  ( 22.07441835734369917, -11.81444662507229992, -52.27160849015929500 ) ) ;
#7849=CARTESIAN_POINT ( 'NONE',  ( 13.17756150054800024, -8.346622950897849336, -46.66455827518229427 ) ) ;
#7850=ORIENTED_EDGE ( 'NONE', *, *, #48497, .F. ) ;
#7863=CARTESIAN_POINT ( 'NONE',  ( 8.382179679036624975, -17.45534441210563159, -44.71833966285539219 ) ) ;
#7864=CARTESIAN_POINT ( 'NONE',  ( 19.37692227700529202, -8.371908506326338539, -77.14162090755425538 ) ) ;
#7866=CARTESIAN_POINT ( 'NONE',  ( 9.081253177307520019, -11.91239544520527005, -48.66177660431670660 ) ) ;
#7870=CARTESIAN_POINT ( 'NONE',  ( 11.27225553591746809, -21.94235124599162390, -36.21600094350794308 ) ) ;
#7875=CARTESIAN_POINT ( 'NONE',  ( 19.73760564896319991, -23.03213764937959951, -70.14834965109328380 ) ) ;
#7876=CARTESIAN_POINT ( 'NONE',  ( 22.72644110385109428, -13.50767635585680715, -38.74801692456930624 ) ) ;
#7880=CARTESIAN_POINT ( 'NONE',  ( 18.54562800134210221, -22.66533373234200255, -66.62772890321430452 ) ) ;
#7882=CARTESIAN_POINT ( 'NONE',  ( 10.42052905183000000, -20.77277191077440222, -32.14999999999999858 ) ) ;
#7888=CARTESIAN_POINT ( 'NONE',  ( 8.703895965235538768, -12.04166729543830172, -70.65040049691889124 ) ) ;
#7889=CARTESIAN_POINT ( 'NONE',  ( 22.52859995526739922, -19.73945381444989877, -32.14999999999999858 ) ) ;
#7896=ORIENTED_EDGE ( 'NONE', *, *, #43818, .T. ) ;
#7900=CARTESIAN_POINT ( 'NONE',  ( 18.20455076684766027, -23.32130774566027753, -72.20902145591645649 ) ) ;
#7902=CARTESIAN_POINT ( 'NONE',  ( 23.45321186227019794, -17.00720120824169612, -76.29243849297590430 ) ) ;
#7922=CARTESIAN_POINT ( 'NONE',  ( 23.04645333911465599, -11.63204389240351588, -55.62566189992365651 ) ) ;
#7925=CARTESIAN_POINT ( 'NONE',  ( 8.428802417734461372, -13.54563645402293659, -58.59099060088449562 ) ) ;
#7926=CARTESIAN_POINT ( 'NONE',  ( 15.10086521727856379, -23.46371762042167575, -78.04932787247608417 ) ) ;
#7930=CARTESIAN_POINT ( 'NONE',  ( 20.71851373775454519, -20.65600983156726045, -80.71802773679567622 ) ) ;
#7932=CARTESIAN_POINT ( 'NONE',  ( 23.92337672836263351, -17.04563464948125073, -65.56543222284031458 ) ) ;
#7934=CARTESIAN_POINT ( 'NONE',  ( 12.66766167757590011, -8.135035779020970637, -41.15422088180859816 ) ) ;
#7935=CARTESIAN_POINT ( 'NONE',  ( 20.99562311489945898, -21.94234805090159313, -67.79933317097351164 ) ) ;
#7937=CARTESIAN_POINT ( 'NONE',  ( 19.72404980843187516, -22.74131306260592567, -50.14348317235646135 ) ) ;
#7940=CARTESIAN_POINT ( 'NONE',  ( 8.428880519735075794, -17.68702540576067506, -42.70899812693631503 ) ) ;
#7941=CARTESIAN_POINT ( 'NONE',  ( 10.02178489954199847, -19.87626377456960114, -33.03890213223969141 ) ) ;
#7946=CARTESIAN_POINT ( 'NONE',  ( 19.01438204251930131, -7.890533027083360018, -39.12126593359850091 ) ) ;
#7956=CARTESIAN_POINT ( 'NONE',  ( 8.222412332301150428, -15.61630761206940043, -38.79233150823699816 ) ) ;
#7962=CARTESIAN_POINT ( 'NONE',  ( 10.22109577499819366, -19.02429973287621578, -65.28615391924572009 ) ) ;
#7964=CARTESIAN_POINT ( 'NONE',  ( 8.222937397696199469, -15.61618894467929941, -32.14999999999999858 ) ) ;
#7970=CARTESIAN_POINT ( 'NONE',  ( 20.43992966667520150, -9.536293804314230016, -62.76349517163679081 ) ) ;
#7975=CARTESIAN_POINT ( 'NONE',  ( 22.48775426134280409, -18.03232780092622889, -34.56855001936997240 ) ) ;
#7976=CARTESIAN_POINT ( 'NONE',  ( 9.438650519103310543, -12.51186047500710075, -81.23899999999999011 ) ) ;
#7977=VERTEX_POINT ( 'NONE', #39235 ) ;
#7982=CYLINDRICAL_SURFACE ( 'NONE', #16016, 6.766999999999998572 ) ;
#7983=CARTESIAN_POINT ( 'NONE',  ( 21.80530958182080070, -10.16180299264429898, -81.23899999999999011 ) ) ;
#7984=CARTESIAN_POINT ( 'NONE',  ( 9.807863175385746146, -10.75439414787492609, -73.00066484403033940 ) ) ;
#7987=CARTESIAN_POINT ( 'NONE',  ( 10.96668629868492317, -20.41640511211885212, -35.60889570735550080 ) ) ;
#7989=DIRECTION ( 'NONE',  ( -1.000000000000000000, -5.367253113454777116E-16, 0.000000000000000000 ) ) ;
#7997=CARTESIAN_POINT ( 'NONE',  ( 10.37507727206246244, -11.93657929354967528, -39.63413252511316642 ) ) ;
#7998=DIRECTION ( 'NONE',  ( 0.000000000000000000, 0.000000000000000000, -1.000000000000000000 ) ) ;
#8003=CARTESIAN_POINT ( 'NONE',  ( 23.95544421880619979, -14.97526833297029825, -67.26148035172319339 ) ) ;
#8011=CARTESIAN_POINT ( 'NONE',  ( 16.13393739769620083, -15.61618894467929941, -81.23899999999999011 ) ) ;
#8016=DIRECTION ( 'NONE',  ( 1.000000000000000000, 0.000000000000000000, 0.000000000000000000 ) ) ;
#8017=ADVANCED_FACE ( 'NONE', ( #612, #363 ), #24436, .T. ) ;
#8023=CARTESIAN_POINT ( 'NONE',  ( 16.34294028551579814, -22.66593182482080238, -79.33774565447309612 ) ) ;
#8031=CARTESIAN_POINT ( 'NONE',  ( 20.99565638127380041, -9.290056386383136910, -35.50066289986691004 ) ) ;
#8034=VERTEX_POINT ( 'NONE', #18155 ) ;
#8038=ORIENTED_EDGE ( 'NONE', *, *, #9938, .T. ) ;
#8039=CARTESIAN_POINT ( 'NONE',  ( 12.24635195013770073, -21.50085024014760293, -59.53301288856830098 ) ) ;
#8040=CARTESIAN_POINT ( 'NONE',  ( 12.14984766995591059, -8.703642186092894306, -79.12566561758120542 ) ) ;
#8046=EDGE_CURVE ( 'NONE', #36938, #12364, #30683, .T. ) ;
#8048=B_SPLINE_CURVE_WITH_KNOTS ( 'NONE', 3,
 ( #1229, #46501, #26291, #6655, #4899, #50158, #21129, #44995, #36868, #33178, #9095, #22358, #37130, #42563, #9363, #25312, #34672, #41314, #6399, #17218, #5174, #14255, #29249, #49200, #17473, #14512, #30223, #40796, #10330, #22615, #46243, #5425, #42300, #50673, #10593, #967, #20867, #38362, #21382, #2455, #18435, #18695, #45258, #38630, #16966, #26547, #13292 ),
 .UNSPECIFIED., .F., .F.,
 ( 4, 2, 2, 2, 2, 2, 2, 1, 1, 1, 2, 2, 2, 2, 2, 2, 2, 1, 1, 1, 1, 2, 2, 2, 2, 2, 4 ),
 ( 0.5000059655526006841, 0.5312555927055534477, 0.5625052198585062113, 0.5937548470114590859, 0.6093796605879354678, 0.6171920673761737142, 0.6210982707702927819, 0.6230513724673523157, 0.6240279233158819716, 0.6245161987401469661, 0.6247603364522794633, 0.6250044741644119606, 0.6562541013173609494, 0.6875037284703100493, 0.7187533556232591492, 0.7343781691997335326, 0.7421905759879710018, 0.7460967793820898475, 0.7480498810791493813, 0.7490264319276790372, 0.7495147073519436987, 0.7497588450640761959, 0.7500029827762088042, 0.8125022370821566309, 0.8750014913881043466, 0.9375007456940522843, 1.000000000000000000 ),
 .UNSPECIFIED. ) ;
#8053=CARTESIAN_POINT ( 'NONE',  ( 22.86958133952598615, -14.94427170521152881, -46.42118020533612111 ) ) ;
#8064=CARTESIAN_POINT ( 'NONE',  ( 8.486932887716839957, -17.37972789121199924, -52.94034771974808962 ) ) ;
#8072=CARTESIAN_POINT ( 'NONE',  ( 13.83887629744999970, -22.28516590674690079, -51.45268192007920049 ) ) ;
#8073=CARTESIAN_POINT ( 'NONE',  ( 18.20470410219303403, -7.911113479266316695, -41.37566450579876687 ) ) ;
#8079=CARTESIAN_POINT ( 'NONE',  ( 5.741632552282960766, -9.616188944679340267, -22.14999999999999858 ) ) ;
#8080=CARTESIAN_POINT ( 'NONE',  ( 16.13393739769620083, -15.61618894467929941, -28.45282021618999835 ) ) ;
#8087=CARTESIAN_POINT ( 'NONE',  ( 9.221436020990983806, -19.60035757305728410, -52.62566441095005842 ) ) ;
#8088=ADVANCED_FACE ( 'NONE', ( #5343 ), #29164, .T. ) ;
#8089=CYLINDRICAL_SURFACE ( 'NONE', #49365, 2.576499999999998902 ) ;
#8094=ORIENTED_EDGE ( 'NONE', *, *, #1565, .F. ) ;
#8101=CARTESIAN_POINT ( 'NONE',  ( 23.18661920690770017, -15.56888149661560128, -58.45068511312169335 ) ) ;
#8106=CARTESIAN_POINT ( 'NONE',  ( 22.36052287337500033, -20.39283855473529883, -43.49580103263740227 ) ) ;
#8115=CARTESIAN_POINT ( 'NONE',  ( 9.221344252930924412, -11.63217719309666975, -74.67431699540968282 ) ) ;
#8122=DIRECTION ( 'NONE',  ( 1.000000000000000000, 0.000000000000000000, 0.000000000000000000 ) ) ;
#8123=CARTESIAN_POINT ( 'NONE',  ( 23.45932441199935425, -12.52460061254321388, -49.38066021020333807 ) ) ;
#8125=CARTESIAN_POINT ( 'NONE',  ( 15.09834424264556318, -23.52718342601810519, -62.33399675319203936 ) ) ;
#8130=CARTESIAN_POINT ( 'NONE',  ( 10.24496007140159826, -21.38703515708219882, -78.54555634383700635 ) ) ;
#8134=CARTESIAN_POINT ( 'NONE',  ( 8.969861584858589865, -13.57102109018409841, -69.32117255937750144 ) ) ;
#8137=CARTESIAN_POINT ( 'NONE',  ( 10.44026233180520080, -20.79788605865429929, -32.14999999999999858 ) ) ;
#8144=CARTESIAN_POINT ( 'NONE',  ( 15.36781655846439953, -23.82568220362479749, -76.03728780924519981 ) ) ;
#8157=CARTESIAN_POINT ( 'NONE',  ( 20.24725285149263598, -22.43897999005509547, -66.11977884462595512 ) ) ;
#8159=CARTESIAN_POINT ( 'NONE',  ( 16.71323853210260069, -8.188463586211829792, -73.75743269894009302 ) ) ;
#8166=CARTESIAN_POINT ( 'NONE',  ( 9.205734167420720482, -3.616188944679329609, -24.14999999999999858 ) ) ;
#8179=CARTESIAN_POINT ( 'NONE',  ( 8.428814366912718015, -13.54559301151024719, -54.87566131310629203 ) ) ;
#8181=CARTESIAN_POINT ( 'NONE',  ( 20.29260965567053887, -21.02750684390549907, -58.74448668235789484 ) ) ;
#8189=CARTESIAN_POINT ( 'NONE',  ( 24.03992025865239768, -15.92081808833121670, -65.51992199243797188 ) ) ;
#8190=CARTESIAN_POINT ( 'NONE',  ( 15.11686583926219996, -7.433995748417090432, -39.25296653628179655 ) ) ;
#8192=CARTESIAN_POINT ( 'NONE',  ( 22.53432111889044975, -20.33647081035346105, -49.99467920166775059 ) ) ;
#8193=ORIENTED_EDGE ( 'NONE', *, *, #26950, .F. ) ;
#8196=CARTESIAN_POINT ( 'NONE',  ( 21.24986970212820125, -10.48466363836469917, -31.98264971805809509 ) ) ;
#8200=CARTESIAN_POINT ( 'NONE',  ( 17.84154075489263391, -23.41191558886454871, -60.22387759140665509 ) ) ;
#8204=CARTESIAN_POINT ( 'NONE',  ( 16.49341532545370015, -23.85351231628670376, -47.99378621272389722 ) ) ;
#8209=CARTESIAN_POINT ( 'NONE',  ( 8.222962928588657405, -16.65192332958894994, -64.75066493400071010 ) ) ;
#8210=CARTESIAN_POINT ( 'NONE',  ( 22.81411325381436228, -16.71917589191833287, -56.50489658860690412 ) ) ;
#8213=ORIENTED_EDGE ( 'NONE', *, *, #38049, .T. ) ;
#8214=DIRECTION ( 'NONE',  ( -1.000000000000000000, 0.000000000000000000, 0.000000000000000000 ) ) ;
#8216=CARTESIAN_POINT ( 'NONE',  ( 10.72267551889550141, -19.77493392430376318, -49.24448729921695644 ) ) ;
#8221=DIRECTION ( 'NONE',  ( 0.000000000000000000, 0.000000000000000000, -1.000000000000000000 ) ) ;
#8222=CARTESIAN_POINT ( 'NONE',  ( 24.04493429539773430, -15.60809896981181844, -75.79200058820715924 ) ) ;
#8231=CARTESIAN_POINT ( 'NONE',  ( 10.95696251514589825, -10.06216002319020042, -81.23899999999999011 ) ) ;
#8234=ORIENTED_EDGE ( 'NONE', *, *, #13307, .T. ) ;
#8238=CARTESIAN_POINT ( 'NONE',  ( 21.26232505384869853, -20.42786076864270228, -81.23899999999999011 ) ) ;
#8258=CARTESIAN_POINT ( 'NONE',  ( 21.78406605850910083, -10.16983288769560012, -65.04335028194189761 ) ) ;
#8261=CARTESIAN_POINT ( 'NONE',  ( 9.375144655580747610, -14.42380164995869762, -75.90328100709491821 ) ) ;
#8276=CARTESIAN_POINT ( 'NONE',  ( 18.20466641262020957, -23.32127506069581102, -54.20900001018016923 ) ) ;
#8278=CARTESIAN_POINT ( 'NONE',  ( 19.57145990817480197, -9.006337712462819667, -34.71999357511560191 ) ) ;
#8279=B_SPLINE_CURVE_WITH_KNOTS ( 'NONE', 3,
 ( #47113, #51545, #34765, #26636, #50773, #15643, #10943, #3332, #23732, #3850 ),
 .UNSPECIFIED., .F., .F.,
 ( 4, 1, 1, 1, 1, 1, 1, 4 ),
 ( 0.000000000000000000, 0.05072724174294171440, 0.1299461728065594013, 0.2091651038701793641, 0.2883840349337947750, 0.3676029659974147656, 0.4468218970610324248, 0.4999964962326966522 ),
 .UNSPECIFIED. ) ;
#8280=CARTESIAN_POINT ( 'NONE',  ( 10.72255522605177447, -19.77477957111918627, -77.24449668687897486 ) ) ;
#8284=CARTESIAN_POINT ( 'NONE',  ( 12.20262858312635146, -8.709503763698991818, -81.12752589049252094 ) ) ;
#8285=CARTESIAN_POINT ( 'NONE',  ( 16.13393739769620083, -15.61618894467929941, -22.14999999999999858 ) ) ;
#8287=CARTESIAN_POINT ( 'NONE',  ( 22.46009329050373537, -20.47787971217975667, -78.00066235776243673 ) ) ;
#8289=CARTESIAN_POINT ( 'NONE',  ( 12.14981476090708945, -22.52871708785758997, -52.17433418267898304 ) ) ;
#8295=DIRECTION ( 'NONE',  ( -1.000000000000000000, 0.000000000000000000, 0.000000000000000000 ) ) ;
#8305=CARTESIAN_POINT ( 'NONE',  ( 24.04476370363584792, -15.55956450748785080, -59.79004764092346846 ) ) ;
#8315=CARTESIAN_POINT ( 'NONE',  ( 8.292221284752539390, -15.92316776411449908, -55.00003992740219871 ) ) ;
#8324=CARTESIAN_POINT ( 'NONE',  ( 12.72600710236050503, -21.52913500508059386, -39.11948792604604108 ) ) ;
#8325=CARTESIAN_POINT ( 'NONE',  ( 18.64395816326110022, -9.025107475687740077, -54.46300130049669264 ) ) ;
#8326=CARTESIAN_POINT ( 'NONE',  ( 12.14992226638847939, -8.703599986432690727, -41.12566464970087310 ) ) ;
#8331=CARTESIAN_POINT ( 'NONE',  ( 12.72592927279295516, -9.703286911501191270, -37.78615459271271249 ) ) ;
#8332=CARTESIAN_POINT ( 'NONE',  ( 11.18221182729259944, -20.63843675327109750, -77.59492917107350252 ) ) ;
#8354=CARTESIAN_POINT ( 'NONE',  ( 9.109991519162420559, -14.97842488795170013, -67.48164325437429056 ) ) ;
#8361=CARTESIAN_POINT ( 'NONE',  ( 9.232756519280840735, -19.35255759171839784, -44.12955248114639772 ) ) ;
#8369=CARTESIAN_POINT ( 'NONE',  ( 18.20470691751352632, -23.32126361575343054, -63.92433611861847709 ) ) ;
#8379=CARTESIAN_POINT ( 'NONE',  ( 11.27221019095833654, -21.94231694163175916, -62.50066393684475230 ) ) ;
#8383=CARTESIAN_POINT ( 'NONE',  ( 8.086907174455379987, -17.41285937694659935, -68.72240889194819147 ) ) ;
#8386=DIRECTION ( 'NONE',  ( 1.000000000000000000, 0.000000000000000000, 0.000000000000000000 ) ) ;
#8391=CARTESIAN_POINT ( 'NONE',  ( 18.50026580205109639, -8.551687285829688179, -65.83553959257810106 ) ) ;
#8395=PLANE ( 'NONE',  #47954 ) ;
#8401=CARTESIAN_POINT ( 'NONE',  ( 15.62259167844689856, -7.386896978515079759, -76.98791498200849048 ) ) ;
#8412=VERTEX_POINT ( 'NONE', #9321 ) ;
#8415=CARTESIAN_POINT ( 'NONE',  ( 12.14970019625365438, -22.52865228160853306, -72.45901836890904235 ) ) ;
#8417=CARTESIAN_POINT ( 'NONE',  ( 12.65851744802729861, -22.20616599455440010, -80.88713649466581046 ) ) ;
#8423=ORIENTED_EDGE ( 'NONE', *, *, #19489, .F. ) ;
#8436=CARTESIAN_POINT ( 'NONE',  ( 24.04464518807997919, -15.61618401921712618, -71.50767245506341396 ) ) ;
#8445=CARTESIAN_POINT ( 'NONE',  ( 17.26073403098808257, -8.923770253816476483, -50.00599002542245586 ) ) ;
#8447=DIRECTION ( 'NONE',  ( -1.000000000000000000, 1.330268894940021809E-33, -1.060511545910580040E-15 ) ) ;
#8449=CARTESIAN_POINT ( 'NONE',  ( 24.04501723819814529, -15.61618889329698412, -35.50767088183642528 ) ) ;
#8450=CARTESIAN_POINT ( 'NONE',  ( 15.87474718106880012, -23.85727749459430314, -38.30233936351829982 ) ) ;
#8456=CARTESIAN_POINT ( 'NONE',  ( 15.89973463379899776, -23.06278836122699971, -38.74266516882029521 ) ) ;
#8464=CARTESIAN_POINT ( 'NONE',  ( 21.64425948049070314, -9.482750165915568630, -43.24065034890669068 ) ) ;
#8470=CARTESIAN_POINT ( 'NONE',  ( 13.10370563145657030, -9.247495623643706253, -56.20581778389941974 ) ) ;
#8484=CARTESIAN_POINT ( 'NONE',  ( 24.04492188529094321, -15.60000870450956789, -75.79167514006502415 ) ) ;
#8493=CARTESIAN_POINT ( 'NONE',  ( 14.10774154971239902, -8.019855601378861110, -81.23899999999999011 ) ) ;
#8494=EDGE_LOOP ( 'NONE', ( #33155, #23740, #13917, #49735 ) ) ;
#8500=CARTESIAN_POINT ( 'NONE',  ( 22.75585767527259762, -18.49336363850369835, -81.23899999999999011 ) ) ;
#8514=ORIENTED_EDGE ( 'NONE', *, *, #29327, .T. ) ;
#8521=CARTESIAN_POINT ( 'NONE',  ( 20.11808723905773988, -22.52870104806199691, -68.12566323940706070 ) ) ;
#8523=DIRECTION ( 'NONE',  ( 0.000000000000000000, 0.000000000000000000, 1.000000000000000000 ) ) ;
#8525=CARTESIAN_POINT ( 'NONE',  ( 20.55998394979739885, -22.09668739015519989, -57.59677076196169310 ) ) ;
#8542=CARTESIAN_POINT ( 'NONE',  ( 17.07732798564219578, -23.50820749086367911, -33.96988921057287314 ) ) ;
#8544=CARTESIAN_POINT ( 'NONE',  ( 11.51802410812858923, -20.94872152101151030, -71.57429041023839034 ) ) ;
#8546=CARTESIAN_POINT ( 'NONE',  ( 22.79714714506240369, -12.28327277397440120, -46.91970895891289928 ) ) ;
#8547=CARTESIAN_POINT ( 'NONE',  ( 22.72480921377356822, -17.38744322059056913, -76.53615365903577583 ) ) ;
#8555=EDGE_CURVE ( 'NONE', #50303, #39386, #31520, .T. ) ;
#8560=ORIENTED_EDGE ( 'NONE', *, *, #3242, .T. ) ;
#8562=ORIENTED_EDGE ( 'NONE', *, *, #11092, .F. ) ;
#8567=ORIENTED_EDGE ( 'NONE', *, *, #33836, .F. ) ;
#8571=CARTESIAN_POINT ( 'NONE',  ( 16.10427296349248394, -8.563410825654969472, -66.34584096005498566 ) ) ;
#8581=CARTESIAN_POINT ( 'NONE',  ( 19.53857308744663257, -9.751301291141226457, -34.12023054736771854 ) ) ;
#8584=CARTESIAN_POINT ( 'NONE',  ( 15.22032918994340100, -7.821827672945169674, -55.47535351378380142 ) ) ;
#8590=CARTESIAN_POINT ( 'NONE',  ( 9.757136478812640235, -12.60305615381579969, -53.98768771411499756 ) ) ;
#8591=CARTESIAN_POINT ( 'NONE',  ( 22.46012617239150799, -10.75454331186309531, -41.58399771921369847 ) ) ;
#8596=FACE_OUTER_BOUND ( 'NONE', #29494, .T. ) ;
#8601=CARTESIAN_POINT ( 'NONE',  ( 8.223585368203801593, -15.61624251583899969, -52.79233150823699816 ) ) ;
#8604=VERTEX_POINT ( 'NONE', #7707 ) ;
#8605=CARTESIAN_POINT ( 'NONE',  ( 16.10427296349259763, -8.563410825682879590, -66.34584096003949583 ) ) ;
#8613=EDGE_CURVE ( 'NONE', #50973, #11348, #21952, .T. ) ;
#8614=CARTESIAN_POINT ( 'NONE',  ( 13.67824910300939933, -22.22770569168709898, -69.06602187564659801 ) ) ;
#8626=CARTESIAN_POINT ( 'NONE',  ( 23.83903869154858413, -17.68685940192425221, -63.59100333396448690 ) ) ;
#8633=CARTESIAN_POINT ( 'NONE',  ( 23.83903513718275846, -17.68687693612751488, -43.59100491536354838 ) ) ;
#8638=EDGE_CURVE ( 'NONE', #39256, #49799, #41370, .T. ) ;
#8639=CARTESIAN_POINT ( 'NONE',  ( 16.77044965268740029, -23.83674684576979885, -74.26773406640140252 ) ) ;
#8643=EDGE_LOOP ( 'NONE', ( #31163, #34681, #44524, #9317 ) ) ;
#8644=CARTESIAN_POINT ( 'NONE',  ( 22.90106509282977854, -15.61618896609811458, -36.45282238757207693 ) ) ;
#8646=CARTESIAN_POINT ( 'NONE',  ( 21.58606382555289827, -10.53868845528379872, -65.99397745470530197 ) ) ;
#8663=VERTEX_POINT ( 'NONE', #37803 ) ;
#8669=CARTESIAN_POINT ( 'NONE',  ( 20.06281976506910070, -10.10654536788180025, -32.14999999999999858 ) ) ;
#8675=EDGE_CURVE ( 'NONE', #10139, #39738, #45080, .T. ) ;
#8695=CARTESIAN_POINT ( 'NONE',  ( 20.99559283022811584, -9.290005664590468726, -55.50065785785324124 ) ) ;
#8707=CARTESIAN_POINT ( 'NONE',  ( 17.88447765263330069, -23.67338007259600019, -46.22423246988029888 ) ) ;
#8708=CARTESIAN_POINT ( 'NONE',  ( 18.20463661421896617, -23.32128348042572341, -67.92433352170111505 ) ) ;
#8713=CARTESIAN_POINT ( 'NONE',  ( 23.83903802589029297, -17.68686261538724125, -41.87566431392930610 ) ) ;
#8714=CARTESIAN_POINT ( 'NONE',  ( 14.99016206921919903, -22.97815008590309915, -34.78171861563929923 ) ) ;
#8715=CARTESIAN_POINT ( 'NONE',  ( 24.04493703497947621, -14.58063303858524939, -33.46599845918103000 ) ) ;
#8718=CARTESIAN_POINT ( 'NONE',  ( 24.04493739318474610, -15.62253491305603426, -59.79258081469907182 ) ) ;
#8721=CARTESIAN_POINT ( 'NONE',  ( 23.49678657892749811, -19.32714200870689680, -41.65627172763429797 ) ) ;
#8746=CARTESIAN_POINT ( 'NONE',  ( 22.89998043194958655, -16.40826371516535431, -60.88444288611811572 ) ) ;
#8754=B_SPLINE_CURVE_WITH_KNOTS ( 'NONE', 3,
 ( #42858, #14288, #6171, #26061, #38137, #10626, #2237, #26580, #10363, #6693, #21872, #38670, #37883, #18213, #26324, #42333, #6432, #42596 ),
 .UNSPECIFIED., .F., .F.,
 ( 4, 2, 2, 2, 2, 2, 2, 2, 4 ),
 ( 0.4999987983750606158, 0.5624989485781780596, 0.6249990987812954479, 0.6874992489844128363, 0.7499993991875302246, 0.8124995493906477240, 0.8749996995937651123, 0.9374998497968825006, 1.000000000000000000 ),
 .UNSPECIFIED. ) ;
#8755=ORIENTED_EDGE ( 'NONE', *, *, #41887, .F. ) ;
#8757=AXIS2_PLACEMENT_3D ( 'NONE', #39722, #51771, #15102 ) ;
#8761=CARTESIAN_POINT ( 'NONE',  ( 21.15506732860339767, -20.52346999403679817, -81.23899999999999011 ) ) ;
#8771=ORIENTED_EDGE ( 'NONE', *, *, #11966, .T. ) ;
#8772=ORIENTED_EDGE ( 'NONE', *, *, #5628, .T. ) ;
#8774=DIRECTION ( 'NONE',  ( 1.000000000000000000, 0.000000000000000000, 0.000000000000000000 ) ) ;
#8780=CARTESIAN_POINT ( 'NONE',  ( 21.12773481075143422, -20.59660524975024387, -55.09675274900580177 ) ) ;
#8782=CARTESIAN_POINT ( 'NONE',  ( 23.97508750825819845, -15.93730127209270009, -63.30053379854238926 ) ) ;
#8784=EDGE_LOOP ( 'NONE', ( #29057, #24703, #39082, #894 ) ) ;
#8787=CARTESIAN_POINT ( 'NONE',  ( 15.87259861546077389, -15.80606268419046678, -24.90346750000000142 ) ) ;
#8796=CARTESIAN_POINT ( 'NONE',  ( 14.26078212116266108, -23.32907417233825598, -34.08344229577145512 ) ) ;
#8798=CARTESIAN_POINT ( 'NONE',  ( 14.62412072909329552, -22.50552946476252458, -71.41585254811130312 ) ) ;
#8801=CARTESIAN_POINT ( 'NONE',  ( 8.741056682034429315, -14.69314557498439910, -40.10688088744169733 ) ) ;
#8805=CARTESIAN_POINT ( 'NONE',  ( 21.98073010695431151, -11.67187985524638805, -34.65826853459201118 ) ) ;
#8811=EDGE_CURVE ( 'NONE', #27118, #35815, #45742, .T. ) ;
#8813=CARTESIAN_POINT ( 'NONE',  ( 24.04504587474531263, -15.61618895646369687, -51.50767080737492165 ) ) ;
#8837=CARTESIAN_POINT ( 'NONE',  ( 19.12892251208798911, -9.528728375619987645, -34.09841683067057971 ) ) ;
#8839=CARTESIAN_POINT ( 'NONE',  ( 8.587688456862030861, -13.46192003979740015, -69.10100965672640427 ) ) ;
#8851=ORIENTED_EDGE ( 'NONE', *, *, #11966, .F. ) ;
#8855=CARTESIAN_POINT ( 'NONE',  ( 9.367501421782780113, -15.61622054991689978, -37.45282021618999835 ) ) ;
#8857=FACE_OUTER_BOUND ( 'NONE', #35496, .T. ) ;
#8858=CARTESIAN_POINT ( 'NONE',  ( 22.96203127631590135, -18.80250976734449964, -32.14999999999999858 ) ) ;
#8867=CARTESIAN_POINT ( 'NONE',  ( 21.40734412481930349, -20.29953610934510166, -65.07833806302160440 ) ) ;
#8868=ORIENTED_EDGE ( 'NONE', *, *, #51660, .F. ) ;
#8869=AXIS2_PLACEMENT_3D ( 'NONE', #4675, #37425, #45035 ) ;
#8871=CARTESIAN_POINT ( 'NONE',  ( 22.90105422030644533, -15.61618894250064571, -66.84718200393152188 ) ) ;
#8875=CARTESIAN_POINT ( 'NONE',  ( 11.74162816692980016, -10.09802092277660002, -65.73882677097459748 ) ) ;
#8887=CARTESIAN_POINT ( 'NONE',  ( 9.807872506304869731, -20.47799571592583234, -64.29933550135423559 ) ) ;
#8891=VECTOR ( 'NONE', #11393, 1000.000000000000000 ) ;
#8893=CARTESIAN_POINT ( 'NONE',  ( 24.04475233726670780, -15.61618925176752271, -59.50766149565701113 ) ) ;
#8897=CARTESIAN_POINT ( 'NONE',  ( 24.04493737916699914, -16.65173673504433793, -43.54933322766937920 ) ) ;
#8900=DIRECTION ( 'NONE',  ( 1.000000000000000000, 2.460964292799963328E-14, 0.000000000000000000 ) ) ;
#8901=ORIENTED_EDGE ( 'NONE', *, *, #48319, .T. ) ;
#8904=CARTESIAN_POINT ( 'NONE',  ( 23.95747192159750227, -15.00051440004449965, -35.98749647213350045 ) ) ;
#8909=VERTEX_POINT ( 'NONE', #43291 ) ;
#8911=CARTESIAN_POINT ( 'NONE',  ( 15.74786552489070068, -8.175917288739990241, -61.71615517726989708 ) ) ;
#8914=FACE_OUTER_BOUND ( 'NONE', #41561, .T. ) ;
#8924=CARTESIAN_POINT ( 'NONE',  ( 9.351992365096680970, -20.30531804342160029, -80.31511008668059048 ) ) ;
#8930=CARTESIAN_POINT ( 'NONE',  ( 8.222937397696199469, -15.61618894467929941, -32.14999999999999858 ) ) ;
#8936=CARTESIAN_POINT ( 'NONE',  ( 8.222961546152424361, -16.65191320241268258, -74.75066484206243445 ) ) ;
#8939=CARTESIAN_POINT ( 'NONE',  ( 13.97436713976919975, -8.902113059071330881, -37.85376303658059527 ) ) ;
#8947=CARTESIAN_POINT ( 'NONE',  ( 23.18909320594459800, -13.22213989345240037, -74.96321055543420186 ) ) ;
#8951=CYLINDRICAL_SURFACE ( 'NONE', #5637, 7.910999999999997812 ) ;
#8954=CARTESIAN_POINT ( 'NONE',  ( 24.04473007462266310, -15.61618926727986789, -75.50766188105974663 ) ) ;
#8956=CARTESIAN_POINT ( 'NONE',  ( 20.11801501725389940, -22.52874440175187942, -71.84094734006453109 ) ) ;
#8959=ORIENTED_EDGE ( 'NONE', *, *, #10497, .F. ) ;
#8964=CARTESIAN_POINT ( 'NONE',  ( 20.29256136589905424, -10.20483249692997241, -70.16115577048812213 ) ) ;
#8968=LINE ( 'NONE', #567, #6754 ) ;
#8972=CARTESIAN_POINT ( 'NONE',  ( 11.38066761511700165, -8.879042187338029635, -55.09675274900569519 ) ) ;
#8974=CARTESIAN_POINT ( 'NONE',  ( 24.04460491192063998, -15.61619351124008404, -49.79233069347445451 ) ) ;
#8976=CARTESIAN_POINT ( 'NONE',  ( 20.11811545784118138, -22.52868417623059472, -42.12566445783141234 ) ) ;
#8977=CARTESIAN_POINT ( 'NONE',  ( 23.38515334021269965, -17.32690840498830198, -34.30640502925760416 ) ) ;
#8979=EDGE_CURVE ( 'NONE', #10190, #14553, #19166, .T. ) ;
#8982=DIRECTION ( 'NONE',  ( 1.000000000000000000, 2.460964292799963328E-14, 0.000000000000000000 ) ) ;
#8985=CARTESIAN_POINT ( 'NONE',  ( 24.34665199147069714, -14.88540873820230104, -51.47941917952310575 ) ) ;
#8989=CARTESIAN_POINT ( 'NONE',  ( 11.52621308753668927, -22.10078695511856850, -40.20443266154408235 ) ) ;
#8990=DIRECTION ( 'NONE',  ( 0.000000000000000000, 0.000000000000000000, -1.000000000000000000 ) ) ;
#8996=AXIS2_PLACEMENT_3D ( 'NONE', #277, #16260, #44296 ) ;
#9001=CYLINDRICAL_SURFACE ( 'NONE', #16891, 6.766999999999998572 ) ;
#9002=CARTESIAN_POINT ( 'NONE',  ( 8.222946520301590567, -14.58057468306158100, -60.83399804565716806 ) ) ;
#9009=CARTESIAN_POINT ( 'NONE',  ( 10.72256262586727793, -19.77478906618366494, -61.24449922350422071 ) ) ;
#9010=CARTESIAN_POINT ( 'NONE',  ( 9.367407790820902136, -15.61608574124520032, -61.84717978381009829 ) ) ;
#9022=CARTESIAN_POINT ( 'NONE',  ( 21.04481148849130179, -20.61575451790190172, -81.23899999999999011 ) ) ;
#9030=CARTESIAN_POINT ( 'NONE',  ( 17.35880188677425551, -23.50009711225479236, -34.24345447869366410 ) ) ;
#9039=VECTOR ( 'NONE', #5336, 1000.000000000000000 ) ;
#9044=CARTESIAN_POINT ( 'NONE',  ( 9.820310712754441340, -10.95519481612969948, -72.48992980192208790 ) ) ;
#9045=ORIENTED_EDGE ( 'NONE', *, *, #20137, .F. ) ;
#9056=CARTESIAN_POINT ( 'NONE',  ( 8.222496981792570381, -15.61604333543320067, -34.50766849176299900 ) ) ;
#9061=CARTESIAN_POINT ( 'NONE',  ( 21.09612888652980089, -21.17346795211530264, -45.33533033764049947 ) ) ;
#9071=CARTESIAN_POINT ( 'NONE',  ( 22.90103297551744177, -15.28543113694585642, -60.83163026540892560 ) ) ;
#9072=CARTESIAN_POINT ( 'NONE',  ( 17.16949042073051857, -23.52718815158684151, -51.96600023950148284 ) ) ;
#9084=VERTEX_POINT ( 'NONE', #39730 ) ;
#9092=B_SPLINE_CURVE_WITH_KNOTS ( 'NONE', 3,
 ( #23244, #2850, #22219, #26938, #22991, #27191, #50290, #3108, #19075, #43200, #7293, #51822, #16434, #23759, #11749, #24524, #36598, #47641 ),
 .UNSPECIFIED., .F., .F.,
 ( 4, 2, 2, 2, 2, 2, 2, 2, 4 ),
 ( 0.5000015279420912950, 0.5625013369493297999, 0.6250011459565683047, 0.6875009549638069206, 0.7500007639710454255, 0.8125005729782841524, 0.8750003819855227682, 0.9375001909927613841, 1.000000000000000000 ),
 .UNSPECIFIED. ) ;
#9095=CARTESIAN_POINT ( 'NONE',  ( 21.48239107889450494, -19.76700007457129615, -46.66288234737064755 ) ) ;
#9097=CARTESIAN_POINT ( 'NONE',  ( 23.96840403421039767, -16.07212766087679867, -64.03099806865479593 ) ) ;
#9101=CARTESIAN_POINT ( 'NONE',  ( 22.90065299155850198, -15.61618013372109637, -50.45281880338879432 ) ) ;
#9102=FACE_OUTER_BOUND ( 'NONE', #35507, .T. ) ;
#9113=DIRECTION ( 'NONE',  ( 0.000000000000000000, 0.000000000000000000, -1.000000000000000000 ) ) ;
#9114=CYLINDRICAL_SURFACE ( 'NONE', #7262, 7.910999999999997812 ) ;
#9115=CARTESIAN_POINT ( 'NONE',  ( 23.03048158991310146, -18.61450947644279807, -32.14999999999999858 ) ) ;
#9119=CARTESIAN_POINT ( 'NONE',  ( 11.27235097447594470, -21.94242344813731904, -74.21600161823359088 ) ) ;
#9124=CARTESIAN_POINT ( 'NONE',  ( 11.64736116879679884, -10.17438842309400115, -64.12771089025820004 ) ) ;
#9129=CARTESIAN_POINT ( 'NONE',  ( 20.29260782020964271, -21.02750830818477823, -42.74448647513240473 ) ) ;
#9132=CARTESIAN_POINT ( 'NONE',  ( 22.69723333660660103, -13.03438625761980063, -70.33352477266448943 ) ) ;
#9137=ORIENTED_EDGE ( 'NONE', *, *, #44527, .T. ) ;
#9148=CARTESIAN_POINT ( 'NONE',  ( 18.20455937407651703, -7.911072576141705781, -75.09096826776161038 ) ) ;
#9160=CARTESIAN_POINT ( 'NONE',  ( 18.77779167496959900, -23.00515247567150112, -34.40311785086109353 ) ) ;
#9161=CARTESIAN_POINT ( 'NONE',  ( 9.367549511386263461, -16.57320966654785011, -65.80214969305676220 ) ) ;
#9168=CARTESIAN_POINT ( 'NONE',  ( 16.91867857995320179, -8.607141901655454674, -46.38267033200752110 ) ) ;
#9170=CARTESIAN_POINT ( 'NONE',  ( 10.41813705297420078, -19.74831615951159947, -31.64794915417429166 ) ) ;
#9190=EDGE_CURVE ( 'NONE', #36469, #20584, #46445, .T. ) ;
#9195=CARTESIAN_POINT ( 'NONE',  ( 11.27236349546028293, -21.94243292154778402, -74.50066484501441266 ) ) ;
#9197=CARTESIAN_POINT ( 'NONE',  ( 9.124464442534721442, -16.39711836812870160, -33.41750289701789711 ) ) ;
#9204=CARTESIAN_POINT ( 'NONE',  ( 11.25790860626830003, -21.24921988401450079, -71.79445331288948751 ) ) ;
#9208=CARTESIAN_POINT ( 'NONE',  ( 19.09037207632416511, -8.257022906990993505, -49.41399161769187032 ) ) ;
#9221=DIRECTION ( 'NONE',  ( 1.000000000000000000, 0.000000000000000000, 0.000000000000000000 ) ) ;
#9224=DIRECTION ( 'NONE',  ( 0.000000000000000000, 0.000000000000000000, -1.000000000000000000 ) ) ;
#9233=CARTESIAN_POINT ( 'NONE',  ( 15.09830364956688697, -7.705199274396241194, -43.25070712488398783 ) ) ;
#9236=CARTESIAN_POINT ( 'NONE',  ( 11.92188350998449842, -22.70430026596570272, -54.46300130049679211 ) ) ;
#9242=CARTESIAN_POINT ( 'NONE',  ( 14.31700556835209959, -8.390854867097690573, -43.65423889476479502 ) ) ;
#9244=CARTESIAN_POINT ( 'NONE',  ( 20.11802547147715359, -8.703639956352418494, -33.17433219651738341 ) ) ;
#9250=CARTESIAN_POINT ( 'NONE',  ( 16.04164975777740310, -7.371541972219340266, -51.00410559314138936 ) ) ;
#9255=CARTESIAN_POINT ( 'NONE',  ( 10.22095591748514032, -19.02406068606311607, -57.28612154450400595 ) ) ;
#9257=EDGE_LOOP ( 'NONE', ( #32253, #35267, #44982, #2043 ) ) ;
#9271=CARTESIAN_POINT ( 'NONE',  ( 10.86891355504775802, -19.90191905193766786, -67.23537444561883092 ) ) ;
#9274=CARTESIAN_POINT ( 'NONE',  ( 23.83903448771030753, -17.68688015324557838, -75.59100382533542017 ) ) ;
#9290=CARTESIAN_POINT ( 'NONE',  ( 23.24856440404530034, -17.32290095377710060, -81.23899999999999011 ) ) ;
#9291=ADVANCED_FACE ( 'NONE', ( #35268 ), #7244, .T. ) ;
#9292=CARTESIAN_POINT ( 'NONE',  ( 24.04493737300782996, -14.58064631294842783, -63.46600340254940420 ) ) ;
#9294=CARTESIAN_POINT ( 'NONE',  ( 11.83723722998052175, -15.61618894467929941, -22.14999999999999858 ) ) ;
#9299=CARTESIAN_POINT ( 'NONE',  ( 24.04493739752251003, -15.61707898208110024, -33.79236563404541016 ) ) ;
#9312=CARTESIAN_POINT ( 'NONE',  ( 17.16951678489040845, -23.52718438587707794, -68.25066353981270595 ) ) ;
#9316=CARTESIAN_POINT ( 'NONE',  ( 11.54452688086499990, -9.250337918211469557, -70.58867545639529339 ) ) ;
#9317=ORIENTED_EDGE ( 'NONE', *, *, #1942, .T. ) ;
#9321=CARTESIAN_POINT ( 'NONE',  ( 16.13393739769620083, -3.616188944679339823, -22.14999999999999858 ) ) ;
#9324=CARTESIAN_POINT ( 'NONE',  ( 14.36265603518875977, -22.20705339233771269, -79.03615224225634961 ) ) ;
#9327=CARTESIAN_POINT ( 'NONE',  ( 10.31119352376266818, -20.99649262406198247, -34.27025585054010293 ) ) ;
#9332=CARTESIAN_POINT ( 'NONE',  ( 21.46166242705329807, -10.40830642393209793, -48.82096330443989984 ) ) ;
#9340=CARTESIAN_POINT ( 'NONE',  ( 9.366543050370410128, -15.61630854221780140, -53.84717978381009829 ) ) ;
#9342=CARTESIAN_POINT ( 'NONE',  ( 9.371116658539381916, -14.45533316995461171, -59.90179829052765825 ) ) ;
#9343=CARTESIAN_POINT ( 'NONE',  ( 23.83903542067694659, -17.68687553889520458, -51.59099914178197110 ) ) ;
#9347=ORIENTED_EDGE ( 'NONE', *, *, #17154, .T. ) ;
#9348=ORIENTED_EDGE ( 'NONE', *, *, #21371, .T. ) ;
#9353=ORIENTED_EDGE ( 'NONE', *, *, #25510, .F. ) ;
#9354=FACE_OUTER_BOUND ( 'NONE', #29229, .T. ) ;
#9363=CARTESIAN_POINT ( 'NONE',  ( 21.05259680842176806, -20.26422748320269918, -46.69380980240473633 ) ) ;
#9365=CARTESIAN_POINT ( 'NONE',  ( 23.96531136779289994, -15.10989917382340053, -67.99194462183569954 ) ) ;
#9367=B_SPLINE_CURVE_WITH_KNOTS ( 'NONE', 3,
 ( #16826, #17091, #29124, #317, #12373, #16554, #28336, #20472, #32506, #48535, #12640, #28597, #32773, #48800, #12907, #28862, #5300, #42226, #41699, #9991, #38293, #25955, #29885, #45904, #18358, #13425, #17853, #2132 ),
 .UNSPECIFIED., .F., .F.,
 ( 4, 2, 2, 2, 2, 2, 2, 2, 2, 2, 1, 1, 1, 1, 2, 4 ),
 ( 0.000000000000000000, 0.06250047518423985926, 0.1250009503684797185, 0.1875014255527195917, 0.2500019007369594370, 0.3125023759211992824, 0.3750028511054391833, 0.4375033262896790287, 0.4687535638817990069, 0.4843786826778589960, 0.4921912420758889350, 0.4960975217749039046, 0.4980506616244113061, 0.4990272315491650623, 0.4995155165115419127, 0.5000038014739186520 ),
 .UNSPECIFIED. ) ;
#9377=DIRECTION ( 'NONE',  ( 1.000000000000000000, 2.460964292799963328E-14, 0.000000000000000000 ) ) ;
#9378=AXIS2_PLACEMENT_3D ( 'NONE', #29415, #45419, #28893 ) ;
#9384=CARTESIAN_POINT ( 'NONE',  ( 17.65356943138449708, -22.50337107214560106, -77.27805344681910071 ) ) ;
#9385=CARTESIAN_POINT ( 'NONE',  ( 22.88613837897879932, -18.98757059450120011, -32.14999999999999858 ) ) ;
#9393=CARTESIAN_POINT ( 'NONE',  ( 23.16321757722399965, -15.04018605219599891, -66.82115454642129748 ) ) ;
#9396=DIRECTION ( 'NONE',  ( 0.000000000000000000, 0.000000000000000000, -1.000000000000000000 ) ) ;
#9400=CARTESIAN_POINT ( 'NONE',  ( 9.114236225456030738, -16.29909021797989865, -65.42195104672009620 ) ) ;
#9403=CARTESIAN_POINT ( 'NONE',  ( 9.807863572223928017, -20.47798425270724465, -80.58399865991046340 ) ) ;
#9405=ADVANCED_FACE ( 'NONE', ( #31063 ), #43400, .T. ) ;
#9409=CARTESIAN_POINT ( 'NONE',  ( 13.39314902935926099, -8.114200813603156703, -38.89594400110460271 ) ) ;
#9411=CARTESIAN_POINT ( 'NONE',  ( 24.04470022272198193, -15.61619473591594698, -59.79232576333501470 ) ) ;
#9422=( NAMED_UNIT ( * ) SI_UNIT ( $, .STERADIAN. ) SOLID_ANGLE_UNIT ( ) );
#9427=CARTESIAN_POINT ( 'NONE',  ( 10.29329494695989844, -20.85771957553910028, -36.77968578276969680 ) ) ;
#9436=CARTESIAN_POINT ( 'NONE',  ( 9.736239135216329998, -12.64768492468660099, -37.98546363926389802 ) ) ;
#9445=CARTESIAN_POINT ( 'NONE',  ( 20.00857004538559991, -22.63715434125480286, -81.84667608724390675 ) ) ;
#9458=CARTESIAN_POINT ( 'NONE',  ( 16.36944352332099939, -22.66507394177369861, -32.94218931063619493 ) ) ;
#9467=CARTESIAN_POINT ( 'NONE',  ( 14.29369635269939920, -8.396756332995028771, -74.48789696905259916 ) ) ;
#9471=CARTESIAN_POINT ( 'NONE',  ( 16.13393739769620083, -15.61618894467929941, -28.45282021618999835 ) ) ;
#9474=ADVANCED_FACE ( 'NONE', ( #28161 ), #48624, .T. ) ;
#9486=CARTESIAN_POINT ( 'NONE',  ( 12.14988109189271626, -22.52875461132841650, -70.17433619596677374 ) ) ;
#9494=CARTESIAN_POINT ( 'NONE',  ( 11.08608504019470153, -22.13553758030240104, -50.50205474731569666 ) ) ;
#9500=CARTESIAN_POINT ( 'NONE',  ( 8.684961965424408348, -15.47669408973130167, -45.23861751603709536 ) ) ;
#9501=CARTESIAN_POINT ( 'NONE',  ( 24.04462826173309153, -15.61618628916268392, -33.50766512250601181 ) ) ;
#9507=CARTESIAN_POINT ( 'NONE',  ( 12.11646325030310045, -8.416006850870608957, -50.84566773101410320 ) ) ;
#9524=CARTESIAN_POINT ( 'NONE',  ( 9.543075519110143290, -17.38747768618387113, -53.36948666754615545 ) ) ;
#9526=CARTESIAN_POINT ( 'NONE',  ( 8.222937397696199469, -15.61618894467929941, -32.14999999999999858 ) ) ;
#9528=CARTESIAN_POINT ( 'NONE',  ( 22.89191656196409497, -15.97301087214540338, -66.46960767138124027 ) ) ;
#9531=CARTESIAN_POINT ( 'NONE',  ( 22.90114886013774864, -15.61618877916400017, -48.45281860778688809 ) ) ;
#9533=CARTESIAN_POINT ( 'NONE',  ( 9.367009201240112048, -16.00442573649115374, -73.82892668254670809 ) ) ;
#9535=DIRECTION ( 'NONE',  ( 1.000000000000000000, 2.460964292799963328E-14, 0.000000000000000000 ) ) ;
#9545=CARTESIAN_POINT ( 'NONE',  ( 24.04492097598215850, -15.63439488930047716, -77.50840237685744682 ) ) ;
#9546=DIRECTION ( 'NONE',  ( 0.000000000000000000, 0.000000000000000000, -1.000000000000000000 ) ) ;
#9564=CARTESIAN_POINT ( 'NONE',  ( 11.96663413069190085, -8.966351979459819432, -76.60931421723039136 ) ) ;
#9567=EDGE_CURVE ( 'NONE', #10507, #1081, #14132, .T. ) ;
#9573=CARTESIAN_POINT ( 'NONE',  ( 8.223439258000311725, -15.61632852289070073, -42.50766849176289952 ) ) ;
#9574=CARTESIAN_POINT ( 'NONE',  ( 20.99558011316242201, -9.289995339025649557, -59.50070245799219748 ) ) ;
#9578=CARTESIAN_POINT ( 'NONE',  ( 24.04225747343017972, -15.83852975785987560, -33.51661210754224385 ) ) ;
#9582=CARTESIAN_POINT ( 'NONE',  ( 15.56802502463160032, -8.187431476276259446, -44.54314102700439548 ) ) ;
#9587=CARTESIAN_POINT ( 'NONE',  ( 12.20533024450969961, -21.47354372396169708, -75.53523696341939342 ) ) ;
#9590=CARTESIAN_POINT ( 'NONE',  ( 22.90070561427262064, -15.61618657793558818, -56.45282510079097449 ) ) ;
#9604=ORIENTED_EDGE ( 'NONE', *, *, #33939, .F. ) ;
#9605=EDGE_LOOP ( 'NONE', ( #13089, #36284, #35297, #3585 ) ) ;
#9606=CARTESIAN_POINT ( 'NONE',  ( 9.543025774841634501, -17.38729682769319851, -73.36947041500459932 ) ) ;
#9614=CARTESIAN_POINT ( 'NONE',  ( 15.72727022423829979, -7.779010281307280117, -61.49599227461899176 ) ) ;
#9619=FACE_OUTER_BOUND ( 'NONE', #28390, .T. ) ;
#9627=EDGE_CURVE ( 'NONE', #39697, #15474, #2215, .T. ) ;
#9629=CARTESIAN_POINT ( 'NONE',  ( 24.04478666521990959, -15.61618936535764668, -45.50767606031119783 ) ) ;
#9630=CARTESIAN_POINT ( 'NONE',  ( 23.31206043505390113, -14.77700110635539943, -32.14999999999999858 ) ) ;
#9633=CARTESIAN_POINT ( 'NONE',  ( 18.52893071939554659, -8.054308810067066560, -45.10530462550206465 ) ) ;
#9637=CARTESIAN_POINT ( 'NONE',  ( 20.21022320103229930, -9.860630481422070659, -62.54333226898589260 ) ) ;
#9641=CARTESIAN_POINT ( 'NONE',  ( 10.72266201305779987, -19.77491659247544220, -43.24448676293776828 ) ) ;
#9644=CARTESIAN_POINT ( 'NONE',  ( 22.33192981211439943, -12.25056140624900003, -74.29447132584550673 ) ) ;
#9647=CARTESIAN_POINT ( 'NONE',  ( 16.13393739769620083, -15.61618894467929941, -32.14999999999999858 ) ) ;
#9671=CONICAL_SURFACE ( 'NONE', #38967, 12.92820323027549989, 0.7481802937784480800 ) ;
#9672=CARTESIAN_POINT ( 'NONE',  ( 23.39608499194349989, -12.64163689252930034, -37.88875081766039443 ) ) ;
#9679=DIRECTION ( 'NONE',  ( 0.000000000000000000, 0.000000000000000000, -1.000000000000000000 ) ) ;
#9682=CARTESIAN_POINT ( 'NONE',  ( 13.85919928309939841, -8.940252629490180070, -36.24264715586419783 ) ) ;
#9683=DIRECTION ( 'NONE',  ( 0.000000000000000000, 0.000000000000000000, -1.000000000000000000 ) ) ;
#9689=CARTESIAN_POINT ( 'NONE',  ( 9.807866499535744964, -10.75438988217695879, -57.00066478260036007 ) ) ;
#9701=ORIENTED_EDGE ( 'NONE', *, *, #43755, .T. ) ;
#9704=CARTESIAN_POINT ( 'NONE',  ( 24.04460285965960864, -15.61618860597671876, -65.79233133698019742 ) ) ;
#9707=CARTESIAN_POINT ( 'NONE',  ( 13.58977759548189823, -9.038209802311760299, -47.83534835059659684 ) ) ;
#9714=CARTESIAN_POINT ( 'NONE',  ( 18.83398544718350109, -8.672383441297080608, -70.68538827799869750 ) ) ;
#9722=CARTESIAN_POINT ( 'NONE',  ( 24.04423775914019501, -15.72983825153451853, -75.79689790679616124 ) ) ;
#9723=CARTESIAN_POINT ( 'NONE',  ( 11.27228755212498434, -9.290002421830825696, -45.08396659437083542 ) ) ;
#9724=CARTESIAN_POINT ( 'NONE',  ( 24.04493739715903544, -15.62387967814676770, -45.50799847524913133 ) ) ;
#9728=CARTESIAN_POINT ( 'NONE',  ( 8.222950439209398610, -14.58054600011118396, -46.83399825817551232 ) ) ;
#9732=CARTESIAN_POINT ( 'NONE',  ( 22.73193228873973837, -14.04747040378604517, -50.37850237016653665 ) ) ;
#9734=VERTEX_POINT ( 'NONE', #1957 ) ;
#9739=CARTESIAN_POINT ( 'NONE',  ( 12.38999535182930067, -22.96231840264049850, -48.44236253966159467 ) ) ;
#9741=CARTESIAN_POINT ( 'NONE',  ( 22.85153108731185867, -14.77300192338831408, -56.41308520645548441 ) ) ;
#9745=B_SPLINE_CURVE_WITH_KNOTS ( 'NONE', 3,
 ( #25956, #25439, #17854, #22026, #34080, #50087, #49588, #45640, #5301, #45122, #30153, #41441, #17092, #1358, #29887, #14182, #33044, #13177, #29125, #9233, #5558, #13677, #45905, #9992, #18359, #22287, #34339, #3429 ),
 .UNSPECIFIED., .F., .F.,
 ( 4, 2, 1, 1, 1, 1, 2, 2, 2, 2, 2, 2, 2, 2, 2, 4 ),
 ( 0.5000036253583125534, 0.5004919030679235714, 0.5009801807775345894, 0.5019567361967566255, 0.5039098470352006975, 0.5078160687120888417, 0.5156285120658652410, 0.5312533987734178176, 0.5625031721885233038, 0.6250027190187341652, 0.6875022658489451377, 0.7500018126791561102, 0.8125013595093670826, 0.8750009063395780551, 0.9375004531697890275, 1.000000000000000000 ),
 .UNSPECIFIED. ) ;
#9747=CARTESIAN_POINT ( 'NONE',  ( 21.20762467232530213, -10.16051380365300005, -43.97111461901920393 ) ) ;
#9749=CARTESIAN_POINT ( 'NONE',  ( 8.916440530500569395, -14.98798906874889880, -32.14999999999999858 ) ) ;
#9754=CARTESIAN_POINT ( 'NONE',  ( 9.366584228470589579, -15.61631960056659985, -37.84717978380999881 ) ) ;
#9759=CARTESIAN_POINT ( 'NONE',  ( 12.95136722755839997, -23.22236852585700007, -58.13380938886719917 ) ) ;
#9760=ORIENTED_EDGE ( 'NONE', *, *, #29926, .T. ) ;
#9768=ORIENTED_EDGE ( 'NONE', *, *, #44527, .F. ) ;
#9781=CARTESIAN_POINT ( 'NONE',  ( 16.25297294464781572, -22.45082257738738107, -66.94693417945528324 ) ) ;
#9792=CARTESIAN_POINT ( 'NONE',  ( 16.44143166354569630, -22.66232309404953327, -47.33329750477101783 ) ) ;
#9796=CARTESIAN_POINT ( 'NONE',  ( 11.27237287438952329, -21.94244001871098249, -80.21600237666562805 ) ) ;
#9800=CARTESIAN_POINT ( 'NONE',  ( 9.366383648607859769, -15.61614502978449970, -45.45282021618989177 ) ) ;
#9806=ORIENTED_EDGE ( 'NONE', *, *, #32990, .T. ) ;
#9809=LINE ( 'NONE', #25249, #23780 ) ;
#9811=CARTESIAN_POINT ( 'NONE',  ( 22.90074241486109585, -15.67170043082192343, -50.45542962239370866 ) ) ;
#9819=PRODUCT_DEFINITION_SHAPE ( 'NONE', 'NONE',  #38253 ) ;
#9823=CARTESIAN_POINT ( 'NONE',  ( 19.44595729680459684, -8.501607272430129925, -76.92618994148479317 ) ) ;
#9829=CARTESIAN_POINT ( 'NONE',  ( 16.13393739769620083, -15.61618894467929941, -40.14999999999999858 ) ) ;
#9830=CARTESIAN_POINT ( 'NONE',  ( 8.222919126920675836, -14.58077523142493526, -42.54932860275096118 ) ) ;
#9836=EDGE_CURVE ( 'NONE', #1162, #28912, #44114, .T. ) ;
#9838=CARTESIAN_POINT ( 'NONE',  ( 23.48471434990800333, -16.82976734642059924, -59.11942434271038849 ) ) ;
#9843=CARTESIAN_POINT ( 'NONE',  ( 9.366701239804031687, -16.70366627111308944, -75.79601146438885451 ) ) ;
#9846=CARTESIAN_POINT ( 'NONE',  ( 16.13393739769620083, -15.61618894467929941, -28.45282021618999835 ) ) ;
#9856=VERTEX_POINT ( 'NONE', #30035 ) ;
#9866=CARTESIAN_POINT ( 'NONE',  ( 15.78203914809910025, -7.776360170156919160, -77.49821634947008420 ) ) ;
#9870=DIRECTION ( 'NONE',  ( 1.000000000000000000, 0.000000000000000000, 0.000000000000000000 ) ) ;
#9888=CARTESIAN_POINT ( 'NONE',  ( 8.428815148825032466, -17.68678772635738383, -46.70901315390379693 ) ) ;
#9891=CARTESIAN_POINT ( 'NONE',  ( 20.92027185089429864, -10.43607681494890116, -74.58460979065598906 ) ) ;
#9895=CARTESIAN_POINT ( 'NONE',  ( 10.22108565793575430, -19.02428243526157559, -43.28615345358821287 ) ) ;
#9898=CARTESIAN_POINT ( 'NONE',  ( 21.87344586468049812, -11.51733529334000039, -78.25541787902638191 ) ) ;
#9901=CARTESIAN_POINT ( 'NONE',  ( 22.81411388107130733, -16.71917211157028760, -40.50489512194194930 ) ) ;
#9903=ORIENTED_EDGE ( 'NONE', *, *, #7102, .T. ) ;
#9906=DIRECTION ( 'NONE',  ( 0.000000000000000000, 0.000000000000000000, -1.000000000000000000 ) ) ;
#9908=CARTESIAN_POINT ( 'NONE',  ( 15.54185229010079716, -7.651191642471210308, -38.98438864213744637 ) ) ;
#9910=ORIENTED_EDGE ( 'NONE', *, *, #26077, .T. ) ;
#9919=ORIENTED_EDGE ( 'NONE', *, *, #48631, .T. ) ;
#9923=CARTESIAN_POINT ( 'NONE',  ( 23.83903865329137517, -13.54551831327839650, -57.42433424745438941 ) ) ;
#9926=VECTOR ( 'NONE', #36138, 1000.000000000000000 ) ;
#9927=CARTESIAN_POINT ( 'NONE',  ( 21.09470678374900032, -9.535274976369610300, -37.73031295553310116 ) ) ;
#9936=CARTESIAN_POINT ( 'NONE',  ( 13.88552899772860094, -22.30103889375499904, -35.45045784522799437 ) ) ;
#9937=CARTESIAN_POINT ( 'NONE',  ( 9.942021269482310686, -12.23939551960640060, -44.00610240009889651 ) ) ;
#9938=EDGE_CURVE ( 'NONE', #27637, #45497, #11346, .T. ) ;
#9950=CARTESIAN_POINT ( 'NONE',  ( 18.20461310658355458, -7.911087764067699091, -69.09100364078624068 ) ) ;
#9954=ORIENTED_EDGE ( 'NONE', *, *, #3116, .T. ) ;
#9961=CARTESIAN_POINT ( 'NONE',  ( 10.75784644233539922, -11.05108163637709850, -47.67691048846939594 ) ) ;
#9969=CARTESIAN_POINT ( 'NONE',  ( 10.14005877276480128, -11.19124675659010038, -72.26976689927128916 ) ) ;
#9976=CARTESIAN_POINT ( 'NONE',  ( 22.46010812062750972, -10.75451853965353877, -45.58397716830953783 ) ) ;
#9977=CARTESIAN_POINT ( 'NONE',  ( 17.90525119180973235, -9.025334454543937568, -58.03615338440669547 ) ) ;
#9979=ORIENTED_EDGE ( 'NONE', *, *, #40507, .F. ) ;
#9982=CARTESIAN_POINT ( 'NONE',  ( 18.20466502140901355, -7.911102438067278086, -47.37566600737606848 ) ) ;
#9991=CARTESIAN_POINT ( 'NONE',  ( 22.87884895980263167, -15.05859401559651012, -72.42657743928000968 ) ) ;
#9992=CARTESIAN_POINT ( 'NONE',  ( 9.807692171626330335, -10.75461346308925847, -43.00069361877111618 ) ) ;
#9993=CARTESIAN_POINT ( 'NONE',  ( 23.07869059287449787, -11.17174037213440130, -51.61111978220640140 ) ) ;
#9998=CARTESIAN_POINT ( 'NONE',  ( 24.04526736911255469, -15.61618908158827068, -41.79233198438217300 ) ) ;
#9999=CARTESIAN_POINT ( 'NONE',  ( 23.51503556311359944, -14.60323105926780052, -46.18924468880049972 ) ) ;
#10002=CARTESIAN_POINT ( 'NONE',  ( 9.759605446949429108, -12.60736725606209951, -32.14999999999999858 ) ) ;
#10007=EDGE_CURVE ( 'NONE', #31006, #38448, #13071, .T. ) ;
#10011=FACE_OUTER_BOUND ( 'NONE', #41997, .T. ) ;
#10012=CARTESIAN_POINT ( 'NONE',  ( 19.56137900467879831, -8.117164692171570550, -61.14412876928469842 ) ) ;
#10018=CARTESIAN_POINT ( 'NONE',  ( 9.580591039042646528, -13.34753578335990021, -51.95386955295301590 ) ) ;
#10023=CARTESIAN_POINT ( 'NONE',  ( 23.39917416771469405, -12.38458952302793570, -65.65924184069716318 ) ) ;
#10031=CARTESIAN_POINT ( 'NONE',  ( 22.90069627724530221, -15.67791111087114864, -66.45572291796443665 ) ) ;
#10046=ORIENTED_EDGE ( 'NONE', *, *, #33363, .F. ) ;
#10047=CARTESIAN_POINT ( 'NONE',  ( 12.14992511062090763, -22.52877951279442925, -80.17433578879456491 ) ) ;
#10051=VERTEX_POINT ( 'NONE', #44171 ) ;
#10054=CARTESIAN_POINT ( 'NONE',  ( 24.04493739344566094, -15.61648521757876473, -77.50768746891878891 ) ) ;
#10056=B_SPLINE_CURVE_WITH_KNOTS ( 'NONE', 3,
 ( #5693, #41324, #26352, #46050, #49973, #33704, #10137, #49721, #25829 ),
 .UNSPECIFIED., .F., .F.,
 ( 4, 1, 1, 1, 1, 1, 4 ),
 ( 0.4999989276629363544, 0.5443677341273740478, 0.6377213455942496445, 0.7310749570611245751, 0.8244285685279998388, 0.9177821799948754355, 1.000000000000000000 ),
 .UNSPECIFIED. ) ;
#10063=CARTESIAN_POINT ( 'NONE',  ( 11.33624769261094123, -21.93600026410923931, -34.49903017084843526 ) ) ;
#10078=CARTESIAN_POINT ( 'NONE',  ( 21.27853140075309923, -21.54239352491439874, -77.55994138999369625 ) ) ;
#10087=CARTESIAN_POINT ( 'NONE',  ( 22.46008452425022384, -10.75448613894550043, -43.29930417090383798 ) ) ;
#10089=CARTESIAN_POINT ( 'NONE',  ( 10.22100000342511628, -19.02413601058341897, -79.28615302661654596 ) ) ;
#10092=CARTESIAN_POINT ( 'NONE',  ( 22.90034300907618103, -15.71306550897696930, -62.45738519496880770 ) ) ;
#10098=CARTESIAN_POINT ( 'NONE',  ( 8.700054830325658628, -15.12214004741750095, -50.08846620145769890 ) ) ;
#10099=B_SPLINE_CURVE_WITH_KNOTS ( 'NONE', 3,
 ( #21762, #25946, #16822, #33308, #25433, #37254, #44860, #1351, #21508, #32768, #48793, #28857, #8964, #24908, #17342, #13417, #40921, #37507 ),
 .UNSPECIFIED., .F., .F.,
 ( 4, 2, 2, 2, 2, 2, 2, 2, 4 ),
 ( 0.000000000000000000, 0.06250019596748117301, 0.1250003919349623460, 0.1875005879024435329, 0.2500007838699246920, 0.3125009798374057679, 0.3750011758048868438, 0.4375013717723678641, 0.5000015677398489400 ),
 .UNSPECIFIED. ) ;
#10105=CARTESIAN_POINT ( 'NONE',  ( 22.90378022332593488, -19.73380898580985132, -61.68156799471553597 ) ) ;
#10110=ORIENTED_EDGE ( 'NONE', *, *, #40111, .T. ) ;
#10115=( GEOMETRIC_REPRESENTATION_CONTEXT ( 3 ) GLOBAL_UNCERTAINTY_ASSIGNED_CONTEXT ( ( #2797 ) ) GLOBAL_UNIT_ASSIGNED_CONTEXT ( ( #44346, #23632, #43837 ) ) REPRESENTATION_CONTEXT ( 'NONE', 'WORKASPACE' ) );
#10124=CARTESIAN_POINT ( 'NONE',  ( 11.97521017558959855, -21.02746670928087624, -73.16111001709356287 ) ) ;
#10127=CARTESIAN_POINT ( 'NONE',  ( 23.44932479906633560, -18.73862524642187211, -49.63616815528890669 ) ) ;
#10130=CARTESIAN_POINT ( 'NONE',  ( 15.27481131963929961, -7.815634478900291171, -71.47757758863500044 ) ) ;
#10137=CARTESIAN_POINT ( 'NONE',  ( 9.835632201235332772, -18.71667422018026272, -33.70134154844654972 ) ) ;
#10139=VERTEX_POINT ( 'NONE', #48895 ) ;
#10145=AXIS2_PLACEMENT_3D ( 'NONE', #25691, #820, #9224 ) ;
#10154=ORIENTED_EDGE ( 'NONE', *, *, #40116, .T. ) ;
#10155=CARTESIAN_POINT ( 'NONE',  ( 19.87062220799639789, -9.634571621335810576, -72.52491758300199365 ) ) ;
#10159=CARTESIAN_POINT ( 'NONE',  ( 22.46012708036917616, -10.75454455491590089, -41.29933415321534795 ) ) ;
#10162=CARTESIAN_POINT ( 'NONE',  ( 21.59580785173019990, -11.15406726996270237, -72.23477911819139763 ) ) ;
#10170=FACE_OUTER_BOUND ( 'NONE', #30720, .T. ) ;
#10171=CARTESIAN_POINT ( 'NONE',  ( 24.04493739770276761, -15.61615029164005364, -39.50766986057545438 ) ) ;
#10177=EDGE_CURVE ( 'NONE', #34347, #7977, #19758, .T. ) ;
#10187=CARTESIAN_POINT ( 'NONE',  ( 24.04012322605720797, -15.32992855636913632, -33.78081268262912573 ) ) ;
#10190=VERTEX_POINT ( 'NONE', #6675 ) ;
#10191=CARTESIAN_POINT ( 'NONE',  ( 8.223585368203801593, -15.61624251583899969, -52.79233150823699816 ) ) ;
#10194=CARTESIAN_POINT ( 'NONE',  ( 9.309817790229448775, -11.74086454863580009, -45.17689247551329146 ) ) ;
#10198=ORIENTED_EDGE ( 'NONE', *, *, #33745, .T. ) ;
#10200=CYLINDRICAL_SURFACE ( 'NONE', #42430, 7.910999999999997812 ) ;
#10202=CARTESIAN_POINT ( 'NONE',  ( 22.78040901162220067, -13.25674531116569987, -42.73859950308109035 ) ) ;
#10204=ORIENTED_EDGE ( 'NONE', *, *, #17325, .F. ) ;
#10230=CARTESIAN_POINT ( 'NONE',  ( 18.88997640609209938, -22.10824622113840121, -44.82502897017909049 ) ) ;
#10236=CARTESIAN_POINT ( 'NONE',  ( 13.63212480980059915, -23.05444693688020052, -35.89078365052999686 ) ) ;
#10238=CARTESIAN_POINT ( 'NONE',  ( 14.15300983787075673, -7.927875040723331601, -81.21199936902040406 ) ) ;
#10242=CARTESIAN_POINT ( 'NONE',  ( 24.04492500005543576, -15.63237907448977637, -75.79297730590246829 ) ) ;
#10244=CARTESIAN_POINT ( 'NONE',  ( 21.54530318899829311, -11.45757911204534807, -58.24448665876980868 ) ) ;
#10245=EDGE_CURVE ( 'NONE', #36323, #31006, #45758, .T. ) ;
#10249=CARTESIAN_POINT ( 'NONE',  ( 22.90003758132117184, -14.80394619968367209, -32.41496898898599710 ) ) ;
#10255=ORIENTED_EDGE ( 'NONE', *, *, #27786, .T. ) ;
#10260=CARTESIAN_POINT ( 'NONE',  ( 9.532069060239026115, -20.02275000618190148, -66.32023582542863949 ) ) ;
#10261=CARTESIAN_POINT ( 'NONE',  ( 8.075524310527260496, -13.87128247942689896, -62.86020799324039388 ) ) ;
#10262=CARTESIAN_POINT ( 'NONE',  ( 20.11812604725867359, -22.52867784916062277, -47.84100274957454957 ) ) ;
#10266=CARTESIAN_POINT ( 'NONE',  ( 11.96399840028469974, -21.79019109587850167, -44.92174179178260118 ) ) ;
#10269=CARTESIAN_POINT ( 'NONE',  ( 9.170653946503200871, -13.93511158109739867, -32.14999999999999858 ) ) ;
#10272=CARTESIAN_POINT ( 'NONE',  ( 8.428884225131936248, -13.54533900620925202, -50.87566462626018904 ) ) ;
#10274=CARTESIAN_POINT ( 'NONE',  ( 10.43684629066897074, -10.04834157992367771, -60.75387912627691378 ) ) ;
#10275=CARTESIAN_POINT ( 'NONE',  ( 8.046702716277120970, -14.01015161116950125, -62.57006952842979075 ) ) ;
#10310=VERTEX_POINT ( 'NONE', #34432 ) ;
#10324=ORIENTED_EDGE ( 'NONE', *, *, #40709, .T. ) ;
#10326=AXIS2_PLACEMENT_3D ( 'NONE', #7250, #10926, #27405 ) ;
#10329=CARTESIAN_POINT ( 'NONE',  ( 22.90054308430137553, -16.11587269579376169, -48.87067656418971495 ) ) ;
#10330=CARTESIAN_POINT ( 'NONE',  ( 16.49581108810665953, -22.37396559151951436, -46.93579869999577170 ) ) ;
#10340=CARTESIAN_POINT ( 'NONE',  ( 10.07106228387759828, -10.02832118826320063, -36.74469800169000422 ) ) ;
#10359=CARTESIAN_POINT ( 'NONE',  ( 9.058892520694989514, -13.28157241797509869, -58.16879716994699834 ) ) ;
#10360=( BOUNDED_CURVE ( )  B_SPLINE_CURVE ( 2, ( #25035, #45250, #2446 ),
 .UNSPECIFIED., .F., .T. ) 
 B_SPLINE_CURVE_WITH_KNOTS ( ( 3, 3 ),
 ( 1.104980434577240045, 2.168627590050209886 ),
 .UNSPECIFIED. ) 
 CURVE ( )  GEOMETRIC_REPRESENTATION_ITEM ( )  RATIONAL_B_SPLINE_CURVE ( ( 1.323085463760209857, 1.425426480542939967, 1.425426480542939967 ) ) 
 REPRESENTATION_ITEM ( '' )  );
#10363=CARTESIAN_POINT ( 'NONE',  ( 17.01976292083999809, -22.38318504511303075, -68.91115224776299897 ) ) ;
#10367=CARTESIAN_POINT ( 'NONE',  ( 22.90122612410699077, -15.61618894223031440, -74.45282020639018583 ) ) ;
#10368=CARTESIAN_POINT ( 'NONE',  ( 9.166869512392668895, -16.70799882457410135, -81.23899999999999011 ) ) ;
#10374=CARTESIAN_POINT ( 'NONE',  ( 8.222988179026620159, -15.61639226004780134, -48.50766849176299189 ) ) ;
#10375=DIRECTION ( 'NONE',  ( 0.000000000000000000, 0.000000000000000000, -1.000000000000000000 ) ) ;
#10378=ORIENTED_EDGE ( 'NONE', *, *, #25769, .F. ) ;
#10380=CARTESIAN_POINT ( 'NONE',  ( 22.90092678307498986, -15.63002908252453516, -72.45347661182641730 ) ) ;
#10385=CARTESIAN_POINT ( 'NONE',  ( 24.04461900158476340, -15.61617122039998051, -49.50766513674645353 ) ) ;
#10388=CARTESIAN_POINT ( 'NONE',  ( 20.40194918913540079, -22.20184175512399705, -74.32945910692518510 ) ) ;
#10397=DIRECTION ( 'NONE',  ( 0.000000000000000000, 0.000000000000000000, -1.000000000000000000 ) ) ;
#10399=CARTESIAN_POINT ( 'NONE',  ( 19.80339606041890121, -8.679199590085181271, -50.94238055261769915 ) ) ;
#10410=ADVANCED_FACE ( 'NONE', ( #45730 ), #19988, .T. ) ;
#10412=CARTESIAN_POINT ( 'NONE',  ( 22.46010835836494479, -20.47785901973523792, -52.00066279612408948 ) ) ;
#10416=CARTESIAN_POINT ( 'NONE',  ( 11.18221182729259944, -20.63843675327109750, -77.59492917107350252 ) ) ;
#10417=ORIENTED_EDGE ( 'NONE', *, *, #18193, .F. ) ;
#10421=CARTESIAN_POINT ( 'NONE',  ( 15.09849997108853081, -7.705175646165889347, -40.96600124313015101 ) ) ;
#10425=CARTESIAN_POINT ( 'NONE',  ( 23.17183048500919895, -16.07513071938780058, -80.47354794880780560 ) ) ;
#10426=CARTESIAN_POINT ( 'NONE',  ( 12.95169883137720035, -21.91030696805099964, -79.49618351660049598 ) ) ;
#10427=CARTESIAN_POINT ( 'NONE',  ( 9.807866034005373379, -10.75439047797270398, -67.00066434089428924 ) ) ;
#10428=CARTESIAN_POINT ( 'NONE',  ( 17.90512202794597130, -22.20708004173628325, -40.86942847551643609 ) ) ;
#10433=ORIENTED_EDGE ( 'NONE', *, *, #21909, .T. ) ;
#10441=CYLINDRICAL_SURFACE ( 'NONE', #19530, 7.910999999999997812 ) ;
#10449=CARTESIAN_POINT ( 'NONE',  ( 22.30993167481387829, -10.65456815221859976, -33.57690324825782113 ) ) ;
#10455=CARTESIAN_POINT ( 'NONE',  ( 10.15194052115590040, -10.53657666019890016, -47.23658468316739345 ) ) ;
#10461=CARTESIAN_POINT ( 'NONE',  ( 22.90093739416913721, -14.73039380284950539, -78.41115054280928121 ) ) ;
#10463=CARTESIAN_POINT ( 'NONE',  ( 16.44143166354569630, -22.66232309404950129, -47.33329750477099651 ) ) ;
#10464=CARTESIAN_POINT ( 'NONE',  ( 15.59821405493169877, -8.583724250529140676, -44.32297812435340489 ) ) ;
#10469=B_SPLINE_CURVE_WITH_KNOTS ( 'NONE', 3,
 ( #32297, #36764, #4540, #23921, #39944, #40963, #36249, #20001, #35996, #16085, #4286, #48066, #20259, #360, #16341, #20513, #24693, #44638 ),
 .UNSPECIFIED., .F., .F.,
 ( 4, 2, 2, 2, 2, 2, 2, 2, 4 ),
 ( 0.000000000000000000, 0.06249995567227221299, 0.1249999113445444260, 0.1874998670168166459, 0.2499998226890888520, 0.3124997783613610580, 0.3749997340336332918, 0.4374996897059054701, 0.4999996453781777039 ),
 .UNSPECIFIED. ) ;
#10470=CARTESIAN_POINT ( 'NONE',  ( 12.14990001803155550, -8.703612571396122988, -50.84100084934565444 ) ) ;
#10480=CARTESIAN_POINT ( 'NONE',  ( 11.35667226720235057, -21.95685860877812701, -32.49793281473952788 ) ) ;
#10481=CARTESIAN_POINT ( 'NONE',  ( 20.11805868952936294, -8.703659767395480529, -69.17433723350387709 ) ) ;
#10483=ORIENTED_EDGE ( 'NONE', *, *, #50004, .T. ) ;
#10487=CARTESIAN_POINT ( 'NONE',  ( 17.16956942387501783, -23.52717687085633713, -74.25066484796637667 ) ) ;
#10490=CARTESIAN_POINT ( 'NONE',  ( 20.93696492682870058, -10.45155098534270088, -44.19127752167009504 ) ) ;
#10496=CARTESIAN_POINT ( 'NONE',  ( 23.79519762219460333, -13.91564786734519998, -39.21797875520189791 ) ) ;
#10497=EDGE_CURVE ( 'NONE', #32691, #16071, #48542, .T. ) ;
#10503=CARTESIAN_POINT ( 'NONE',  ( 11.25620920242847234, -21.92965579961755296, -76.50142983389866913 ) ) ;
#10504=CARTESIAN_POINT ( 'NONE',  ( 15.24822751835945489, -8.849178269573220845, -57.91115341978882469 ) ) ;
#10507=VERTEX_POINT ( 'NONE', #15311 ) ;
#10510=CARTESIAN_POINT ( 'NONE',  ( 22.14986259033789651, -18.71508664667078747, -32.60422815991633172 ) ) ;
#10517=LINE ( 'NONE', #38292, #4983 ) ;
#10518=DIRECTION ( 'NONE',  ( 0.000000000000000000, 0.000000000000000000, -1.000000000000000000 ) ) ;
#10519=CARTESIAN_POINT ( 'NONE',  ( 20.11804697652824814, -8.703652762251346431, -69.45900026522410542 ) ) ;
#10522=CARTESIAN_POINT ( 'NONE',  ( 21.79099334230729923, -9.617819324901351052, -59.53301288856840046 ) ) ;
#10524=CARTESIAN_POINT ( 'NONE',  ( 8.222734977135019108, -15.61599928274970139, -66.79233150823698395 ) ) ;
#10528=CARTESIAN_POINT ( 'NONE',  ( 22.65619759003989842, -12.01524243181439999, -58.07208434834339528 ) ) ;
#10529=CARTESIAN_POINT ( 'NONE',  ( 9.300370600410550637, -13.57546037233679925, -32.14999999999999858 ) ) ;
#10530=CARTESIAN_POINT ( 'NONE',  ( 9.366403394718119557, -15.61612932825470068, -61.45282021618999124 ) ) ;
#10537=CARTESIAN_POINT ( 'NONE',  ( 8.923001793905660506, -11.61804832347029937, -60.66881518290298914 ) ) ;
#10538=EDGE_CURVE ( 'NONE', #1610, #22194, #26610, .T. ) ;
#10545=CARTESIAN_POINT ( 'NONE',  ( 29.99034385824719706, -15.61618894467929941, -32.14999999999999858 ) ) ;
#10560=CARTESIAN_POINT ( 'NONE',  ( 8.222412332301150428, -15.61630761206940043, -38.79233150823699816 ) ) ;
#10568=B_SPLINE_CURVE_WITH_KNOTS ( 'NONE', 3,
 ( #23873, #311, #19453, #68, #23618, #8181, #31735, #35439, #31484, #11868, #39382, #31996, #19192, #15782, #24123, #47509, #23111, #48270 ),
 .UNSPECIFIED., .F., .F.,
 ( 4, 2, 2, 2, 2, 2, 2, 2, 4 ),
 ( 0.4999998584714454020, 0.5624998761625147337, 0.6249998938535841209, 0.6874999115446533970, 0.7499999292357226732, 0.8124999469267920604, 0.8749999646178614476, 0.9374999823089307238, 1.000000000000000000 ),
 .UNSPECIFIED. ) ;
#10575=B_SPLINE_CURVE_WITH_KNOTS ( 'NONE', 3,
 ( #50066, #46150, #14161, #29360, #38272, #26197, #17070, #13402, #13153, #33022, #29103, #42208, #49568, #17831, #37755, #38014, #41420, #49047, #25933, #45101, #5279, #25418, #9208, #1593, #25160, #21230, #5538, #17328, #33291, #6047, #21493, #17581, #1853, #33551, #29615, #45618, #25677, #41679 ),
 .UNSPECIFIED., .F., .F.,
 ( 4, 2, 1, 1, 1, 1, 2, 2, 2, 2, 2, 2, 2, 2, 2, 2, 2, 2, 2, 2, 4 ),
 ( 0.5000031186356694857, 0.5004913968401268898, 0.5009796750445841829, 0.5019562314534988801, 0.5039093442713282744, 0.5078155699069871742, 0.5156280211783047518, 0.5312529237209401289, 0.5625027288062107722, 0.6250023389767520587, 0.6875019491472932343, 0.7187517542325639885, 0.7500015593178346318, 0.7812513644031052751, 0.8125011694883760294, 0.8437509745736466726, 0.8750007796589173159, 0.9062505847441879592, 0.9375003898294587135, 0.9687501949147294678, 1.000000000000000000 ),
 .UNSPECIFIED. ) ;
#10576=ORIENTED_EDGE ( 'NONE', *, *, #50096, .T. ) ;
#10579=CARTESIAN_POINT ( 'NONE',  ( 10.72257032501696727, -19.77479894534321403, -45.24450163928270996 ) ) ;
#10580=FACE_OUTER_BOUND ( 'NONE', #23945, .T. ) ;
#10586=ORIENTED_EDGE ( 'NONE', *, *, #23622, .T. ) ;
#10587=CARTESIAN_POINT ( 'NONE',  ( 9.211626495204299658, -11.13686624773779954, -34.97514425884639877 ) ) ;
#10588=EDGE_CURVE ( 'NONE', #17098, #50522, #45981, .T. ) ;
#10589=CARTESIAN_POINT ( 'NONE',  ( 9.205734167420709824, -3.616188944679339823, -32.14999999999999858 ) ) ;
#10593=CARTESIAN_POINT ( 'NONE',  ( 16.14884424877395830, -22.38317489321702070, -46.95212254701444721 ) ) ;
#10601=CARTESIAN_POINT ( 'NONE',  ( 8.668407554846540464, -19.11598675061409836, -34.36813006978140095 ) ) ;
#10602=ADVANCED_FACE ( 'NONE', ( #50030 ), #10200, .T. ) ;
#10604=CARTESIAN_POINT ( 'NONE',  ( 22.90020510100978157, -14.99288303432257052, -48.81786394348062430 ) ) ;
#10623=CARTESIAN_POINT ( 'NONE',  ( 21.73894157828249973, -20.52440883318790199, -49.29627689082150255 ) ) ;
#10625=VERTEX_POINT ( 'NONE', #41641 ) ;
#10626=CARTESIAN_POINT ( 'NONE',  ( 20.29258866489369595, -21.02752359692314243, -68.74448518055469037 ) ) ;
#10628=DIRECTION ( 'NONE',  ( 0.8090169943749457859, 0.5877852522924753575, 0.000000000000000000 ) ) ;
#10630=CARTESIAN_POINT ( 'NONE',  ( 10.83684432477319959, -19.82762902495380075, -81.23899999999999011 ) ) ;
#10644=ADVANCED_FACE ( 'NONE', ( #26159 ), #45846, .T. ) ;
#10646=ORIENTED_EDGE ( 'NONE', *, *, #21525, .F. ) ;
#10647=DIRECTION ( 'NONE',  ( 1.000000000000000000, 0.000000000000000000, 0.000000000000000000 ) ) ;
#10651=DIRECTION ( 'NONE',  ( 0.000000000000000000, 0.000000000000000000, -1.000000000000000000 ) ) ;
#10658=CARTESIAN_POINT ( 'NONE',  ( 10.40061235411570095, -10.25748274562010032, -52.52675917389010607 ) ) ;
#10671=CARTESIAN_POINT ( 'NONE',  ( 24.03409986133361187, -15.19376807180136346, -45.49067444776833469 ) ) ;
#10675=CARTESIAN_POINT ( 'NONE',  ( 21.66930937907060084, -19.98679716348209823, -75.05992337703780493 ) ) ;
#10676=ORIENTED_EDGE ( 'NONE', *, *, #33262, .T. ) ;
#10680=VECTOR ( 'NONE', #8990, 1000.000000000000000 ) ;
#10684=CARTESIAN_POINT ( 'NONE',  ( 16.68233526804289824, -8.584701301767282189, -73.97759560159100545 ) ) ;
#10707=CYLINDRICAL_SURFACE ( 'NONE', #32469, 6.766999999999998572 ) ;
#10712=CARTESIAN_POINT ( 'NONE',  ( 9.073062699144459842, -12.19116396915949885, -39.15625371467830007 ) ) ;
#10719=CARTESIAN_POINT ( 'NONE',  ( 22.22400857603370028, -12.05900013647219993, -40.67890729542689598 ) ) ;
#10727=CARTESIAN_POINT ( 'NONE',  ( 17.16957227836324762, -7.705201425624105482, -57.33399802158175618 ) ) ;
#10734=CARTESIAN_POINT ( 'NONE',  ( 24.04441141871755505, -15.51763852015655054, -71.50370833047819019 ) ) ;
#10735=CARTESIAN_POINT ( 'NONE',  ( 20.99560978300444702, -9.290019194129630620, -69.21600402986263134 ) ) ;
#10743=CARTESIAN_POINT ( 'NONE',  ( 16.13393739769620083, -15.61618894467929941, -32.14999999999999858 ) ) ;
#10744=CARTESIAN_POINT ( 'NONE',  ( 21.65517505013649924, -20.00463895372590173, -44.66659110805180433 ) ) ;
#10750=CARTESIAN_POINT ( 'NONE',  ( 8.531823529735639511, -17.56416556716440169, -36.20765937478439866 ) ) ;
#10753=CYLINDRICAL_SURFACE ( 'NONE', #35313, 7.910999999999997812 ) ;
#10760=CARTESIAN_POINT ( 'NONE',  ( 20.81696382897727915, -10.69163607886408052, -62.19491938749155935 ) ) ;
#10780=CARTESIAN_POINT ( 'NONE',  ( 23.61751225746720095, -19.07723320532340239, -67.93021958131190274 ) ) ;
#10781=CARTESIAN_POINT ( 'NONE',  ( 13.55743739769620149, -15.61618894467929941, -31.39999999999999858 ) ) ;
#10786=CARTESIAN_POINT ( 'NONE',  ( 15.26659807257079926, -8.216566231308268797, -55.69551641643479911 ) ) ;
#10788=CARTESIAN_POINT ( 'NONE',  ( 8.886858354639530333, -15.19560952241709906, -32.14999999999999858 ) ) ;
#10789=CARTESIAN_POINT ( 'NONE',  ( 10.46514124946499713, -11.84713790509142228, -61.63947181667826669 ) ) ;
#10794=CARTESIAN_POINT ( 'NONE',  ( 14.74094437746738784, -7.760244216757398839, -60.95208477195205887 ) ) ;
#10796=CARTESIAN_POINT ( 'NONE',  ( 16.09925802146080187, -7.371098402433019281, -67.00632966799250312 ) ) ;
#10798=CARTESIAN_POINT ( 'NONE',  ( 21.11367553470149971, -21.58581933017369892, -32.14999999999999858 ) ) ;
#10803=ORIENTED_EDGE ( 'NONE', *, *, #45929, .F. ) ;
#10811=DIRECTION ( 'NONE',  ( 0.5720614028176839172, 0.4156269377774525209, 0.7071067811865484609 ) ) ;
#10814=CARTESIAN_POINT ( 'NONE',  ( 24.04526354826459666, -15.61618910718878794, -73.50766907743336276 ) ) ;
#10817=CARTESIAN_POINT ( 'NONE',  ( 20.11805645080274019, -8.703658428487978327, -37.45900026128192906 ) ) ;
#10825=VERTEX_POINT ( 'NONE', #40550 ) ;
#10827=CARTESIAN_POINT ( 'NONE',  ( 16.13393739769620083, -15.61618894467929941, -81.23899999999999011 ) ) ;
#10845=CARTESIAN_POINT ( 'NONE',  ( 13.60927945319200028, -7.767060182887570718, -37.19327432862769456 ) ) ;
#10847=CARTESIAN_POINT ( 'NONE',  ( 26.52624224310950396, -21.61618894467929763, -22.14999999999999858 ) ) ;
#10848=CARTESIAN_POINT ( 'NONE',  ( 13.64424757191504867, -21.92950919661451081, -51.07239313048388851 ) ) ;
#10856=CARTESIAN_POINT ( 'NONE',  ( 17.11601836966919876, -7.830158814151449320, -78.82744428701180084 ) ) ;
#10862=DIRECTION ( 'NONE',  ( 0.000000000000000000, 0.000000000000000000, -1.000000000000000000 ) ) ;
#10865=CARTESIAN_POINT ( 'NONE',  ( 9.367097141674031846, -15.61601956221279863, -71.84717978381000592 ) ) ;
#10866=CARTESIAN_POINT ( 'NONE',  ( 22.46011653503687810, -20.47784780404496274, -38.00066731914451168 ) ) ;
#10870=LINE ( 'NONE', #21150, #12252 ) ;
#10872=DIRECTION ( 'NONE',  ( 0.000000000000000000, 0.000000000000000000, 1.000000000000000000 ) ) ;
#10882=CARTESIAN_POINT ( 'NONE',  ( 20.03694594417709851, -9.270070554321430123, -56.74285641080169995 ) ) ;
#10888=CARTESIAN_POINT ( 'NONE',  ( 17.90524883137746670, -9.025333787991407064, -74.03615355641134954 ) ) ;
#10889=CARTESIAN_POINT ( 'NONE',  ( 9.828799619648670216, -18.43223393006180189, -81.23899999999999011 ) ) ;
#10895=CARTESIAN_POINT ( 'NONE',  ( 23.38451280374270169, -13.27842595937890025, -81.23899999999999011 ) ) ;
#10898=ADVANCED_FACE ( 'NONE', ( #9619 ), #25574, .T. ) ;
#10899=CARTESIAN_POINT ( 'NONE',  ( 8.222935796957566268, -14.58065318844518288, -52.54933528575815416 ) ) ;
#10901=CARTESIAN_POINT ( 'NONE',  ( 15.09843553512047265, -7.705183434958806643, -63.25066585830453647 ) ) ;
#10904=CONICAL_SURFACE ( 'NONE', #16718, 12.92820323027549989, 0.7481802937784480800 ) ;
#10919=CARTESIAN_POINT ( 'NONE',  ( 10.34713824738410004, -20.91710431630430023, -52.05144558750829731 ) ) ;
#10920=ORIENTED_EDGE ( 'NONE', *, *, #2144, .F. ) ;
#10925=CARTESIAN_POINT ( 'NONE',  ( 21.12141086460500006, -10.88484145508220102, -32.14999999999999858 ) ) ;
#10926=DIRECTION ( 'NONE',  ( 0.000000000000000000, 0.000000000000000000, -1.000000000000000000 ) ) ;
#10929=CARTESIAN_POINT ( 'NONE',  ( 24.04374919936876154, -15.46808838925558405, -45.50171747978662040 ) ) ;
#10935=CARTESIAN_POINT ( 'NONE',  ( 15.69653675527930226, -8.576924789068980814, -76.32742627405558267 ) ) ;
#10939=CARTESIAN_POINT ( 'NONE',  ( 17.16955428432172681, -23.52717903123599896, -57.96600128679276054 ) ) ;
#10943=CARTESIAN_POINT ( 'NONE',  ( 20.88396115700760092, -10.40276075773470055, -58.58238571580489662 ) ) ;
#10946=CARTESIAN_POINT ( 'NONE',  ( 24.04493742164818926, -14.58064954397486268, -67.75066253846064512 ) ) ;
#10947=CARTESIAN_POINT ( 'NONE',  ( 9.221485035723937074, -11.63193652317346505, -66.67433469079290376 ) ) ;
#10955=CARTESIAN_POINT ( 'NONE',  ( 9.367432603602109609, -15.61609789975089946, -77.84717978380999170 ) ) ;
#10960=CARTESIAN_POINT ( 'NONE',  ( 24.04493430356115269, -15.62427093480796358, -55.50799714576009336 ) ) ;
#10967=CARTESIAN_POINT ( 'NONE',  ( 18.58559990215474045, -8.073364231484838172, -33.39234495213820253 ) ) ;
#10972=CARTESIAN_POINT ( 'NONE',  ( 23.82331477792010332, -14.04767911172229944, -39.94844302531450353 ) ) ;
#10975=CARTESIAN_POINT ( 'NONE',  ( 14.81467456660999993, -7.815966731016759539, -81.23899999999999011 ) ) ;
#10982=CARTESIAN_POINT ( 'NONE',  ( 19.76827833599989859, -21.66053548658279837, -47.17485964264358955 ) ) ;
#10990=CARTESIAN_POINT ( 'NONE',  ( 12.14988595507787039, -8.703620529061049993, -46.84100228733535687 ) ) ;
#10993=CARTESIAN_POINT ( 'NONE',  ( 24.04493739160588461, -16.65172911444284765, -57.83399790364183701 ) ) ;
#10997=ORIENTED_EDGE ( 'NONE', *, *, #47916, .T. ) ;
#11001=CARTESIAN_POINT ( 'NONE',  ( 10.72267410870809456, -11.45744577544797238, -41.66115342960441836 ) ) ;
#11004=CARTESIAN_POINT ( 'NONE',  ( 22.67903386406930011, -12.98859100311820036, -54.33130069781340410 ) ) ;
#11008=VERTEX_POINT ( 'NONE', #38833 ) ;
#11009=CARTESIAN_POINT ( 'NONE',  ( 8.301939929713778810, -16.11274090036949858, -38.26735158243850066 ) ) ;
#11014=VECTOR ( 'NONE', #9396, 1000.000000000000000 ) ;
#11028=CARTESIAN_POINT ( 'NONE',  ( 8.222931483157154275, -16.52762990423480716, -44.75564699102723409 ) ) ;
#11031=EDGE_LOOP ( 'NONE', ( #1588, #26272 ) ) ;
#11033=CARTESIAN_POINT ( 'NONE',  ( 9.367366684597708826, -15.61630833865650025, -41.84717978380999170 ) ) ;
#11034=CARTESIAN_POINT ( 'NONE',  ( 22.14986259033789651, -18.71508664667078747, -32.60422815991633172 ) ) ;
#11036=CARTESIAN_POINT ( 'NONE',  ( 9.886430078882730399, -10.23554099510050008, -63.01864585536759478 ) ) ;
#11037=CARTESIAN_POINT ( 'NONE',  ( 11.27237428567958410, -21.94244108617342803, -48.21600222955554926 ) ) ;
#11042=CARTESIAN_POINT ( 'NONE',  ( 21.65368711269129776, -20.62009310932489825, -50.46706696623599697 ) ) ;
#11045=DIRECTION ( 'NONE',  ( 1.000000000000000000, 2.460964292799963328E-14, 0.000000000000000000 ) ) ;
#11046=B_SPLINE_CURVE_WITH_KNOTS ( 'NONE', 3,
 ( #8601, #32157, #24033, #8087, #20121, #36114, #28236, #24550, #40564, #4658, #44759, #45537, #17747, #10412, #37410, #37157, #25843, #26363 ),
 .UNSPECIFIED., .F., .F.,
 ( 4, 2, 2, 2, 2, 2, 2, 2, 4 ),
 ( 0.000000000000000000, 0.06250016148259907034, 0.1250003229651981407, 0.1875004844477972110, 0.2500006459303962814, 0.3125008074129953517, 0.3750009688955944220, 0.4375011303781934924, 0.5000012918607925627 ),
 .UNSPECIFIED. ) ;
#11047=FACE_OUTER_BOUND ( 'NONE', #48638, .T. ) ;
#11052=CIRCLE ( 'NONE', #44523, 12.00000000000000000 ) ;
#11054=CARTESIAN_POINT ( 'NONE',  ( 11.70687558403979978, -8.660339290823859670, -60.82725304503019714 ) ) ;
#11055=CARTESIAN_POINT ( 'NONE',  ( 22.35155673883920002, -20.04374387662789658, -32.14999999999999858 ) ) ;
#11058=CARTESIAN_POINT ( 'NONE',  ( 14.36260343933235717, -9.025338114671583867, -59.86946046379193831 ) ) ;
#11059=EDGE_CURVE ( 'NONE', #41415, #13824, #46964, .T. ) ;
#11065=ADVANCED_FACE ( 'NONE', ( #11047 ), #18637, .T. ) ;
#11092=EDGE_CURVE ( 'NONE', #15209, #7516, #7119, .T. ) ;
#11097=B_SPLINE_CURVE_WITH_KNOTS ( 'NONE', 3,
 ( #38031, #5802, #31103, #30144, #26926, #2125, #49832, #6061, #45634, #5552, #21510, #9486, #18105, #25692, #13418, #37508, #34072, #50081 ),
 .UNSPECIFIED., .F., .F.,
 ( 4, 2, 2, 2, 2, 2, 2, 2, 4 ),
 ( 0.5000015563056314782, 0.5625013617674274879, 0.6250011672292233866, 0.6875009726910192853, 0.7500007781528152950, 0.8125005836146115268, 0.8750003890764076475, 0.9375001945382037682, 1.000000000000000000 ),
 .UNSPECIFIED. ) ;
#11100=CARTESIAN_POINT ( 'NONE',  ( 11.32935210725529274, -20.44672669700188905, -81.20178769548542164 ) ) ;
#11104=CARTESIAN_POINT ( 'NONE',  ( 19.84088292136570075, -22.98105655655680124, -38.14390150139109892 ) ) ;
#11106=CARTESIAN_POINT ( 'NONE',  ( 8.996606508577366768, -19.09621130954815271, -50.64797206822856879 ) ) ;
#11107=CARTESIAN_POINT ( 'NONE',  ( 14.62654628050830041, -22.23316257708228605, -51.02402753104211541 ) ) ;
#11116=CARTESIAN_POINT ( 'NONE',  ( 9.451848358669201033, -20.44687586599430063, -32.30843786212729896 ) ) ;
#11123=CONICAL_SURFACE ( 'NONE', #27009, 7.500000000000000000, 0.7853981633974476129 ) ;
#11124=CARTESIAN_POINT ( 'NONE',  ( 22.90093739769620029, -15.61618894467913243, -28.45282021618999835 ) ) ;
#11133=DIRECTION ( 'NONE',  ( 0.000000000000000000, 0.000000000000000000, -1.000000000000000000 ) ) ;
#11137=CARTESIAN_POINT ( 'NONE',  ( 17.78999742675459927, -22.88008318389400131, -61.49599227461889939 ) ) ;
#11144=DIRECTION ( 'NONE',  ( 1.000000000000000000, 0.000000000000000000, 0.000000000000000000 ) ) ;
#11149=AXIS2_PLACEMENT_3D ( 'NONE', #21747, #45366, #18088 ) ;
#11150=B_SPLINE_CURVE_WITH_KNOTS ( 'NONE', 3,
 ( #26898, #38715, #26364, #42382, #42645, #6742, #2808, #7000, #22952, #19297 ),
 .UNSPECIFIED., .F., .F.,
 ( 4, 1, 1, 1, 1, 1, 1, 4 ),
 ( 0.000000000000000000, 0.03929582389989015601, 0.1185147549635394842, 0.1977336860271887986, 0.2769526170908375162, 0.3561715481544868722, 0.4353904792181367278, 0.4999961688222710476 ),
 .UNSPECIFIED. ) ;
#11154=CARTESIAN_POINT ( 'NONE',  ( 23.59018480163760145, -15.43460167357770096, -81.23899999999999011 ) ) ;
#11169=DIRECTION ( 'NONE',  ( 0.9441240636101839723, 0.3295902797598760925, 0.000000000000000000 ) ) ;
#11171=EDGE_CURVE ( 'NONE', #17972, #48341, #6337, .T. ) ;
#11176=CARTESIAN_POINT ( 'NONE',  ( 22.67019233514569976, -11.27290452205059879, -51.10081841474480058 ) ) ;
#11184=EDGE_CURVE ( 'NONE', #12868, #35817, #43467, .T. ) ;
#11186=EDGE_CURVE ( 'NONE', #47210, #3678, #20391, .T. ) ;
#11189=CARTESIAN_POINT ( 'NONE',  ( 23.87475871378720882, -13.95126914312736055, -45.44025617180926702 ) ) ;
#11192=EDGE_LOOP ( 'NONE', ( #46252, #38805, #44398, #14563 ) ) ;
#11194=CARTESIAN_POINT ( 'NONE',  ( 13.75882690376460005, -22.67774291531760156, -35.67062074787899206 ) ) ;
#11198=CARTESIAN_POINT ( 'NONE',  ( 14.06333627717456736, -23.32130915692496842, -58.09100141101665571 ) ) ;
#11204=CARTESIAN_POINT ( 'NONE',  ( 9.807841437222569070, -20.47795584766477717, -42.29933489389950552 ) ) ;
#11210=DIRECTION ( 'NONE',  ( 0.000000000000000000, 0.000000000000000000, -1.000000000000000000 ) ) ;
#11212=LINE ( 'NONE', #27175, #29401 ) ;
#11220=CARTESIAN_POINT ( 'NONE',  ( 10.22108795246918689, -12.20809152911458106, -35.61948642598461134 ) ) ;
#11227=CARTESIAN_POINT ( 'NONE',  ( 22.04686225415732892, -12.20822244819830438, -52.28615139641824783 ) ) ;
#11229=CARTESIAN_POINT ( 'NONE',  ( 16.63475156800449994, -7.784462905139830191, -41.53282164658689624 ) ) ;
#11238=CARTESIAN_POINT ( 'NONE',  ( 13.47700760496489991, -9.082944478799580779, -46.22423246988029888 ) ) ;
#11245=CARTESIAN_POINT ( 'NONE',  ( 8.222954944519177189, -14.58051301874622929, -46.54933521620945669 ) ) ;
#11259=CARTESIAN_POINT ( 'NONE',  ( 14.36277944305668264, -22.20708534457719452, -75.03615355444333090 ) ) ;
#11262=CARTESIAN_POINT ( 'NONE',  ( 20.01090992632330057, -21.50784768470290231, -58.76756083737610226 ) ) ;
#11267=VERTEX_POINT ( 'NONE', #25909 ) ;
#11269=CARTESIAN_POINT ( 'NONE',  ( 18.87553618764729890, -8.262932233661949510, -38.90110303094750321 ) ) ;
#11278=VERTEX_POINT ( 'NONE', #41922 ) ;
#11285=VECTOR ( 'NONE', #36091, 1000.000000000000000 ) ;
#11286=CARTESIAN_POINT ( 'NONE',  ( 23.99766558267342376, -14.69524935265806853, -49.47055337157053856 ) ) ;
#11291=CARTESIAN_POINT ( 'NONE',  ( 19.63028852933850388, -21.45851978622926381, -32.78102164913964600 ) ) ;
#11292=CARTESIAN_POINT ( 'NONE',  ( 24.91854708852281419, -6.831579253852850364, -22.15000000000000924 ) ) ;
#11293=CARTESIAN_POINT ( 'NONE',  ( 11.82717660292169803, -8.585219487162939700, -61.11739150984070079 ) ) ;
#11299=ORIENTED_EDGE ( 'NONE', *, *, #50279, .T. ) ;
#11302=CARTESIAN_POINT ( 'NONE',  ( 23.44411912466889802, -14.17815663496550016, -56.17083000281660077 ) ) ;
#11308=B_SPLINE_CURVE_WITH_KNOTS ( 'NONE', 3,
 ( #45487, #21606, #25539, #1716, #24492, #44700, #33668, #8805, #13777, #33410, #48911 ),
 .UNSPECIFIED., .F., .F.,
 ( 4, 1, 1, 1, 1, 1, 1, 1, 4 ),
 ( 0.000000000000000000, 0.009449720072804113427, 0.08866865113642231899, 0.1678875822000404916, 0.2471065132636587058, 0.3263254443272768923, 0.4055443753908951066, 0.4847633064545138759, 0.5000038964883081194 ),
 .UNSPECIFIED. ) ;
#11311=CARTESIAN_POINT ( 'NONE',  ( 10.14973811047410024, -9.944145256573110103, -68.74914615139218199 ) ) ;
#11312=EDGE_CURVE ( 'NONE', #40977, #3031, #49281, .T. ) ;
#11316=CARTESIAN_POINT ( 'NONE',  ( 22.04683803730932112, -12.20817710762339559, -60.28613482586189321 ) ) ;
#11327=CARTESIAN_POINT ( 'NONE',  ( 14.41814848605539900, -8.366170860851109836, -75.65868704446700121 ) ) ;
#11334=CARTESIAN_POINT ( 'NONE',  ( 22.07209798807642187, -20.84472431681153992, -61.73745665553851580 ) ) ;
#11342=CARTESIAN_POINT ( 'NONE',  ( 21.66748157623074889, -11.66111095713660362, -66.25520808017488150 ) ) ;
#11345=CARTESIAN_POINT ( 'NONE',  ( 16.35280278772694018, -15.45717393091348590, -41.53556505950739819 ) ) ;
#11346=CIRCLE ( 'NONE', #42281, 6.766999999999998572 ) ;
#11348=VERTEX_POINT ( 'NONE', #50310 ) ;
#11350=CARTESIAN_POINT ( 'NONE',  ( 22.39879365395156086, -20.46795300909408155, -77.71742782580190578 ) ) ;
#11352=CARTESIAN_POINT ( 'NONE',  ( 22.52288591994712164, -13.38583005777697466, -80.34591106198659816 ) ) ;
#11359=CARTESIAN_POINT ( 'NONE',  ( 18.25786897914040452, -23.25431244405651299, -50.20598339505968966 ) ) ;
#11367=CARTESIAN_POINT ( 'NONE',  ( 14.32661840841879908, -7.979413076383879755, -75.43852414181590404 ) ) ;
#11376=CARTESIAN_POINT ( 'NONE',  ( 19.82180142157249847, -22.29872327844429947, -81.62651318459289485 ) ) ;
#11383=EDGE_CURVE ( 'NONE', #8604, #42604, #12273, .T. ) ;
#11386=CARTESIAN_POINT ( 'NONE',  ( 20.11810147990814457, -22.52869253661944526, -38.12566692794859335 ) ) ;
#11393=DIRECTION ( 'NONE',  ( 0.000000000000000000, 0.000000000000000000, -1.000000000000000000 ) ) ;
#11394=CARTESIAN_POINT ( 'NONE',  ( 19.54190960938017341, -21.52911196706135755, -62.78615272955352822 ) ) ;
#11397=CARTESIAN_POINT ( 'NONE',  ( 18.37840078928829968, -8.512029710671050964, -64.66474951716369901 ) ) ;
#11398=CARTESIAN_POINT ( 'NONE',  ( 24.04493739357032212, -14.58064507484895600, -77.75066183485554916 ) ) ;
#11407=CARTESIAN_POINT ( 'NONE',  ( 11.35884076446889956, -9.662862216420530004, -81.23899999999999011 ) ) ;
#11412=ORIENTED_EDGE ( 'NONE', *, *, #32524, .T. ) ;
#11414=CARTESIAN_POINT ( 'NONE',  ( 23.53330766295639975, -16.05940602913920046, -81.23899999999999011 ) ) ;
#11416=CARTESIAN_POINT ( 'NONE',  ( 9.221491376032949105, -11.63192568655906811, -72.95899817687167399 ) ) ;
#11418=CARTESIAN_POINT ( 'NONE',  ( 14.22291958798985156, -9.076607112612990136, -79.86215060077572048 ) ) ;
#11424=CARTESIAN_POINT ( 'NONE',  ( 9.429374979154360403, -19.86130208636912542, -50.32791445271212183 ) ) ;
#11437=CARTESIAN_POINT ( 'NONE',  ( 9.367002091613079173, -15.61601527432330094, -39.84717978380999881 ) ) ;
#11438=CARTESIAN_POINT ( 'NONE',  ( 22.03794483230869972, -20.78624159385250181, -49.51643979347250024 ) ) ;
#11439=ORIENTED_EDGE ( 'NONE', *, *, #49546, .T. ) ;
#11455=CARTESIAN_POINT ( 'NONE',  ( 10.33272111206849964, -19.62722883991240153, -79.65462137872758319 ) ) ;
#11456=B_SPLINE_CURVE_WITH_KNOTS ( 'NONE', 3,
 ( #9340, #37615, #29487, #1980, #5664, #42074, #6176, #22135, #33673, #38142 ),
 .UNSPECIFIED., .F., .F.,
 ( 4, 1, 1, 1, 1, 1, 1, 4 ),
 ( 0.000000000000000000, 0.07025396515245213580, 0.1494728962160721542, 0.2286918272796876761, 0.3079107583433076667, 0.3871296894069435335, 0.4663486204705432625, 0.5000017723907246303 ),
 .UNSPECIFIED. ) ;
#11472=ORIENTED_EDGE ( 'NONE', *, *, #18678, .F. ) ;
#11473=FACE_OUTER_BOUND ( 'NONE', #11192, .T. ) ;
#11476=AXIS2_PLACEMENT_3D ( 'NONE', #44846, #5280, #12619 ) ;
#11489=CARTESIAN_POINT ( 'NONE',  ( 22.90103018812914115, -15.61618888866172483, -50.84718209631233066 ) ) ;
#11493=CARTESIAN_POINT ( 'NONE',  ( 23.27962512014929786, -18.86055245155780113, -52.14815840911190037 ) ) ;
#11499=CARTESIAN_POINT ( 'NONE',  ( 20.29259834648541627, -21.02751587290103075, -38.74448909963410870 ) ) ;
#11500=CARTESIAN_POINT ( 'NONE',  ( 20.11167749483229983, -21.44028912359850025, -57.15644495665969771 ) ) ;
#11501=DIRECTION ( 'NONE',  ( 1.000000000000000000, 2.460964292799963328E-14, 0.000000000000000000 ) ) ;
#11512=CARTESIAN_POINT ( 'NONE',  ( 22.90093739769620029, -15.61618894467913243, -28.45282021618999835 ) ) ;
#11520=CARTESIAN_POINT ( 'NONE',  ( 22.04686233763795755, -19.02415527507118398, -74.61948689269669899 ) ) ;
#11524=CARTESIAN_POINT ( 'NONE',  ( 17.49041801669580209, -8.695024373098599213, -54.01442497355889572 ) ) ;
#11530=CARTESIAN_POINT ( 'NONE',  ( 9.755795275148487988, -11.04387538940279967, -40.48548165221990303 ) ) ;
#11536=CARTESIAN_POINT ( 'NONE',  ( 15.09828380796259495, -23.52717612394415170, -40.33401154759039997 ) ) ;
#11539=ORIENTED_EDGE ( 'NONE', *, *, #20567, .F. ) ;
#11544=CARTESIAN_POINT ( 'NONE',  ( 16.42164688025587793, -23.58948881890144733, -44.28055537063491442 ) ) ;
#11548=FILL_AREA_STYLE_COLOUR ( '', #17447 ) ;
#11549=DIRECTION ( 'NONE',  ( 0.000000000000000000, 0.000000000000000000, -1.000000000000000000 ) ) ;
#11554=CARTESIAN_POINT ( 'NONE',  ( 22.84374255246390106, -10.82440067280909979, -77.59492917107350252 ) ) ;
#11558=SHAPE_DEFINITION_REPRESENTATION ( #9819, #19070 ) ;
#11561=CARTESIAN_POINT ( 'NONE',  ( 15.84771036213319917, -23.06097019662070124, -54.74488924367149423 ) ) ;
#11569=CARTESIAN_POINT ( 'NONE',  ( 22.92255752238139976, -20.29565018628549922, -69.69977332415550109 ) ) ;
#11583=CARTESIAN_POINT ( 'NONE',  ( 10.85782713917238063, -21.54498903828860179, -66.52372767296536438 ) ) ;
#11585=CARTESIAN_POINT ( 'NONE',  ( 22.67920996314880000, -19.17513553729349951, -74.39118414744899610 ) ) ;
#11591=CARTESIAN_POINT ( 'NONE',  ( 24.04483843941790866, -15.61617050235280679, -77.50767555791956909 ) ) ;
#11592=CARTESIAN_POINT ( 'NONE',  ( 9.807706123504049245, -20.47778153303312365, -62.29930259591785813 ) ) ;
#11593=CARTESIAN_POINT ( 'NONE',  ( 8.222932560853145390, -14.58067687905736953, -36.83399830530230190 ) ) ;
#11595=CARTESIAN_POINT ( 'NONE',  ( 22.04685567601379503, -19.02416774546152922, -70.61948949575641166 ) ) ;
#11603=ORIENTED_EDGE ( 'NONE', *, *, #41265, .T. ) ;
#11608=CARTESIAN_POINT ( 'NONE',  ( 17.70136110659009532, -23.38214466260832225, -77.94427081745516261 ) ) ;
#11610=CARTESIAN_POINT ( 'NONE',  ( 11.93124446071863787, -20.97860508548876624, -81.16457539097082474 ) ) ;
#11614=CARTESIAN_POINT ( 'NONE',  ( 12.44141513252709963, -22.98831137825300175, -32.44013846481049512 ) ) ;
#11616=CARTESIAN_POINT ( 'NONE',  ( 24.04123512108865768, -15.87802979434204254, -49.80286409962939587 ) ) ;
#11622=CARTESIAN_POINT ( 'NONE',  ( 14.32234953326219973, -23.25195328107799853, -72.58664262352560570 ) ) ;
#11630=CARTESIAN_POINT ( 'NONE',  ( 9.758119116160459683, -10.38821974528549852, -46.72628331570599869 ) ) ;
#11631=ORIENTED_EDGE ( 'NONE', *, *, #6864, .F. ) ;
#11640=CARTESIAN_POINT ( 'NONE',  ( 9.366859039486531202, -15.61635947376150035, -49.45282021618999835 ) ) ;
#11651=CARTESIAN_POINT ( 'NONE',  ( 19.92837444633610033, -22.02781446573479940, -63.39724662014580048 ) ) ;
#11652=CARTESIAN_POINT ( 'NONE',  ( 15.09843720942611256, -7.705183231044903103, -77.25066340357626871 ) ) ;
#11659=FACE_OUTER_BOUND ( 'NONE', #44112, .T. ) ;
#11662=CARTESIAN_POINT ( 'NONE',  ( 9.052227180162510933, -14.02043803924360077, -81.23899999999999011 ) ) ;
#11669=CARTESIAN_POINT ( 'NONE',  ( 23.53254287302059922, -14.04113270188789997, -81.23899999999999011 ) ) ;
#11670=CARTESIAN_POINT ( 'NONE',  ( 12.14991513904929121, -8.703604018978865042, -73.12566484550632140 ) ) ;
#11672=CARTESIAN_POINT ( 'NONE',  ( 8.223605785152290792, -15.61620117245469963, -52.50766849176299900 ) ) ;
#11678=DIRECTION ( 'NONE',  ( 0.000000000000000000, 0.000000000000000000, -1.000000000000000000 ) ) ;
#11687=FACE_OUTER_BOUND ( 'NONE', #39532, .T. ) ;
#11691=CARTESIAN_POINT ( 'NONE',  ( 14.01353913340800084, -23.17202505883549790, -61.87459303939719746 ) ) ;
#11700=CARTESIAN_POINT ( 'NONE',  ( 11.42275550116415417, -22.01442326570142782, -32.20961141529382132 ) ) ;
#11708=CARTESIAN_POINT ( 'NONE',  ( 15.08788150892120150, -8.239708658262170360, -38.52250226616929751 ) ) ;
#11718=EDGE_CURVE ( 'NONE', #17773, #27518, #27100, .T. ) ;
#11720=CARTESIAN_POINT ( 'NONE',  ( 12.14990643715953311, -8.703608940057563359, -66.84100088982287957 ) ) ;
#11726=CARTESIAN_POINT ( 'NONE',  ( 15.52768592298719952, -22.64292490982440142, -59.37457502644110008 ) ) ;
#11727=AXIS2_PLACEMENT_3D ( 'NONE', #12967, #21570, #33369 ) ;
#11734=ORIENTED_EDGE ( 'NONE', *, *, #17499, .F. ) ;
#11736=CARTESIAN_POINT ( 'NONE',  ( 24.04492190160353005, -15.63236120819791175, -55.50832257871742570 ) ) ;
#11739=CARTESIAN_POINT ( 'NONE',  ( 22.90085165683744250, -15.57936011607131555, -46.45109595593834939 ) ) ;
#11749=CARTESIAN_POINT ( 'NONE',  ( 9.221472665190642459, -19.60042021849464788, -54.34100233441036210 ) ) ;
#11750=CARTESIAN_POINT ( 'NONE',  ( 10.25681452098029922, -20.81678259190509905, -52.78190985762079634 ) ) ;
#11756=CARTESIAN_POINT ( 'NONE',  ( 22.04685790523001998, -19.02416357525799384, -38.61948949083011229 ) ) ;
#11758=CARTESIAN_POINT ( 'NONE',  ( 9.289762948636740347, -17.31907921868189959, -51.76955764433359519 ) ) ;
#11759=CARTESIAN_POINT ( 'NONE',  ( 9.366859039486531202, -15.61635947376150035, -49.45282021618999835 ) ) ;
#11767=CARTESIAN_POINT ( 'NONE',  ( 13.08847648858512969, -8.234862729930275904, -54.88289519625694624 ) ) ;
#11769=CARTESIAN_POINT ( 'NONE',  ( 22.72480788795719775, -13.84492799828816345, -76.36947556904178214 ) ) ;
#11781=CARTESIAN_POINT ( 'NONE',  ( 17.01980794770872407, -22.38317861683710319, -74.91115355591935554 ) ) ;
#11782=CARTESIAN_POINT ( 'NONE',  ( 16.13393739769629676, -15.61618894467929941, -20.75000000000000000 ) ) ;
#11784=CARTESIAN_POINT ( 'NONE',  ( 10.23956942737700082, -11.74333664603669902, -51.63785704165039192 ) ) ;
#11790=CARTESIAN_POINT ( 'NONE',  ( 23.14187571796059828, -19.14826321945789900, -41.43610882498329318 ) ) ;
#11798=ORIENTED_EDGE ( 'NONE', *, *, #41580, .F. ) ;
#11804=CARTESIAN_POINT ( 'NONE',  ( 11.42703244249149819, -9.192886441045931889, -76.80656519119119707 ) ) ;
#11808=CARTESIAN_POINT ( 'NONE',  ( 20.11806571293955059, -22.52871392151443786, -35.84099981003727464 ) ) ;
#11809=CARTESIAN_POINT ( 'NONE',  ( 16.13393739769620083, -15.61618894467929941, -32.14999999999999858 ) ) ;
#11814=CARTESIAN_POINT ( 'NONE',  ( 15.76421757133440060, -7.379318950180220327, -77.27805344681898703 ) ) ;
#11819=CARTESIAN_POINT ( 'NONE',  ( 23.56869833393620084, -15.13553977313539889, -68.21210752448669723 ) ) ;
#11831=CARTESIAN_POINT ( 'NONE',  ( 21.32529432998289920, -9.210524739417378370, -69.22445973777388417 ) ) ;
#11832=CARTESIAN_POINT ( 'NONE',  ( 22.31435075509589794, -12.28517517030200068, -32.14999999999999858 ) ) ;
#11838=CARTESIAN_POINT ( 'NONE',  ( 8.222951331889666093, -14.58053946526866262, -78.54933523722530708 ) ) ;
#11841=VECTOR ( 'NONE', #42390, 1000.000000000000000 ) ;
#11845=CARTESIAN_POINT ( 'NONE',  ( 14.02640371334330816, -23.26397146298620200, -66.37784655330483474 ) ) ;
#11848=CARTESIAN_POINT ( 'NONE',  ( 23.22795750573990148, -17.89249571482650225, -72.33149193979500069 ) ) ;
#11854=VERTEX_POINT ( 'NONE', #10814 ) ;
#11864=CARTESIAN_POINT ( 'NONE',  ( 15.23359603239730653, -8.891264927876337154, -65.91044689600897755 ) ) ;
#11866=VERTEX_POINT ( 'NONE', #26773 ) ;
#11868=CARTESIAN_POINT ( 'NONE',  ( 15.24822091983413763, -22.38319882176496378, -58.99448675312215329 ) ) ;
#11869=B_SPLINE_CURVE_WITH_KNOTS ( 'NONE', 3,
 ( #27910, #47595, #8261, #40238, #23711, #32340, #4582, #39981, #4074, #16912, #41270 ),
 .UNSPECIFIED., .F., .F.,
 ( 4, 1, 1, 1, 1, 1, 1, 1, 4 ),
 ( 0.000000000000000000, 0.002466451932003523115, 0.08168538299555488935, 0.1609043140592600896, 0.2401232451228069165, 0.3193421761865211650, 0.3985611072500679919, 0.4777800383136148743, 0.5000039623326250071 ),
 .UNSPECIFIED. ) ;
#11877=CARTESIAN_POINT ( 'NONE',  ( 15.09846882468793616, -7.705179410057033884, -34.96600043974325445 ) ) ;
#11878=CARTESIAN_POINT ( 'NONE',  ( 8.816801753752139703, -19.41648446266970396, -44.63985384860789907 ) ) ;
#11880=CARTESIAN_POINT ( 'NONE',  ( 24.04493739739171687, -15.61672302095869469, -49.79235199249318100 ) ) ;
#11884=CARTESIAN_POINT ( 'NONE',  ( 22.51680126320929887, -19.45871121662710124, -32.40515068373069596 ) ) ;
#11885=CONICAL_SURFACE ( 'NONE', #30256, 12.92820323027549989, 0.7481802937784480800 ) ;
#11889=EDGE_CURVE ( 'NONE', #637, #37798, #42791, .T. ) ;
#11894=CARTESIAN_POINT ( 'NONE',  ( 8.286183717290461104, -13.08725974823009963, -42.60689890039779470 ) ) ;
#11899=DIRECTION ( 'NONE',  ( 0.000000000000000000, 0.000000000000000000, -1.000000000000000000 ) ) ;
#11903=DIRECTION ( 'NONE',  ( 1.000000000000000000, 0.000000000000000000, 0.000000000000000000 ) ) ;
#11911=CARTESIAN_POINT ( 'NONE',  ( 12.14969989039511944, -8.703725779495739445, -75.12571185134946461 ) ) ;
#11912=CARTESIAN_POINT ( 'NONE',  ( 9.543046712767974782, -17.38737308065900322, -63.36948542607716206 ) ) ;
#11916=CARTESIAN_POINT ( 'NONE',  ( 14.71419660400150065, -8.302432699283889050, -64.50631165503649811 ) ) ;
#11918=CARTESIAN_POINT ( 'NONE',  ( 22.09873218501700265, -19.37966938420589713, -80.63198581093500650 ) ) ;
#11925=CARTESIAN_POINT ( 'NONE',  ( 9.847451328762401701, -11.61977205256459911, -81.23899999999999011 ) ) ;
#11931=CARTESIAN_POINT ( 'NONE',  ( 21.81516569332449862, -10.17359938674849928, -81.23899999999999011 ) ) ;
#11932=CARTESIAN_POINT ( 'NONE',  ( 23.83903832650269905, -13.54551673756389363, -73.70899818572770812 ) ) ;
#11936=CARTESIAN_POINT ( 'NONE',  ( 14.29653415316120046, -8.806893203457351049, -42.26328591669919632 ) ) ;
#11944=CARTESIAN_POINT ( 'NONE',  ( 16.13393739769629676, -15.61618894467929941, -20.75000000000000000 ) ) ;
#11948=DIRECTION ( 'NONE',  ( 0.000000000000000000, 0.000000000000000000, -1.000000000000000000 ) ) ;
#11950=CARTESIAN_POINT ( 'NONE',  ( 15.59252480001009999, -7.787164702652099812, -60.76552800450640035 ) ) ;
#11952=B_SPLINE_CURVE_WITH_KNOTS ( 'NONE', 3,
 ( #23635, #15547, #46763, #2725, #35194, #38892, #19470, #35457, #47275, #51452, #39399, #39651, #43334, #31504, #7426, #47523, #51197, #34932 ),
 .UNSPECIFIED., .F., .F.,
 ( 4, 2, 2, 2, 2, 2, 2, 2, 4 ),
 ( 0.000000000000000000, 0.06250013864589283596, 0.1250002772917856719, 0.1875004159376785218, 0.2500005545835713439, 0.3125006932294640549, 0.3750008318753568215, 0.4375009705212495326, 0.5000011091671422436 ),
 .UNSPECIFIED. ) ;
#11966=EDGE_CURVE ( 'NONE', #8034, #20276, #2946, .T. ) ;
#11969=CARTESIAN_POINT ( 'NONE',  ( 19.44826417394619966, -21.62186115282320031, -81.18618737929101314 ) ) ;
#11977=CARTESIAN_POINT ( 'NONE',  ( 24.04493741700738951, -14.58064883687476154, -35.75066221455982429 ) ) ;
#11979=CARTESIAN_POINT ( 'NONE',  ( 14.06334626515088537, -7.911066143799638795, -66.92433398933782485 ) ) ;
#11984=CARTESIAN_POINT ( 'NONE',  ( 24.04493739769619864, -15.61618894467929941, -32.14999999999999858 ) ) ;
#11993=CARTESIAN_POINT ( 'NONE',  ( 20.19692254461188696, -10.17265177529750275, -46.15686990965734537 ) ) ;
#11999=CARTESIAN_POINT ( 'NONE',  ( 22.90093658489038475, -15.39729050644079678, -34.44252498390390826 ) ) ;
#12001=CARTESIAN_POINT ( 'NONE',  ( 11.32940628474790046, -21.82128591219670000, -50.72221764996669435 ) ) ;
#12005=CARTESIAN_POINT ( 'NONE',  ( 14.78993376734673149, -8.692590644934696797, -64.28614875239208004 ) ) ;
#12011=CARTESIAN_POINT ( 'NONE',  ( 10.13629284140139930, -19.32709435317449831, -53.67081198986049628 ) ) ;
#12017=CARTESIAN_POINT ( 'NONE',  ( 21.54527898443459932, -11.45754588894539516, -38.24448936043144442 ) ) ;
#12021=DIRECTION ( 'NONE',  ( 0.000000000000000000, 0.000000000000000000, -1.000000000000000000 ) ) ;
#12022=EDGE_CURVE ( 'NONE', #31864, #37534, #45166, .T. ) ;
#12024=DIRECTION ( 'NONE',  ( 0.000000000000000000, 0.000000000000000000, -1.000000000000000000 ) ) ;
#12025=CARTESIAN_POINT ( 'NONE',  ( 17.07866728675466206, -7.737244263286628509, -65.04561884461543286 ) ) ;
#12035=CARTESIAN_POINT ( 'NONE',  ( 20.29261124649605819, -21.02750557501780548, -74.74448689122068856 ) ) ;
#12038=CARTESIAN_POINT ( 'NONE',  ( 12.53098345279100023, -21.67929718777690340, -55.12349000844969993 ) ) ;
#12042=AXIS2_PLACEMENT_3D ( 'NONE', #11782, #4155, #28510 ) ;
#12044=CARTESIAN_POINT ( 'NONE',  ( 14.08945181123240076, -8.039459645705720803, -42.70361172200129118 ) ) ;
#12063=CARTESIAN_POINT ( 'NONE',  ( 15.69662371953226376, -7.686623656191616583, -48.99006696521935567 ) ) ;
#12064=B_SPLINE_CURVE_WITH_KNOTS ( 'NONE', 3,
 ( #49450, #18429, #25303, #37378, #17465, #9168, #49015, #34021, #45329, #50031 ),
 .UNSPECIFIED., .F., .F.,
 ( 4, 1, 1, 1, 1, 1, 1, 4 ),
 ( 0.000000000000000000, 0.03008848090787212201, 0.1093074119714910891, 0.1885263430351258873, 0.2677452740987448787, 0.3469642051623627044, 0.4261831362259816403, 0.4999981796106400811 ),
 .UNSPECIFIED. ) ;
#12066=( LENGTH_UNIT ( ) NAMED_UNIT ( * ) SI_UNIT ( .MILLI., .METRE. ) );
#12070=CARTESIAN_POINT ( 'NONE',  ( 13.71480148060770077, -23.49847931751850183, -78.38711848170969176 ) ) ;
#12074=CARTESIAN_POINT ( 'NONE',  ( 22.43708255015009811, -11.64415483200579970, -68.05366966235949633 ) ) ;
#12075=LINE ( 'NONE', #43528, #2984 ) ;
#12076=CARTESIAN_POINT ( 'NONE',  ( 10.40096277903999855, -20.74754741771700139, -32.14999999999999858 ) ) ;
#12083=CARTESIAN_POINT ( 'NONE',  ( 21.53907483071889928, -21.84252093382090010, -77.78010429264469394 ) ) ;
#12094=CARTESIAN_POINT ( 'NONE',  ( 19.36025468743955358, -22.91325498030835206, -66.15954722856929493 ) ) ;
#12096=CARTESIAN_POINT ( 'NONE',  ( 15.31832100281680020, -8.210686686118460642, -71.69774049128589866 ) ) ;
#12120=CARTESIAN_POINT ( 'NONE',  ( 8.222917554388192940, -14.58078674515130757, -58.54932919163416472 ) ) ;
#12121=CARTESIAN_POINT ( 'NONE',  ( 14.60414996492981388, -9.001304452785721111, -49.88044619144234559 ) ) ;
#12122=EDGE_LOOP ( 'NONE', ( #42167, #47607, #36576, #9768 ) ) ;
#12126=CARTESIAN_POINT ( 'NONE',  ( 15.64915313475499836, -7.385289584685909681, -45.27360529711689452 ) ) ;
#12132=ORIENTED_EDGE ( 'NONE', *, *, #42673, .F. ) ;
#12134=CARTESIAN_POINT ( 'NONE',  ( 22.46012250960815138, -20.47783959759377126, -42.00066438588036988 ) ) ;
#12135=CARTESIAN_POINT ( 'NONE',  ( 16.12664591956130167, -8.165911054638401723, -35.73234578840269648 ) ) ;
#12142=CARTESIAN_POINT ( 'NONE',  ( 9.432779887650410089, -10.81231459843210096, -40.70564455487080124 ) ) ;
#12148=CARTESIAN_POINT ( 'NONE',  ( 22.46012609900209256, -20.47783468274219132, -64.00066659774759614 ) ) ;
#12149=CARTESIAN_POINT ( 'NONE',  ( 22.90090025472304447, -15.64040673669522796, -56.45396410355146344 ) ) ;
#12154=CARTESIAN_POINT ( 'NONE',  ( 17.01981387517692568, -22.38317777230120953, -48.91115463206005387 ) ) ;
#12170=CARTESIAN_POINT ( 'NONE',  ( 12.11738391771149992, -9.045897184923541445, -81.23899999999999011 ) ) ;
#12174=ORIENTED_EDGE ( 'NONE', *, *, #37604, .T. ) ;
#12177=CARTESIAN_POINT ( 'NONE',  ( 22.01014902171679921, -19.63241407121610038, -81.23899999999999011 ) ) ;
#12179=CARTESIAN_POINT ( 'NONE',  ( 8.222961468781386785, -14.58046525346367517, -72.83399817539567778 ) ) ;
#12191=EDGE_CURVE ( 'NONE', #40924, #16548, #20288, .T. ) ;
#12192=CARTESIAN_POINT ( 'NONE',  ( 16.13393739769620083, -15.61618894467929941, -28.45282021618999835 ) ) ;
#12195=CARTESIAN_POINT ( 'NONE',  ( 16.13393739769620083, -15.61618894467929941, -32.14999999999999858 ) ) ;
#12197=CARTESIAN_POINT ( 'NONE',  ( 23.50277980578040271, -18.31561661513139683, -61.39927945301550238 ) ) ;
#12207=DIRECTION ( 'NONE',  ( 0.000000000000000000, 0.000000000000000000, -1.000000000000000000 ) ) ;
#12215=CARTESIAN_POINT ( 'NONE',  ( 12.45840162589710154, -9.135669594468568633, -34.40311785086109353 ) ) ;
#12223=CARTESIAN_POINT ( 'NONE',  ( 23.83903818915907991, -13.54551600724768967, -35.70899566211102183 ) ) ;
#12225=CARTESIAN_POINT ( 'NONE',  ( 22.46010325183906176, -20.47786603196966837, -51.71599950768847265 ) ) ;
#12226=ORIENTED_EDGE ( 'NONE', *, *, #18193, .T. ) ;
#12242=CARTESIAN_POINT ( 'NONE',  ( 17.01980371681801074, -8.849198666827120974, -35.99448539802248348 ) ) ;
#12247=B_SPLINE_CURVE_WITH_KNOTS ( 'NONE', 3,
 ( #39735, #38974, #3583, #35281, #27668, #47356, #3066, #27410, #7514, #43413, #23460, #43670, #3839, #19553, #35545, #28691, #16395, #28173 ),
 .UNSPECIFIED., .F., .F.,
 ( 4, 2, 2, 2, 2, 2, 2, 2, 4 ),
 ( 0.5000014860460771926, 0.5625013002903175297, 0.6250011145345578667, 0.6875009287787983148, 0.7500007430230386518, 0.8125005572672789889, 0.8750003715115193259, 0.9375001857557596630, 1.000000000000000000 ),
 .UNSPECIFIED. ) ;
#12252=VECTOR ( 'NONE', #37156, 1000.000000000000000 ) ;
#12253=CARTESIAN_POINT ( 'NONE',  ( 16.79442214605479933, -23.43606793918860021, -58.48567289420149962 ) ) ;
#12258=CARTESIAN_POINT ( 'NONE',  ( 16.13393739769620083, -15.61618894467929941, -82.15000000000000568 ) ) ;
#12262=CARTESIAN_POINT ( 'NONE',  ( 23.15239633160939903, -16.31174150734070238, -52.87862267922439230 ) ) ;
#12270=LINE ( 'NONE', #718, #21458 ) ;
#12272=CARTESIAN_POINT ( 'NONE',  ( 15.24805376294812476, -8.849199263491749790, -75.91113090210829739 ) ) ;
#12273=LINE ( 'NONE', #23521, #25000 ) ;
#12288=CARTESIAN_POINT ( 'NONE',  ( 18.84454860543339905, -22.12734441641509875, -60.82725304503019714 ) ) ;
#12295=CARTESIAN_POINT ( 'NONE',  ( 21.37864584282510094, -9.778399850443678432, -43.02048744625579246 ) ) ;
#12296=VERTEX_POINT ( 'NONE', #50964 ) ;
#12312=CARTESIAN_POINT ( 'NONE',  ( 8.428818883866691536, -17.68680130685687857, -62.70899791641065946 ) ) ;
#12316=CARTESIAN_POINT ( 'NONE',  ( 7.893032080596238842, -15.88114103568579871, -70.78210109960230056 ) ) ;
#12317=CARTESIAN_POINT ( 'NONE',  ( 9.367445776641041277, -14.63655315608641239, -37.89327440229485688 ) ) ;
#12321=ORIENTED_EDGE ( 'NONE', *, *, #49044, .F. ) ;
#12322=CARTESIAN_POINT ( 'NONE',  ( 11.92096193908029989, -21.76090468995549898, -60.92396586663380020 ) ) ;
#12330=CARTESIAN_POINT ( 'NONE',  ( 22.42849628649389615, -10.29066088593869921, -71.28415194542799327 ) ) ;
#12338=( BOUNDED_CURVE ( )  B_SPLINE_CURVE ( 2, ( #18625, #11292, #39838 ),
 .UNSPECIFIED., .F., .T. ) 
 B_SPLINE_CURVE_WITH_KNOTS ( ( 3, 3 ),
 ( 1.104980434577240045, 2.168627590050209886 ),
 .UNSPECIFIED. ) 
 CURVE ( )  GEOMETRIC_REPRESENTATION_ITEM ( )  RATIONAL_B_SPLINE_CURVE ( ( 1.323085463760209857, 1.425426480542949959, 1.425426480542939967 ) ) 
 REPRESENTATION_ITEM ( '' )  );
#12343=CARTESIAN_POINT ( 'NONE',  ( 15.31418126070190056, -23.02123409518320329, -76.76775207935769174 ) ) ;
#12360=CARTESIAN_POINT ( 'NONE',  ( 23.98146851043909678, -16.64924265148496829, -71.54932861355067075 ) ) ;
#12364=VERTEX_POINT ( 'NONE', #26849 ) ;
#12373=CARTESIAN_POINT ( 'NONE',  ( 10.70456637417987622, -11.48191128173198905, -71.65978603205104491 ) ) ;
#12376=CARTESIAN_POINT ( 'NONE',  ( 15.34132565853509966, -23.82316687122930077, -44.32297812435340489 ) ) ;
#12383=CARTESIAN_POINT ( 'NONE',  ( 18.64389600481149856, -22.63094492865949903, -34.62328075351209122 ) ) ;
#12391=CARTESIAN_POINT ( 'NONE',  ( 18.02280865088329875, -23.64207743741700085, -45.93409400506969575 ) ) ;
#12393=B_SPLINE_CURVE_WITH_KNOTS ( 'NONE', 3,
 ( #30651, #9724, #26720, #17587, #21753, #6567, #33810, #26203, #14682, #46676, #42738, #2115, #6836, #14425, #37500, #26462, #25939, #37765, #42476, #1599, #13660, #6053, #38021, #2641, #33559, #49576, #25684, #14167 ),
 .UNSPECIFIED., .F., .F.,
 ( 4, 2, 2, 2, 2, 2, 2, 2, 2, 2, 2, 2, 2, 4 ),
 ( 0.5000053122294032537, 0.5625046482007277637, 0.6250039841720522737, 0.6875033201433767838, 0.7187529881290390943, 0.7500026561147015158, 0.7812523241003637153, 0.8125019920860261369, 0.8437516600716883364, 0.8750013280573507579, 0.9062509960430130684, 0.9375006640286753790, 0.9687503320143376895, 1.000000000000000000 ),
 .UNSPECIFIED. ) ;
#12397=CARTESIAN_POINT ( 'NONE',  ( 22.88773899167640025, -14.38585658271974133, -56.78929433555941841 ) ) ;
#12399=ORIENTED_EDGE ( 'NONE', *, *, #34409, .F. ) ;
#12406=CARTESIAN_POINT ( 'NONE',  ( 10.72261433029855127, -19.77485540986135604, -53.24448634458038754 ) ) ;
#12407=CARTESIAN_POINT ( 'NONE',  ( 9.543105166377426229, -17.38758548366874024, -65.36948706771786988 ) ) ;
#12415=CARTESIAN_POINT ( 'NONE',  ( 15.24810681485378616, -22.38318503380609314, -60.99450452302099279 ) ) ;
#12421=CARTESIAN_POINT ( 'NONE',  ( 8.981108893502280921, -14.73393040951099842, -81.23899999999999011 ) ) ;
#12422=EDGE_CURVE ( 'NONE', #30160, #47211, #18475, .T. ) ;
#12430=CARTESIAN_POINT ( 'NONE',  ( 20.99565867520791329, -9.290058221069106281, -73.50066484993433846 ) ) ;
#12437=CIRCLE ( 'NONE', #24978, 12.00000000000000000 ) ;
#12440=ORIENTED_EDGE ( 'NONE', *, *, #48631, .F. ) ;
#12445=CARTESIAN_POINT ( 'NONE',  ( 15.09842766289428262, -23.52719350332821335, -68.33399707341648366 ) ) ;
#12450=CARTESIAN_POINT ( 'NONE',  ( 21.31981268913839855, -21.50630317487819809, -61.55771731514259670 ) ) ;
#12460=CARTESIAN_POINT ( 'NONE',  ( 11.27227933505587032, -21.94236925040859632, -36.50066404204540049 ) ) ;
#12466=CARTESIAN_POINT ( 'NONE',  ( 21.46302885113694359, -21.53080627074261955, -33.77437669800720244 ) ) ;
#12468=CARTESIAN_POINT ( 'NONE',  ( 8.222373579151801337, -15.61629175287649929, -54.79233150823699816 ) ) ;
#12470=CARTESIAN_POINT ( 'NONE',  ( 22.78696485699360252, -18.96938443020880172, -41.21594592233239496 ) ) ;
#12472=EDGE_LOOP ( 'NONE', ( #13638, #37318, #29600, #30053 ) ) ;
#12492=AXIS2_PLACEMENT_3D ( 'NONE', #45061, #20413, #8386 ) ;
#12493=EDGE_LOOP ( 'NONE', ( #47258, #17531, #37702, #26706 ) ) ;
#12494=ORIENTED_EDGE ( 'NONE', *, *, #4010, .T. ) ;
#12499=CARTESIAN_POINT ( 'NONE',  ( 23.98146842033044024, -14.58313461376996933, -59.75066739342922517 ) ) ;
#12500=B_SPLINE_CURVE_WITH_KNOTS ( 'NONE', 3,
 ( #47428, #20128, #31400, #11520, #47678, #12035, #15698, #27481, #11781, #51858, #11259, #47934, #44243, #31912, #27740, #27988, #20379, #7587 ),
 .UNSPECIFIED., .F., .F.,
 ( 4, 2, 2, 2, 2, 2, 2, 2, 4 ),
 ( 0.5000000059040078382, 0.5625000051660068445, 0.6250000044280057399, 0.6875000036900047462, 0.7500000029520037526, 0.8125000022140027589, 0.8750000014760018763, 0.9375000007380009936, 1.000000000000000000 ),
 .UNSPECIFIED. ) ;
#12506=CARTESIAN_POINT ( 'NONE',  ( 11.17268199994810196, -10.96232122111623575, -33.69277564961296179 ) ) ;
#12510=CARTESIAN_POINT ( 'NONE',  ( 8.760241513115010648, -18.30233052570079977, -56.90129427292900033 ) ) ;
#12511=B_SPLINE_CURVE_WITH_KNOTS ( 'NONE', 3,
 ( #47708, #27772, #43767, #12, #15990, #31942, #45319, #29061, #50022, #33757, #37706, #1803, #26150, #21187, #25628, #9923, #1546, #17784 ),
 .UNSPECIFIED., .F., .F.,
 ( 4, 2, 2, 2, 2, 2, 2, 2, 4 ),
 ( 0.000000000000000000, 0.06249993788804932004, 0.1249998757760986401, 0.1874998136641479740, 0.2499997515521972802, 0.3124996894402465863, 0.3749996273282959480, 0.4374995652163452542, 0.4999995031043945604 ),
 .UNSPECIFIED. ) ;
#12518=CARTESIAN_POINT ( 'NONE',  ( 22.90093740060443395, -16.50198292282657775, -38.49448988202613720 ) ) ;
#12519=CARTESIAN_POINT ( 'NONE',  ( 15.98424424538390198, -22.66744068707240345, -53.35393626560600211 ) ) ;
#12520=CARTESIAN_POINT ( 'NONE',  ( 24.04493740941656910, -14.58064971957864486, -41.75066428994564660 ) ) ;
#12523=EDGE_CURVE ( 'NONE', #14401, #50703, #44081, .T. ) ;
#12527=CARTESIAN_POINT ( 'NONE',  ( 20.29256778889454793, -10.20483762520559168, -38.16115576630075878 ) ) ;
#12534=CARTESIAN_POINT ( 'NONE',  ( 24.04492574745081868, -15.60216321284723762, -71.50710845886689526 ) ) ;
#12538=CARTESIAN_POINT ( 'NONE',  ( 10.20031836582380080, -11.80374558653580053, -66.02896523578509402 ) ) ;
#12539=VERTEX_POINT ( 'NONE', #20006 ) ;
#12547=CARTESIAN_POINT ( 'NONE',  ( 17.08797267472250070, -8.628172388687518790, -63.99601028757499677 ) ) ;
#12566=CARTESIAN_POINT ( 'NONE',  ( 23.04645959055375215, -19.60032229269020831, -59.67434578082231411 ) ) ;
#12569=CARTESIAN_POINT ( 'NONE',  ( 15.09838756275151539, -23.52718865851687013, -44.04936391593793843 ) ) ;
#12570=ORIENTED_EDGE ( 'NONE', *, *, #12191, .F. ) ;
#12571=CARTESIAN_POINT ( 'NONE',  ( 15.24822711595714253, -8.849178317015910622, -67.91115244803380335 ) ) ;
#12575=CARTESIAN_POINT ( 'NONE',  ( 24.37910050976440246, -15.61849357583439968, -73.79242048001989929 ) ) ;
#12582=CARTESIAN_POINT ( 'NONE',  ( 12.70463616226759918, -22.23030920680289668, -64.88491241981458302 ) ) ;
#12606=CARTESIAN_POINT ( 'NONE',  ( 13.77244605588369986, -8.765738305821798804, -81.62651318459289485 ) ) ;
#12611=CARTESIAN_POINT ( 'NONE',  ( 16.13393739769620083, -15.61618894467929941, -28.45282021618999835 ) ) ;
#12614=ADVANCED_FACE ( 'NONE', ( #49116 ), #17651, .T. ) ;
#12615=CARTESIAN_POINT ( 'NONE',  ( 23.04644611198230209, -19.60034754886721586, -39.95900824456602152 ) ) ;
#12619=DIRECTION ( 'NONE',  ( 1.000000000000000000, 0.000000000000000000, 0.000000000000000000 ) ) ;
#12627=CARTESIAN_POINT ( 'NONE',  ( 8.222911478911663963, -16.65154701704570428, -72.46599137466046159 ) ) ;
#12634=DIRECTION ( 'NONE',  ( 1.000000000000000000, 0.000000000000000000, 0.000000000000000000 ) ) ;
#12640=CARTESIAN_POINT ( 'NONE',  ( 17.86241643334011187, -9.013718618831822127, -72.03414713418756321 ) ) ;
#12642=CARTESIAN_POINT ( 'NONE',  ( 20.26051206097820057, -22.75440311940770144, -48.12548681540710049 ) ) ;
#12645=ORIENTED_EDGE ( 'NONE', *, *, #19489, .T. ) ;
#12647=CARTESIAN_POINT ( 'NONE',  ( 13.64647048605240087, -8.400295753671970900, -81.40635028194188294 ) ) ;
#12648=CARTESIAN_POINT ( 'NONE',  ( 11.27217865805896935, -9.290084831313485836, -32.79933351145292875 ) ) ;
#12651=PRODUCT_DEFINITION_FORMATION_WITH_SPECIFIED_SOURCE ( 'ANY', '', #34076, .NOT_KNOWN. ) ;
#12653=CARTESIAN_POINT ( 'NONE',  ( 24.04415599056204300, -15.73629021646003423, -59.79715706112911278 ) ) ;
#12657=CIRCLE ( 'NONE', #6834, 12.00000000000000000 ) ;
#12661=CARTESIAN_POINT ( 'NONE',  ( 23.90403299955350036, -12.85786788886049870, -43.39908821103399816 ) ) ;
#12666=CARTESIAN_POINT ( 'NONE',  ( 11.27236956094300524, -21.94243751200594517, -64.50066548858299598 ) ) ;
#12667=CARTESIAN_POINT ( 'NONE',  ( 9.367050196127319595, -15.61601677469269944, -55.84717978380999881 ) ) ;
#12672=CARTESIAN_POINT ( 'NONE',  ( 17.90525427422480576, -22.20704256537504406, -48.86948804866545260 ) ) ;
#12677=CARTESIAN_POINT ( 'NONE',  ( 8.428856623959452676, -13.54543936269719140, -60.87566458307732375 ) ) ;
#12678=DIRECTION ( 'NONE',  ( 1.000000000000000000, 0.000000000000000000, 0.000000000000000000 ) ) ;
#12681=CARTESIAN_POINT ( 'NONE',  ( 9.761022321705594251, -12.73102580472821188, -79.98287061730054859 ) ) ;
#12684=CARTESIAN_POINT ( 'NONE',  ( 9.221450368820928389, -11.63199578712598914, -76.95899765199676779 ) ) ;
#12685=CARTESIAN_POINT ( 'NONE',  ( 17.01977459420146843, -8.849194511386347273, -47.99448796539336826 ) ) ;
#12698=CARTESIAN_POINT ( 'NONE',  ( 22.56752014421309838, -18.82624589827599948, -81.23899999999999011 ) ) ;
#12708=CARTESIAN_POINT ( 'NONE',  ( 16.13393739769620083, -15.61618894467929941, -23.15000000000000213 ) ) ;
#12722=CARTESIAN_POINT ( 'NONE',  ( 8.640695177360781187, -17.94815575631400151, -62.19146876365159216 ) ) ;
#12735=CARTESIAN_POINT ( 'NONE',  ( 8.220189996527228260, -15.80974140266152084, -34.49988352258923641 ) ) ;
#12737=CARTESIAN_POINT ( 'NONE',  ( 8.428864736639086530, -17.68696802423094994, -54.70899843708602361 ) ) ;
#12740=CARTESIAN_POINT ( 'NONE',  ( 14.17109353987640041, -22.80325638057830417, -45.65220606189499364 ) ) ;
#12748=CARTESIAN_POINT ( 'NONE',  ( 23.83903410062788808, -17.68688213715710589, -77.87566196558225329 ) ) ;
#12750=DIRECTION ( 'NONE',  ( -0.4096086573010331855, 0.9122613374817791776, 0.000000000000000000 ) ) ;
#12761=ADVANCED_FACE ( 'NONE', ( #44908 ), #24957, .T. ) ;
#12772=ORIENTED_EDGE ( 'NONE', *, *, #40810, .F. ) ;
#12778=CARTESIAN_POINT ( 'NONE',  ( 19.97010344705880414, -8.769979947482401172, -67.67506889758131194 ) ) ;
#12791=EDGE_LOOP ( 'NONE', ( #13477, #39959, #51409, #50871 ) ) ;
#12794=CARTESIAN_POINT ( 'NONE',  ( 20.99561754527899282, -9.290025391674188171, -37.21600393032817777 ) ) ;
#12797=CARTESIAN_POINT ( 'NONE',  ( 23.42912986796590147, -16.70365468919549912, -32.14999999999999858 ) ) ;
#12808=CARTESIAN_POINT ( 'NONE',  ( 22.93259508256310042, -13.73980602574960130, -64.76146233876720260 ) ) ;
#12815=CARTESIAN_POINT ( 'NONE',  ( 12.14570635151480005, -21.43311010788070092, -61.14412876928479790 ) ) ;
#12818=CARTESIAN_POINT ( 'NONE',  ( 14.06335524534715908, -23.32131407103912579, -80.37566581158391443 ) ) ;
#12827=CARTESIAN_POINT ( 'NONE',  ( 23.83903255575460278, -13.54548804232147852, -75.42431961480706093 ) ) ;
#12830=VECTOR ( 'NONE', #44809, 1000.000000000000000 ) ;
#12842=CARTESIAN_POINT ( 'NONE',  ( 22.71421499214610051, -11.33989447733160105, -35.82905861000619296 ) ) ;
#12849=CARTESIAN_POINT ( 'NONE',  ( 19.81752810327339631, -22.09213314756820168, -64.56803669556019543 ) ) ;
#12868=VERTEX_POINT ( 'NONE', #31354 ) ;
#12873=CARTESIAN_POINT ( 'NONE',  ( 10.34784237018260100, -19.64900680999069849, -33.25906503489069621 ) ) ;
#12880=CARTESIAN_POINT ( 'NONE',  ( 10.22095430177014208, -19.02405797898098427, -41.28611931081641728 ) ) ;
#12881=CARTESIAN_POINT ( 'NONE',  ( 22.94884485421729892, -18.62679199014949560, -67.19975531119949608 ) ) ;
#12882=B_SPLINE_CURVE_WITH_KNOTS ( 'NONE', 3,
 ( #40351, #12317, #19405, #28278, #35383, #44278, #35901, #7876, #23822, #32448 ),
 .UNSPECIFIED., .F., .F.,
 ( 4, 1, 1, 1, 1, 1, 1, 4 ),
 ( 0.000000000000000000, 0.06914192772689449484, 0.1483608587905285991, 0.2275797898541468967, 0.3067987209177651664, 0.3860176519813834362, 0.4652365830450022610, 0.5000014761122578699 ),
 .UNSPECIFIED. ) ;
#12893=CARTESIAN_POINT ( 'NONE',  ( 24.04489399257771254, -15.64449612002278833, -71.50881132904470405 ) ) ;
#12899=DIRECTION ( 'NONE',  ( 0.000000000000000000, 0.000000000000000000, -1.000000000000000000 ) ) ;
#12907=CARTESIAN_POINT ( 'NONE',  ( 22.03478274538166204, -12.18589228887625886, -72.28500474705791135 ) ) ;
#12909=CARTESIAN_POINT ( 'NONE',  ( 19.14684319004119928, -7.941221925702031115, -39.41140439840899745 ) ) ;
#12911=CARTESIAN_POINT ( 'NONE',  ( 22.89878139006187396, -15.43167601270388900, -56.44414743042131022 ) ) ;
#12914=ORIENTED_EDGE ( 'NONE', *, *, #22640, .F. ) ;
#12916=CARTESIAN_POINT ( 'NONE',  ( 10.58908913721369949, -20.59226687547690204, -36.99984868542069449 ) ) ;
#12917=CARTESIAN_POINT ( 'NONE',  ( 12.04075003782359943, -10.20414989105540116, -32.14999999999999858 ) ) ;
#12921=CARTESIAN_POINT ( 'NONE',  ( 24.04511355972104170, -15.61618909363076924, -51.79233356384455078 ) ) ;
#12923=CARTESIAN_POINT ( 'NONE',  ( 19.06829150976720300, -7.910847508120689930, -55.12349000844960045 ) ) ;
#12933=CARTESIAN_POINT ( 'NONE',  ( 16.13393739769620083, -27.61618894467930119, -22.14999999999999858 ) ) ;
#12938=CARTESIAN_POINT ( 'NONE',  ( 22.04686311925793873, -19.02415382287680501, -64.61948873146855021 ) ) ;
#12941=CARTESIAN_POINT ( 'NONE',  ( 9.366764248923921343, -15.61602670952840199, -67.45282021618999124 ) ) ;
#12942=VECTOR ( 'NONE', #41702, 1000.000000000000114 ) ;
#12945=CARTESIAN_POINT ( 'NONE',  ( 17.01970822797235172, -22.38319285542060655, -60.91117069208365820 ) ) ;
#12946=CARTESIAN_POINT ( 'NONE',  ( 11.21742354769409999, -20.67291226489259870, -61.59270509622239587 ) ) ;
#12947=B_SPLINE_CURVE_WITH_KNOTS ( 'NONE', 3,
 ( #13668, #49583, #17846, #49322, #45380, #25434, #33818, #1607, #17595, #29631, #13924 ),
 .UNSPECIFIED., .F., .F.,
 ( 4, 1, 1, 1, 1, 1, 1, 1, 4 ),
 ( 0.4999960598860723193, 0.5157214477071244696, 0.5949403787707443492, 0.6741593098343618973, 0.7533782408979794454, 0.8325971719615969935, 0.9118161030252167620, 0.9910350340888344212, 1.000000000000000000 ),
 .UNSPECIFIED. ) ;
#12958=EDGE_CURVE ( 'NONE', #39697, #15276, #40269, .T. ) ;
#12963=CARTESIAN_POINT ( 'NONE',  ( 22.97220002312930376, -18.05331211082319953, -81.23899999999999011 ) ) ;
#12967=CARTESIAN_POINT ( 'NONE',  ( 16.13393739769620083, -15.61618894467929941, -32.14999999999999858 ) ) ;
#12973=LINE ( 'NONE', #19332, #5378 ) ;
#12978=CARTESIAN_POINT ( 'NONE',  ( 9.205734167420699166, -27.61618894467930119, -24.14999999999999858 ) ) ;
#12988=CARTESIAN_POINT ( 'NONE',  ( 15.14076279674840109, -7.831566128176559616, -70.74711331852249430 ) ) ;
#13000=CARTESIAN_POINT ( 'NONE',  ( 8.223201290577328848, -15.61599831009169925, -56.79233150823699816 ) ) ;
#13001=CARTESIAN_POINT ( 'NONE',  ( 22.64777119364662994, -20.19351164595759585, -33.70249042454723565 ) ) ;
#13003=CARTESIAN_POINT ( 'NONE',  ( 20.99564007730179327, -21.94233451394929091, -54.08400040345370741 ) ) ;
#13005=CARTESIAN_POINT ( 'NONE',  ( 8.816398121954771128, -14.21607706117750070, -46.12751964827680240 ) ) ;
#13010=CARTESIAN_POINT ( 'NONE',  ( 8.761423512428116567, -12.64911493208424531, -80.91422037451174276 ) ) ;
#13013=CARTESIAN_POINT ( 'NONE',  ( 11.27221920674516120, -21.94232376229728132, -78.50066392648321312 ) ) ;
#13019=VERTEX_POINT ( 'NONE', #24000 ) ;
#13029=VERTEX_POINT ( 'NONE', #50147 ) ;
#13031=ADVANCED_FACE ( 'NONE', ( #34400 ), #26785, .F. ) ;
#13036=CARTESIAN_POINT ( 'NONE',  ( 22.04686165056448743, -12.20822131928401788, -36.28615126516305622 ) ) ;
#13038=CARTESIAN_POINT ( 'NONE',  ( 12.72592096703445996, -9.703291609758796454, -53.78615459825274314 ) ) ;
#13042=CARTESIAN_POINT ( 'NONE',  ( 12.89372882336123638, -8.399748356796177262, -81.15800232914327239 ) ) ;
#13046=CARTESIAN_POINT ( 'NONE',  ( 9.144406050478650627, -19.18454979216170386, -60.86224082610989683 ) ) ;
#13055=CYLINDRICAL_SURFACE ( 'NONE', #42730, 6.766999999999998572 ) ;
#13062=CARTESIAN_POINT ( 'NONE',  ( 8.222431652840050731, -15.61631456792169992, -70.50766849176299900 ) ) ;
#13063=DIRECTION ( 'NONE',  ( 1.000000000000000000, 0.000000000000000000, 0.000000000000000000 ) ) ;
#13064=CARTESIAN_POINT ( 'NONE',  ( 23.38426144667019813, -17.11500491999589713, -32.14999999999999858 ) ) ;
#13071=CIRCLE ( 'NONE', #42350, 2.576499999999998902 ) ;
#13075=CARTESIAN_POINT ( 'NONE',  ( 21.77263034913930184, -11.37971624043620089, -60.64207792345899151 ) ) ;
#13083=CARTESIAN_POINT ( 'NONE',  ( 13.63580056716289945, -9.020594121423519240, -63.83757242544779587 ) ) ;
#13089=ORIENTED_EDGE ( 'NONE', *, *, #17482, .F. ) ;
#13094=ADVANCED_FACE ( 'NONE', ( #9354 ), #46756, .T. ) ;
#13096=CARTESIAN_POINT ( 'NONE',  ( 24.04521450903870061, -15.61618868716203501, -63.50766715510244609 ) ) ;
#13105=CARTESIAN_POINT ( 'NONE',  ( 8.222787824498201559, -15.61638397318239946, -64.79233150823698395 ) ) ;
#13106=VERTEX_POINT ( 'NONE', #25300 ) ;
#13112=CARTESIAN_POINT ( 'NONE',  ( 9.924177576303440773, -10.19202054563570137, -79.02086993021879380 ) ) ;
#13114=FACE_OUTER_BOUND ( 'NONE', #22685, .T. ) ;
#13119=CARTESIAN_POINT ( 'NONE',  ( 11.95218966202809874, -21.29558555530719843, -33.54920349970119986 ) ) ;
#13124=CYLINDRICAL_SURFACE ( 'NONE', #44011, 7.910999999999997812 ) ;
#13142=CARTESIAN_POINT ( 'NONE',  ( 22.47358672090329890, -12.52528092440720009, -32.30843786212719948 ) ) ;
#13146=CARTESIAN_POINT ( 'NONE',  ( 16.13393739769620083, -15.61618894467929941, -23.74958330439410048 ) ) ;
#13147=CYLINDRICAL_SURFACE ( 'NONE', #3900, 6.766999999999998572 ) ;
#13149=CARTESIAN_POINT ( 'NONE',  ( 23.51172799066640096, -14.57941495549949984, -77.02290276308829675 ) ) ;
#13153=CARTESIAN_POINT ( 'NONE',  ( 24.04166718631601896, -15.38336571792064866, -49.78296408212683133 ) ) ;
#13160=CARTESIAN_POINT ( 'NONE',  ( 12.14969441541569672, -22.52864909168088658, -72.17427940389318053 ) ) ;
#13169=CARTESIAN_POINT ( 'NONE',  ( 22.90150794149753111, -15.57801490272766110, -72.84538554144812394 ) ) ;
#13173=ORIENTED_EDGE ( 'NONE', *, *, #3672, .F. ) ;
#13177=CARTESIAN_POINT ( 'NONE',  ( 18.20456276067269386, -7.911073408245188787, -43.37570542978183852 ) ) ;
#13178=CARTESIAN_POINT ( 'NONE',  ( 14.28670337130830070, -23.65176275789830029, -56.36425564602360083 ) ) ;
#13180=CARTESIAN_POINT ( 'NONE',  ( 22.90088944531260395, -15.58987521438611346, -56.45158775362976655 ) ) ;
#13183=LINE ( 'NONE', #48545, #6644 ) ;
#13184=CARTESIAN_POINT ( 'NONE',  ( 23.25907355585459868, -17.79314290212749938, -40.32704379009269502 ) ) ;
#13189=CARTESIAN_POINT ( 'NONE',  ( 22.03008559642460185, -9.852669435941031395, -49.26128910974178865 ) ) ;
#13194=DIRECTION ( 'NONE',  ( 0.000000000000000000, 0.000000000000000000, -1.000000000000000000 ) ) ;
#13195=CARTESIAN_POINT ( 'NONE',  ( 21.51824785155721997, -11.06077896193409060, -70.62366323747509966 ) ) ;
#13204=DIRECTION ( 'NONE',  ( 0.000000000000000000, 0.000000000000000000, -1.000000000000000000 ) ) ;
#13208=CARTESIAN_POINT ( 'NONE',  ( 21.43677159062993809, -19.88198936106610759, -66.66855547569113583 ) ) ;
#13210=CARTESIAN_POINT ( 'NONE',  ( 17.90516118349662023, -22.20706887017997033, -60.86950335209443352 ) ) ;
#13211=FACE_OUTER_BOUND ( 'NONE', #9605, .T. ) ;
#13212=ORIENTED_EDGE ( 'NONE', *, *, #5628, .F. ) ;
#13220=ORIENTED_EDGE ( 'NONE', *, *, #1639, .F. ) ;
#13227=CARTESIAN_POINT ( 'NONE',  ( 23.30658763286460200, -17.14219254102309975, -81.23899999999999011 ) ) ;
#13234=CARTESIAN_POINT ( 'NONE',  ( 23.93272017389292827, -16.99025993377153654, -33.84783788291247220 ) ) ;
#13242=AXIS2_PLACEMENT_3D ( 'NONE', #29162, #28380, #45160 ) ;
#13243=CARTESIAN_POINT ( 'NONE',  ( 24.04513930477782679, -15.61618913701998146, -67.79233342760500136 ) ) ;
#13245=CARTESIAN_POINT ( 'NONE',  ( 22.18801361179549758, -19.23429899943539922, -63.01864585536749530 ) ) ;
#13247=CARTESIAN_POINT ( 'NONE',  ( 20.29176081427040046, -8.960420572825411156, -72.96524338830390377 ) ) ;
#13255=CARTESIAN_POINT ( 'NONE',  ( 20.11802031537004609, -8.703636685625692593, -59.45903915183253474 ) ) ;
#13258=CARTESIAN_POINT ( 'NONE',  ( 9.459753751615320283, -19.88776835366272877, -34.32646034695605408 ) ) ;
#13262=CARTESIAN_POINT ( 'NONE',  ( 14.66312945716499883, -8.312531070681380641, -48.50408758018539146 ) ) ;
#13286=CARTESIAN_POINT ( 'NONE',  ( 8.222281512103441159, -15.61614627842319969, -76.50766849176299900 ) ) ;
#13288=CARTESIAN_POINT ( 'NONE',  ( 10.20031836580031914, -11.80374558652071393, -66.02896523580054122 ) ) ;
#13289=EDGE_LOOP ( 'NONE', ( #35948, #10586, #48191, #32108, #35436 ) ) ;
#13292=CARTESIAN_POINT ( 'NONE',  ( 9.367442997458502063, -15.61610373232760018, -47.45282021618999835 ) ) ;
#13294=CARTESIAN_POINT ( 'NONE',  ( 14.27330375828070075, -7.992227372671099950, -59.43630006696489687 ) ) ;
#13303=VECTOR ( 'NONE', #13348, 1000.000000000000000 ) ;
#13307=EDGE_CURVE ( 'NONE', #26370, #45497, #6479, .T. ) ;
#13313=CARTESIAN_POINT ( 'NONE',  ( 22.45778058535230315, -19.86412798156090176, -32.14999999999999858 ) ) ;
#13322=CARTESIAN_POINT ( 'NONE',  ( 11.01510582436389818, -10.76437253241610037, -68.08865744343920312 ) ) ;
#13330=CARTESIAN_POINT ( 'NONE',  ( 22.51615883520530303, -12.61455468660830093, -64.31288601182949094 ) ) ;
#13331=CARTESIAN_POINT ( 'NONE',  ( 8.222496981792570381, -15.61604333543320067, -34.50766849176299900 ) ) ;
#13347=CARTESIAN_POINT ( 'NONE',  ( 14.06323637774060842, -23.32128329111424492, -60.09102755594223311 ) ) ;
#13348=DIRECTION ( 'NONE',  ( 0.6803061734058448717, 0.000000000000000000, -0.7329280390501489162 ) ) ;
#13353=CARTESIAN_POINT ( 'NONE',  ( 16.13393739769620083, -15.61618894467929941, -28.45282021618999835 ) ) ;
#13355=LINE ( 'NONE', #17535, #27682 ) ;
#13358=CARTESIAN_POINT ( 'NONE',  ( 9.695727428901339096, -20.10352073914850379, -32.81873922958869372 ) ) ;
#13365=CARTESIAN_POINT ( 'NONE',  ( 12.67868222463649808, -21.76466606210399846, -37.51015005288219584 ) ) ;
#13376=CARTESIAN_POINT ( 'NONE',  ( 14.61931855295529914, -7.511323792149719125, -80.94886153518950778 ) ) ;
#13378=ADVANCED_FACE ( 'NONE', ( #37258 ), #4117, .F. ) ;
#13379=CYLINDRICAL_SURFACE ( 'NONE', #33656, 6.766999999999998572 ) ;
#13384=CARTESIAN_POINT ( 'NONE',  ( 24.04519454997480210, -15.61618869140488997, -79.50766696426083513 ) ) ;
#13392=CARTESIAN_POINT ( 'NONE',  ( 22.04771027143680229, -11.77303280754949810, -36.26938441530820256 ) ) ;
#13399=CARTESIAN_POINT ( 'NONE',  ( 21.82166399653609901, -10.80407293660230117, -70.84382614012608315 ) ) ;
#13402=CARTESIAN_POINT ( 'NONE',  ( 24.04355859723787248, -15.45599216157355293, -49.78588638766495933 ) ) ;
#13403=DIRECTION ( 'NONE',  ( 0.000000000000000000, 0.000000000000000000, -1.000000000000000000 ) ) ;
#13408=CARTESIAN_POINT ( 'NONE',  ( 8.428791191321906240, -17.68670080509079057, -72.42431558369844424 ) ) ;
#13417=CARTESIAN_POINT ( 'NONE',  ( 22.72480950581076087, -13.84493606381021280, -70.36948975704638087 ) ) ;
#13418=CARTESIAN_POINT ( 'NONE',  ( 9.221466634667571327, -19.60040990916195369, -70.34100234386488637 ) ) ;
#13425=CARTESIAN_POINT ( 'NONE',  ( 22.90092669556440086, -15.60227691359268754, -72.45217148944418284 ) ) ;
#13426=CARTESIAN_POINT ( 'NONE',  ( 8.222922666418535087, -16.30600728892422069, -66.47990195030855887 ) ) ;
#13429=CARTESIAN_POINT ( 'NONE',  ( 8.740794891635950137, -11.96596101467000040, -54.93831488687840192 ) ) ;
#13431=CARTESIAN_POINT ( 'NONE',  ( 9.366925336875675967, -14.68809727733580495, -55.49649026802917007 ) ) ;
#13436=CARTESIAN_POINT ( 'NONE',  ( 23.43389303623280284, -14.12711491007119946, -40.16860592796539464 ) ) ;
#13440=FACE_OUTER_BOUND ( 'NONE', #16943, .T. ) ;
#13442=CARTESIAN_POINT ( 'NONE',  ( 23.47067812491659922, -19.37849624346840116, -57.65849580248539752 ) ) ;
#13467=CARTESIAN_POINT ( 'NONE',  ( 22.90083016047308462, -15.61618874168370752, -60.84718745454353694 ) ) ;
#13475=ORIENTED_EDGE ( 'NONE', *, *, #18962, .F. ) ;
#13476=CARTESIAN_POINT ( 'NONE',  ( 20.11812534144297970, -22.52867827160516256, -79.84100308582628713 ) ) ;
#13477=ORIENTED_EDGE ( 'NONE', *, *, #15359, .T. ) ;
#13480=CARTESIAN_POINT ( 'NONE',  ( 9.366931649850915420, -16.50194508580061381, -45.41115730554007968 ) ) ;
#13481=CYLINDRICAL_SURFACE ( 'NONE', #45737, 7.910999999999997812 ) ;
#13484=ORIENTED_EDGE ( 'NONE', *, *, #23382, .F. ) ;
#13488=EDGE_CURVE ( 'NONE', #33336, #45208, #8968, .T. ) ;
#13489=CARTESIAN_POINT ( 'NONE',  ( 24.04486687715447601, -15.65228672134179710, -33.79378184229195625 ) ) ;
#13502=CARTESIAN_POINT ( 'NONE',  ( 16.13393739769620083, -15.61618894467929941, -32.14999999999999858 ) ) ;
#13504=CARTESIAN_POINT ( 'NONE',  ( 19.68480220708229922, -22.61462500487489891, -69.63804828363188903 ) ) ;
#13516=CARTESIAN_POINT ( 'NONE',  ( 24.04493741807383600, -16.65174055729265135, -55.83400547657857516 ) ) ;
#13521=CARTESIAN_POINT ( 'NONE',  ( 10.06561770371539843, -19.93847889677480012, -47.87033613167638890 ) ) ;
#13527=CARTESIAN_POINT ( 'NONE',  ( 22.77438730286804258, -17.50876119793745289, -74.93619413684334063 ) ) ;
#13535=VERTEX_POINT ( 'NONE', #44338 ) ;
#13543=CARTESIAN_POINT ( 'NONE',  ( 14.36260000156801553, -22.20703888855211616, -73.03610280558059742 ) ) ;
#13546=CARTESIAN_POINT ( 'NONE',  ( 17.90520375179345436, -22.20705683982200185, -52.86948537568310513 ) ) ;
#13550=CARTESIAN_POINT ( 'NONE',  ( 11.69621752664579972, -22.08869927203039651, -60.70380296398279540 ) ) ;
#13565=DIRECTION ( 'NONE',  ( 1.000000000000000000, 0.000000000000000000, 0.000000000000000000 ) ) ;
#13566=LINE ( 'NONE', #26358, #49400 ) ;
#13567=CARTESIAN_POINT ( 'NONE',  ( 22.47052291036699856, -19.84169571818189937, -32.14999999999999858 ) ) ;
#13574=CARTESIAN_POINT ( 'NONE',  ( 9.081352278131740619, -15.55616973317930096, -59.84988861282279515 ) ) ;
#13578=FACE_OUTER_BOUND ( 'NONE', #29507, .T. ) ;
#13581=CARTESIAN_POINT ( 'NONE',  ( 10.05028766160000053, -12.04802911289969991, -77.62166643051759252 ) ) ;
#13584=CARTESIAN_POINT ( 'NONE',  ( 9.221491714471486745, -19.60045278370350985, -80.62566522957574477 ) ) ;
#13590=CARTESIAN_POINT ( 'NONE',  ( 9.387003650334634131, -11.44024311550892037, -38.68416691240651772 ) ) ;
#13591=CIRCLE ( 'NONE', #34478, 2.576499999999998902 ) ;
#13612=CARTESIAN_POINT ( 'NONE',  ( 14.92914649562269958, -23.37087955876669909, -34.56155571298829443 ) ) ;
#13613=CARTESIAN_POINT ( 'NONE',  ( 21.40734412482820304, -20.29953610935300290, -65.07833806302818402 ) ) ;
#13618=CARTESIAN_POINT ( 'NONE',  ( 21.54529218309743044, -11.45756400702632760, -78.24448439904941210 ) ) ;
#13621=CARTESIAN_POINT ( 'NONE',  ( 11.92983776680200059, -9.953318164945169855, -38.14390150139109892 ) ) ;
#13622=CARTESIAN_POINT ( 'NONE',  ( 12.30558705848279999, -9.692820574005770240, -44.16454026222620399 ) ) ;
#13638=ORIENTED_EDGE ( 'NONE', *, *, #11889, .F. ) ;
#13645=CARTESIAN_POINT ( 'NONE',  ( 17.63133417498849909, -22.50823955302369939, -46.88472117783319959 ) ) ;
#13651=CARTESIAN_POINT ( 'NONE',  ( 8.754676953983009824, -14.58992891808219916, -72.11132903714390352 ) ) ;
#13658=CARTESIAN_POINT ( 'NONE',  ( 17.14513548805572540, -23.53033894168608953, -76.25158136700031264 ) ) ;
#13659=CARTESIAN_POINT ( 'NONE',  ( 17.67054341374410242, -9.002906339670014191, -62.02556814933810614 ) ) ;
#13660=CARTESIAN_POINT ( 'NONE',  ( 13.02825699543591220, -22.94029734278106858, -46.13525268572119131 ) ) ;
#13666=LINE ( 'NONE', #29629, #6600 ) ;
#13668=CARTESIAN_POINT ( 'NONE',  ( 22.90099491887654182, -15.61618908163285546, -52.84717737022585027 ) ) ;
#13671=VECTOR ( 'NONE', #36626, 1000.000000000000000 ) ;
#13672=EDGE_LOOP ( 'NONE', ( #7850, #33830, #46873, #11631, #32435, #32827, #36971, #1057, #12132, #29310, #2049, #45967, #40424, #21271, #31409, #22463, #18685, #49002, #5499, #32399, #21766, #21425, #9979, #25032, #12321, #4358, #45374, #8094, #38300, #42717, #1501, #40567, #11472, #19512, #44588, #49470, #48929, #45318, #5171, #46620, #1993, #27444, #34855, #28398, #41341, #13484, #2968, #34523, #22536, #18042, #10920, #17008, #22954, #51242, #41782, #32281, #50465, #1983, #8959, #24049, #13979, #43735, #13890, #133, #28957, #50218, #20843, #4929, #23619, #49751, #23826, #32118, #12772, #4628, #3662, #33564, #39802, #18540, #40354, #4364, #37576, #50204, #15715, #23975, #42595, #32054, #15272, #14814, #46742, #27888, #36262, #13776, #45161, #24706, #31200, #935, #31516, #9604, #43089, #92, #7776, #9045, #51494 ) ) ;
#13677=CARTESIAN_POINT ( 'NONE',  ( 12.14971260091438765, -8.703718504070650397, -43.12570318788042556 ) ) ;
#13679=CARTESIAN_POINT ( 'NONE',  ( 23.35206755134019829, -11.63105191554319973, -57.63175854304149937 ) ) ;
#13684=CARTESIAN_POINT ( 'NONE',  ( 22.13578182761139956, -11.20205740560600027, -46.03080682667329881 ) ) ;
#13686=CARTESIAN_POINT ( 'NONE',  ( 8.823988302720360721, -15.97264899720290288, -32.14999999999999858 ) ) ;
#13691=CARTESIAN_POINT ( 'NONE',  ( 23.99659259676478484, -14.72524117505133390, -61.47176532453648434 ) ) ;
#13692=CARTESIAN_POINT ( 'NONE',  ( 23.28245223885990356, -11.50748400581630015, -57.34162007823099572 ) ) ;
#13699=CARTESIAN_POINT ( 'NONE',  ( 18.68994930968701240, -9.042806080414303338, -70.46522537534779929 ) ) ;
#13702=ORIENTED_EDGE ( 'NONE', *, *, #39986, .T. ) ;
#13704=VECTOR ( 'NONE', #32764, 1000.000000000000000 ) ;
#13707=EDGE_CURVE ( 'NONE', #5521, #13106, #10517, .T. ) ;
#13716=CARTESIAN_POINT ( 'NONE',  ( 22.90065123677362635, -15.61618748955864433, -66.45281999012681240 ) ) ;
#13725=CARTESIAN_POINT ( 'NONE',  ( 9.367407790820902136, -15.61608574124520032, -61.84717978381009829 ) ) ;
#13730=CARTESIAN_POINT ( 'NONE',  ( 8.222963689089544559, -16.65192889645067353, -80.46600190389186480 ) ) ;
#13738=ORIENTED_EDGE ( 'NONE', *, *, #6459, .T. ) ;
#13746=ORIENTED_EDGE ( 'NONE', *, *, #1153, .F. ) ;
#13754=CARTESIAN_POINT ( 'NONE',  ( 8.361024636538020971, -14.53518228854489891, -72.33149193979490121 ) ) ;
#13761=CARTESIAN_POINT ( 'NONE',  ( 23.83903582647615593, -17.68687351299132970, -35.87566232877769323 ) ) ;
#13762=CARTESIAN_POINT ( 'NONE',  ( 9.221354005738056969, -11.63216052016282909, -42.67431283448043189 ) ) ;
#13763=CARTESIAN_POINT ( 'NONE',  ( 11.27215929994608246, -9.290099381825209335, -59.08403816176677736 ) ) ;
#13765=CARTESIAN_POINT ( 'NONE',  ( 23.83903208326023559, -17.68689219033248960, -55.87567441642309518 ) ) ;
#13768=CARTESIAN_POINT ( 'NONE',  ( 22.90092414013790645, -15.63002369583071172, -62.45347908067368081 ) ) ;
#13771=ADVANCED_FACE ( 'NONE', ( #7106 ), #6848, .T. ) ;
#13774=CARTESIAN_POINT ( 'NONE',  ( 17.91338361966710124, -8.381531697687238491, -58.64411075632859394 ) ) ;
#13776=ORIENTED_EDGE ( 'NONE', *, *, #28121, .F. ) ;
#13777=CARTESIAN_POINT ( 'NONE',  ( 22.83850260844683433, -14.06168006131323622, -34.77405416936607452 ) ) ;
#13782=CARTESIAN_POINT ( 'NONE',  ( 8.222960110812529422, -14.58047518749336291, -34.83399806068581483 ) ) ;
#13801=CARTESIAN_POINT ( 'NONE',  ( 22.80008605052550053, -19.75734937745210118, -64.18943593078199683 ) ) ;
#13811=ORIENTED_EDGE ( 'NONE', *, *, #23622, .F. ) ;
#13820=CARTESIAN_POINT ( 'NONE',  ( 22.77360043544521417, -11.26806673883854337, -45.32308785462522849 ) ) ;
#13824=VERTEX_POINT ( 'NONE', #11033 ) ;
#13826=CARTESIAN_POINT ( 'NONE',  ( 23.14736512976970317, -16.36076306552550008, -68.88084675407539237 ) ) ;
#13833=CARTESIAN_POINT ( 'NONE',  ( 18.79898847303969944, -22.14612473781209800, -76.82947711988119011 ) ) ;
#13845=CARTESIAN_POINT ( 'NONE',  ( 8.302058585374817667, -14.33516931341604561, -38.55923738394448463 ) ) ;
#13846=CARTESIAN_POINT ( 'NONE',  ( 10.72263499592188118, -19.77488192770410080, -55.24448753831254066 ) ) ;
#13848=EDGE_LOOP ( 'NONE', ( #31560, #14426, #43016, #47104 ) ) ;
#13853=ADVANCED_FACE ( 'NONE', ( #30918 ), #51379, .T. ) ;
#13858=DIRECTION ( 'NONE',  ( 1.000000000000000000, 2.460964292799963328E-14, 0.000000000000000000 ) ) ;
#13864=CARTESIAN_POINT ( 'NONE',  ( 10.45564697911039964, -10.19920034271800091, -37.25499936915139187 ) ) ;
#13871=CARTESIAN_POINT ( 'NONE',  ( 17.01976985042453805, -8.849193832279162564, -77.99448518340960845 ) ) ;
#13890=ORIENTED_EDGE ( 'NONE', *, *, #46340, .F. ) ;
#13896=CARTESIAN_POINT ( 'NONE',  ( 9.119179062043329509, -16.34812076460110220, -49.41972697186909613 ) ) ;
#13904=CARTESIAN_POINT ( 'NONE',  ( 15.92376862201360233, -23.06350546971500037, -69.57632324310819172 ) ) ;
#13914=CARTESIAN_POINT ( 'NONE',  ( 12.72604310356256185, -9.703222519325121809, -57.78615345517096102 ) ) ;
#13917=ORIENTED_EDGE ( 'NONE', *, *, #29950, .T. ) ;
#13919=CARTESIAN_POINT ( 'NONE',  ( 22.19035827901491587, -12.49215051982365132, -32.30141085084914465 ) ) ;
#13924=CARTESIAN_POINT ( 'NONE',  ( 9.366543050370410128, -15.61630854221780140, -53.84717978381009829 ) ) ;
#13932=CARTESIAN_POINT ( 'NONE',  ( 18.69804252995849936, -7.779857856303769914, -49.39298971242509850 ) ) ;
#13934=CARTESIAN_POINT ( 'NONE',  ( 23.06214062797170072, -3.616188944679339823, -32.14999999999999858 ) ) ;
#13938=CARTESIAN_POINT ( 'NONE',  ( 16.81282819544960105, -23.03547469802990122, -42.70361172200119881 ) ) ;
#13939=CARTESIAN_POINT ( 'NONE',  ( 8.818632591069450299, -16.16764275473400048, -32.14999999999999858 ) ) ;
#13940=AXIS2_PLACEMENT_3D ( 'NONE', #39234, #19309, #38725 ) ;
#13942=CARTESIAN_POINT ( 'NONE',  ( 20.99565841940248490, -9.290058012837690171, -51.50066301143422720 ) ) ;
#13944=CARTESIAN_POINT ( 'NONE',  ( 23.92517191223645057, -14.20005315669235202, -61.45044126124142991 ) ) ;
#13945=CARTESIAN_POINT ( 'NONE',  ( 24.19548247469570157, -13.88580988780200087, -55.44036573270409463 ) ) ;
#13955=ORIENTED_EDGE ( 'NONE', *, *, #38640, .F. ) ;
#13965=CARTESIAN_POINT ( 'NONE',  ( 9.367054778780087076, -16.02018512892366786, -57.82818532426606595 ) ) ;
#13969=CARTESIAN_POINT ( 'NONE',  ( 22.89996919748105952, -15.73990749768590369, -66.45863867653210377 ) ) ;
#13979=ORIENTED_EDGE ( 'NONE', *, *, #1467, .F. ) ;
#13995=CARTESIAN_POINT ( 'NONE',  ( 22.32569053158739081, -20.61273240502229243, -34.00854356534225786 ) ) ;
#14008=CARTESIAN_POINT ( 'NONE',  ( 22.44091603520600131, -10.94620300795959977, -77.08462780361209354 ) ) ;
#14012=CARTESIAN_POINT ( 'NONE',  ( 22.90075166721855737, -15.61618922411645727, -44.45281379938008115 ) ) ;
#14018=ADVANCED_FACE ( 'NONE', ( #37192 ), #32708, .T. ) ;
#14026=CARTESIAN_POINT ( 'NONE',  ( 13.78034597000720041, -8.547433627804178258, -52.46503413336629507 ) ) ;
#14033=CARTESIAN_POINT ( 'NONE',  ( 21.80601387979700689, -21.13100886278292379, -61.75318708358965836 ) ) ;
#14035=CARTESIAN_POINT ( 'NONE',  ( 17.16956447778131079, -7.705200310418222287, -35.33399669007164334 ) ) ;
#14036=CARTESIAN_POINT ( 'NONE',  ( 9.469768305572209499, -17.67289628306980021, -81.23899999999999011 ) ) ;
#14038=ORIENTED_EDGE ( 'NONE', *, *, #44073, .F. ) ;
#14046=ORIENTED_EDGE ( 'NONE', *, *, #25335, .F. ) ;
#14049=CARTESIAN_POINT ( 'NONE',  ( 22.04685344253070056, -19.02417191927269613, -52.61948472975157642 ) ) ;
#14051=ORIENTED_EDGE ( 'NONE', *, *, #11312, .T. ) ;
#14056=CARTESIAN_POINT ( 'NONE',  ( 8.741653217529419706, -18.25074435142980178, -72.90351834778009277 ) ) ;
#14062=DIRECTION ( 'NONE',  ( 0.000000000000000000, 0.000000000000000000, -1.000000000000000000 ) ) ;
#14077=CARTESIAN_POINT ( 'NONE',  ( 8.222937779697582883, -14.90190862121987792, -44.53641600745626761 ) ) ;
#14081=CARTESIAN_POINT ( 'NONE',  ( 14.18091115246270029, -22.39322721071389921, -77.43649130894630161 ) ) ;
#14085=CARTESIAN_POINT ( 'NONE',  ( 23.04646839281239679, -11.63207206855464015, -77.62566222703568997 ) ) ;
#14088=CARTESIAN_POINT ( 'NONE',  ( 12.48870797616079997, -21.65397505889350072, -71.12571408330069289 ) ) ;
#14089=CARTESIAN_POINT ( 'NONE',  ( 22.90145954991004729, -15.72428510330016849, -78.85226058911112546 ) ) ;
#14099=ORIENTED_EDGE ( 'NONE', *, *, #1639, .T. ) ;
#14109=CARTESIAN_POINT ( 'NONE',  ( 21.35490516321459609, -9.654190832205486572, -33.52126662197601092 ) ) ;
#14111=ORIENTED_EDGE ( 'NONE', *, *, #43268, .T. ) ;
#14112=CARTESIAN_POINT ( 'NONE',  ( 15.09836090117696017, -7.705192450957612849, -53.25066628357330956 ) ) ;
#14116=CARTESIAN_POINT ( 'NONE',  ( 18.29348190141509889, -23.16092983672059802, -40.42375661169609913 ) ) ;
#14126=CARTESIAN_POINT ( 'NONE',  ( 10.66652299674349891, -20.07151597450609870, -41.62953446819029324 ) ) ;
#14132=B_SPLINE_CURVE_WITH_KNOTS ( 'NONE', 3,
 ( #34423, #30491, #42313, #5890, #14523, #1698, #33391, #41783, #10604, #1440 ),
 .UNSPECIFIED., .F., .F.,
 ( 4, 1, 1, 1, 1, 1, 1, 4 ),
 ( 0.000000000000000000, 0.05993458473492679905, 0.1391535157985444027, 0.2183724468621642545, 0.2975913779257818859, 0.3768103089894005997, 0.4560292400530182033, 0.4999984997257186370 ),
 .UNSPECIFIED. ) ;
#14140=EDGE_CURVE ( 'NONE', #20583, #48341, #50205, .T. ) ;
#14151=CARTESIAN_POINT ( 'NONE',  ( 14.86072368984219949, -8.679223790466799926, -49.89504055825069884 ) ) ;
#14158=B_SPLINE_CURVE_WITH_KNOTS ( 'NONE', 3,
 ( #44931, #10329, #45972, #2203, #42037, #49139, #25760, #25505, #29448, #17409 ),
 .UNSPECIFIED., .F., .F.,
 ( 4, 1, 1, 1, 1, 1, 1, 4 ),
 ( 0.4999984997257186370, 0.5352481711166380274, 0.6144671021802581290, 0.6936860332438941068, 0.7729049643075164289, 0.8521238953711365305, 0.9313428264347566321, 1.000000000000000000 ),
 .UNSPECIFIED. ) ;
#14159=CARTESIAN_POINT ( 'NONE',  ( 11.48089076940169839, -21.93567517873050221, -33.98952930500309577 ) ) ;
#14161=CARTESIAN_POINT ( 'NONE',  ( 24.04493594278903146, -15.61063966555162708, -49.79210729519485312 ) ) ;
#14167=CARTESIAN_POINT ( 'NONE',  ( 8.223454620794861114, -15.61605491354059971, -46.50766849176290663 ) ) ;
#14172=CARTESIAN_POINT ( 'NONE',  ( 14.06330661571832863, -7.911076412684214354, -47.20899900762205448 ) ) ;
#14176=PLANE ( 'NONE',  #34519 ) ;
#14182=CARTESIAN_POINT ( 'NONE',  ( 20.99558350725401112, -9.289997995219156479, -43.50069810257394920 ) ) ;
#14183=CARTESIAN_POINT ( 'NONE',  ( 7.895084482184580921, -15.93871443592090031, -54.77987702475120102 ) ) ;
#14185=CARTESIAN_POINT ( 'NONE',  ( 12.14992655622318551, -22.52878033032515148, -48.17433562066877784 ) ) ;
#14191=CARTESIAN_POINT ( 'NONE',  ( 9.151664503347209489, -18.21514239443270355, -41.11923310072890558 ) ) ;
#14194=CARTESIAN_POINT ( 'NONE',  ( 8.880059303195860565, -15.24727849168679938, -32.14999999999999858 ) ) ;
#14196=B_SPLINE_CURVE_WITH_KNOTS ( 'NONE', 3,
 ( #18524, #50501, #14852, #30561, #46581, #30815, #47101 ),
 .UNSPECIFIED., .F., .F.,
 ( 4, 1, 1, 1, 4 ),
 ( 0.6416644417609895790, 0.6584949831503380535, 0.7723299887668140240, 0.8861649943832899945, 1.000000000000000000 ),
 .UNSPECIFIED. ) ;
#14199=B_SPLINE_CURVE_WITH_KNOTS ( 'NONE', 3,
 ( #18215, #5910, #29733, #45749, #25795, #6173, #30258, #22132, #41804, #46540 ),
 .UNSPECIFIED., .F., .F.,
 ( 4, 1, 1, 1, 1, 1, 1, 4 ),
 ( 0.000000000000000000, 0.05183927916845956774, 0.1310582102320191900, 0.2102771412957371577, 0.2894960723593013596, 0.3687150034230238238, 0.4479339344865834738, 0.4999968673859223056 ),
 .UNSPECIFIED. ) ;
#14201=CARTESIAN_POINT ( 'NONE',  ( 9.855508381251125272, -10.73142913993969394, -60.71829047705996629 ) ) ;
#14202=CARTESIAN_POINT ( 'NONE',  ( 22.29884365131979962, -21.09128269666270228, -65.73882677097451221 ) ) ;
#14210=CARTESIAN_POINT ( 'NONE',  ( 3.205734167420700498, -15.61618894467930652, -23.15000000000000213 ) ) ;
#14214=CARTESIAN_POINT ( 'NONE',  ( 11.12952202957884573, -9.453362623693060129, -65.07532067451190017 ) ) ;
#14222=AXIS2_PLACEMENT_3D ( 'NONE', #2276, #5954, #18251 ) ;
#14228=CARTESIAN_POINT ( 'NONE',  ( 20.07088694243709881, -21.46793974735500043, -73.15866903151078304 ) ) ;
#14234=CARTESIAN_POINT ( 'NONE',  ( 10.40721251143282977, -10.10600624985592333, -80.75144566232624754 ) ) ;
#14246=DIRECTION ( 'NONE',  ( 0.000000000000000000, 0.000000000000000000, -1.000000000000000000 ) ) ;
#14255=CARTESIAN_POINT ( 'NONE',  ( 20.02379755832415498, -21.17856784602826181, -46.75851876412026087 ) ) ;
#14256=EDGE_CURVE ( 'NONE', #4764, #10139, #26412, .T. ) ;
#14267=CARTESIAN_POINT ( 'NONE',  ( 23.20097397146510332, -12.20389611180989853, -79.14432001126608895 ) ) ;
#14285=CARTESIAN_POINT ( 'NONE',  ( 11.67472944696460146, -21.58461912274730210, -49.77159047720329710 ) ) ;
#14288=CARTESIAN_POINT ( 'NONE',  ( 22.90093737722143885, -16.50198483417289097, -68.49448457974217774 ) ) ;
#14291=CARTESIAN_POINT ( 'NONE',  ( 23.60684277050431845, -18.32442953224958515, -61.61821266173036804 ) ) ;
#14294=CARTESIAN_POINT ( 'NONE',  ( 9.283276003734380666, -17.14284064744749969, -81.23899999999999011 ) ) ;
#14302=VERTEX_POINT ( 'NONE', #46881 ) ;
#14306=CARTESIAN_POINT ( 'NONE',  ( 11.97532584595513683, -21.02755421326961383, -53.16115279593655885 ) ) ;
#14309=CARTESIAN_POINT ( 'NONE',  ( 21.35165372367944059, -21.64041393852045658, -49.78022346639211548 ) ) ;
#14313=CARTESIAN_POINT ( 'NONE',  ( 10.89649166119029999, -21.46049469889319994, -72.74508048565289187 ) ) ;
#14322=ORIENTED_EDGE ( 'NONE', *, *, #12022, .T. ) ;
#14336=CARTESIAN_POINT ( 'NONE',  ( 18.20458473725057758, -23.32129814441765703, -46.20904756636038968 ) ) ;
#14339=CARTESIAN_POINT ( 'NONE',  ( 22.88559359100839785, -17.65523230413990063, -70.94053896172950147 ) ) ;
#14347=CARTESIAN_POINT ( 'NONE',  ( 20.34823716830939944, -9.960904602951780262, -80.15667222455330432 ) ) ;
#14349=CARTESIAN_POINT ( 'NONE',  ( 11.27233786307961516, -21.94241352851297933, -42.21600145475415644 ) ) ;
#14355=B_SPLINE_CURVE_WITH_KNOTS ( 'NONE', 3,
 ( #44831, #8936, #49032, #29089, #45086, #9195, #25147, #22252, #42978, #10487, #26443, #35084, #42459, #6814, #18326, #6294, #41934, #14406 ),
 .UNSPECIFIED., .F., .F.,
 ( 4, 2, 2, 2, 2, 2, 2, 2, 4 ),
 ( 0.000000000000000000, 0.06249999926200177497, 0.1249999985240035499, 0.1874999977860053180, 0.2499999970480070999, 0.3124999963100088540, 0.3749999955720106359, 0.4374999948340124178, 0.4999999940960141998 ),
 .UNSPECIFIED. ) ;
#14359=CARTESIAN_POINT ( 'NONE',  ( 21.24080222438520948, -9.496642911058136960, -39.22927993103733257 ) ) ;
#14362=ORIENTED_EDGE ( 'NONE', *, *, #31660, .T. ) ;
#14366=CARTESIAN_POINT ( 'NONE',  ( 9.627976488470578076, -13.67980814752628227, -45.54496871415931736 ) ) ;
#14379=CARTESIAN_POINT ( 'NONE',  ( 17.14114147996649962, -7.833368920533811064, -47.55346040742190183 ) ) ;
#14386=CARTESIAN_POINT ( 'NONE',  ( 18.59784447790319817, -9.007730646819130271, -38.46077722564549362 ) ) ;
#14387=CARTESIAN_POINT ( 'NONE',  ( 22.90080846266944548, -15.61618871746016879, -44.84718732428002852 ) ) ;
#14391=DIRECTION ( 'NONE',  ( 0.000000000000000000, 0.000000000000000000, -1.000000000000000000 ) ) ;
#14399=CARTESIAN_POINT ( 'NONE',  ( 22.76950726391698154, -11.20136067151295833, -71.32103239729558197 ) ) ;
#14401=VERTEX_POINT ( 'NONE', #24200 ) ;
#14406=CARTESIAN_POINT ( 'NONE',  ( 24.04527493495583457, -15.61618894149694192, -73.79233149842438877 ) ) ;
#14409=CARTESIAN_POINT ( 'NONE',  ( 12.93140221574939908, -21.90000363839990172, -49.10285124761459485 ) ) ;
#14416=CARTESIAN_POINT ( 'NONE',  ( 20.98937642605960008, -9.450845481008398608, -36.99984868542069449 ) ) ;
#14423=CARTESIAN_POINT ( 'NONE',  ( 17.25281598583982401, -22.57971318746314893, -67.29646813281843265 ) ) ;
#14424=CARTESIAN_POINT ( 'NONE',  ( 9.807798170205042965, -10.75447755698773200, -45.00063938649487483 ) ) ;
#14425=CARTESIAN_POINT ( 'NONE',  ( 19.92014648307743130, -22.58664708275372135, -45.84940091502108572 ) ) ;
#14426=ORIENTED_EDGE ( 'NONE', *, *, #3205, .T. ) ;
#14435=EDGE_LOOP ( 'NONE', ( #8851, #9348, #2375, #12440 ) ) ;
#14441=EDGE_CURVE ( 'NONE', #34841, #19315, #2513, .T. ) ;
#14442=CARTESIAN_POINT ( 'NONE',  ( 15.28400219184669950, -23.81742849744160040, -60.32520219920449733 ) ) ;
#14448=CARTESIAN_POINT ( 'NONE',  ( 16.66132627741290051, -8.184597272991679162, -57.75520862408900058 ) ) ;
#14450=CARTESIAN_POINT ( 'NONE',  ( 9.442544990296008578, -13.22597753588140002, -32.14999999999999858 ) ) ;
#14453=DIRECTION ( 'NONE',  ( 0.000000000000000000, 0.000000000000000000, -1.000000000000000000 ) ) ;
#14454=B_SPLINE_CURVE_WITH_KNOTS ( 'NONE', 3,
 ( #31299, #15346, #51253, #47328, #23692, #27638, #6709, #34722, #43132, #10901, #2773, #15605, #42874, #35772, #7744, #26598, #26867, #42615 ),
 .UNSPECIFIED., .F., .F.,
 ( 4, 2, 2, 2, 2, 2, 2, 2, 4 ),
 ( 0.4999988908354166539, 0.5624990294809895097, 0.6249991681265623100, 0.6874993067721352213, 0.7499994454177081327, 0.8124995840632810440, 0.8749997227088539553, 0.9374998613544269777, 1.000000000000000000 ),
 .UNSPECIFIED. ) ;
#14456=CARTESIAN_POINT ( 'NONE',  ( 24.04493568462940090, -15.61079658766591649, -61.50745927652321399 ) ) ;
#14457=CARTESIAN_POINT ( 'NONE',  ( 17.10857306732300032, -7.428832471405029558, -63.04538311481149293 ) ) ;
#14458=ORIENTED_EDGE ( 'NONE', *, *, #22986, .T. ) ;
#14464=CARTESIAN_POINT ( 'NONE',  ( 22.90071877914020249, -15.61618922162072565, -76.45281474520940890 ) ) ;
#14482=CARTESIAN_POINT ( 'NONE',  ( 8.222290034161709116, -15.61613760572089937, -44.79233150823699816 ) ) ;
#14492=CARTESIAN_POINT ( 'NONE',  ( 19.41271919554131031, -21.86055833610470955, -37.19327432862769456 ) ) ;
#14512=CARTESIAN_POINT ( 'NONE',  ( 17.43063470081056821, -22.26741796077540059, -46.89152911514357669 ) ) ;
#14521=CARTESIAN_POINT ( 'NONE',  ( 13.50542271583660003, -23.43115095844289897, -36.11094655318100166 ) ) ;
#14523=CARTESIAN_POINT ( 'NONE',  ( 14.74159083669217729, -8.702150310962082358, -48.28392467753529615 ) ) ;
#14543=CARTESIAN_POINT ( 'NONE',  ( 22.76337341064190056, -19.01578781639930327, -57.21816999718349450 ) ) ;
#14547=CARTESIAN_POINT ( 'NONE',  ( 9.366937397696199596, -15.61618894467949836, -28.45282021618999835 ) ) ;
#14550=CARTESIAN_POINT ( 'NONE',  ( 9.140883284797808983, -16.59444103326700315, -81.23899999999999011 ) ) ;
#14553=VERTEX_POINT ( 'NONE', #51760 ) ;
#14554=AXIS2_PLACEMENT_3D ( 'NONE', #4544, #20516, #36510 ) ;
#14563=ORIENTED_EDGE ( 'NONE', *, *, #16258, .T. ) ;
#14575=CARTESIAN_POINT ( 'NONE',  ( 22.46012682185303078, -20.47783369061121661, -79.71600332221316876 ) ) ;
#14578=CARTESIAN_POINT ( 'NONE',  ( 22.90097160515300345, -15.96958584066058151, -42.86379408845288452 ) ) ;
#14579=CARTESIAN_POINT ( 'NONE',  ( 22.90091122653545241, -15.61618862529044804, -78.45282272177526295 ) ) ;
#14580=CARTESIAN_POINT ( 'NONE',  ( 22.89829579906880141, -19.59490778382370024, -47.45674758581829877 ) ) ;
#14583=VECTOR ( 'NONE', #11899, 1000.000000000000000 ) ;
#14591=CARTESIAN_POINT ( 'NONE',  ( 24.04493583903491682, -15.61104923254273835, -45.50746918787013584 ) ) ;
#14597=CARTESIAN_POINT ( 'NONE',  ( 14.62412072909330085, -22.50552946476250327, -71.41585254811130312 ) ) ;
#14605=CARTESIAN_POINT ( 'NONE',  ( 9.831878794972480406, -12.44970571174390095, -71.60102766968249455 ) ) ;
#14613=VERTEX_POINT ( 'NONE', #10975 ) ;
#14616=CARTESIAN_POINT ( 'NONE',  ( 10.71149743639709939, -11.10623284283549950, -62.06801868260409094 ) ) ;
#14619=ORIENTED_EDGE ( 'NONE', *, *, #17325, .T. ) ;
#14631=CARTESIAN_POINT ( 'NONE',  ( 22.47876248253967901, -18.58448477081164896, -50.98678728705716878 ) ) ;
#14635=CARTESIAN_POINT ( 'NONE',  ( 20.06159909528509999, -22.41032032263160190, -48.34564971805809819 ) ) ;
#14643=CARTESIAN_POINT ( 'NONE',  ( 12.28756344725089988, -21.52786946782889999, -43.53078881371720144 ) ) ;
#14644=ORIENTED_EDGE ( 'NONE', *, *, #17574, .F. ) ;
#14648=CARTESIAN_POINT ( 'NONE',  ( 20.99565279412726682, -9.290053523812696668, -51.21599975162614982 ) ) ;
#14652=CONICAL_SURFACE ( 'NONE', #43949, 0.3230324999999999447, 0.7853981633974469467 ) ;
#14657=CARTESIAN_POINT ( 'NONE',  ( 9.530058881327454046, -20.02245067740681961, -32.60498688510223531 ) ) ;
#14667=CARTESIAN_POINT ( 'NONE',  ( 18.71115058146540022, -9.051089486024348929, -40.07189310636189816 ) ) ;
#14668=CARTESIAN_POINT ( 'NONE',  ( 12.72590404555789512, -21.52907670588500721, -77.11949976459347056 ) ) ;
#14671=CARTESIAN_POINT ( 'NONE',  ( 22.52295300047549276, -13.38580680388945332, -80.74026669357201058 ) ) ;
#14674=CARTESIAN_POINT ( 'NONE',  ( 12.87814453327409936, -22.40556983950980197, -31.92983709734899378 ) ) ;
#14680=CARTESIAN_POINT ( 'NONE',  ( 24.04487507994048201, -15.64862276394573115, -75.79363074543330470 ) ) ;
#14681=AXIS2_PLACEMENT_3D ( 'NONE', #18061, #14391, #38243 ) ;
#14682=CARTESIAN_POINT ( 'NONE',  ( 22.89016887680049450, -19.75659366885420098, -45.68273552378035163 ) ) ;
#14683=EDGE_LOOP ( 'NONE', ( #51837, #14619, #40300, #22853 ) ) ;
#14688=CARTESIAN_POINT ( 'NONE',  ( 23.83903686589412629, -13.54550955106036980, -47.70900000688411069 ) ) ;
#14696=CARTESIAN_POINT ( 'NONE',  ( 15.27024859253024403, -22.36980594194034566, -32.99316856505028994 ) ) ;
#14699=CARTESIAN_POINT ( 'NONE',  ( 22.81009815672139851, -10.77763569235409946, -61.59270509622250245 ) ) ;
#14703=ORIENTED_EDGE ( 'NONE', *, *, #33262, .F. ) ;
#14705=CARTESIAN_POINT ( 'NONE',  ( 8.874208692728860370, -17.29041501526199909, -53.16051062239899494 ) ) ;
#14708=CARTESIAN_POINT ( 'NONE',  ( 9.872657506090700252, -12.41267197780759979, -32.14999999999999858 ) ) ;
#14716=CARTESIAN_POINT ( 'NONE',  ( 24.03960203508535187, -15.30246675214741181, -61.49505239560236447 ) ) ;
#14718=CARTESIAN_POINT ( 'NONE',  ( 7.942461939831210849, -16.55557732664409798, -64.47132387395669184 ) ) ;
#14719=VERTEX_POINT ( 'NONE', #19340 ) ;
#14736=EDGE_CURVE ( 'NONE', #22390, #586, #45841, .T. ) ;
#14737=CARTESIAN_POINT ( 'NONE',  ( 9.807815151057885927, -20.47792212130217493, -70.58399882812879866 ) ) ;
#14741=CARTESIAN_POINT ( 'NONE',  ( 12.14978603429348958, -8.703677051011474930, -37.12566588475947071 ) ) ;
#14747=DIRECTION ( 'NONE',  ( 0.000000000000000000, 0.000000000000000000, -1.000000000000000000 ) ) ;
#14752=CARTESIAN_POINT ( 'NONE',  ( 9.405693712298736742, -17.02440160981913309, -37.78093115865203089 ) ) ;
#14766=CARTESIAN_POINT ( 'NONE',  ( 21.14893523691819865, -22.16084452985059983, -36.08420929373698982 ) ) ;
#14770=CARTESIAN_POINT ( 'NONE',  ( 13.15886326406111451, -21.71786568543119955, -51.09713416873294278 ) ) ;
#14779=CARTESIAN_POINT ( 'NONE',  ( 18.55035336995420181, -8.149777981444650266, -80.88713649466590994 ) ) ;
#14802=EDGE_LOOP ( 'NONE', ( #36198, #44059, #8423, #19190, #39287 ) ) ;
#14803=CARTESIAN_POINT ( 'NONE',  ( 20.78426059192069886, -9.795433965503590912, -52.78190985762079634 ) ) ;
#14814=ORIENTED_EDGE ( 'NONE', *, *, #47918, .F. ) ;
#14824=ORIENTED_EDGE ( 'NONE', *, *, #7623, .F. ) ;
#14832=FACE_OUTER_BOUND ( 'NONE', #13848, .T. ) ;
#14840=CARTESIAN_POINT ( 'NONE',  ( 18.85312695456509857, -22.97776189731640173, -49.67487765559980062 ) ) ;
#14848=CARTESIAN_POINT ( 'NONE',  ( 21.25580764232959652, -11.01228238293339956, -32.14999999999999858 ) ) ;
#14852=CARTESIAN_POINT ( 'NONE',  ( 22.95878781942407443, -14.77418192080419068, -80.80869067174239717 ) ) ;
#14854=EDGE_CURVE ( 'NONE', #20584, #36469, #41827, .T. ) ;
#14855=CARTESIAN_POINT ( 'NONE',  ( 9.807730840030560060, -10.75456395163743117, -71.00065483045410986 ) ) ;
#14857=CARTESIAN_POINT ( 'NONE',  ( 18.09661853408499965, -22.39043738500939895, -71.25741468598400274 ) ) ;
#14858=ORIENTED_EDGE ( 'NONE', *, *, #36462, .T. ) ;
#14863=CARTESIAN_POINT ( 'NONE',  ( 11.78046264069759985, -10.06712384583619979, -81.74105084582579650 ) ) ;
#14873=CARTESIAN_POINT ( 'NONE',  ( 23.04645209240441162, -11.63204155749060931, -39.62566383368776002 ) ) ;
#14876=VERTEX_POINT ( 'NONE', #9101 ) ;
#14877=ORIENTED_EDGE ( 'NONE', *, *, #42673, .T. ) ;
#14880=CARTESIAN_POINT ( 'NONE',  ( 22.90093739769648806, -15.61618495405599560, -46.45282767544845370 ) ) ;
#14887=ORIENTED_EDGE ( 'NONE', *, *, #43137, .T. ) ;
#14888=CARTESIAN_POINT ( 'NONE',  ( 9.366917463373315655, -14.83999494934982621, -33.48934057612472515 ) ) ;
#14890=CARTESIAN_POINT ( 'NONE',  ( 22.82885795094379944, -19.71067137562029714, -48.18721185593089729 ) ) ;
#14893=CARTESIAN_POINT ( 'NONE',  ( 18.25866816537099169, -8.891006542728039364, -64.44458661451926673 ) ) ;
#14899=CARTESIAN_POINT ( 'NONE',  ( 22.44169310211590229, -12.46106974759469921, -46.69954605626199395 ) ) ;
#14902=ORIENTED_EDGE ( 'NONE', *, *, #25335, .T. ) ;
#14906=CARTESIAN_POINT ( 'NONE',  ( 18.20468874562406825, -7.911109138856854628, -51.09100011753265136 ) ) ;
#14908=CARTESIAN_POINT ( 'NONE',  ( 23.04647201731028616, -11.63207886453984052, -47.34100298069407842 ) ) ;
#14919=ORIENTED_EDGE ( 'NONE', *, *, #48105, .T. ) ;
#14923=CARTESIAN_POINT ( 'NONE',  ( 10.40182605014470063, -11.50699697134410115, -40.04515584691789343 ) ) ;
#14926=CARTESIAN_POINT ( 'NONE',  ( 16.17631379709270334, -8.563475783249899109, -51.95473276590480083 ) ) ;
#14930=ORIENTED_EDGE ( 'NONE', *, *, #2428, .T. ) ;
#14931=CARTESIAN_POINT ( 'NONE',  ( 10.38431742451460060, -20.95740775194419925, -36.04922151265729724 ) ) ;
#14955=CARTESIAN_POINT ( 'NONE',  ( 9.985151944901502929, -18.54018250714871741, -33.31138893891623809 ) ) ;
#14956=CARTESIAN_POINT ( 'NONE',  ( 24.04490452168148451, -15.61618923948461557, -69.79232899952297942 ) ) ;
#14957=CARTESIAN_POINT ( 'NONE',  ( 10.59188935906489881, -9.511402003807539529, -59.05769930218669828 ) ) ;
#14958=FACE_OUTER_BOUND ( 'NONE', #39064, .T. ) ;
#14959=LINE ( 'NONE', #3949, #46819 ) ;
#14963=CARTESIAN_POINT ( 'NONE',  ( 16.76097247798089995, -23.04003705824129966, -58.70583579685249731 ) ) ;
#14966=FACE_OUTER_BOUND ( 'NONE', #47107, .T. ) ;
#14968=CARTESIAN_POINT ( 'NONE',  ( 16.13393739769620083, -15.61618894467929941, -32.14999999999999858 ) ) ;
#14973=CARTESIAN_POINT ( 'NONE',  ( 14.04158334993860002, -7.640928745299749636, -58.92599869950329605 ) ) ;
#14975=CARTESIAN_POINT ( 'NONE',  ( 20.92244642525459852, -21.76386151488839715, -32.14999999999999858 ) ) ;
#14991=CARTESIAN_POINT ( 'NONE',  ( 23.04646828283125615, -19.60030602656101451, -69.95900078780417175 ) ) ;
#15001=ADVANCED_FACE ( 'NONE', ( #28218 ), #44219, .T. ) ;
#15003=CARTESIAN_POINT ( 'NONE',  ( 8.222623404330700936, -15.61601543569009820, -34.79233150823699816 ) ) ;
#15009=ORIENTED_EDGE ( 'NONE', *, *, #34409, .T. ) ;
#15014=CYLINDRICAL_SURFACE ( 'NONE', #47398, 7.910999999999997812 ) ;
#15015=AXIS2_PLACEMENT_3D ( 'NONE', #11809, #11549, #46947 ) ;
#15019=AXIS2_PLACEMENT_3D ( 'NONE', #39464, #7998, #50991 ) ;
#15023=CARTESIAN_POINT ( 'NONE',  ( 17.41568895538090089, -23.76111577064400393, -36.24264715586419783 ) ) ;
#15026=CARTESIAN_POINT ( 'NONE',  ( 8.327182772215820705, -17.08089162929084637, -50.73335963105622426 ) ) ;
#15027=CARTESIAN_POINT ( 'NONE',  ( 10.02873241999632370, -18.59298069272300680, -51.30846019940189962 ) ) ;
#15035=CARTESIAN_POINT ( 'NONE',  ( 19.96701598536469646, -22.91620464669880164, -37.85376303658059527 ) ) ;
#15052=DIRECTION ( 'NONE',  ( 0.000000000000000000, 0.000000000000000000, -1.000000000000000000 ) ) ;
#15059=CARTESIAN_POINT ( 'NONE',  ( 20.82481716059549726, -9.828068231670309629, -68.78413393247190299 ) ) ;
#15066=CARTESIAN_POINT ( 'NONE',  ( 16.13393739769620083, -15.61618894467929941, -22.14999999999999858 ) ) ;
#15071=EDGE_CURVE ( 'NONE', #41372, #10507, #19468, .T. ) ;
#15075=CARTESIAN_POINT ( 'NONE',  ( 22.60922503113999937, -11.32550468333229965, -81.23899999999999011 ) ) ;
#15079=CARTESIAN_POINT ( 'NONE',  ( 16.58604368022989561, -8.818121607810667228, -79.97378616020819209 ) ) ;
#15086=CARTESIAN_POINT ( 'NONE',  ( 8.847469766316544693, -18.75936127001048348, -50.37806134412886649 ) ) ;
#15091=EDGE_CURVE ( 'NONE', #27518, #51178, #38219, .T. ) ;
#15097=( BOUNDED_CURVE ( )  B_SPLINE_CURVE ( 2, ( #12978, #28148, #44152 ),
 .UNSPECIFIED., .F., .T. ) 
 B_SPLINE_CURVE_WITH_KNOTS ( ( 3, 3 ),
 ( 1.104980434577240045, 2.168627590050199672 ),
 .UNSPECIFIED. ) 
 CURVE ( )  GEOMETRIC_REPRESENTATION_ITEM ( )  RATIONAL_B_SPLINE_CURVE ( ( 1.323085463760209857, 1.425426480542939967, 1.425426480542939967 ) ) 
 REPRESENTATION_ITEM ( '' )  );
#15100=CARTESIAN_POINT ( 'NONE',  ( 23.97941690387960278, -15.42857364349520033, -57.27989503770719892 ) ) ;
#15102=DIRECTION ( 'NONE',  ( 1.000000000000000000, 2.460964292799963328E-14, 0.000000000000000000 ) ) ;
#15109=DIRECTION ( 'NONE',  ( 0.000000000000000000, 0.000000000000000000, -1.000000000000000000 ) ) ;
#15115=CARTESIAN_POINT ( 'NONE',  ( 17.16944539447341711, -7.705183308742559412, -71.33398442287155206 ) ) ;
#15119=CARTESIAN_POINT ( 'NONE',  ( 8.909593156947090975, -13.79532524041309927, -36.14593433426069424 ) ) ;
#15123=CARTESIAN_POINT ( 'NONE',  ( 12.14989623194125201, -22.52876317393949890, -58.17433482716594995 ) ) ;
#15130=CARTESIAN_POINT ( 'NONE',  ( 20.11810741955662607, -22.52868898135160336, -41.84100097860003586 ) ) ;
#15137=DIRECTION ( 'NONE',  ( 1.000000000000000000, 0.000000000000000000, 0.000000000000000000 ) ) ;
#15145=CARTESIAN_POINT ( 'NONE',  ( 22.88146960594603385, -14.93411597101013299, -50.42079114153778363 ) ) ;
#15146=CARTESIAN_POINT ( 'NONE',  ( 9.543100655325421400, -13.84480880723966756, -35.53615332108730485 ) ) ;
#15153=CARTESIAN_POINT ( 'NONE',  ( 10.72266837725936384, -11.45745312862252518, -51.66115301124705184 ) ) ;
#15155=CARTESIAN_POINT ( 'NONE',  ( 8.397759403314990934, -16.93463410123079882, -42.95876240573199567 ) ) ;
#15165=CARTESIAN_POINT ( 'NONE',  ( 12.30558705848279999, -9.692820574005770240, -44.16454026222620399 ) ) ;
#15173=CARTESIAN_POINT ( 'NONE',  ( 24.04493737487536009, -14.58064688416050281, -47.46600315403375703 ) ) ;
#15178=CARTESIAN_POINT ( 'NONE',  ( 8.223295469878840080, -15.61636541503349918, -58.79233150823709764 ) ) ;
#15185=CARTESIAN_POINT ( 'NONE',  ( 17.90525307069644612, -9.025334985065097015, -42.03615321375040992 ) ) ;
#15188=CARTESIAN_POINT ( 'NONE',  ( 14.02133164252290065, -8.887187858349010483, -53.85598711143169481 ) ) ;
#15194=CARTESIAN_POINT ( 'NONE',  ( 8.350530164053800775, -16.61895995459930120, -32.24671282160349506 ) ) ;
#15196=EDGE_CURVE ( 'NONE', #33336, #30137, #21306, .T. ) ;
#15201=CARTESIAN_POINT ( 'NONE',  ( 22.46007751831445276, -20.47790136755202184, -40.00067590845137033 ) ) ;
#15204=LINE ( 'NONE', #35634, #43407 ) ;
#15209=VERTEX_POINT ( 'NONE', #15003 ) ;
#15214=CARTESIAN_POINT ( 'NONE',  ( 23.54919931531921762, -18.42977095681591138, -43.90770150007058703 ) ) ;
#15216=CARTESIAN_POINT ( 'NONE',  ( 22.09114981806095557, -10.39072778660224472, -49.27845259825229363 ) ) ;
#15218=SURFACE_SIDE_STYLE ('',( #23562 ) ) ;
#15222=CARTESIAN_POINT ( 'NONE',  ( 23.04645602048810460, -11.63204889956642596, -69.62566745447085736 ) ) ;
#15223=CARTESIAN_POINT ( 'NONE',  ( 7.927515648975639984, -16.41453857865010235, -64.76146233876730207 ) ) ;
#15231=CARTESIAN_POINT ( 'NONE',  ( 10.77928268962459946, -10.43599910622039850, -53.47738634665349622 ) ) ;
#15233=CARTESIAN_POINT ( 'NONE',  ( 11.14075301740580137, -21.57559600035230218, -32.14999999999999858 ) ) ;
#15237=VECTOR ( 'NONE', #29463, 1000.000000000000000 ) ;
#15241=CARTESIAN_POINT ( 'NONE',  ( 8.261206528015369699, -18.06625616060409811, -62.41163166630260406 ) ) ;
#15245=CARTESIAN_POINT ( 'NONE',  ( 15.24805746485052715, -8.849198816118178712, -59.91112637248544104 ) ) ;
#15254=CARTESIAN_POINT ( 'NONE',  ( 9.117428229974370524, -13.11113547131370005, -75.34181132021248573 ) ) ;
#15257=CARTESIAN_POINT ( 'NONE',  ( 23.83903667619928868, -17.68686933249846405, -69.87566771576088342 ) ) ;
#15261=CARTESIAN_POINT ( 'NONE',  ( 17.14078862016341276, -23.46602985074793679, -61.96707586313608118 ) ) ;
#15272=ORIENTED_EDGE ( 'NONE', *, *, #16144, .F. ) ;
#15276=VERTEX_POINT ( 'NONE', #47445 ) ;
#15278=CARTESIAN_POINT ( 'NONE',  ( 16.13128530227220025, -23.52718894015337980, -78.00777821068726325 ) ) ;
#15293=CARTESIAN_POINT ( 'NONE',  ( 8.586485337726889711, -17.76623897297480070, -78.92415710861520495 ) ) ;
#15294=CARTESIAN_POINT ( 'NONE',  ( 12.72596619939935003, -21.52911186578291236, -37.11948596911255294 ) ) ;
#15300=CARTESIAN_POINT ( 'NONE',  ( 12.59304842796170121, -22.61967803536170152, -79.93650932190239189 ) ) ;
#15311=CARTESIAN_POINT ( 'NONE',  ( 9.366980835600751121, -15.61636285886159925, -47.84717978380999881 ) ) ;
#15323=CARTESIAN_POINT ( 'NONE',  ( 15.01392763274439979, -22.98180313935129959, -65.61537668992708916 ) ) ;
#15324=CARTESIAN_POINT ( 'NONE',  ( 17.16952488601623728, -7.705194658554545661, -77.33399647545617484 ) ) ;
#15328=CARTESIAN_POINT ( 'NONE',  ( 18.88229416847884679, -21.86306642924426313, -34.82060356745882501 ) ) ;
#15330=CARTESIAN_POINT ( 'NONE',  ( 10.22109171085586965, -12.20808510601136909, -73.61948688482468128 ) ) ;
#15331=CARTESIAN_POINT ( 'NONE',  ( 10.69159450438010062, -10.36448435242919963, -81.23899999999999011 ) ) ;
#15340=CARTESIAN_POINT ( 'NONE',  ( 23.28014774377560059, -12.88775224658349927, -81.23899999999999011 ) ) ;
#15343=ORIENTED_EDGE ( 'NONE', *, *, #24047, .F. ) ;
#15344=CARTESIAN_POINT ( 'NONE',  ( 22.46010023493453645, -10.75450771427420449, -53.29933757767130231 ) ) ;
#15346=CARTESIAN_POINT ( 'NONE',  ( 24.04493737255387487, -14.58064479785229217, -63.75066696746915795 ) ) ;
#15359=EDGE_CURVE ( 'NONE', #44438, #5111, #50098, .T. ) ;
#15360=CARTESIAN_POINT ( 'NONE',  ( 18.44579043026860177, -8.116716713984079234, -48.88268834496359716 ) ) ;
#15371=CARTESIAN_POINT ( 'NONE',  ( 9.647229718197021242, -18.13221079759153298, -45.72885989622667324 ) ) ;
#15379=CARTESIAN_POINT ( 'NONE',  ( 16.02785660032570192, -23.06571518483509919, -37.57187509340590026 ) ) ;
#15393=ORIENTED_EDGE ( 'NONE', *, *, #49637, .T. ) ;
#15394=CARTESIAN_POINT ( 'NONE',  ( 21.69971205180370077, -19.94801438831689921, -59.05769930218669828 ) ) ;
#15395=CARTESIAN_POINT ( 'NONE',  ( 17.16943041195074926, -7.705181169127810037, -39.33399222304974074 ) ) ;
#15401=CARTESIAN_POINT ( 'NONE',  ( 22.90571047178253394, -13.64498330036649421, -32.75701418906501772 ) ) ;
#15416=CARTESIAN_POINT ( 'NONE',  ( 8.372471907742799146, -14.45584372025490083, -57.05973213505629360 ) ) ;
#15425=AXIS2_PLACEMENT_3D ( 'NONE', #8080, #43976, #19609 ) ;
#15426=CARTESIAN_POINT ( 'NONE',  ( 22.24871428180119892, -12.10163878398070025, -56.68113137027810211 ) ) ;
#15427=CARTESIAN_POINT ( 'NONE',  ( 14.36260794969588162, -9.025336946788870662, -43.86945627782853308 ) ) ;
#15432=CARTESIAN_POINT ( 'NONE',  ( 22.46012145614304245, -10.75453683683663719, -51.29933284102181545 ) ) ;
#15434=CARTESIAN_POINT ( 'NONE',  ( 20.11810581040045776, -8.703687945963876516, -47.17433608290784974 ) ) ;
#15437=AXIS2_PLACEMENT_3D ( 'NONE', #7685, #23630, #48804 ) ;
#15439=LINE ( 'NONE', #11512, #23926 ) ;
#15450=CARTESIAN_POINT ( 'NONE',  ( 11.39331812359460194, -10.39420775028169963, -59.71818801013959899 ) ) ;
#15456=AXIS2_PLACEMENT_3D ( 'NONE', #20043, #7499, #26883 ) ;
#15457=CARTESIAN_POINT ( 'NONE',  ( 8.346677780718652073, -14.64390511730509914, -40.32704379009269502 ) ) ;
#15471=CARTESIAN_POINT ( 'NONE',  ( 14.35970537249007428, -23.39490274268978709, -44.36388938044733266 ) ) ;
#15474=VERTEX_POINT ( 'NONE', #48993 ) ;
#15475=CARTESIAN_POINT ( 'NONE',  ( 24.04501723819814529, -15.61618889329698412, -35.50767088183642528 ) ) ;
#15479=CARTESIAN_POINT ( 'NONE',  ( 21.47519512629029848, -21.89740585963049568, -62.06801868260419752 ) ) ;
#15487=CARTESIAN_POINT ( 'NONE',  ( 9.133675843628138225, -18.16629325230719871, -57.12145717557989855 ) ) ;
#15496=CIRCLE ( 'NONE', #15611, 7.910999999999997812 ) ;
#15497=CARTESIAN_POINT ( 'NONE',  ( 8.010480352932539461, -17.02763017648989674, -74.45290918797269342 ) ) ;
#15509=CARTESIAN_POINT ( 'NONE',  ( 9.978830895481387131, -20.62644581997769322, -66.57488575740745773 ) ) ;
#15511=CARTESIAN_POINT ( 'NONE',  ( 22.68119848469680377, -12.06090188681830000, -74.07430842319459430 ) ) ;
#15514=CARTESIAN_POINT ( 'NONE',  ( 17.16952425154805084, -23.52718332138170254, -70.25066653995565957 ) ) ;
#15518=CARTESIAN_POINT ( 'NONE',  ( 21.73319121277129540, -21.20477496534300244, -61.75735875115385909 ) ) ;
#15530=DIRECTION ( 'NONE',  ( 0.000000000000000000, 0.000000000000000000, -1.000000000000000000 ) ) ;
#15537=ORIENTED_EDGE ( 'NONE', *, *, #41065, .T. ) ;
#15538=CARTESIAN_POINT ( 'NONE',  ( 22.17097752751971029, -18.77408084603302996, -80.60639082325192817 ) ) ;
#15542=CARTESIAN_POINT ( 'NONE',  ( 23.66514557999009938, -18.97232114870620023, -35.92577143160979602 ) ) ;
#15543=FACE_OUTER_BOUND ( 'NONE', #14435, .T. ) ;
#15547=CARTESIAN_POINT ( 'NONE',  ( 9.366946845712353920, -14.73032155540524535, -63.49448697528727337 ) ) ;
#15549=CARTESIAN_POINT ( 'NONE',  ( 22.51775971307619884, -20.18056844656550197, -70.21007469161699532 ) ) ;
#15561=CARTESIAN_POINT ( 'NONE',  ( 11.65838256785770000, -8.691441319380301067, -44.82502897017919707 ) ) ;
#15570=CARTESIAN_POINT ( 'NONE',  ( 9.543106074036904474, -17.38758878367239546, -49.36948704940078869 ) ) ;
#15577=VECTOR ( 'NONE', #49166, 1000.000000000000000 ) ;
#15583=CARTESIAN_POINT ( 'NONE',  ( 21.05717860469869862, -21.20800352994709925, -61.33755441249169849 ) ) ;
#15584=CARTESIAN_POINT ( 'NONE',  ( 23.83903669993742369, -13.54550867393122360, -77.70899529891561031 ) ) ;
#15588=CARTESIAN_POINT ( 'NONE',  ( 10.86459002806530272, -19.89652023075066722, -35.23569143810544091 ) ) ;
#15590=CYLINDRICAL_SURFACE ( 'NONE', #34032, 6.766999999999998572 ) ;
#15591=VECTOR ( 'NONE', #23015, 1000.000000000000000 ) ;
#15592=CARTESIAN_POINT ( 'NONE',  ( 11.09570125422289877, -9.916272040889650086, -81.23899999999999011 ) ) ;
#15599=CARTESIAN_POINT ( 'NONE',  ( 23.55432945165479808, -14.23915780199780023, -81.23899999999999011 ) ) ;
#15603=CARTESIAN_POINT ( 'NONE',  ( 22.52288591994712164, -13.38583005777697466, -80.34591106198659816 ) ) ;
#15605=CARTESIAN_POINT ( 'NONE',  ( 12.14985691594747941, -8.703636955929068719, -63.12566558101337222 ) ) ;
#15611=AXIS2_PLACEMENT_3D ( 'NONE', #29215, #49423, #22124 ) ;
#15612=CARTESIAN_POINT ( 'NONE',  ( 13.16593781093261128, -9.467269466126328581, -39.80947853294870242 ) ) ;
#15613=DIRECTION ( 'NONE',  ( -1.000000000000000000, 9.391392475159538137E-33, -1.071169953407190059E-15 ) ) ;
#15619=CARTESIAN_POINT ( 'NONE',  ( 9.787898087487839405, -10.99942240775409985, -56.48770572707109494 ) ) ;
#15620=EDGE_LOOP ( 'NONE', ( #3998, #10198, #14051, #39964 ) ) ;
#15635=CARTESIAN_POINT ( 'NONE',  ( 11.69292874863820053, -9.634204615267030647, -38.36406440404199714 ) ) ;
#15636=CARTESIAN_POINT ( 'NONE',  ( 14.36264681009404498, -22.20705100211725735, -77.03616734294827495 ) ) ;
#15643=CARTESIAN_POINT ( 'NONE',  ( 17.81845769390660195, -8.767470046512547910, -58.42394785367769572 ) ) ;
#15645=CARTESIAN_POINT ( 'NONE',  ( 18.20469318812960324, -7.911110394061046769, -67.09100018836774382 ) ) ;
#15652=DIRECTION ( 'NONE',  ( 0.000000000000000000, 0.000000000000000000, -1.000000000000000000 ) ) ;
#15661=CARTESIAN_POINT ( 'NONE',  ( 22.85093860592767712, -14.77854013293515756, -46.41334110918311495 ) ) ;
#15670=CARTESIAN_POINT ( 'NONE',  ( 8.313598522135590585, -14.96117179759260019, -51.03909337422119563 ) ) ;
#15674=CARTESIAN_POINT ( 'NONE',  ( 22.90024361696743327, -15.00864283141770628, -64.81860591268294058 ) ) ;
#15678=CARTESIAN_POINT ( 'NONE',  ( 19.36900924991789807, -21.88331502330690270, -53.19549840347880121 ) ) ;
#15685=FACE_OUTER_BOUND ( 'NONE', #25251, .T. ) ;
#15687=CIRCLE ( 'NONE', #37457, 2.576499999999998902 ) ;
#15691=CARTESIAN_POINT ( 'NONE',  ( 23.04647541986281567, -19.60029266307493501, -57.95899793902382413 ) ) ;
#15692=DIRECTION ( 'NONE',  ( 0.000000000000000000, 0.000000000000000000, -1.000000000000000000 ) ) ;
#15698=CARTESIAN_POINT ( 'NONE',  ( 19.54197266774264818, -21.52907415010898973, -74.78615355739535175 ) ) ;
#15701=CARTESIAN_POINT ( 'NONE',  ( 9.173233944167900944, -16.75248385739550017, -59.40131228588499823 ) ) ;
#15705=ORIENTED_EDGE ( 'NONE', *, *, #46958, .T. ) ;
#15706=CARTESIAN_POINT ( 'NONE',  ( 8.426038367632161297, -14.14138701712409940, -46.34768255092779299 ) ) ;
#15714=CARTESIAN_POINT ( 'NONE',  ( 23.06214062797170072, -3.616188944679339823, -32.14999999999999858 ) ) ;
#15715=ORIENTED_EDGE ( 'NONE', *, *, #44786, .F. ) ;
#15718=EDGE_CURVE ( 'NONE', #3924, #9734, #5732, .T. ) ;
#15719=CYLINDRICAL_SURFACE ( 'NONE', #38636, 6.766999999999998572 ) ;
#15720=ORIENTED_EDGE ( 'NONE', *, *, #16495, .F. ) ;
#15731=CARTESIAN_POINT ( 'NONE',  ( 11.42407264781889964, -22.38375084641400292, -76.48586413618279778 ) ) ;
#15734=VECTOR ( 'NONE', #20769, 1000.000000000000000 ) ;
#15738=CARTESIAN_POINT ( 'NONE',  ( 12.66219100592389957, -9.024249109064799157, -67.57835607597777994 ) ) ;
#15747=CARTESIAN_POINT ( 'NONE',  ( 21.93114081399549775, -21.47922171441739891, -71.75946553180968124 ) ) ;
#15748=CARTESIAN_POINT ( 'NONE',  ( 19.73427364139330109, -22.64788242709790111, -32.14999999999999858 ) ) ;
#15760=CARTESIAN_POINT ( 'NONE',  ( 12.37461265888050654, -22.60375392215577151, -66.44936340057275004 ) ) ;
#15762=CARTESIAN_POINT ( 'NONE',  ( 9.476745794552989821, -12.27126835306809838, -71.38086476703149685 ) ) ;
#15766=DIRECTION ( 'NONE',  ( 0.000000000000000000, 0.000000000000000000, -1.000000000000000000 ) ) ;
#15770=CARTESIAN_POINT ( 'NONE',  ( 8.428830500064028897, -13.54553434705470139, -36.87566510236762696 ) ) ;
#15779=ORIENTED_EDGE ( 'NONE', *, *, #48943, .F. ) ;
#15780=CARTESIAN_POINT ( 'NONE',  ( 22.46008894638382003, -10.75449222223970658, -55.58399371059939398 ) ) ;
#15782=CARTESIAN_POINT ( 'NONE',  ( 10.72266589679370341, -19.77492157605291467, -59.24448682388644727 ) ) ;
#15789=CARTESIAN_POINT ( 'NONE',  ( 14.06333294549902924, -7.911069592903273495, -34.92433389901778895 ) ) ;
#15790=CARTESIAN_POINT ( 'NONE',  ( 11.77815578209330027, -8.615482796503201257, -45.11516743498959414 ) ) ;
#15792=CARTESIAN_POINT ( 'NONE',  ( 24.04493240159784406, -15.62537587214817059, -49.79270004542557615 ) ) ;
#15795=CARTESIAN_POINT ( 'NONE',  ( 11.65470348258009992, -9.172338300440578962, -71.31913972650768585 ) ) ;
#15800=EDGE_CURVE ( 'NONE', #31302, #637, #30682, .T. ) ;
#15802=B_SPLINE_CURVE_WITH_KNOTS ( 'NONE', 3,
 ( #13716, #42009, #49874, #29670, #10031, #13969, #28897, #9528, #40960, #25997, #21033, #49108, #45680, #25218, #13208, #24949, #25732, #41740, #36759, #9781, #871, #37034, #25475, #16865, #9271, #32812, #5845, #48838, #21289, #21549, #12941 ),
 .UNSPECIFIED., .F., .F.,
 ( 4, 2, 1, 1, 1, 2, 2, 2, 2, 2, 2, 2, 2, 2, 2, 2, 4 ),
 ( 0.4999999368682983003, 0.5009764994916026115, 0.5019530621149068672, 0.5039061873615149345, 0.5078124378547310691, 0.5156249388411637824, 0.5312499408140293200, 0.5624999447597606173, 0.6249999526512233228, 0.6874999605426860283, 0.7499999684341487338, 0.8124999763256113283, 0.8749999842170741449, 0.9062499881628056642, 0.9374999921085371835, 0.9687499960542684807, 1.000000000000000000 ),
 .UNSPECIFIED. ) ;
#15804=CARTESIAN_POINT ( 'NONE',  ( 23.04647657677116612, -11.63208738592670421, -57.62566460569046711 ) ) ;
#15805=CARTESIAN_POINT ( 'NONE',  ( 13.00458990189400055, -23.24441973297430053, -42.13158531401599305 ) ) ;
#15809=CARTESIAN_POINT ( 'NONE',  ( 22.32536594118367645, -20.56154573459575374, -39.72222021323458563 ) ) ;
#15810=CARTESIAN_POINT ( 'NONE',  ( 22.90034296864962471, -15.71306839012465772, -56.45738126217962360 ) ) ;
#15814=CARTESIAN_POINT ( 'NONE',  ( 11.27232597222496757, -21.94240453461146245, -38.50066575436082417 ) ) ;
#15820=CARTESIAN_POINT ( 'NONE',  ( 17.01981217550311598, -22.38317801499556481, -64.91115475112107447 ) ) ;
#15824=CARTESIAN_POINT ( 'NONE',  ( 10.72255721402834361, -19.77478218903828378, -63.24448401478402815 ) ) ;
#15827=CARTESIAN_POINT ( 'NONE',  ( 16.40674540481250077, -23.06147403858910039, -63.55568448227298717 ) ) ;
#15832=CARTESIAN_POINT ( 'NONE',  ( 9.366668810525878186, -15.61604052661200015, -35.45282021618999835 ) ) ;
#15837=CARTESIAN_POINT ( 'NONE',  ( 9.023362915854630018, -14.22815957666089837, -81.23899999999999011 ) ) ;
#15845=CARTESIAN_POINT ( 'NONE',  ( 21.39066400359539699, -9.703911137440838885, -81.23899999999999011 ) ) ;
#15851=CARTESIAN_POINT ( 'NONE',  ( 8.223360643215830379, -15.61635149015999957, -74.50766849176298479 ) ) ;
#15857=ORIENTED_EDGE ( 'NONE', *, *, #5319, .F. ) ;
#15859=CARTESIAN_POINT ( 'NONE',  ( 8.222546438703959737, -15.61603098320130201, -50.50766849176299900 ) ) ;
#15873=CARTESIAN_POINT ( 'NONE',  ( 10.66331371621759949, -21.24282423753659899, -62.03303090152439125 ) ) ;
#15881=DIRECTION ( 'NONE',  ( 1.000000000000000000, 0.000000000000000000, 0.000000000000000000 ) ) ;
#15883=CARTESIAN_POINT ( 'NONE',  ( 14.27580295341549999, -22.41985674678640095, -45.43204315924410253 ) ) ;
#15888=CARTESIAN_POINT ( 'NONE',  ( 11.27220924270882207, -9.290061667250862243, -71.08398583345959310 ) ) ;
#15889=ORIENTED_EDGE ( 'NONE', *, *, #7531, .F. ) ;
#15890=CARTESIAN_POINT ( 'NONE',  ( 14.83834572504270000, -8.683358393905999506, -80.28837282723659996 ) ) ;
#15891=CARTESIAN_POINT ( 'NONE',  ( 22.90093737956978970, -16.50199041861013782, -76.49448436988512867 ) ) ;
#15892=EDGE_LOOP ( 'NONE', ( #10576, #22919, #21047, #14902, #47991 ) ) ;
#15898=CARTESIAN_POINT ( 'NONE',  ( 24.04508668034977248, -15.61618904219531778, -35.79233368253564862 ) ) ;
#15900=CARTESIAN_POINT ( 'NONE',  ( 20.99565532440523441, -9.290055542993323812, -67.21599983764021147 ) ) ;
#15901=ORIENTED_EDGE ( 'NONE', *, *, #50427, .T. ) ;
#15918=CARTESIAN_POINT ( 'NONE',  ( 14.23915348030984873, -9.102733633742271735, -45.86270462862681541 ) ) ;
#15924=CARTESIAN_POINT ( 'NONE',  ( 11.66468727650932102, -10.49346430533042529, -33.72439379513514979 ) ) ;
#15926=CARTESIAN_POINT ( 'NONE',  ( 9.390298412734489730, -19.62992546220089807, -54.84160206527489123 ) ) ;
#15929=ADVANCED_FACE ( 'NONE', ( #30186 ), #23337, .T. ) ;
#15933=CARTESIAN_POINT ( 'NONE',  ( 22.72481220864853668, -17.38742840828553327, -38.53615641829414074 ) ) ;
#15934=CARTESIAN_POINT ( 'NONE',  ( 22.89967574327219779, -17.60800816681120295, -54.93831488687830245 ) ) ;
#15940=CARTESIAN_POINT ( 'NONE',  ( 10.72257637282393361, -11.45757118250618944, -37.66115420151670179 ) ) ;
#15942=AXIS2_PLACEMENT_3D ( 'NONE', #12258, #48679, #24272 ) ;
#15950=CARTESIAN_POINT ( 'NONE',  ( 18.29760214348302227, -7.981476198048588877, -65.09563924883536856 ) ) ;
#15952=CARTESIAN_POINT ( 'NONE',  ( 9.221482312219526634, -19.60043670736297372, -74.34100170688905962 ) ) ;
#15962=CARTESIAN_POINT ( 'NONE',  ( 11.81604877385439956, -21.19278257598529791, -51.16254345526859737 ) ) ;
#15967=CARTESIAN_POINT ( 'NONE',  ( 23.88558989793769882, -16.84037508194900212, -43.33736317051029374 ) ) ;
#15972=ADVANCED_FACE ( 'NONE', ( #31205 ), #46724, .T. ) ;
#15985=CARTESIAN_POINT ( 'NONE',  ( 9.560391798445262879, -11.12854194998381274, -48.69820437222687559 ) ) ;
#15986=VERTEX_POINT ( 'NONE', #26252 ) ;
#15990=CARTESIAN_POINT ( 'NONE',  ( 9.807871728238577447, -10.75438317229078322, -56.71600161805649520 ) ) ;
#15993=CARTESIAN_POINT ( 'NONE',  ( 9.021811926696198469, -11.44481131364510063, -76.96117772256459943 ) ) ;
#15997=CARTESIAN_POINT ( 'NONE',  ( 8.718662699962571594, -16.33757300486989905, -65.20178814406908430 ) ) ;
#15998=LINE ( 'NONE', #36159, #47329 ) ;
#15999=CARTESIAN_POINT ( 'NONE',  ( 10.02935865344080035, -20.22754759784489664, -32.14999999999999858 ) ) ;
#16004=CARTESIAN_POINT ( 'NONE',  ( 9.500562652744140024, -10.71914287566930035, -72.71009270457309981 ) ) ;
#16012=EDGE_CURVE ( 'NONE', #22570, #4148, #26318, .T. ) ;
#16016=AXIS2_PLACEMENT_3D ( 'NONE', #23683, #44653, #36521 ) ;
#16018=CARTESIAN_POINT ( 'NONE',  ( 12.91798985874082639, -22.86794439454725847, -66.42520807091403867 ) ) ;
#16020=VECTOR ( 'NONE', #43690, 1000.000000000000000 ) ;
#16021=CARTESIAN_POINT ( 'NONE',  ( 19.39019095385939906, -22.31719682283620187, -70.58867545639529339 ) ) ;
#16037=CARTESIAN_POINT ( 'NONE',  ( 22.34855670084171209, -12.85190603941985721, -66.31973049179434554 ) ) ;
#16038=ORIENTED_EDGE ( 'NONE', *, *, #34344, .T. ) ;
#16042=VERTEX_POINT ( 'NONE', #31974 ) ;
#16043=CARTESIAN_POINT ( 'NONE',  ( 17.16941547515002497, -7.705179032722160315, -59.04929731532414650 ) ) ;
#16044=CARTESIAN_POINT ( 'NONE',  ( 12.43552644545811425, -9.914939322250329923, -49.76975001323243930 ) ) ;
#16049=CARTESIAN_POINT ( 'NONE',  ( 24.21273651960749973, -13.96824331337349889, -39.72828012266349873 ) ) ;
#16050=CARTESIAN_POINT ( 'NONE',  ( 24.04507396969289346, -15.61618901627517531, -67.50767071486835391 ) ) ;
#16054=CARTESIAN_POINT ( 'NONE',  ( 15.09848046148962020, -23.52719988351775982, -42.33399791108317345 ) ) ;
#16055=CARTESIAN_POINT ( 'NONE',  ( 8.318016906984530223, -16.32137358708479979, -80.98384931626918615 ) ) ;
#16062=CARTESIAN_POINT ( 'NONE',  ( 8.035678613309558571, -14.06669697307060041, -46.56784545357859173 ) ) ;
#16067=CARTESIAN_POINT ( 'NONE',  ( 22.85082190356551735, -19.82021127139173799, -39.68565907844063645 ) ) ;
#16068=CARTESIAN_POINT ( 'NONE',  ( 9.221496127252056141, -19.60046032720535436, -64.62566521129184594 ) ) ;
#16071=VERTEX_POINT ( 'NONE', #20441 ) ;
#16074=CARTESIAN_POINT ( 'NONE',  ( 9.366959721612127865, -16.50215060180284254, -49.41115363279539707 ) ) ;
#16078=CARTESIAN_POINT ( 'NONE',  ( 14.06328960009770412, -7.911080816989770170, -61.20899688243854087 ) ) ;
#16081=CARTESIAN_POINT ( 'NONE',  ( 8.428794369977973489, -13.54566571443409906, -74.87568142060762000 ) ) ;
#16085=CARTESIAN_POINT ( 'NONE',  ( 17.16957569431084707, -7.705201912737116743, -73.04933477425599619 ) ) ;
#16087=EDGE_LOOP ( 'NONE', ( #1736, #36515, #7498, #44202 ) ) ;
#16091=CARTESIAN_POINT ( 'NONE',  ( 11.95635311929369848, -9.163797422253020741, -81.23899999999999011 ) ) ;
#16099=CARTESIAN_POINT ( 'NONE',  ( 21.83477058027380124, -10.19727932716529928, -81.23899999999999011 ) ) ;
#16105=CARTESIAN_POINT ( 'NONE',  ( 17.77056402554710246, -8.755867344676808273, -42.42172377882659617 ) ) ;
#16108=EDGE_LOOP ( 'NONE', ( #33752, #14930, #45562, #50 ) ) ;
#16119=CARTESIAN_POINT ( 'NONE',  ( 19.39616629670310033, -8.478639589776950203, -60.92396586663380020 ) ) ;
#16137=CARTESIAN_POINT ( 'NONE',  ( 9.810283122618720597, -11.67688811027330154, -34.24467998873389973 ) ) ;
#16144=EDGE_CURVE ( 'NONE', #35823, #27459, #21856, .T. ) ;
#16149=ORIENTED_EDGE ( 'NONE', *, *, #31890, .T. ) ;
#16155=CARTESIAN_POINT ( 'NONE',  ( 16.13393739769620083, -15.61618894467929941, -32.14999999999999858 ) ) ;
#16163=CARTESIAN_POINT ( 'NONE',  ( 11.27214541155795047, -21.94226801064548837, -56.21594714068361043 ) ) ;
#16172=CARTESIAN_POINT ( 'NONE',  ( 18.23096359433825242, -9.164089042641412775, -34.05282851151127232 ) ) ;
#16174=CARTESIAN_POINT ( 'NONE',  ( 15.83244136102879907, -23.45811777191660141, -54.52472634102049653 ) ) ;
#16181=LINE ( 'NONE', #40296, #42172 ) ;
#16182=CARTESIAN_POINT ( 'NONE',  ( 23.02971233589060063, -14.13603787934130018, -54.77987702475120102 ) ) ;
#16190=CARTESIAN_POINT ( 'NONE',  ( 22.46010233604985373, -10.75451059975396895, -37.29933751133587805 ) ) ;
#16192=EDGE_CURVE ( 'NONE', #5413, #8909, #21480, .T. ) ;
#16194=CARTESIAN_POINT ( 'NONE',  ( 23.87157417762563227, -13.91310202843878230, -55.43871031765390001 ) ) ;
#16195=AXIS2_PLACEMENT_3D ( 'NONE', #24410, #32272, #334 ) ;
#16196=CARTESIAN_POINT ( 'NONE',  ( 9.543025643916356771, -13.84508154717068962, -75.53614680028508133 ) ) ;
#16200=CARTESIAN_POINT ( 'NONE',  ( 15.09847792035051128, -23.52719957632157488, -74.04933483335966571 ) ) ;
#16211=CARTESIAN_POINT ( 'NONE',  ( 21.84466674371100225, -11.47733293930889964, -62.25319380417529658 ) ) ;
#16217=CARTESIAN_POINT ( 'NONE',  ( 9.244168744909480040, -11.85881804280390028, -44.44642820540079953 ) ) ;
#16218=B_SPLINE_CURVE_WITH_KNOTS ( 'NONE', 3,
 ( #42534, #27046, #50645, #47245, #3471, #43307, #10817, #22585, #47496, #19442, #19181, #14741, #30711, #35692, #35425, #15770, #11593, #46474 ),
 .UNSPECIFIED., .F., .F.,
 ( 4, 2, 2, 2, 2, 2, 2, 2, 4 ),
 ( 0.4999984352163039381, 0.5624986308142660985, 0.6249988264122281478, 0.6874990220101903082, 0.7499992176081524686, 0.8124994132061142960, 0.8749996088040762343, 0.9374998044020381727, 1.000000000000000000 ),
 .UNSPECIFIED. ) ;
#16242=CARTESIAN_POINT ( 'NONE',  ( 14.23060326220489991, -23.63865983740360122, -72.36647972087459380 ) ) ;
#16247=CARTESIAN_POINT ( 'NONE',  ( 17.66480776815700082, -22.90749402086359865, -62.66678235003330144 ) ) ;
#16255=B_SPLINE_CURVE_WITH_KNOTS ( 'NONE', 3,
 ( #4642, #12520, #48160, #29008, #8591, #49210, #37144, #8073, #24535, #20108, #36100, #8326, #5185, #20617, #44744, #17230, #16702, #20883 ),
 .UNSPECIFIED., .F., .F.,
 ( 4, 2, 2, 2, 2, 2, 2, 2, 4 ),
 ( 0.5000002878041880372, 0.5625002518286645881, 0.6250002158531410279, 0.6875001798776174677, 0.7500001439020940186, 0.8125001079265705695, 0.8750000719510470093, 0.9375000359755234491, 1.000000000000000000 ),
 .UNSPECIFIED. ) ;
#16257=CARTESIAN_POINT ( 'NONE',  ( 10.34509433763069985, -21.48747643008940145, -78.25541787902648139 ) ) ;
#16258=EDGE_CURVE ( 'NONE', #37842, #1665, #14355, .T. ) ;
#16259=B_SPLINE_CURVE_WITH_KNOTS ( 'NONE', 3,
 ( #30133, #18093, #50335, #34061, #14423, #31670, #7090, #46673, #19890, #18862 ),
 .UNSPECIFIED., .F., .F.,
 ( 4, 1, 1, 1, 1, 1, 1, 4 ),
 ( 0.5000036202821666054, 0.5662063123692606670, 0.6454252434329685872, 0.7246441744965181897, 0.8038631055600700126, 0.8830820366237779329, 0.9623009676873275353, 1.000000000000000000 ),
 .UNSPECIFIED. ) ;
#16260=DIRECTION ( 'NONE',  ( 0.000000000000000000, 0.000000000000000000, -1.000000000000000000 ) ) ;
#16265=CARTESIAN_POINT ( 'NONE',  ( 11.27231895528897887, -9.289978665370313138, -78.79933570999904191 ) ) ;
#16267=ORIENTED_EDGE ( 'NONE', *, *, #39349, .T. ) ;
#16273=CARTESIAN_POINT ( 'NONE',  ( 23.06556184739849868, -18.34735651441920012, -78.35213070062998497 ) ) ;
#16282=CARTESIAN_POINT ( 'NONE',  ( 22.90093739391126348, -16.50198413763800431, -70.49448988769137259 ) ) ;
#16287=CARTESIAN_POINT ( 'NONE',  ( 24.04493430405305787, -15.62427045307345530, -71.50799773700714468 ) ) ;
#16291=CIRCLE ( 'NONE', #37249, 2.576499999999998902 ) ;
#16295=CARTESIAN_POINT ( 'NONE',  ( 12.14971906056685924, -8.703714936188482909, -58.84096898769573869 ) ) ;
#16296=CARTESIAN_POINT ( 'NONE',  ( 11.00289117509757553, -11.15506890091918457, -49.68074223147661428 ) ) ;
#16300=CARTESIAN_POINT ( 'NONE',  ( 19.17739448125563584, -22.99139521707102318, -65.88280214780220945 ) ) ;
#16301=EDGE_CURVE ( 'NONE', #41415, #3035, #23702, .T. ) ;
#16302=CARTESIAN_POINT ( 'NONE',  ( 23.84659521662570114, -18.53125831332900120, -45.90735674562579760 ) ) ;
#16304=CARTESIAN_POINT ( 'NONE',  ( 9.807787300107081663, -20.47788638414121820, -68.29933457388374052 ) ) ;
#16311=CARTESIAN_POINT ( 'NONE',  ( 19.48351169319580123, -22.27104024610400046, -38.58422730669299483 ) ) ;
#16314=CARTESIAN_POINT ( 'NONE',  ( 16.78922646229311511, -23.56772248962323246, -60.26586126249986819 ) ) ;
#16317=CARTESIAN_POINT ( 'NONE',  ( 24.04527307164895333, -15.61618901697373119, -57.79233174308600951 ) ) ;
#16318=CARTESIAN_POINT ( 'NONE',  ( 8.895242482623048730, -11.66852930440259861, -44.66659110805180433 ) ) ;
#16319=EDGE_CURVE ( 'NONE', #38732, #20276, #28725, .T. ) ;
#16325=CARTESIAN_POINT ( 'NONE',  ( 20.99566134352006586, -21.94231754292628267, -64.08399974622017226 ) ) ;
#16326=CARTESIAN_POINT ( 'NONE',  ( 21.54526434311726746, -19.77485224925768037, -56.66111849060637695 ) ) ;
#16328=ORIENTED_EDGE ( 'NONE', *, *, #11092, .T. ) ;
#16331=CARTESIAN_POINT ( 'NONE',  ( 12.72604749850384032, -21.52915785728961851, -49.11948754903311709 ) ) ;
#16341=CARTESIAN_POINT ( 'NONE',  ( 23.04647718490594599, -11.63208852034076202, -73.34100123405998772 ) ) ;
#16346=CARTESIAN_POINT ( 'NONE',  ( 22.86366527778791280, -16.34140995983870681, -34.48697822539197944 ) ) ;
#16347=CARTESIAN_POINT ( 'NONE',  ( 9.254905727752488431, -13.06732500719120083, -81.23899999999999011 ) ) ;
#16355=CARTESIAN_POINT ( 'NONE',  ( 11.27232706326269884, -9.289972531400195521, -62.79933563852407730 ) ) ;
#16357=B_SPLINE_CURVE_WITH_KNOTS ( 'NONE', 3,
 ( #35333, #51585, #3636, #34552, #31128, #42702, #10470, #6799, #22751, #51332, #14906, #2863, #14648, #15432, #31383, #43465, #22493, #18828 ),
 .UNSPECIFIED., .F., .F.,
 ( 4, 2, 2, 2, 2, 2, 2, 2, 4 ),
 ( 0.000000000000000000, 0.06249981704674846539, 0.1249996340934969308, 0.1874994511402454100, 0.2499992681869938616, 0.3124990852337423131, 0.3749989022804908201, 0.4374987193272392716, 0.4999985363739877231 ),
 .UNSPECIFIED. ) ;
#16361=CARTESIAN_POINT ( 'NONE',  ( 22.90100569266936148, -15.61618883250986300, -34.84718217067427304 ) ) ;
#16378=CARTESIAN_POINT ( 'NONE',  ( 14.95417985139190087, -23.37472748715750015, -65.83553959257810106 ) ) ;
#16385=EDGE_CURVE ( 'NONE', #50858, #2213, #34044, .T. ) ;
#16395=CARTESIAN_POINT ( 'NONE',  ( 8.222957392148765976, -16.65188279910073987, -38.46600194893341040 ) ) ;
#16396=DIRECTION ( 'NONE',  ( 1.000000000000000000, 0.000000000000000000, 0.000000000000000000 ) ) ;
#16398=CARTESIAN_POINT ( 'NONE',  ( 19.16281492688910149, -22.42299401398249969, -43.43407599211369075 ) ) ;
#16403=CARTESIAN_POINT ( 'NONE',  ( 10.40721626785641440, -10.10600253351913480, -81.03610924078645894 ) ) ;
#16418=CARTESIAN_POINT ( 'NONE',  ( 22.90122453025153249, -15.61618899996915211, -58.45282045073077626 ) ) ;
#16426=EDGE_CURVE ( 'NONE', #16669, #49951, #12500, .T. ) ;
#16427=CARTESIAN_POINT ( 'NONE',  ( 22.72481302096315403, -13.84495347910004881, -36.36948437006035562 ) ) ;
#16428=CARTESIAN_POINT ( 'NONE',  ( 23.79191524431698213, -13.56499663094212949, -59.70900831695890787 ) ) ;
#16434=CARTESIAN_POINT ( 'NONE',  ( 11.27233804322889199, -21.94241366705713148, -54.21600271639588442 ) ) ;
#16436=CARTESIAN_POINT ( 'NONE',  ( 16.18108977866110010, -7.768608155381779845, -51.51440696060279834 ) ) ;
#16437=AXIS2_PLACEMENT_3D ( 'NONE', #51729, #24169, #36502 ) ;
#16443=CARTESIAN_POINT ( 'NONE',  ( 15.12242003932709977, -22.59611672426049722, -49.39298971242499192 ) ) ;
#16450=CARTESIAN_POINT ( 'NONE',  ( 9.366933260303092368, -14.73042100787367481, -37.49448701325534472 ) ) ;
#16452=DIRECTION ( 'NONE',  ( 0.000000000000000000, 0.000000000000000000, -1.000000000000000000 ) ) ;
#16456=CARTESIAN_POINT ( 'NONE',  ( 17.16955932200438184, -23.52717831220308753, -73.96600144092269602 ) ) ;
#16467=CARTESIAN_POINT ( 'NONE',  ( 17.13287240097439934, -22.59792852417169939, -68.90758401351929763 ) ) ;
#16481=CARTESIAN_POINT ( 'NONE',  ( 20.11802023908898818, -8.703636772384703235, -75.17430357709265820 ) ) ;
#16485=CARTESIAN_POINT ( 'NONE',  ( 8.428833774104951715, -17.68685544396012688, -60.42434371803280158 ) ) ;
#16489=CARTESIAN_POINT ( 'NONE',  ( 18.20462312208350397, -23.32128729342234763, -43.92436229106515810 ) ) ;
#16495=EDGE_CURVE ( 'NONE', #29027, #31864, #7647, .T. ) ;
#16496=CARTESIAN_POINT ( 'NONE',  ( 10.24818704271000058, -9.842051535964911224, -69.03928461620270696 ) ) ;
#16501=CARTESIAN_POINT ( 'NONE',  ( 21.24562006453919949, -10.19609723709329963, -59.97333869387029637 ) ) ;
#16511=CARTESIAN_POINT ( 'NONE',  ( 10.73767760254780157, -21.85021661002049953, -72.23477911819139763 ) ) ;
#16512=DIRECTION ( 'NONE',  ( 0.000000000000000000, 0.000000000000000000, -1.000000000000000000 ) ) ;
#16517=CARTESIAN_POINT ( 'NONE',  ( 20.11809781826896781, -8.703683167413712951, -79.17433641915961573 ) ) ;
#16525=CARTESIAN_POINT ( 'NONE',  ( 9.788246253542011388, -12.53807871279539832, -39.59657951998019598 ) ) ;
#16531=ORIENTED_EDGE ( 'NONE', *, *, #8613, .F. ) ;
#16548=VERTEX_POINT ( 'NONE', #24301 ) ;
#16549=DIRECTION ( 'NONE',  ( 0.8889875008987390137, -0.4579314612972278375, 0.000000000000000000 ) ) ;
#16551=DIRECTION ( 'NONE',  ( 1.000000000000000000, 0.000000000000000000, 0.000000000000000000 ) ) ;
#16552=ORIENTED_EDGE ( 'NONE', *, *, #31136, .T. ) ;
#16554=CARTESIAN_POINT ( 'NONE',  ( 11.94575855162158895, -10.22828773375895750, -71.74277772556011712 ) ) ;
#16557=CARTESIAN_POINT ( 'NONE',  ( 24.36831978584559977, -16.03769427284349902, -47.80861109115269869 ) ) ;
#16558=CARTESIAN_POINT ( 'NONE',  ( 11.27227490617820749, -21.94236589989201747, -68.21600100673204281 ) ) ;
#16562=CARTESIAN_POINT ( 'NONE',  ( 8.222959289743867473, -16.65189668176488524, -42.75066481758663883 ) ) ;
#16563=CARTESIAN_POINT ( 'NONE',  ( 23.96502783409409787, -16.12685520490740387, -80.03322214350599495 ) ) ;
#16567=CARTESIAN_POINT ( 'NONE',  ( 22.94235624568159793, -19.78777630944221855, -59.96754204519741904 ) ) ;
#16570=CARTESIAN_POINT ( 'NONE',  ( 14.48159539877110014, -23.69409007229680242, -40.07189310636189816 ) ) ;
#16574=CARTESIAN_POINT ( 'NONE',  ( 23.57991226013853847, -18.40053178290571978, -39.62147127257066614 ) ) ;
#16575=CARTESIAN_POINT ( 'NONE',  ( 15.09849564581118209, -23.52720172089252060, -64.33399919163787217 ) ) ;
#16576=CARTESIAN_POINT ( 'NONE',  ( 22.90150103265647630, -15.56225260969818969, -56.84464468012870242 ) ) ;
#16582=CARTESIAN_POINT ( 'NONE',  ( 22.04686341290252471, -19.02415327330857764, -48.61948854829778810 ) ) ;
#16587=CARTESIAN_POINT ( 'NONE',  ( 20.99563245081073148, -9.290037288924558823, -61.50066264437961649 ) ) ;
#16590=CARTESIAN_POINT ( 'NONE',  ( 24.04468182044177738, -15.61618932230105017, -75.79232603942232060 ) ) ;
#16595=CARTESIAN_POINT ( 'NONE',  ( 9.366929594780975421, -16.50193003949960868, -61.41115669688573320 ) ) ;
#16601=CARTESIAN_POINT ( 'NONE',  ( 12.97929546375549847, -8.510229299769831002, -81.23899999999999011 ) ) ;
#16604=VERTEX_POINT ( 'NONE', #41603 ) ;
#16605=VERTEX_POINT ( 'NONE', #17000 ) ;
#16609=CARTESIAN_POINT ( 'NONE',  ( 21.50583062810030199, -20.19292315969019924, -81.23899999999999011 ) ) ;
#16612=ORIENTED_EDGE ( 'NONE', *, *, #14736, .T. ) ;
#16614=CARTESIAN_POINT ( 'NONE',  ( 9.396225823997797377, -16.96132441765022136, -69.78389659178685633 ) ) ;
#16624=ORIENTED_EDGE ( 'NONE', *, *, #16319, .F. ) ;
#16629=CARTESIAN_POINT ( 'NONE',  ( 19.34932770686961945, -3.616188944679342931, -22.15000000000000924 ) ) ;
#16634=CARTESIAN_POINT ( 'NONE',  ( 11.80820626746120006, -22.16407397513750155, -59.97333869387029637 ) ) ;
#16642=CARTESIAN_POINT ( 'NONE',  ( 14.06327089604441127, -23.32129222870931784, -36.37566369939185762 ) ) ;
#16650=CARTESIAN_POINT ( 'NONE',  ( 8.520859443580489412, -17.83227332291358280, -34.41746388773530185 ) ) ;
#16652=CARTESIAN_POINT ( 'NONE',  ( 9.221456941219052794, -19.60039333794279415, -54.62566536593503486 ) ) ;
#16655=CARTESIAN_POINT ( 'NONE',  ( 10.97781814925719956, -20.99402574345059946, -45.81064392402229402 ) ) ;
#16664=CARTESIAN_POINT ( 'NONE',  ( 9.965766340832269421, -12.19621453136610079, -60.00832647495010264 ) ) ;
#16669=VERTEX_POINT ( 'NONE', #45545 ) ;
#16678=EDGE_CURVE ( 'NONE', #34659, #586, #40571, .T. ) ;
#16684=CARTESIAN_POINT ( 'NONE',  ( 24.04215776945413907, -15.38968793046390182, -59.78321309548368134 ) ) ;
#16685=FACE_OUTER_BOUND ( 'NONE', #3282, .T. ) ;
#16694=CARTESIAN_POINT ( 'NONE',  ( 12.47698802750519853, -8.672597014313410568, -67.35819317332689593 ) ) ;
#16702=CARTESIAN_POINT ( 'NONE',  ( 8.222963058980525375, -14.58045360959418169, -40.83399815091998164 ) ) ;
#16706=CARTESIAN_POINT ( 'NONE',  ( 15.09839247718639932, -7.705188636603384822, -36.96600318730514090 ) ) ;
#16709=CARTESIAN_POINT ( 'NONE',  ( 22.19862325585670249, -12.11392824337299956, -32.14999999999999858 ) ) ;
#16712=CARTESIAN_POINT ( 'NONE',  ( 8.222937397696199469, -15.61618894467929941, -32.14999999999999858 ) ) ;
#16718=AXIS2_PLACEMENT_3D ( 'NONE', #18496, #6452, #42351 ) ;
#16721=CARTESIAN_POINT ( 'NONE',  ( 13.95270971513190084, -8.909117678376349048, -68.24709530556648929 ) ) ;
#16726=CARTESIAN_POINT ( 'NONE',  ( 16.13393739769620083, -15.61618894467929941, -28.45282021618999835 ) ) ;
#16730=CARTESIAN_POINT ( 'NONE',  ( 11.77719006542909952, -21.16247701684149973, -67.16476753011978928 ) ) ;
#16736=AXIS2_PLACEMENT_3D ( 'NONE', #24839, #36385, #1019 ) ;
#16737=EDGE_LOOP ( 'NONE', ( #14877, #35343, #43058, #37364 ) ) ;
#16742=CARTESIAN_POINT ( 'NONE',  ( 23.04647760069162032, -19.60028859616953412, -63.67433653012798089 ) ) ;
#16745=CARTESIAN_POINT ( 'NONE',  ( 14.06315725531258387, -7.911115082366269924, -74.92430270396020831 ) ) ;
#16752=VERTEX_POINT ( 'NONE', #8871 ) ;
#16753=CARTESIAN_POINT ( 'NONE',  ( 14.36278203781940555, -9.025291871498199114, -67.86948588150255546 ) ) ;
#16758=CARTESIAN_POINT ( 'NONE',  ( 20.10897586428119865, -22.38276145748530155, -32.34342564320699864 ) ) ;
#16765=CARTESIAN_POINT ( 'NONE',  ( 17.18916429022859660, -22.99136284164080024, -68.68742111086839941 ) ) ;
#16770=AXIS2_PLACEMENT_3D ( 'NONE', #26734, #10518, #22544 ) ;
#16775=CARTESIAN_POINT ( 'NONE',  ( 16.13393739769620083, -15.61618894467929941, -22.64999999999999858 ) ) ;
#16781=FACE_OUTER_BOUND ( 'NONE', #31710, .T. ) ;
#16793=CARTESIAN_POINT ( 'NONE',  ( 22.66051486065669707, -12.94292402765340100, -38.32907662296229745 ) ) ;
#16802=CARTESIAN_POINT ( 'NONE',  ( 8.732168080967809942, -16.46501479270679980, -64.03099806865479593 ) ) ;
#16813=CARTESIAN_POINT ( 'NONE',  ( 24.04424254486977475, -15.72944168295483536, -71.51222841874697167 ) ) ;
#16821=CARTESIAN_POINT ( 'NONE',  ( 10.45980683277509904, -11.42729869705060075, -72.04960399662019199 ) ) ;
#16822=CARTESIAN_POINT ( 'NONE',  ( 9.543049661443221865, -13.84499421749102943, -69.53615381081331748 ) ) ;
#16826=CARTESIAN_POINT ( 'NONE',  ( 9.366426063424411197, -15.61626247110940113, -71.45282021618990598 ) ) ;
#16827=CARTESIAN_POINT ( 'NONE',  ( 24.04491815576623637, -15.63504520850458590, -65.50842498917839407 ) ) ;
#16828=CARTESIAN_POINT ( 'NONE',  ( 8.063529214243020604, -13.92762985232080020, -46.85798391838919486 ) ) ;
#16829=CARTESIAN_POINT ( 'NONE',  ( 15.50293243011315525, -8.820692638884411352, -55.92317534179022687 ) ) ;
#16833=CARTESIAN_POINT ( 'NONE',  ( 17.29212060902849757, -22.97589718985749840, -36.68297296116619322 ) ) ;
#16835=CARTESIAN_POINT ( 'NONE',  ( 22.46008322700772908, -10.75448448616132957, -33.29933195708130000 ) ) ;
#16843=CARTESIAN_POINT ( 'NONE',  ( 8.644136429342630379, -19.06373911304890001, -50.37035414463240102 ) ) ;
#16850=CARTESIAN_POINT ( 'NONE',  ( 24.04460285965960864, -15.61618860597671876, -65.79233133698019742 ) ) ;
#16865=CARTESIAN_POINT ( 'NONE',  ( 11.62079934899224476, -20.68763287804364737, -67.18421635681791315 ) ) ;
#16868=CARTESIAN_POINT ( 'NONE',  ( 14.06329967161854633, -7.911078209043669318, -77.20899686763637249 ) ) ;
#16870=ORIENTED_EDGE ( 'NONE', *, *, #14441, .T. ) ;
#16874=EDGE_CURVE ( 'NONE', #36898, #10310, #45807, .T. ) ;
#16881=EDGE_LOOP ( 'NONE', ( #10110, #24212, #21757, #4912 ) ) ;
#16885=CARTESIAN_POINT ( 'NONE',  ( 22.89050912567230256, -18.23020240017759974, -81.23899999999999011 ) ) ;
#16891=AXIS2_PLACEMENT_3D ( 'NONE', #20504, #13204, #350 ) ;
#16905=CARTESIAN_POINT ( 'NONE',  ( 14.06328963345900895, -23.32129707982529254, -68.37566384021832278 ) ) ;
#16907=DIRECTION ( 'NONE',  ( 1.000000000000000000, 0.000000000000000000, 0.000000000000000000 ) ) ;
#16909=CARTESIAN_POINT ( 'NONE',  ( 23.64653095223680168, -17.88504025480479953, -71.38086476703149685 ) ) ;
#16910=EDGE_LOOP ( 'NONE', ( #48844, #8234, #40628, #17965 ) ) ;
#16911=CARTESIAN_POINT ( 'NONE',  ( 16.13393739769620083, -15.61618894467929941, -28.45282021618999835 ) ) ;
#16912=CARTESIAN_POINT ( 'NONE',  ( 22.90107427039792398, -15.30119754763367723, -76.83237175912924499 ) ) ;
#16918=VECTOR ( 'NONE', #3858, 1000.000000000000000 ) ;
#16921=CARTESIAN_POINT ( 'NONE',  ( 8.983363407049850480, -12.11911435556131522, -64.65261122085350110 ) ) ;
#16926=CARTESIAN_POINT ( 'NONE',  ( 23.94899987533918662, -16.86903691006758521, -33.55826008002186001 ) ) ;
#16930=CARTESIAN_POINT ( 'NONE',  ( 9.035825935529210540, -17.87970567954010193, -45.96908178614949492 ) ) ;
#16943=EDGE_LOOP ( 'NONE', ( #37206, #48014, #1463, #39306 ) ) ;
#16955=CARTESIAN_POINT ( 'NONE',  ( 23.21788048646474323, -12.02478094032549727, -77.35840597922448580 ) ) ;
#16960=CARTESIAN_POINT ( 'NONE',  ( 9.543053068164105923, -13.84498183095752744, -53.53615381170569520 ) ) ;
#16961=AXIS2_PLACEMENT_3D ( 'NONE', #39763, #35308, #39511 ) ;
#16966=CARTESIAN_POINT ( 'NONE',  ( 9.543042969328475067, -17.38735874139107196, -47.36946835774308084 ) ) ;
#16969=CARTESIAN_POINT ( 'NONE',  ( 22.24317136614079971, -20.54203992805110346, -60.22848937760110033 ) ) ;
#16985=CARTESIAN_POINT ( 'NONE',  ( 24.04492723490795569, -15.60308853973110743, -55.50714508028963934 ) ) ;
#16986=CARTESIAN_POINT ( 'NONE',  ( 22.58420829334310298, -19.63597092156729573, -32.14999999999999858 ) ) ;
#16996=CARTESIAN_POINT ( 'NONE',  ( 9.399672476051630809, -17.71195494773369816, -61.75114295834970335 ) ) ;
#17000=CARTESIAN_POINT ( 'NONE',  ( 9.367462981151710721, -15.61611677545310073, -63.45282021618999124 ) ) ;
#17004=CARTESIAN_POINT ( 'NONE',  ( 15.76846082554300033, -8.572824296172690595, -61.93631807992079530 ) ) ;
#17008=ORIENTED_EDGE ( 'NONE', *, *, #9836, .F. ) ;
#17009=ORIENTED_EDGE ( 'NONE', *, *, #7215, .F. ) ;
#17014=CARTESIAN_POINT ( 'NONE',  ( 9.366937397696199596, -15.61618894467949836, -28.45282021618999835 ) ) ;
#17022=ORIENTED_EDGE ( 'NONE', *, *, #24110, .F. ) ;
#17028=CARTESIAN_POINT ( 'NONE',  ( 16.39598596041420109, -23.45951012094470300, -32.50186350533419954 ) ) ;
#17033=ORIENTED_EDGE ( 'NONE', *, *, #18335, .T. ) ;
#17036=CARTESIAN_POINT ( 'NONE',  ( 23.02517239383359993, -17.11733762112250190, -32.91545205119220441 ) ) ;
#17048=DIRECTION ( 'NONE',  ( 0.000000000000000000, 0.000000000000000000, -1.000000000000000000 ) ) ;
#17058=CARTESIAN_POINT ( 'NONE',  ( 23.17990796417380395, -15.92769928319889772, -32.46687572425449275 ) ) ;
#17064=B_SPLINE_CURVE_WITH_KNOTS ( 'NONE', 3,
 ( #11672, #10899, #26865, #43130, #7224, #47831, #46812, #19004, #34981, #3288, #19261, #23429, #35250, #15344, #7480, #39454, #3552, #19522 ),
 .UNSPECIFIED., .F., .F.,
 ( 4, 2, 2, 2, 2, 2, 2, 2, 4 ),
 ( 0.000000000000000000, 0.06250019099276141188, 0.1250003819855228238, 0.1875005729782842356, 0.2500007639710456475, 0.3125009549638070316, 0.3750011459565684713, 0.4375013369493299109, 0.5000015279420912950 ),
 .UNSPECIFIED. ) ;
#17066=CARTESIAN_POINT ( 'NONE',  ( 23.58315219326460266, -15.49012044018099843, -73.06195620990739314 ) ) ;
#17070=CARTESIAN_POINT ( 'NONE',  ( 24.04460130197620416, -15.53725597405745518, -49.78915545177867585 ) ) ;
#17071=DIRECTION ( 'NONE',  ( 1.000000000000000000, 0.000000000000000000, 0.000000000000000000 ) ) ;
#17083=CYLINDRICAL_SURFACE ( 'NONE', #44449, 6.766999999999998572 ) ;
#17085=CARTESIAN_POINT ( 'NONE',  ( 9.366799914231096480, -15.30430012326571187, -71.86184190070434852 ) ) ;
#17089=ORIENTED_EDGE ( 'NONE', *, *, #33034, .T. ) ;
#17091=CARTESIAN_POINT ( 'NONE',  ( 9.366927855485558396, -14.73794263637672053, -71.49414492364064699 ) ) ;
#17092=CARTESIAN_POINT ( 'NONE',  ( 23.64088913729917962, -13.06713224951208829, -43.68817631689275771 ) ) ;
#17093=CARTESIAN_POINT ( 'NONE',  ( 9.048772758708359731, -19.83319761130199765, -54.62143916262379406 ) ) ;
#17098=VERTEX_POINT ( 'NONE', #51544 ) ;
#17100=CARTESIAN_POINT ( 'NONE',  ( 20.84347298952850025, -9.843237505908138729, -37.95047585818409885 ) ) ;
#17107=CARTESIAN_POINT ( 'NONE',  ( 12.59142764408279902, -8.170831642673661577, -56.86630649184929354 ) ) ;
#17112=CARTESIAN_POINT ( 'NONE',  ( 22.74102521302617319, -13.57078198115511825, -70.75098275705227024 ) ) ;
#17122=CARTESIAN_POINT ( 'NONE',  ( 9.366359996283680545, -15.61618532483699973, -43.84717978381009118 ) ) ;
#17124=LINE ( 'NONE', #49105, #15734 ) ;
#17129=CARTESIAN_POINT ( 'NONE',  ( 22.72480946629929832, -17.38744196642808149, -60.53615444368751497 ) ) ;
#17130=CARTESIAN_POINT ( 'NONE',  ( 9.367504675961500382, -15.61621390379479912, -67.84717978381009118 ) ) ;
#17146=CARTESIAN_POINT ( 'NONE',  ( 19.78634850713340043, -21.45480175648069832, -81.23899999999999011 ) ) ;
#17151=CARTESIAN_POINT ( 'NONE',  ( 20.51938203757293167, -21.13981406646989214, -35.13358212097380573 ) ) ;
#17154=EDGE_CURVE ( 'NONE', #50665, #4707, #27755, .T. ) ;
#17155=DIRECTION ( 'NONE',  ( 0.000000000000000000, 0.000000000000000000, -1.000000000000000000 ) ) ;
#17166=CARTESIAN_POINT ( 'NONE',  ( 23.83903636936457104, -17.68687080692383162, -67.87566263859582705 ) ) ;
#17167=B_SPLINE_CURVE_WITH_KNOTS ( 'NONE', 3,
 ( #8644, #7174, #19214, #31507, #35196, #47278, #27843, #36665, #4708, #40609, #31761, #15294, #51705, #43843, #20676, #23638, #31248, #39146 ),
 .UNSPECIFIED., .F., .F.,
 ( 4, 2, 2, 2, 2, 2, 2, 2, 4 ),
 ( 0.4999986293838318829, 0.5624988007108528976, 0.6249989720378739122, 0.6874991433648949268, 0.7499993146919159415, 0.8124994860189369561, 0.8749996573459579707, 0.9374998286729789854, 1.000000000000000000 ),
 .UNSPECIFIED. ) ;
#17168=CARTESIAN_POINT ( 'NONE',  ( 16.39219225208960040, -22.66429958545629830, -63.33552157962199658 ) ) ;
#17170=CARTESIAN_POINT ( 'NONE',  ( 23.09183490400689820, -19.24584601868189893, -73.44055697468560595 ) ) ;
#17179=CARTESIAN_POINT ( 'NONE',  ( 23.83903293615504637, -13.54548993678350222, -43.42431647374369419 ) ) ;
#17184=CARTESIAN_POINT ( 'NONE',  ( 8.222281512103441159, -15.61614627842319969, -76.50766849176299900 ) ) ;
#17186=CARTESIAN_POINT ( 'NONE',  ( 23.29546477256420189, -17.67026294465070180, -39.15625371467830007 ) ) ;
#17197=CYLINDRICAL_SURFACE ( 'NONE', #42030, 7.910999999999997812 ) ;
#17207=ORIENTED_EDGE ( 'NONE', *, *, #51867, .T. ) ;
#17218=CARTESIAN_POINT ( 'NONE',  ( 20.92206059044043442, -20.39804927675944413, -46.70260504768381793 ) ) ;
#17222=CARTESIAN_POINT ( 'NONE',  ( 22.48828768571790349, -11.01086810800570071, -61.81286799887340067 ) ) ;
#17230=CARTESIAN_POINT ( 'NONE',  ( 8.428887576146721017, -13.54532682478765615, -40.87566479360295801 ) ) ;
#17237=CARTESIAN_POINT ( 'NONE',  ( 16.13393739769620083, -15.61618894467929941, -32.14999999999999858 ) ) ;
#17238=CARTESIAN_POINT ( 'NONE',  ( 22.49678922309009721, -12.58636461612879920, -32.14999999999999858 ) ) ;
#17241=CARTESIAN_POINT ( 'NONE',  ( 22.90073451867936072, -15.61618922653637931, -60.45281425156898791 ) ) ;
#17246=CARTESIAN_POINT ( 'NONE',  ( 22.18801361179549758, -19.23429899943539922, -63.01864585536749530 ) ) ;
#17251=CARTESIAN_POINT ( 'NONE',  ( 8.222963976945624864, -14.58044688709260761, -40.54933510552366016 ) ) ;
#17255=CARTESIAN_POINT ( 'NONE',  ( 9.364619995196390434, -17.59581027231719830, -63.36225883906600131 ) ) ;
#17286=CARTESIAN_POINT ( 'NONE',  ( 23.93509063369040035, -16.46986088408009863, -38.04718867978759533 ) ) ;
#17294=CARTESIAN_POINT ( 'NONE',  ( 9.294981350531470454, -13.89246061358539919, -35.92577143160979602 ) ) ;
#17295=DIRECTION ( 'NONE',  ( -0.4999999999999998890, 0.8660254037844387076, 0.000000000000000000 ) ) ;
#17303=CARTESIAN_POINT ( 'NONE',  ( 22.26030898828220117, -21.13465079480659981, -81.74105084582579650 ) ) ;
#17306=CARTESIAN_POINT ( 'NONE',  ( 22.90093739769620029, -15.61618894467913243, -28.45282021618999835 ) ) ;
#17315=CARTESIAN_POINT ( 'NONE',  ( 21.39220184427749771, -20.31653082709010150, -34.68500579403580275 ) ) ;
#17320=LINE ( 'NONE', #38793, #7234 ) ;
#17324=CARTESIAN_POINT ( 'NONE',  ( 9.004889010588179588, -17.78029694363090130, -77.97352993585178638 ) ) ;
#17325=EDGE_CURVE ( 'NONE', #42078, #40450, #24905, .T. ) ;
#17328=CARTESIAN_POINT ( 'NONE',  ( 14.34562453388149805, -7.882998418872065649, -49.21996134945802481 ) ) ;
#17334=CARTESIAN_POINT ( 'NONE',  ( 8.222546438703959737, -15.61603098320130201, -50.50766849176299900 ) ) ;
#17342=CARTESIAN_POINT ( 'NONE',  ( 22.04684518689748529, -12.20819050132398154, -70.28615616242308306 ) ) ;
#17348=CARTESIAN_POINT ( 'NONE',  ( 12.76916528160270836, -22.79959822632163835, -66.14710272702825478 ) ) ;
#17350=CARTESIAN_POINT ( 'NONE',  ( 20.57352930747810049, -8.668330013286569269, -57.47332068091419188 ) ) ;
#17351=CARTESIAN_POINT ( 'NONE',  ( 10.29045043687441918, -12.08236487558636263, -55.62624849296779672 ) ) ;
#17354=ORIENTED_EDGE ( 'NONE', *, *, #22169, .T. ) ;
#17356=CARTESIAN_POINT ( 'NONE',  ( 20.10156355740380008, -9.310268198115061011, -41.91142241136510194 ) ) ;
#17357=CARTESIAN_POINT ( 'NONE',  ( 10.83099421739539991, -11.18954735718040006, -32.14999999999999858 ) ) ;
#17361=CARTESIAN_POINT ( 'NONE',  ( 16.57604039667560158, -7.382886712447779942, -57.02474435397640207 ) ) ;
#17362=ORIENTED_EDGE ( 'NONE', *, *, #28279, .T. ) ;
#17390=B_SPLINE_CURVE_WITH_KNOTS ( 'NONE', 3,
 ( #37380, #1483, #30275, #14049, #17467, #49705, #49452, #13546, #38157, #18230, #34195, #50214, #14306, #12406, #33343, #9524, #40956, #5073 ),
 .UNSPECIFIED., .F., .F.,
 ( 4, 2, 2, 2, 2, 2, 2, 2, 4 ),
 ( 0.4999987081369468012, 0.5624988696198284233, 0.6249990311027100454, 0.6874991925855915564, 0.7499993540684731785, 0.8124995155513548006, 0.8749996770342365338, 0.9374998385171182669, 1.000000000000000000 ),
 .UNSPECIFIED. ) ;
#17396=EDGE_LOOP ( 'NONE', ( #3165, #21300, #49134, #35753 ) ) ;
#17407=CARTESIAN_POINT ( 'NONE',  ( 24.04491986954906935, -15.63419043126502217, -33.79305392942131192 ) ) ;
#17409=CARTESIAN_POINT ( 'NONE',  ( 9.366602974803960535, -15.61605382581650048, -49.84717978381009118 ) ) ;
#17423=CARTESIAN_POINT ( 'NONE',  ( 8.698833068341928154, -13.10501953685350074, -74.39118414744899610 ) ) ;
#17427=CARTESIAN_POINT ( 'NONE',  ( 22.90076005816202809, -15.61619656631699193, -74.84717351858182610 ) ) ;
#17440=CARTESIAN_POINT ( 'NONE',  ( 8.738279572154599606, -16.51671082994739947, -48.02877399380358980 ) ) ;
#17446=FACE_OUTER_BOUND ( 'NONE', #30990, .T. ) ;
#17447=COLOUR_RGB ( '', 0.08235294, 0.09019608, 0.10196078) ;
#17450=CARTESIAN_POINT ( 'NONE',  ( 18.20469504372072223, -7.911110918348574828, -35.37566324252046002 ) ) ;
#17452=CARTESIAN_POINT ( 'NONE',  ( 22.79638959291578360, -13.83202789291152968, -60.76326040478846124 ) ) ;
#17454=VERTEX_POINT ( 'NONE', #47848 ) ;
#17460=CARTESIAN_POINT ( 'NONE',  ( 22.52295300047549276, -13.38580680388945332, -80.74026669357201058 ) ) ;
#17464=CARTESIAN_POINT ( 'NONE',  ( 10.72251481771434811, -19.77472772824552294, -73.24445191944960243 ) ) ;
#17465=CARTESIAN_POINT ( 'NONE',  ( 13.47700760496488925, -9.082944478799559462, -46.22423246988032020 ) ) ;
#17467=CARTESIAN_POINT ( 'NONE',  ( 21.54528854056280451, -19.77481887735858024, -52.66115150407350143 ) ) ;
#17470=VERTEX_POINT ( 'NONE', #36549 ) ;
#17473=CARTESIAN_POINT ( 'NONE',  ( 17.82378463084905462, -22.18374869735217558, -46.87269942184638438 ) ) ;
#17475=CARTESIAN_POINT ( 'NONE',  ( 8.908058192899041217, -12.55458522942449839, -65.14006310354548646 ) ) ;
#17482=EDGE_CURVE ( 'NONE', #27600, #39738, #24476, .T. ) ;
#17491=CARTESIAN_POINT ( 'NONE',  ( 23.24784027632620109, -14.48172169338479875, -32.14999999999999858 ) ) ;
#17495=CARTESIAN_POINT ( 'NONE',  ( 8.768740832044489508, -12.62132957242803322, -44.63073338636281306 ) ) ;
#17497=CARTESIAN_POINT ( 'NONE',  ( 8.223528471986069732, -15.61608932669300032, -46.79233150823699816 ) ) ;
#17499=EDGE_CURVE ( 'NONE', #11866, #37399, #4329, .T. ) ;
#17500=CARTESIAN_POINT ( 'NONE',  ( 9.216187797245829927, -14.24239869871029995, -61.90958082047689004 ) ) ;
#17507=CARTESIAN_POINT ( 'NONE',  ( 21.00866568523840172, -10.51917189357370042, -76.19572567137240071 ) ) ;
#17517=AXIS2_PLACEMENT_3D ( 'NONE', #2909, #39836, #39323 ) ;
#17531=ORIENTED_EDGE ( 'NONE', *, *, #16678, .T. ) ;
#17532=CARTESIAN_POINT ( 'NONE',  ( 9.366764248923921343, -15.61602670952840199, -67.45282021618999124 ) ) ;
#17535=CARTESIAN_POINT ( 'NONE',  ( 22.90093739769620029, -15.61618894467913243, -28.45282021618999835 ) ) ;
#17537=CARTESIAN_POINT ( 'NONE',  ( 11.16127494616910099, -9.544997455588569935, -33.29405281597039590 ) ) ;
#17545=CARTESIAN_POINT ( 'NONE',  ( 21.14288210468430051, -10.65101126812110088, -32.59857632693769602 ) ) ;
#17547=EDGE_CURVE ( 'NONE', #40988, #34513, #11869, .T. ) ;
#17557=CARTESIAN_POINT ( 'NONE',  ( 24.09704775629829854, -13.47827939507680028, -81.42417512157139470 ) ) ;
#17566=EDGE_CURVE ( 'NONE', #41648, #51612, #25263, .T. ) ;
#17571=CARTESIAN_POINT ( 'NONE',  ( 20.59223919530819913, -10.15120003544670091, -38.17063876083509655 ) ) ;
#17574=EDGE_CURVE ( 'NONE', #3482, #31804, #5379, .T. ) ;
#17578=CARTESIAN_POINT ( 'NONE',  ( 10.43935959611360076, -10.81218249130760078, -78.29040566010630187 ) ) ;
#17581=CARTESIAN_POINT ( 'NONE',  ( 10.66328804357033633, -9.855181135427269368, -49.05049542099398963 ) ) ;
#17585=CARTESIAN_POINT ( 'NONE',  ( 23.94268579721757817, -16.91034996406515489, -75.84458980966927300 ) ) ;
#17586=CARTESIAN_POINT ( 'NONE',  ( 22.90092890316272900, -15.60509115818101122, -62.45230633468198533 ) ) ;
#17587=CARTESIAN_POINT ( 'NONE',  ( 24.02073126551701776, -16.28883017867714855, -45.53480547859069816 ) ) ;
#17595=CARTESIAN_POINT ( 'NONE',  ( 9.400903757049320575, -16.99286248564640900, -53.78241387521948269 ) ) ;
#17607=CARTESIAN_POINT ( 'NONE',  ( 16.35167375485299956, -23.85847691190700104, -48.28392467753440087 ) ) ;
#17608=CARTESIAN_POINT ( 'NONE',  ( 12.92633465669690551, -9.590651413721559493, -55.79692252247223649 ) ) ;
#17612=CARTESIAN_POINT ( 'NONE',  ( 10.15437084639799892, -11.17192548897130067, -41.43610882498329318 ) ) ;
#17618=CARTESIAN_POINT ( 'NONE',  ( 20.11811997673071772, -8.703696410388799265, -51.45899645242261045 ) ) ;
#17620=CARTESIAN_POINT ( 'NONE',  ( 23.85449792131219482, -13.85627121030026565, -61.43635185904214779 ) ) ;
#17621=CARTESIAN_POINT ( 'NONE',  ( 20.78413717728000165, -22.42488652343350353, -57.81693366461269079 ) ) ;
#17626=CARTESIAN_POINT ( 'NONE',  ( 9.367163129351689932, -15.61602587752549809, -57.45282021618999835 ) ) ;
#17629=AXIS2_PLACEMENT_3D ( 'NONE', #4385, #20611, #36602 ) ;
#17631=VECTOR ( 'NONE', #41144, 1000.000000000000000 ) ;
#17651=CYLINDRICAL_SURFACE ( 'NONE', #46039, 6.766999999999998572 ) ;
#17653=CARTESIAN_POINT ( 'NONE',  ( 22.88157195713212744, -16.89179476805239943, -46.90719394731226544 ) ) ;
#17660=CARTESIAN_POINT ( 'NONE',  ( 22.91042337000040163, -19.72316792142765962, -77.68106494717130772 ) ) ;
#17672=CYLINDRICAL_SURFACE ( 'NONE', #29539, 7.910999999999997812 ) ;
#17679=CARTESIAN_POINT ( 'NONE',  ( 21.07505574528920178, -9.519296485543838671, -69.00429683512300016 ) ) ;
#17688=CARTESIAN_POINT ( 'NONE',  ( 10.72256312216934759, -19.77478970487977961, -79.24448622922319885 ) ) ;
#17691=CARTESIAN_POINT ( 'NONE',  ( 24.04476951127059792, -15.67185460577278100, -33.50990501219975215 ) ) ;
#17695=CARTESIAN_POINT ( 'NONE',  ( 22.59329360082070437, -11.90358719125920040, -56.90129427292909270 ) ) ;
#17698=VERTEX_POINT ( 'NONE', #1569 ) ;
#17700=VECTOR ( 'NONE', #3983, 1000.000000000000000 ) ;
#17702=CARTESIAN_POINT ( 'NONE',  ( 15.47860435268529855, -22.63851745982070085, -75.37679910129230620 ) ) ;
#17703=CARTESIAN_POINT ( 'NONE',  ( 21.73883909943680948, -21.19911057316521052, -61.75703682941048811 ) ) ;
#17705=CARTESIAN_POINT ( 'NONE',  ( 14.06334888173089759, -7.911065466241970157, -35.20899703272518622 ) ) ;
#17708=EDGE_LOOP ( 'NONE', ( #12174, #36909, #39894, #44534 ) ) ;
#17718=CARTESIAN_POINT ( 'NONE',  ( 22.90088432124023043, -15.64386971747752675, -72.45412750913828859 ) ) ;
#17720=CARTESIAN_POINT ( 'NONE',  ( 15.24811434726632520, -8.849191943919105796, -53.91115499152626711 ) ) ;
#17722=LINE ( 'NONE', #46297, #5769 ) ;
#17726=CARTESIAN_POINT ( 'NONE',  ( 21.21773088487490000, -21.59463283680559798, -62.28818158525510285 ) ) ;
#17727=CARTESIAN_POINT ( 'NONE',  ( 16.13393739769620083, -15.61618894467929941, -32.14999999999999858 ) ) ;
#17747=CARTESIAN_POINT ( 'NONE',  ( 20.99562869291927569, -21.94234359756718789, -52.08399634476754159 ) ) ;
#17752=CARTESIAN_POINT ( 'NONE',  ( 9.593587546094811458, -12.97679829661129958, -63.96927302813099203 ) ) ;
#17753=EDGE_LOOP ( 'NONE', ( #40503, #44680, #20438, #29938 ) ) ;
#17759=CARTESIAN_POINT ( 'NONE',  ( 13.25862789803809960, -9.176068295359060656, -73.81915773946379034 ) ) ;
#17762=CARTESIAN_POINT ( 'NONE',  ( 14.36259696023510024, -22.20703816934632968, -41.03609446384544412 ) ) ;
#17768=CARTESIAN_POINT ( 'NONE',  ( 23.41492785263701748, -12.40909292437391009, -39.37550526180498167 ) ) ;
#17770=CARTESIAN_POINT ( 'NONE',  ( 22.90093739720710531, -16.50198351292171495, -54.49448989795372000 ) ) ;
#17773=VERTEX_POINT ( 'NONE', #4989 ) ;
#17784=CARTESIAN_POINT ( 'NONE',  ( 24.04525281611314824, -15.61618915252426376, -57.50766930885080086 ) ) ;
#17786=CARTESIAN_POINT ( 'NONE',  ( 8.204251278821899973, -17.87512636207440053, -78.70399420596430673 ) ) ;
#17804=CARTESIAN_POINT ( 'NONE',  ( 18.20470190565380619, -7.911112859053382351, -57.37566467645442714 ) ) ;
#17812=ADVANCED_FACE ( 'NONE', ( #41141 ), #48757, .T. ) ;
#17820=CARTESIAN_POINT ( 'NONE',  ( 20.26879960982470052, -9.902567222571891037, -48.15222407485109812 ) ) ;
#17824=CARTESIAN_POINT ( 'NONE',  ( 18.20468603776837924, -23.32126951240223178, -57.92433457871812408 ) ) ;
#17828=CARTESIAN_POINT ( 'NONE',  ( 8.684550524703789520, -15.50073525340130054, -76.07227559032499187 ) ) ;
#17831=CARTESIAN_POINT ( 'NONE',  ( 23.84737858440118075, -13.78234710530517937, -49.71801685587017516 ) ) ;
#17835=CARTESIAN_POINT ( 'NONE',  ( 23.63805141649122277, -18.17389567441268383, -75.89683657592323129 ) ) ;
#17836=CARTESIAN_POINT ( 'NONE',  ( 22.90053501923144808, -15.53643117899985349, -62.44907673796289060 ) ) ;
#17838=CARTESIAN_POINT ( 'NONE',  ( 9.366958745649954565, -14.73023443675878141, -57.49448687106261957 ) ) ;
#17843=EDGE_LOOP ( 'NONE', ( #43886, #24716, #19516, #27119 ) ) ;
#17846=CARTESIAN_POINT ( 'NONE',  ( 22.83615144563630395, -17.18444790103682607, -52.92095170805273341 ) ) ;
#17853=CARTESIAN_POINT ( 'NONE',  ( 22.90093739739452516, -15.61117588207490492, -72.45258998807413775 ) ) ;
#17854=CARTESIAN_POINT ( 'NONE',  ( 24.04492500652006370, -15.60001781178229230, -43.79167453644526375 ) ) ;
#17855=CARTESIAN_POINT ( 'NONE',  ( 10.95413457039449945, -9.201178209987370238, -49.07611398817059722 ) ) ;
#17856=CARTESIAN_POINT ( 'NONE',  ( 22.90080294078536483, -15.57010463074422191, -56.45065799404199680 ) ) ;
#17859=ADVANCED_FACE ( 'NONE', ( #49025 ), #13379, .T. ) ;
#17861=CARTESIAN_POINT ( 'NONE',  ( 11.23975427116819858, -21.23345387782550020, -40.96079523860159810 ) ) ;
#17862=CARTESIAN_POINT ( 'NONE',  ( 9.105463204092400176, -18.18851464184960065, -32.14999999999999858 ) ) ;
#17868=CARTESIAN_POINT ( 'NONE',  ( 16.13393739769620083, -15.61618894467929941, -28.45282021618999835 ) ) ;
#17869=CARTESIAN_POINT ( 'NONE',  ( 15.95893776300690092, -23.85949506763950367, -54.01442497355899519 ) ) ;
#17886=CARTESIAN_POINT ( 'NONE',  ( 24.04493739769619864, -15.61618894467929941, -32.14999999999999858 ) ) ;
#17906=B_SPLINE_CURVE_WITH_KNOTS ( 'NONE', 3,
 ( #1255, #41338, #26108, #1511, #45798, #34225, #50244, #2280, #21657, #30303, #33967 ),
 .UNSPECIFIED., .F., .F.,
 ( 4, 1, 1, 1, 1, 1, 1, 1, 4 ),
 ( 0.000000000000000000, 0.01056175749839638640, 0.08978068856201353032, 0.1689996196256284000, 0.2482185506892432836, 0.3274374817528581394, 0.4066564128164730230, 0.4858753438800901270, 0.5000037738926587094 ),
 .UNSPECIFIED. ) ;
#17912=CARTESIAN_POINT ( 'NONE',  ( 22.04684636386204133, -19.02418517277557442, -44.61949510988410594 ) ) ;
#17921=CARTESIAN_POINT ( 'NONE',  ( 22.90093394831552942, -15.62408632508305217, -50.45319058549613089 ) ) ;
#17931=CARTESIAN_POINT ( 'NONE',  ( 10.43819401510400091, -10.21755434852080135, -68.52898324874108482 ) ) ;
#17949=ORIENTED_EDGE ( 'NONE', *, *, #36399, .T. ) ;
#17951=CARTESIAN_POINT ( 'NONE',  ( 21.78790251819230051, -10.76444979726480078, -54.84160206527499781 ) ) ;
#17956=DIRECTION ( 'NONE',  ( 1.000000000000000000, 0.000000000000000000, 0.000000000000000000 ) ) ;
#17959=CARTESIAN_POINT ( 'NONE',  ( 8.428882060193004122, -13.54534687768648382, -34.87566461313462440 ) ) ;
#17964=ADVANCED_FACE ( 'NONE', ( #30645 ), #10753, .T. ) ;
#17965=ORIENTED_EDGE ( 'NONE', *, *, #41065, .F. ) ;
#17972=VERTEX_POINT ( 'NONE', #42404 ) ;
#17974=CARTESIAN_POINT ( 'NONE',  ( 17.01966384186565051, -22.38319920177791289, -72.91110236449276272 ) ) ;
#17978=CARTESIAN_POINT ( 'NONE',  ( 23.81444512486869414, -17.55625779023211663, -49.58638733271747157 ) ) ;
#17981=CARTESIAN_POINT ( 'NONE',  ( 9.362418724986730112, -19.58270913960189930, -70.84382614012599788 ) ) ;
#17982=ADVANCED_FACE ( 'NONE', ( #10170 ), #50270, .T. ) ;
#17983=CYLINDRICAL_SURFACE ( 'NONE', #33898, 7.910999999999997812 ) ;
#18000=CARTESIAN_POINT ( 'NONE',  ( 20.55055518814909732, -10.42440965293470079, -32.14999999999999858 ) ) ;
#18009=CARTESIAN_POINT ( 'NONE',  ( 20.75744454082159862, -20.94213870710139958, -77.11961558469170086 ) ) ;
#18010=ORIENTED_EDGE ( 'NONE', *, *, #3892, .T. ) ;
#18013=CARTESIAN_POINT ( 'NONE',  ( 14.06336572833587439, -7.911061104356444496, -40.92433462936950406 ) ) ;
#18016=CARTESIAN_POINT ( 'NONE',  ( 15.81374359445209699, -22.66175738342070289, -70.96727622117349199 ) ) ;
#18017=PLANE ( 'NONE',  #295 ) ;
#18040=CARTESIAN_POINT ( 'NONE',  ( 12.14736671544911673, -8.740801174314317024, -33.12518389567012633 ) ) ;
#18042=ORIENTED_EDGE ( 'NONE', *, *, #575, .F. ) ;
#18047=CARTESIAN_POINT ( 'NONE',  ( 15.37953186211669987, -23.42756653633809805, -44.54314102700439548 ) ) ;
#18051=ADVANCED_FACE ( 'NONE', ( #48132 ), #31348, .T. ) ;
#18055=CARTESIAN_POINT ( 'NONE',  ( 12.72599142185514509, -9.703251754813100760, -77.78615250370977208 ) ) ;
#18057=CARTESIAN_POINT ( 'NONE',  ( 22.43205399602669914, -18.79050564095980036, -40.99578301968129068 ) ) ;
#18061=CARTESIAN_POINT ( 'NONE',  ( 16.13393739769620083, -15.61618894467929941, -28.45282021618999835 ) ) ;
#18062=CARTESIAN_POINT ( 'NONE',  ( 9.221494253780836203, -11.63192076660207697, -56.95899812772770332 ) ) ;
#18078=CARTESIAN_POINT ( 'NONE',  ( 10.00102083869919944, -12.13338932698580130, -45.61721828081540053 ) ) ;
#18084=EDGE_CURVE ( 'NONE', #31691, #47210, #177, .T. ) ;
#18085=CARTESIAN_POINT ( 'NONE',  ( 21.98123812872290017, -20.23308925758140120, -75.28008627968870314 ) ) ;
#18088=DIRECTION ( 'NONE',  ( 1.000000000000000000, 0.000000000000000000, 0.000000000000000000 ) ) ;
#18092=EDGE_CURVE ( 'NONE', #38448, #41688, #13591, .T. ) ;
#18093=CARTESIAN_POINT ( 'NONE',  ( 22.90022923424639600, -16.55435297866762667, -66.89132215244777058 ) ) ;
#18105=CARTESIAN_POINT ( 'NONE',  ( 11.27232994224335627, -21.94240753817051726, -70.21600273294129124 ) ) ;
#18113=CARTESIAN_POINT ( 'NONE',  ( 8.585943987534939481, -18.93439863306510063, -50.66049260944299704 ) ) ;
#18115=CARTESIAN_POINT ( 'NONE',  ( 23.04647763113142389, -19.60028853819085981, -47.67433631402742833 ) ) ;
#18117=ADVANCED_FACE ( 'NONE', ( #11473 ), #27690, .T. ) ;
#18120=CARTESIAN_POINT ( 'NONE',  ( 21.96630730344370264, -20.25193646667360170, -44.44642820540089900 ) ) ;
#18122=CARTESIAN_POINT ( 'NONE',  ( 9.367926042023849931, -13.39941049220499991, -32.14999999999999858 ) ) ;
#18127=CARTESIAN_POINT ( 'NONE',  ( 24.04493243794458834, -15.60658242780756488, -61.50728973154512147 ) ) ;
#18128=EDGE_CURVE ( 'NONE', #7094, #50433, #44197, .T. ) ;
#18129=CARTESIAN_POINT ( 'NONE',  ( 17.96668501577229904, -23.65507922116720252, -61.93631807992090188 ) ) ;
#18137=FACE_OUTER_BOUND ( 'NONE', #16881, .T. ) ;
#18142=CARTESIAN_POINT ( 'NONE',  ( 14.49513316393093909, -7.853150399841008600, -65.22618568674107564 ) ) ;
#18155=CARTESIAN_POINT ( 'NONE',  ( 22.90069280194860113, -15.61618434420927670, -40.45282443214609458 ) ) ;
#18169=CARTESIAN_POINT ( 'NONE',  ( 24.04493739746428815, -15.61625192653408867, -77.50767849141614363 ) ) ;
#18180=EDGE_CURVE ( 'NONE', #11866, #42806, #37002, .T. ) ;
#18181=CARTESIAN_POINT ( 'NONE',  ( 26.52624224310950396, -21.61618894467929763, -22.14999999999999858 ) ) ;
#18190=CARTESIAN_POINT ( 'NONE',  ( 8.146821171731881250, -17.66281912668999965, -36.42782227743549583 ) ) ;
#18191=ORIENTED_EDGE ( 'NONE', *, *, #38086, .F. ) ;
#18193=EDGE_CURVE ( 'NONE', #16042, #49834, #51212, .T. ) ;
#18204=CARTESIAN_POINT ( 'NONE',  ( 11.27214961228822077, -21.94227111097665883, -56.50067963292104878 ) ) ;
#18209=ADVANCED_FACE ( 'NONE', ( #29495 ), #4614, .T. ) ;
#18210=CARTESIAN_POINT ( 'NONE',  ( 23.28093797997669867, -17.72025097209759892, -55.15847778952939962 ) ) ;
#18213=CARTESIAN_POINT ( 'NONE',  ( 10.72262114908336983, -19.77486415900381900, -69.24448638217960195 ) ) ;
#18215=CARTESIAN_POINT ( 'NONE',  ( 9.367299438200719308, -15.61632798465739924, -73.84717978381010539 ) ) ;
#18216=CARTESIAN_POINT ( 'NONE',  ( 11.27217523151439948, -21.94228989780888028, -62.21597027386932410 ) ) ;
#18217=CARTESIAN_POINT ( 'NONE',  ( 22.72481313846669337, -13.84495410388251280, -74.36948689368070120 ) ) ;
#18218=CARTESIAN_POINT ( 'NONE',  ( 10.34909372178839959, -19.24960104513710135, -81.23899999999999011 ) ) ;
#18225=CARTESIAN_POINT ( 'NONE',  ( 9.367243689500000414, -15.61633989587210003, -59.45282021618999835 ) ) ;
#18229=CARTESIAN_POINT ( 'NONE',  ( 24.04483843941790866, -15.61617050235280679, -77.50767555791956909 ) ) ;
#18230=CARTESIAN_POINT ( 'NONE',  ( 15.24816392691948508, -22.38319193469252610, -52.99448569864885883 ) ) ;
#18231=CARTESIAN_POINT ( 'NONE',  ( 20.29256454187332537, -10.20483503270093628, -54.16115577807332215 ) ) ;
#18236=CARTESIAN_POINT ( 'NONE',  ( 23.92239988244430293, -16.57878944086319706, -70.05163682948989390 ) ) ;
#18241=DIRECTION ( 'NONE',  ( 0.000000000000000000, 0.000000000000000000, -1.000000000000000000 ) ) ;
#18244=CARTESIAN_POINT ( 'NONE',  ( 8.223454620794861114, -15.61605491354059971, -46.50766849176290663 ) ) ;
#18251=DIRECTION ( 'NONE',  ( 0.000000000000000000, -1.000000000000000000, 0.000000000000000000 ) ) ;
#18260=CARTESIAN_POINT ( 'NONE',  ( 13.14827817127709864, -9.226478610231410471, -72.20804185874739289 ) ) ;
#18268=CARTESIAN_POINT ( 'NONE',  ( 13.68194553784909928, -9.003300359821770016, -79.83979650029878883 ) ) ;
#18271=DIRECTION ( 'NONE',  ( 1.000000000000000000, 0.000000000000000000, 0.000000000000000000 ) ) ;
#18276=ORIENTED_EDGE ( 'NONE', *, *, #40869, .T. ) ;
#18278=CARTESIAN_POINT ( 'NONE',  ( 24.04462281140675728, -15.61619016268715399, -39.50767146438039390 ) ) ;
#18282=VERTEX_POINT ( 'NONE', #10374 ) ;
#18290=CARTESIAN_POINT ( 'NONE',  ( 20.11426146801901993, -8.759875404557478262, -33.45974718993613806 ) ) ;
#18297=CARTESIAN_POINT ( 'NONE',  ( 13.30304109838990101, -8.296846506033869417, -47.39502254529469383 ) ) ;
#18302=CARTESIAN_POINT ( 'NONE',  ( 22.90115736359569354, -15.61618877121331295, -78.84717825834033533 ) ) ;
#18305=CARTESIAN_POINT ( 'NONE',  ( 20.84741856749390365, -10.36969921949989981, -42.58016164095369760 ) ) ;
#18319=CARTESIAN_POINT ( 'NONE',  ( 15.01656936500493167, -23.47607714972237147, -32.33735170919545254 ) ) ;
#18326=CARTESIAN_POINT ( 'NONE',  ( 23.04647607065054160, -19.60029144796367007, -73.95899818474369170 ) ) ;
#18329=VECTOR ( 'NONE', #41395, 1000.000000000000000 ) ;
#18330=CARTESIAN_POINT ( 'NONE',  ( 19.13110865206880007, -9.231870408720430632, -46.09253186719689666 ) ) ;
#18335=EDGE_CURVE ( 'NONE', #44797, #27637, #43049, .T. ) ;
#18338=CARTESIAN_POINT ( 'NONE',  ( 22.05366437006999902, -10.46414267589130098, -39.05954089307479649 ) ) ;
#18340=DIRECTION ( 'NONE',  ( 0.000000000000000000, 0.000000000000000000, -1.000000000000000000 ) ) ;
#18345=CARTESIAN_POINT ( 'NONE',  ( 8.427199782394856342, -17.67924411827841524, -76.70928524612517663 ) ) ;
#18346=CARTESIAN_POINT ( 'NONE',  ( 22.90088705258820667, -15.61618575905976414, -62.45282818884277276 ) ) ;
#18347=CYLINDRICAL_SURFACE ( 'NONE', #41047, 7.910999999999997812 ) ;
#18351=ORIENTED_EDGE ( 'NONE', *, *, #44721, .F. ) ;
#18358=CARTESIAN_POINT ( 'NONE',  ( 22.90088360717968285, -15.58831960617060375, -72.45151510512926052 ) ) ;
#18359=CARTESIAN_POINT ( 'NONE',  ( 9.221342996571138428, -11.63217922216438005, -42.95902251082229384 ) ) ;
#18360=CARTESIAN_POINT ( 'NONE',  ( 14.75440393491079938, -23.74512537455679961, -66.34584096003959530 ) ) ;
#18367=CARTESIAN_POINT ( 'NONE',  ( 9.453537067250739057, -12.31786433510400158, -55.37864069218029073 ) ) ;
#18370=CARTESIAN_POINT ( 'NONE',  ( 8.821128736879460419, -16.36262873326029776, -32.14999999999999858 ) ) ;
#18377=CARTESIAN_POINT ( 'NONE',  ( 14.06335392814032836, -7.911064159492109837, -51.20899709835300939 ) ) ;
#18380=CARTESIAN_POINT ( 'NONE',  ( 24.04460466267867247, -15.53778724920028331, -61.50452191719739403 ) ) ;
#18381=CARTESIAN_POINT ( 'NONE',  ( 18.61786603712990029, -7.754076046534380318, -65.10507532246559492 ) ) ;
#18390=CARTESIAN_POINT ( 'NONE',  ( 21.39066400359539699, -9.703911137440838885, -81.23899999999999011 ) ) ;
#18393=CARTESIAN_POINT ( 'NONE',  ( 10.17245219797972844, -10.37354689578340228, -65.02189718388713402 ) ) ;
#18397=CARTESIAN_POINT ( 'NONE',  ( 20.11167749483549727, -21.44028912360316497, -57.15644495666281699 ) ) ;
#18415=CARTESIAN_POINT ( 'NONE',  ( 22.90148701646199925, -15.69275899496028970, -46.85077873481721156 ) ) ;
#18423=CARTESIAN_POINT ( 'NONE',  ( 23.11602277574511177, -19.35578214976509415, -77.66417765721635647 ) ) ;
#18426=ORIENTED_EDGE ( 'NONE', *, *, #38949, .T. ) ;
#18429=CARTESIAN_POINT ( 'NONE',  ( 9.367121035360348458, -15.18956524623389726, -45.86723877108192937 ) ) ;
#18431=CARTESIAN_POINT ( 'NONE',  ( 20.06347647389389977, -8.367641317401169232, -35.45045784522799437 ) ) ;
#18434=CARTESIAN_POINT ( 'NONE',  ( 19.20490796821585278, -21.71094733663775855, -50.80397083643239853 ) ) ;
#18435=CARTESIAN_POINT ( 'NONE',  ( 12.72589019024139745, -21.52906861929441718, -47.11946018635927658 ) ) ;
#18444=EDGE_CURVE ( 'NONE', #33168, #50858, #19265, .T. ) ;
#18450=EDGE_CURVE ( 'NONE', #21295, #27800, #38027, .T. ) ;
#18451=CARTESIAN_POINT ( 'NONE',  ( 21.26076650159200199, -22.07361444172130049, -35.79407082892649328 ) ) ;
#18471=CARTESIAN_POINT ( 'NONE',  ( 11.73483375864000067, -9.603320950852721083, -54.36628847889309668 ) ) ;
#18475=LINE ( 'NONE', #14547, #7540 ) ;
#18476=DIRECTION ( 'NONE',  ( 0.000000000000000000, 0.000000000000000000, -1.000000000000000000 ) ) ;
#18477=CARTESIAN_POINT ( 'NONE',  ( 23.10892566284617544, -19.36881467858842498, -61.66477234305963862 ) ) ;
#18478=FACE_OUTER_BOUND ( 'NONE', #13289, .T. ) ;
#18479=CARTESIAN_POINT ( 'NONE',  ( 9.157312613638797671, -16.66687816016379742, -81.23899999999999011 ) ) ;
#18481=ORIENTED_EDGE ( 'NONE', *, *, #11889, .T. ) ;
#18492=VECTOR ( 'NONE', #39818, 1000.000000000000000 ) ;
#18494=CARTESIAN_POINT ( 'NONE',  ( 22.90034292835611751, -15.71307119870275848, -72.45738199783259859 ) ) ;
#18496=CARTESIAN_POINT ( 'NONE',  ( 16.13393739769620083, -15.61618894467929941, -23.15000000000000213 ) ) ;
#18498=CARTESIAN_POINT ( 'NONE',  ( 13.53092308830080093, -23.16807188358326641, -50.11355989224952623 ) ) ;
#18501=CARTESIAN_POINT ( 'NONE',  ( 9.119644240547859937, -19.13562627146119866, -76.86446490096111006 ) ) ;
#18502=DIRECTION ( 'NONE',  ( 1.000000000000000000, 0.000000000000000000, 0.000000000000000000 ) ) ;
#18509=CARTESIAN_POINT ( 'NONE',  ( 9.205734167420720482, -3.616188944679329165, -24.15000000000000213 ) ) ;
#18511=CARTESIAN_POINT ( 'NONE',  ( 23.36532317189500318, -12.56761420098369975, -53.16051062239899494 ) ) ;
#18520=CARTESIAN_POINT ( 'NONE',  ( 22.06174470004240007, -11.92280751385899862, -32.14999999999999858 ) ) ;
#18521=AXIS2_PLACEMENT_3D ( 'NONE', #45376, #12899, #9221 ) ;
#18524=CARTESIAN_POINT ( 'NONE',  ( 22.52295300047549276, -13.38580680388945332, -80.74026669357201058 ) ) ;
#18528=CARTESIAN_POINT ( 'NONE',  ( 12.20533024450969961, -21.47354372396169708, -75.53523696341939342 ) ) ;
#18533=CARTESIAN_POINT ( 'NONE',  ( 16.67840439675140018, -22.64798205764600070, -74.92822277435448086 ) ) ;
#18535=CARTESIAN_POINT ( 'NONE',  ( 9.221493846662148997, -11.63192146079378908, -66.95899777436285660 ) ) ;
#18540=ORIENTED_EDGE ( 'NONE', *, *, #31136, .F. ) ;
#18546=ADVANCED_FACE ( 'NONE', ( #40404 ), #11123, .T. ) ;
#18547=ORIENTED_EDGE ( 'NONE', *, *, #18084, .F. ) ;
#18554=ADVANCED_FACE ( 'NONE', ( #28594 ), #41225, .T. ) ;
#18556=ORIENTED_EDGE ( 'NONE', *, *, #49418, .F. ) ;
#18563=CARTESIAN_POINT ( 'NONE',  ( 20.31321962299979944, -8.973874011401631989, -41.69125950871409003 ) ) ;
#18568=CARTESIAN_POINT ( 'NONE',  ( 9.366428224829499882, -15.61611423639980067, -77.45282021618989177 ) ) ;
#18570=CARTESIAN_POINT ( 'NONE',  ( 11.26840393093330128, -10.51039387845690065, -42.10484805457209490 ) ) ;
#18584=CARTESIAN_POINT ( 'NONE',  ( 24.03648926733799840, -15.22123262239629504, -71.49178105483443346 ) ) ;
#18593=CARTESIAN_POINT ( 'NONE',  ( 9.366721379915048828, -15.33582998764832617, -39.86035918413693224 ) ) ;
#18596=CARTESIAN_POINT ( 'NONE',  ( 14.41393119263600120, -8.776295864288348625, -43.87440179741569324 ) ) ;
#18602=CARTESIAN_POINT ( 'NONE',  ( 18.39333206953279998, -8.100734545543689435, -32.88046427011239814 ) ) ;
#18608=CARTESIAN_POINT ( 'NONE',  ( 24.04476267751569551, -15.67298808999131232, -75.79461090121749578 ) ) ;
#18624=DIRECTION ( 'NONE',  ( 0.000000000000000000, 0.000000000000000000, 1.000000000000000000 ) ) ;
#18625=CARTESIAN_POINT ( 'NONE',  ( 23.06214062797170072, -3.616188944679349149, -24.14999999999999858 ) ) ;
#18626=CARTESIAN_POINT ( 'NONE',  ( 16.24108513978070079, -7.371721744350270278, -67.29646813280308493 ) ) ;
#18629=B_SPLINE_CURVE_WITH_KNOTS ( 'NONE', 3,
 ( #48620, #21328, #37076, #8780, #33387, #45202, #5120, #29195, #32333, #25258 ),
 .UNSPECIFIED., .F., .F.,
 ( 4, 1, 1, 1, 1, 1, 1, 4 ),
 ( 0.5000017723907246303, 0.5455675515341791293, 0.6247864825977968994, 0.7040054136614146696, 0.7832243447250346602, 0.8624432757886524303, 0.9416622068522703115, 1.000000000000000000 ),
 .UNSPECIFIED. ) ;
#18632=CARTESIAN_POINT ( 'NONE',  ( 10.55445623026200153, -20.55340310930620262, -53.00207276027180114 ) ) ;
#18635=CARTESIAN_POINT ( 'NONE',  ( 8.975904575304079813, -14.67896029866649954, -32.14999999999999858 ) ) ;
#18637=CYLINDRICAL_SURFACE ( 'NONE', #28171, 7.910999999999997812 ) ;
#18642=CARTESIAN_POINT ( 'NONE',  ( 22.63786127318122965, -11.06313073300040095, -61.31321979917446185 ) ) ;
#18643=CARTESIAN_POINT ( 'NONE',  ( 23.67593780178180296, -18.94799785482829790, -67.64008111650160515 ) ) ;
#18668=CARTESIAN_POINT ( 'NONE',  ( 8.428829098684769150, -17.68683844382469061, -76.42434267299502437 ) ) ;
#18673=CARTESIAN_POINT ( 'NONE',  ( 9.366937397696199596, -15.61618894467949836, -28.45282021618999835 ) ) ;
#18678=EDGE_CURVE ( 'NONE', #30160, #14876, #22935, .T. ) ;
#18683=CARTESIAN_POINT ( 'NONE',  ( 19.14634567751863514, -22.94949537724593824, -77.88358313659429655 ) ) ;
#18685=ORIENTED_EDGE ( 'NONE', *, *, #15196, .F. ) ;
#18686=B_SPLINE_CURVE_WITH_KNOTS ( 'NONE', 3,
 ( #38217, #34257, #50280, #14366, #46356, #31614, #7285, #19584, #23489, #46876, #15918, #43952, #39513, #3613, #51560, #47133, #43442, #19329, #11993, #51812, #3355, #35309, #23235, #39765, #27698, #15661, #8053, #26927, #47632, #38747, #51309, #11739, #7545, #43696, #34785, #7800, #14880, #42933 ),
 .UNSPECIFIED., .F., .F.,
 ( 4, 2, 2, 2, 2, 2, 2, 2, 2, 2, 2, 2, 2, 2, 1, 1, 1, 1, 1, 1, 2, 4 ),
 ( 0.000000000000000000, 0.06250074569407504388, 0.1250014913881500878, 0.1875022370822251316, 0.2500029827763001755, 0.2812533556233377530, 0.3125037284703753304, 0.3437541013174129079, 0.3750044741644504298, 0.4062548470114880628, 0.4375052198585256402, 0.4687555927055632177, 0.4843807791290819509, 0.4921933723408414285, 0.4960996689467210841, 0.4980528172496609396, 0.4990293914011308951, 0.4995176784768657896, 0.4997618220147331813, 0.4998838937836668772, 0.4999449296681337529, 0.5000059655526006841 ),
 .UNSPECIFIED. ) ;
#18690=CARTESIAN_POINT ( 'NONE',  ( 10.90943883812770032, -9.237527312442798788, -33.07388991331939820 ) ) ;
#18691=AXIS2_PLACEMENT_3D ( 'NONE', #6738, #39217, #35795 ) ;
#18694=DIRECTION ( 'NONE',  ( 1.000000000000000000, 0.000000000000000000, 0.000000000000000000 ) ) ;
#18695=CARTESIAN_POINT ( 'NONE',  ( 11.97524499910796969, -21.02749279390264192, -47.16112356747648704 ) ) ;
#18705=CARTESIAN_POINT ( 'NONE',  ( 12.06625306698470013, -8.444253027749869744, -34.84344365616309602 ) ) ;
#18725=CARTESIAN_POINT ( 'NONE',  ( 10.69097154885009893, -10.52886969908080061, -52.30659627123909416 ) ) ;
#18731=CARTESIAN_POINT ( 'NONE',  ( 9.367206039829609310, -15.61603166621950045, -73.45282021618999124 ) ) ;
#18742=EDGE_CURVE ( 'NONE', #41285, #31407, #11097, .T. ) ;
#18745=ADVANCED_FACE ( 'NONE', ( #37774 ), #14176, .T. ) ;
#18746=CARTESIAN_POINT ( 'NONE',  ( 10.45401511118626026, -11.85366287480093561, -79.63887948191079147 ) ) ;
#18751=DIRECTION ( 'NONE',  ( 0.000000000000000000, 0.000000000000000000, -1.000000000000000000 ) ) ;
#18754=FACE_OUTER_BOUND ( 'NONE', #36068, .T. ) ;
#18764=CARTESIAN_POINT ( 'NONE',  ( 21.69055479405609788, -21.15791713123389783, -55.53707855430759821 ) ) ;
#18766=B_SPLINE_CURVE_WITH_KNOTS ( 'NONE', 3,
 ( #50070, #25681, #18345, #21497, #38018, #10503, #21751, #37497, #34586, #13658, #33808, #1597, #30392, #38540, #37761, #17835, #2637, #17585, #29620, #50590, #45622, #46155, #9722, #18608, #14680, #10242, #26201, #22268 ),
 .UNSPECIFIED., .F., .F.,
 ( 4, 2, 2, 2, 2, 2, 2, 2, 2, 2, 1, 1, 1, 1, 2, 4 ),
 ( 0.000000000000000000, 0.06250047608285554113, 0.1250009521657110823, 0.1875014282485666095, 0.2500019043314221645, 0.3125023804142777473, 0.3750028564971332190, 0.4375033325799887463, 0.4687535706214165376, 0.4843786896421304333, 0.4921912491524875199, 0.4960975289076660077, 0.4980506687852552239, 0.4990272387240497487, 0.4995155236934472054, 0.5000038086628445511 ),
 .UNSPECIFIED. ) ;
#18782=CARTESIAN_POINT ( 'NONE',  ( 9.451921682515308731, -13.35937146058209990, -73.95085834214719966 ) ) ;
#18789=DIRECTION ( 'NONE',  ( 0.000000000000000000, 0.000000000000000000, 1.000000000000000000 ) ) ;
#18790=CARTESIAN_POINT ( 'NONE',  ( 20.99566010709231634, -9.290059359670648220, -67.50066313927187878 ) ) ;
#18797=CARTESIAN_POINT ( 'NONE',  ( 24.04493739769619864, -15.61618894467929941, -32.14999999999999858 ) ) ;
#18811=FACE_OUTER_BOUND ( 'NONE', #1922, .T. ) ;
#18816=CARTESIAN_POINT ( 'NONE',  ( 15.67252115383410072, -7.782043002620109284, -45.49376819976779984 ) ) ;
#18820=CARTESIAN_POINT ( 'NONE',  ( 14.36273205168262912, -9.025304815231496747, -77.86948557558969242 ) ) ;
#18822=CARTESIAN_POINT ( 'NONE',  ( 20.15227385440210028, -21.41235416792470048, -41.15422088180869054 ) ) ;
#18828=CARTESIAN_POINT ( 'NONE',  ( 24.04504587474531263, -15.61618895646369687, -51.50767080737492165 ) ) ;
#18831=EDGE_CURVE ( 'NONE', #39738, #38090, #12947, .T. ) ;
#18839=CARTESIAN_POINT ( 'NONE',  ( 23.72997357701965626, -13.35730697104988174, -71.41570937345944969 ) ) ;
#18842=ADVANCED_FACE ( 'NONE', ( #47385 ), #35827, .T. ) ;
#18847=CARTESIAN_POINT ( 'NONE',  ( 22.72481333191009156, -13.84495503856223309, -42.36948635521349615 ) ) ;
#18850=CARTESIAN_POINT ( 'NONE',  ( 22.73127723598420147, -18.10971370989899754, -46.56784545357869121 ) ) ;
#18852=CARTESIAN_POINT ( 'NONE',  ( 14.83834572504270000, -8.683358393905999506, -80.28837282723659996 ) ) ;
#18855=CARTESIAN_POINT ( 'NONE',  ( 22.65693326085800052, -19.97936131720339858, -37.47516227180238957 ) ) ;
#18856=ORIENTED_EDGE ( 'NONE', *, *, #1662, .T. ) ;
#18860=CARTESIAN_POINT ( 'NONE',  ( 11.27214654185450726, -21.94226878787483415, -40.50067558586400196 ) ) ;
#18862=CARTESIAN_POINT ( 'NONE',  ( 9.367504675961500382, -15.61621390379479912, -67.84717978381009118 ) ) ;
#18872=VERTEX_POINT ( 'NONE', #40279 ) ;
#18882=CARTESIAN_POINT ( 'NONE',  ( 19.68986098307310328, -8.177228835168328658, -61.43426723409519496 ) ) ;
#18886=ORIENTED_EDGE ( 'NONE', *, *, #25566, .F. ) ;
#18889=CARTESIAN_POINT ( 'NONE',  ( 10.18556923319409968, -11.13025426117309991, -57.43833289983439272 ) ) ;
#18890=CARTESIAN_POINT ( 'NONE',  ( 8.867200650584759813, -15.35517633189170006, -32.14999999999999858 ) ) ;
#18896=CARTESIAN_POINT ( 'NONE',  ( 15.56510543608290043, -7.390670668702870039, -60.98569090715739804 ) ) ;
#18926=VECTOR ( 'NONE', #9683, 1000.000000000000000 ) ;
#18930=CARTESIAN_POINT ( 'NONE',  ( 10.04828159318836001, -12.59815513276911858, -65.59931143651195384 ) ) ;
#18939=CARTESIAN_POINT ( 'NONE',  ( 9.221374816805001373, -19.60025404329541487, -78.34097178294052810 ) ) ;
#18948=CARTESIAN_POINT ( 'NONE',  ( 20.31028818469260244, -22.72544855982049938, -32.12326274055609332 ) ) ;
#18952=CARTESIAN_POINT ( 'NONE',  ( 11.79147378256356937, -20.83640137970460771, -51.17359023759287595 ) ) ;
#18960=CARTESIAN_POINT ( 'NONE',  ( 18.64396758981110125, -22.71517679829500125, -81.67932580530198550 ) ) ;
#18962=EDGE_CURVE ( 'NONE', #45208, #16752, #24785, .T. ) ;
#18974=LINE ( 'NONE', #34955, #19911 ) ;
#18982=CARTESIAN_POINT ( 'NONE',  ( 10.72664991973389981, -10.49096344046840024, -68.30882034609030029 ) ) ;
#18985=CARTESIAN_POINT ( 'NONE',  ( 22.90103018812914115, -15.61618888866172483, -50.84718209631233066 ) ) ;
#18999=CARTESIAN_POINT ( 'NONE',  ( 23.15496243216929884, -12.51723427498050079, -81.23899999999999011 ) ) ;
#19003=VERTEX_POINT ( 'NONE', #5167 ) ;
#19004=CARTESIAN_POINT ( 'NONE',  ( 14.06324288281645352, -7.911092913131379412, -52.92433643171475666 ) ) ;
#19014=CARTESIAN_POINT ( 'NONE',  ( 22.90046023677898646, -15.52937730499472657, -40.44874214335946760 ) ) ;
#19020=CARTESIAN_POINT ( 'NONE',  ( 11.03937652346400000, -21.58546006282470131, -56.01239214068929329 ) ) ;
#19031=CARTESIAN_POINT ( 'NONE',  ( 11.25287529172470080, -20.70714090792739981, -45.59048102137129632 ) ) ;
#19039=CARTESIAN_POINT ( 'NONE',  ( 21.51824785155720221, -11.06077896193409948, -70.62366323747509966 ) ) ;
#19042=CARTESIAN_POINT ( 'NONE',  ( 20.11811090880234332, -22.52868689541044489, -57.84100116256885116 ) ) ;
#19048=CARTESIAN_POINT ( 'NONE',  ( 22.16258581960079965, -19.27651095769689604, -79.02086993021860906 ) ) ;
#19050=CARTESIAN_POINT ( 'NONE',  ( 24.04493741561075737, -14.58064863577438075, -67.46599913618511835 ) ) ;
#19058=CARTESIAN_POINT ( 'NONE',  ( 22.46008698234219381, -10.75448952574305395, -39.58399611284257702 ) ) ;
#19065=CARTESIAN_POINT ( 'NONE',  ( 2.277530937145189949, -15.61618894467929941, -32.14999999999999858 ) ) ;
#19070=SHAPE_REPRESENTATION ( 'Height Adjustment Lead Screw', ( #20940 ), #10115 ) ;
#19073=CARTESIAN_POINT ( 'NONE',  ( 17.16957635348524747, -23.52717588353839773, -48.25066592410423283 ) ) ;
#19075=CARTESIAN_POINT ( 'NONE',  ( 17.16954899286013614, -23.52717978940560073, -53.96600348036692907 ) ) ;
#19077=CARTESIAN_POINT ( 'NONE',  ( 8.294557586283641371, -15.97795097143059984, -38.99781585255099259 ) ) ;
#19084=CARTESIAN_POINT ( 'NONE',  ( 11.59299064767419907, -21.01270279974499999, -39.56984226053629783 ) ) ;
#19095=EDGE_CURVE ( 'NONE', #17698, #30160, #37344, .T. ) ;
#19099=CARTESIAN_POINT ( 'NONE',  ( 9.366937397696199596, -15.61618894467949836, -28.45282021618999835 ) ) ;
#19100=CARTESIAN_POINT ( 'NONE',  ( 23.25180567546468779, -12.03939683248547787, -71.35930991703870063 ) ) ;
#19102=VERTEX_POINT ( 'NONE', #32032 ) ;
#19107=CARTESIAN_POINT ( 'NONE',  ( 9.452223072063393516, -13.93305368010741851, -39.92635120517288527 ) ) ;
#19110=CARTESIAN_POINT ( 'NONE',  ( 9.475322139430359059, -13.29123700130180019, -59.55975014801229861 ) ) ;
#19112=CARTESIAN_POINT ( 'NONE',  ( 21.10095754687662861, -10.66581710795787785, -80.59744018890606299 ) ) ;
#19115=CARTESIAN_POINT ( 'NONE',  ( 21.70740924569160057, -10.09141683809470003, -33.03890213223969141 ) ) ;
#19121=CARTESIAN_POINT ( 'NONE',  ( 9.221330038119877059, -19.60017639455499250, -40.62567196025226934 ) ) ;
#19132=CARTESIAN_POINT ( 'NONE',  ( 20.49062781741232797, -22.31005579585255560, -44.10890486331368265 ) ) ;
#19141=CARTESIAN_POINT ( 'NONE',  ( 12.82100586541850085, -23.16650050900399904, -58.42394785367758914 ) ) ;
#19143=CARTESIAN_POINT ( 'NONE',  ( 17.16957815729259806, -23.52717562567822185, -47.96600257623488517 ) ) ;
#19144=DIRECTION ( 'NONE',  ( 0.000000000000000000, 0.000000000000000000, -1.000000000000000000 ) ) ;
#19150=CARTESIAN_POINT ( 'NONE',  ( 11.12617520208469912, -10.09993916812369896, -59.49802510748859419 ) ) ;
#19152=CARTESIAN_POINT ( 'NONE',  ( 11.92405982532479847, -22.23876938295769889, -32.14999999999999858 ) ) ;
#19159=CARTESIAN_POINT ( 'NONE',  ( 23.87596833625310211, -18.45232675081680185, -61.61944235566640060 ) ) ;
#19162=CARTESIAN_POINT ( 'NONE',  ( 20.10523294086599932, -22.40662673471619826, -32.14999999999999858 ) ) ;
#19166=LINE ( 'NONE', #10545, #3754 ) ;
#19174=CARTESIAN_POINT ( 'NONE',  ( 15.79986072486390114, -8.173401390133609112, -77.71837925212089715 ) ) ;
#19181=CARTESIAN_POINT ( 'NONE',  ( 14.06322880297374489, -7.911096558319137273, -37.20899947889007819 ) ) ;
#19189=ORIENTED_EDGE ( 'NONE', *, *, #34405, .F. ) ;
#19190=ORIENTED_EDGE ( 'NONE', *, *, #17566, .T. ) ;
#19191=CARTESIAN_POINT ( 'NONE',  ( 9.366584228470589579, -15.61631960056659985, -37.84717978380999881 ) ) ;
#19192=CARTESIAN_POINT ( 'NONE',  ( 11.97538582446263256, -21.02759958964866982, -59.16115346696501831 ) ) ;
#19195=CARTESIAN_POINT ( 'NONE',  ( 15.48732851072162298, -23.50178174477514403, -78.03370670278647481 ) ) ;
#19198=CARTESIAN_POINT ( 'NONE',  ( 22.73658440641116130, -17.29642323430746131, -80.53196621422273438 ) ) ;
#19201=CARTESIAN_POINT ( 'NONE',  ( 8.428875223629747282, -13.54537173489410762, -34.59100157321395130 ) ) ;
#19204=CARTESIAN_POINT ( 'NONE',  ( 16.40925717896080016, -23.85672821053029935, -32.28170060268320185 ) ) ;
#19214=CARTESIAN_POINT ( 'NONE',  ( 22.72481099998648091, -17.38743435906051715, -36.53615103672703412 ) ) ;
#19219=CARTESIAN_POINT ( 'NONE',  ( 24.19017502950390153, -17.37111537874790201, -33.57594075914509091 ) ) ;
#19230=AXIS2_PLACEMENT_3D ( 'NONE', #42831, #23641, #22877 ) ;
#19243=CARTESIAN_POINT ( 'NONE',  ( 19.11518129813550004, -22.44399087095360201, -59.43630006696479740 ) ) ;
#19244=CARTESIAN_POINT ( 'NONE',  ( 9.221499526225441556, -11.63191175217212958, -40.67433494680559392 ) ) ;
#19248=CARTESIAN_POINT ( 'NONE',  ( 22.90069508915062002, -15.67807337085623942, -34.45572864665300017 ) ) ;
#19251=CARTESIAN_POINT ( 'NONE',  ( 9.018910532691149839, -15.87964395708210041, -81.23899999999999011 ) ) ;
#19253=ORIENTED_EDGE ( 'NONE', *, *, #4651, .F. ) ;
#19261=CARTESIAN_POINT ( 'NONE',  ( 18.20461993357798036, -7.911089693863461392, -53.09100360769544125 ) ) ;
#19265=B_SPLINE_CURVE_WITH_KNOTS ( 'NONE', 3,
 ( #29690, #30469, #1931, #17912, #42549, #33881, #46489, #30213, #29946, #42286, #38350, #45700, #6127, #10579, #33367, #45443, #13480, #9800 ),
 .UNSPECIFIED., .F., .F.,
 ( 4, 2, 2, 2, 2, 2, 2, 2, 4 ),
 ( 0.5000000032861632304, 0.5625000028753927017, 0.6250000024646221730, 0.6875000020538517553, 0.7500000016430812266, 0.8125000012323109200, 0.8750000008215406133, 0.9375000004107703067, 1.000000000000000000 ),
 .UNSPECIFIED. ) ;
#19270=LINE ( 'NONE', #36022, #36686 ) ;
#19277=CARTESIAN_POINT ( 'NONE',  ( 22.89902617865969958, -15.44245184754445965, -40.44465385252913592 ) ) ;
#19278=B_SPLINE_CURVE_WITH_KNOTS ( 'NONE', 3,
 ( #51484, #11398, #15584, #14085, #30046, #2556, #35226, #47556, #15324, #11652, #16868, #33082, #37036, #32044, #12684, #44128, #29161, #24173 ),
 .UNSPECIFIED., .F., .F.,
 ( 4, 2, 2, 2, 2, 2, 2, 2, 4 ),
 ( 0.5000015687207624016, 0.5625013726306670181, 0.6250011765405716346, 0.6875009804504761401, 0.7500007843603807567, 0.8125005882702855953, 0.8750003921801903228, 0.9375001960900952724, 1.000000000000000000 ),
 .UNSPECIFIED. ) ;
#19283=DIRECTION ( 'NONE',  ( -0.8090169943749487835, -0.5877852522924713607, 0.000000000000000000 ) ) ;
#19284=CARTESIAN_POINT ( 'NONE',  ( 23.33437357335099804, -18.73716107904780159, -51.41769413899939423 ) ) ;
#19296=CARTESIAN_POINT ( 'NONE',  ( 23.38479371968623255, -12.38874807463486505, -45.37444489943354142 ) ) ;
#19297=CARTESIAN_POINT ( 'NONE',  ( 22.90101955563642733, -15.61618902498797290, -36.84717743668400658 ) ) ;
#19299=ORIENTED_EDGE ( 'NONE', *, *, #2191, .T. ) ;
#19301=CARTESIAN_POINT ( 'NONE',  ( 22.97870654863990225, -12.67410981443290119, -36.93812364489689770 ) ) ;
#19309=DIRECTION ( 'NONE',  ( 0.000000000000000000, 0.000000000000000000, -1.000000000000000000 ) ) ;
#19310=VECTOR ( 'NONE', #32130, 1000.000000000000114 ) ;
#19312=CARTESIAN_POINT ( 'NONE',  ( 23.83903846881501210, -13.54551738375433523, -67.70899597192914143 ) ) ;
#19315=VERTEX_POINT ( 'NONE', #12933 ) ;
#19319=CARTESIAN_POINT ( 'NONE',  ( 22.90077909847273219, -15.61618896438501203, -58.84717277627543552 ) ) ;
#19329=CARTESIAN_POINT ( 'NONE',  ( 19.71665332066073617, -9.848143450206167770, -46.12982609512481247 ) ) ;
#19332=CARTESIAN_POINT ( 'NONE',  ( 8.222937397696199469, -15.61618894467929941, -32.14999999999999858 ) ) ;
#19336=CARTESIAN_POINT ( 'NONE',  ( 22.90093741645776504, -14.73039735216230284, -52.41115107345247992 ) ) ;
#19338=CARTESIAN_POINT ( 'NONE',  ( 13.45295195435610047, -22.99176110175159948, -52.62347199549349597 ) ) ;
#19340=CARTESIAN_POINT ( 'NONE',  ( 22.14986259033789651, -18.71508664667078747, -32.60422815991633172 ) ) ;
#19345=CARTESIAN_POINT ( 'NONE',  ( 19.82873695480079590, -9.608609115224629349, -56.52269350815070226 ) ) ;
#19362=DIRECTION ( 'NONE',  ( 0.000000000000000000, 0.000000000000000000, 1.000000000000000000 ) ) ;
#19370=CARTESIAN_POINT ( 'NONE',  ( 13.72450424504459932, -22.24470239639139635, -53.06379780079559794 ) ) ;
#19375=CARTESIAN_POINT ( 'NONE',  ( 18.90449655907080029, -22.95858338196050141, -33.67265358074869397 ) ) ;
#19376=B_SPLINE_CURVE_WITH_KNOTS ( 'NONE', 3,
 ( #20889, #986, #28230, #48168, #9384, #21403, #8332, #24285, #40305, #4397 ),
 .UNSPECIFIED., .F., .F.,
 ( 4, 1, 1, 1, 1, 1, 1, 4 ),
 ( 0.5000039623326250071, 0.5569989693773305106, 0.6362179004408794469, 0.7154368315045867011, 0.7946557625681401893, 0.8738746936316936775, 0.9530936246954009317, 1.000000000000000000 ),
 .UNSPECIFIED. ) ;
#19394=CARTESIAN_POINT ( 'NONE',  ( 12.25210256922130725, -8.645705515954809073, -76.84572645005218305 ) ) ;
#19403=CARTESIAN_POINT ( 'NONE',  ( 18.75273301534850034, -7.797964749320120070, -65.39521378727619094 ) ) ;
#19405=CARTESIAN_POINT ( 'NONE',  ( 9.829250996703903454, -12.53343974589846788, -37.99218164148856403 ) ) ;
#19411=CARTESIAN_POINT ( 'NONE',  ( 22.22458528030719904, -19.90695835996979923, -54.42801351941700005 ) ) ;
#19418=B_SPLINE_CURVE_WITH_KNOTS ( 'NONE', 3,
 ( #16317, #51710, #48552, #15804, #50557, #37988, #41653, #17804, #10727, #2084, #46641, #6532, #34812, #9689, #18062, #5757, #33777, #26680 ),
 .UNSPECIFIED., .F., .F.,
 ( 4, 2, 2, 2, 2, 2, 2, 2, 4 ),
 ( 0.5000001415279446970, 0.5625001238369514711, 0.6250001061459582452, 0.6875000884549651303, 0.7500000707639719044, 0.8125000530729789006, 0.8750000353819860077, 0.9375000176909930039, 1.000000000000000000 ),
 .UNSPECIFIED. ) ;
#19421=CARTESIAN_POINT ( 'NONE',  ( 9.092216188204538696, -19.90534773362269760, -70.33352477266458891 ) ) ;
#19425=CARTESIAN_POINT ( 'NONE',  ( 9.366917638880204677, -14.73053537850788075, -59.49448256068535557 ) ) ;
#19428=ORIENTED_EDGE ( 'NONE', *, *, #22169, .F. ) ;
#19435=CARTESIAN_POINT ( 'NONE',  ( 12.28329235829779975, -21.99421580145110156, -70.90555118064979467 ) ) ;
#19441=CARTESIAN_POINT ( 'NONE',  ( 21.94685905566085182, -20.98253927633499671, -61.74495104792147515 ) ) ;
#19442=CARTESIAN_POINT ( 'NONE',  ( 15.09836989202466384, -7.705191364866749382, -37.25066627595537483 ) ) ;
#19443=CARTESIAN_POINT ( 'NONE',  ( 19.54194828133133299, -21.52908873155781677, -70.78615563984314463 ) ) ;
#19453=CARTESIAN_POINT ( 'NONE',  ( 22.72481302302869821, -17.38742434606708187, -58.53615329005432244 ) ) ;
#19462=EDGE_CURVE ( 'NONE', #27459, #34702, #7372, .T. ) ;
#19464=CARTESIAN_POINT ( 'NONE',  ( 24.37106953178879820, -15.98036188512979727, -31.80638701630159915 ) ) ;
#19465=B_SPLINE_CURVE_WITH_KNOTS ( 'NONE', 3,
 ( #32780, #16562, #7940, #82, #32263, #20743, #23887, #4007, #16054, #36470, #576, #8976, #32009, #12134, #44605, #8713, #24663, #9998 ),
 .UNSPECIFIED., .F., .F.,
 ( 4, 2, 2, 2, 2, 2, 2, 2, 4 ),
 ( 0.000000000000000000, 0.06250003597552350465, 0.1250000719510470093, 0.1875001079265705139, 0.2500001439020940186, 0.3125001798776175232, 0.3750002158531410279, 0.4375002518286645325, 0.5000002878041880372 ),
 .UNSPECIFIED. ) ;
#19468=B_SPLINE_CURVE_WITH_KNOTS ( 'NONE', 3,
 ( #37555, #18415, #17653, #29682, #38084, #9792, #21821, #38342, #34389, #26008, #30719 ),
 .UNSPECIFIED., .F., .F.,
 ( 4, 1, 1, 1, 1, 1, 1, 1, 4 ),
 ( 0.4999981796106400811, 0.5054020672895994659, 0.5846209983532170140, 0.6638399294168356723, 0.7430588604804532205, 0.8222777915440718788, 0.9014967226076894269, 0.9807156536713079742, 1.000000000000000000 ),
 .UNSPECIFIED. ) ;
#19470=CARTESIAN_POINT ( 'NONE',  ( 12.72598990436487298, -9.703252614503353968, -63.78615428896809902 ) ) ;
#19472=CARTESIAN_POINT ( 'NONE',  ( 10.89975959942620065, -9.768956234441111164, -75.28008627968870314 ) ) ;
#19475=CARTESIAN_POINT ( 'NONE',  ( 24.04485091158800003, -15.61618876680915236, -45.79233931912149558 ) ) ;
#19478=CARTESIAN_POINT ( 'NONE',  ( 22.69111796763029787, -10.61757876961529945, -45.30034255656079978 ) ) ;
#19479=ORIENTED_EDGE ( 'NONE', *, *, #32909, .F. ) ;
#19489=EDGE_CURVE ( 'NONE', #41648, #33306, #3461, .T. ) ;
#19503=CARTESIAN_POINT ( 'NONE',  ( 12.54931810734220043, -9.084941063794440552, -66.40756600056330683 ) ) ;
#19508=CARTESIAN_POINT ( 'NONE',  ( 22.90092240734290385, -15.63158582780186912, -34.45354257009029908 ) ) ;
#19511=CARTESIAN_POINT ( 'NONE',  ( 12.01177931914589969, -9.122389888939819613, -81.23899999999999011 ) ) ;
#19512=ORIENTED_EDGE ( 'NONE', *, *, #19095, .F. ) ;
#19516=ORIENTED_EDGE ( 'NONE', *, *, #49462, .T. ) ;
#19518=CARTESIAN_POINT ( 'NONE',  ( 23.60199757122739683, -15.03637316203499985, -81.23899999999999011 ) ) ;
#19520=ORIENTED_EDGE ( 'NONE', *, *, #28279, .F. ) ;
#19522=CARTESIAN_POINT ( 'NONE',  ( 24.04500464303940888, -15.61618902416171295, -53.50766607493442706 ) ) ;
#19523=VERTEX_POINT ( 'NONE', #5001 ) ;
#19529=CARTESIAN_POINT ( 'NONE',  ( 8.305413682485042415, -16.92329869104723628, -50.45504831420910108 ) ) ;
#19530=AXIS2_PLACEMENT_3D ( 'NONE', #26394, #22466, #38475 ) ;
#19536=DIRECTION ( 'NONE',  ( 1.000000000000000000, 0.000000000000000000, 0.000000000000000000 ) ) ;
#19537=DIRECTION ( 'NONE',  ( 1.062456999999999985E-16, -7.719205000000000365E-17, 1.000000000000000000 ) ) ;
#19538=CARTESIAN_POINT ( 'NONE',  ( 14.50756117850610138, -23.29353539881530111, -55.85395427856200001 ) ) ;
#19547=FACE_OUTER_BOUND ( 'NONE', #33427, .T. ) ;
#19550=CARTESIAN_POINT ( 'NONE',  ( 23.62715585835232091, -12.99531037559654401, -45.40052716342902528 ) ) ;
#19553=CARTESIAN_POINT ( 'NONE',  ( 9.807847918142682531, -20.47796416623571858, -38.29933577761543262 ) ) ;
#19556=ORIENTED_EDGE ( 'NONE', *, *, #25510, .T. ) ;
#19558=CARTESIAN_POINT ( 'NONE',  ( 22.32658188330890070, -19.75839229714189926, -37.25499936915149135 ) ) ;
#19560=VECTOR ( 'NONE', #19853, 1000.000000000000000 ) ;
#19574=DIRECTION ( 'NONE',  ( 1.000000000000000000, 0.000000000000000000, 0.000000000000000000 ) ) ;
#19575=CARTESIAN_POINT ( 'NONE',  ( 24.04460491192063998, -15.61619351124008404, -49.79233069347445451 ) ) ;
#19584=CARTESIAN_POINT ( 'NONE',  ( 11.90533122472848149, -10.27749421695417986, -45.73977238055704220 ) ) ;
#19592=CARTESIAN_POINT ( 'NONE',  ( 12.72379725809246587, -9.735079474130024835, -33.78566920041453159 ) ) ;
#19594=CARTESIAN_POINT ( 'NONE',  ( 8.572820610417089426, -13.51469887315669993, -53.09878558187529052 ) ) ;
#19602=CARTESIAN_POINT ( 'NONE',  ( 9.366950684753225786, -16.50208444525215867, -39.41115367992199481 ) ) ;
#19603=CARTESIAN_POINT ( 'NONE',  ( 16.05499536011179984, -8.563790251386850017, -50.34361688518850286 ) ) ;
#19609=DIRECTION ( 'NONE',  ( 1.000000000000000000, 2.460964292799963328E-14, 0.000000000000000000 ) ) ;
#19610=CARTESIAN_POINT ( 'NONE',  ( 24.04461900158476340, -15.61617122039998051, -49.50766513674645353 ) ) ;
#19611=CARTESIAN_POINT ( 'NONE',  ( 11.97520979020713128, -10.20491147569583923, -75.74446850450661373 ) ) ;
#19628=CARTESIAN_POINT ( 'NONE',  ( 23.05415186443769926, -14.25486957328740090, -56.39099290546759846 ) ) ;
#19635=CARTESIAN_POINT ( 'NONE',  ( 8.657171726495921149, -18.00045471869519886, -46.18924468880049972 ) ) ;
#19646=DIRECTION ( 'NONE',  ( 1.000000000000000000, 2.460964292799963328E-14, 0.000000000000000000 ) ) ;
#19653=CARTESIAN_POINT ( 'NONE',  ( 9.807770640268937967, -20.47786500802574849, -36.29933452872364796 ) ) ;
#19656=CARTESIAN_POINT ( 'NONE',  ( 9.366931599644679807, -15.61636246440640008, -63.84717978381009118 ) ) ;
#19657=CARTESIAN_POINT ( 'NONE',  ( 7.988116397819459813, -14.34013240443429993, -72.84179330725640966 ) ) ;
#19664=CARTESIAN_POINT ( 'NONE',  ( 13.49502580069180091, -8.648919796128959447, -63.61740952279680528 ) ) ;
#19666=DIRECTION ( 'NONE',  ( 0.000000000000000000, 0.000000000000000000, -1.000000000000000000 ) ) ;
#19671=CARTESIAN_POINT ( 'NONE',  ( 24.29887580492210120, -14.46879994560240057, -77.46322856839019266 ) ) ;
#19690=CARTESIAN_POINT ( 'NONE',  ( 8.968719396631879448, -17.65735158387520087, -79.14432001126618843 ) ) ;
#19695=CARTESIAN_POINT ( 'NONE',  ( 22.90093739769620029, -15.61618894467913243, -28.45282021618999835 ) ) ;
#19698=CARTESIAN_POINT ( 'NONE',  ( 22.90034302961675294, -15.71306413766174614, -40.45738043218361213 ) ) ;
#19704=DIRECTION ( 'NONE',  ( 1.000000000000000000, 2.460964292799963328E-14, 0.000000000000000000 ) ) ;
#19706=EDGE_CURVE ( 'NONE', #11854, #1665, #36367, .T. ) ;
#19708=CARTESIAN_POINT ( 'NONE',  ( 13.73800010538356453, -9.266389088679069630, -65.83795360124345564 ) ) ;
#19710=ORIENTED_EDGE ( 'NONE', *, *, #18831, .T. ) ;
#19711=CARTESIAN_POINT ( 'NONE',  ( 9.205734167420699166, -27.61618894467930119, -32.14999999999999858 ) ) ;
#19715=DIRECTION ( 'NONE',  ( -0.4999999999999998890, -0.8660254037844387076, 0.000000000000000000 ) ) ;
#19716=CARTESIAN_POINT ( 'NONE',  ( 16.10561099735067714, -23.52714547073744100, -78.00881095716772506 ) ) ;
#19718=CARTESIAN_POINT ( 'NONE',  ( 15.58086402661377257, -22.40678867047189726, -80.97851386839785448 ) ) ;
#19721=CARTESIAN_POINT ( 'NONE',  ( 24.01926528025970242, -18.02540546471280081, -39.88671798479069963 ) ) ;
#19723=CARTESIAN_POINT ( 'NONE',  ( 11.05733698530690745, -21.71889251823660771, -50.51310250095467325 ) ) ;
#19726=CARTESIAN_POINT ( 'NONE',  ( 15.77765653362640030, -23.45581977383699979, -70.52695041587149660 ) ) ;
#19731=CIRCLE ( 'NONE', #4644, 3.076499999999999346 ) ;
#19734=DIRECTION ( 'NONE',  ( 1.000000000000000000, 2.460964292799963328E-14, 0.000000000000000000 ) ) ;
#19735=CARTESIAN_POINT ( 'NONE',  ( 7.952298879402861509, -14.59466465962590043, -40.54720669274369982 ) ) ;
#19744=CARTESIAN_POINT ( 'NONE',  ( 9.221463679254590318, -19.60040485680393729, -38.62566536316489874 ) ) ;
#19745=AXIS2_PLACEMENT_3D ( 'NONE', #7018, #51031, #38990 ) ;
#19751=CARTESIAN_POINT ( 'NONE',  ( 23.83903639717342671, -13.54550718029785905, -61.70899533148040206 ) ) ;
#19755=CARTESIAN_POINT ( 'NONE',  ( 17.16940049168541549, -7.705176891496546610, -75.33404972303934244 ) ) ;
#19756=CARTESIAN_POINT ( 'NONE',  ( 10.22099471833763396, -19.02412705075455790, -63.28615105807855201 ) ) ;
#19758=B_SPLINE_CURVE_WITH_KNOTS ( 'NONE', 3,
 ( #4335, #36554, #33131, #32344, #48363, #12460, #24480, #16642, #48630, #49157, #26565, #33908, #21858, #34689, #46779, #13761, #42056, #1963 ),
 .UNSPECIFIED., .F., .F.,
 ( 4, 2, 2, 2, 2, 2, 2, 2, 4 ),
 ( 0.000000000000000000, 0.06250017132677161691, 0.1250003426535432338, 0.1875005139803148646, 0.2500006853070864676, 0.3125008566338578486, 0.3750010279606292851, 0.4375011992874006661, 0.5000013706141720471 ),
 .UNSPECIFIED. ) ;
#19759=CARTESIAN_POINT ( 'NONE',  ( 15.61994416393740082, -8.183658736601330475, -60.54536510185550213 ) ) ;
#19764=CARTESIAN_POINT ( 'NONE',  ( 9.447966713677070416, -16.81209814564785177, -35.39653371675596105 ) ) ;
#19766=CYLINDRICAL_SURFACE ( 'NONE', #11476, 2.576499999999998902 ) ;
#19769=CARTESIAN_POINT ( 'NONE',  ( 9.059951416200188845, -13.96889917543390069, -81.23899999999999011 ) ) ;
#19777=CARTESIAN_POINT ( 'NONE',  ( 23.48321685645310097, -16.39228337977660033, -81.23899999999999011 ) ) ;
#19778=ORIENTED_EDGE ( 'NONE', *, *, #40805, .F. ) ;
#19789=CONICAL_SURFACE ( 'NONE', #41524, 12.92820323027549989, 0.7481802937784480800 ) ;
#19796=CARTESIAN_POINT ( 'NONE',  ( 14.72053854714293664, -22.52595470508762077, -39.41140439840920351 ) ) ;
#19797=CARTESIAN_POINT ( 'NONE',  ( 9.531576907524980768, -11.37406870345459886, -66.46929104108710362 ) ) ;
#19811=VECTOR ( 'NONE', #23071, 1000.000000000000000 ) ;
#19813=CARTESIAN_POINT ( 'NONE',  ( 12.14975734981553757, -8.703693278909492292, -71.12565168373707536 ) ) ;
#19815=CARTESIAN_POINT ( 'NONE',  ( 21.75386501390569904, -10.72506351928820045, -38.83937799042379879 ) ) ;
#19818=CARTESIAN_POINT ( 'NONE',  ( 8.223295469878840080, -15.61636541503349918, -58.79233150823709764 ) ) ;
#19826=CARTESIAN_POINT ( 'NONE',  ( 22.46012283054650638, -10.75453872237786612, -67.29933293715515674 ) ) ;
#19830=CARTESIAN_POINT ( 'NONE',  ( 9.366553929154591174, -16.71943377812493736, -59.79527010610524940 ) ) ;
#19844=CARTESIAN_POINT ( 'NONE',  ( 22.78876382550086532, -14.33000611521636003, -34.39203900008635628 ) ) ;
#19846=CARTESIAN_POINT ( 'NONE',  ( 23.96158271707849963, -15.05519309305950060, -51.98972054698459289 ) ) ;
#19853=DIRECTION ( 'NONE',  ( 0.000000000000000000, 0.000000000000000000, -1.000000000000000000 ) ) ;
#19854=CARTESIAN_POINT ( 'NONE',  ( 20.48068097648700103, -21.17032068912790166, -51.13580619582469922 ) ) ;
#19861=CARTESIAN_POINT ( 'NONE',  ( 9.221470195977161666, -11.63196189502579792, -46.67433538954914241 ) ) ;
#19878=CARTESIAN_POINT ( 'NONE',  ( 12.06803212418919991, -9.853292710710359614, -55.75724145695859590 ) ) ;
#19883=CARTESIAN_POINT ( 'NONE',  ( 8.421582175205850618, -17.06750734713569884, -42.22829813561959611 ) ) ;
#19888=CARTESIAN_POINT ( 'NONE',  ( 8.222911740864116581, -16.65154857562174229, -40.75066691665454499 ) ) ;
#19890=CARTESIAN_POINT ( 'NONE',  ( 9.367435715182674372, -16.15063196774820398, -67.82204709561700895 ) ) ;
#19891=ORIENTED_EDGE ( 'NONE', *, *, #22875, .F. ) ;
#19896=DIRECTION ( 'NONE',  ( 0.000000000000000000, 0.000000000000000000, 1.000000000000000000 ) ) ;
#19897=CARTESIAN_POINT ( 'NONE',  ( 22.02679469870373552, -10.29530854175601640, -77.27397928379470216 ) ) ;
#19899=CARTESIAN_POINT ( 'NONE',  ( 19.53423428272744999, -8.449927945536709117, -49.14865470901539624 ) ) ;
#19906=CARTESIAN_POINT ( 'NONE',  ( 23.37973582986149879, -11.68158284795669921, -73.63398261789259891 ) ) ;
#19907=B_SPLINE_CURVE_WITH_KNOTS ( 'NONE', 3,
 ( #47827, #4302, #11932, #31295, #20273, #12430, #36266, #43381, #20017, #27885, #23687, #11670, #43891, #7984, #11416, #23936, #12179, #51500 ),
 .UNSPECIFIED., .F., .F.,
 ( 4, 2, 2, 2, 2, 2, 2, 2, 4 ),
 ( 0.4999999940960141998, 0.5624999948340123623, 0.6249999955720106914, 0.6874999963100087985, 0.7499999970480071276, 0.8124999977860052347, 0.8749999985240035638, 0.9374999992620016709, 1.000000000000000000 ),
 .UNSPECIFIED. ) ;
#19909=FACE_OUTER_BOUND ( 'NONE', #8784, .T. ) ;
#19911=VECTOR ( 'NONE', #15052, 1000.000000000000000 ) ;
#19913=CARTESIAN_POINT ( 'NONE',  ( 23.46275231366020364, -16.95602689483970238, -60.29021441812479765 ) ) ;
#19914=CARTESIAN_POINT ( 'NONE',  ( 9.367509928541279507, -15.61618483373539767, -35.84717978380999881 ) ) ;
#19918=B_SPLINE_CURVE_WITH_KNOTS ( 'NONE', 3,
 ( #47098, #39481, #11700, #39729, #23716, #26894, #38968, #51273, #31836, #23199 ),
 .UNSPECIFIED., .F., .F.,
 ( 4, 2, 2, 2, 4 ),
 ( 0.000000000000000000, 0.2500000000000000000, 0.5000000000000000000, 0.7500000000000000000, 1.000000000000000000 ),
 .UNSPECIFIED. ) ;
#19921=CARTESIAN_POINT ( 'NONE',  ( 22.60509562802760186, -20.72567344578009951, -75.72041208499069853 ) ) ;
#19934=CARTESIAN_POINT ( 'NONE',  ( 8.222734977135019108, -15.61599928274970139, -66.79233150823698395 ) ) ;
#19937=CARTESIAN_POINT ( 'NONE',  ( 21.28035516724290233, -21.00331043453270397, -72.48992980192200264 ) ) ;
#19942=ORIENTED_EDGE ( 'NONE', *, *, #39986, .F. ) ;
#19943=CARTESIAN_POINT ( 'NONE',  ( 5.741632552282960766, -9.616188944679340267, -22.14999999999999858 ) ) ;
#19945=CARTESIAN_POINT ( 'NONE',  ( 9.367504675961500382, -15.61621390379479912, -67.84717978381009118 ) ) ;
#19957=CARTESIAN_POINT ( 'NONE',  ( 8.223401571539490362, -15.61634053766229968, -58.50766849176299900 ) ) ;
#19958=CARTESIAN_POINT ( 'NONE',  ( 10.23658038545237758, -12.23234384576881695, -49.61855340168781936 ) ) ;
#19965=CARTESIAN_POINT ( 'NONE',  ( 12.65588489087358859, -22.74937664833755591, -50.43664658305362991 ) ) ;
#19966=ADVANCED_FACE ( 'NONE', ( #37937 ), #26634, .T. ) ;
#19969=CARTESIAN_POINT ( 'NONE',  ( 13.85267124424349916, -8.523762100343390102, -37.63360013392959758 ) ) ;
#19978=CARTESIAN_POINT ( 'NONE',  ( 11.63731196220440012, -22.52727282507490258, -44.19127752167019452 ) ) ;
#19982=CARTESIAN_POINT ( 'NONE',  ( 20.83810373529012239, -22.00309413542400350, -39.80555329850007240 ) ) ;
#19988=CYLINDRICAL_SURFACE ( 'NONE', #23941, 7.910999999999997812 ) ;
#19993=CARTESIAN_POINT ( 'NONE',  ( 23.04646698902364221, -11.63206944219079908, -61.62566225664009067 ) ) ;
#20001=CARTESIAN_POINT ( 'NONE',  ( 14.06336284780051216, -7.911061850705019438, -72.92433486291146494 ) ) ;
#20006=CARTESIAN_POINT ( 'NONE',  ( 22.90100569266936148, -15.61618883250986300, -34.84718217067427304 ) ) ;
#20009=CARTESIAN_POINT ( 'NONE',  ( 10.82420443828550027, -10.21340657480750025, -81.23899999999999011 ) ) ;
#20013=B_SPLINE_CURVE_WITH_KNOTS ( 'NONE', 3,
 ( #29133, #12917, #45133, #4511, #48810, #37269, #28873, #44874, #25448, #1367, #24925, #40937, #5049, #17357, #49336, #22036, #46441, #30164, #46702, #42763, #50614, #45914, #50095, #14708, #38048, #10002, #22812, #34874, #1885, #46182, #41979, #30678, #30418, #2142, #14450, #18122, #10529, #34087, #10269, #25968, #45651, #2921, #18635, #6081, #9749, #37788, #10788, #14194, #26748, #26487, #18890, #29644, #49847, #22554, #13686, #13939, #18370, #26229, #42237, #34351, #38303, #6860, #6591, #25706, #38831, #38568, #41709, #5819, #21782, #50362, #33833, #17862, #29895, #6335, #22296, #42502, #2663, #34611, #39341, #26, #3442, #43529, #23069, #35906, #47975, #15999, #7369, #31952, #27782, #27266, #27522, #3955, #3697, #12076, #7882, #8137, #23829, #51647, #28031, #30934, #23574, #15233, #46963, #44034, #43779, #7630, #19152, #35131, #24082, #47719, #4196, #40102 ),
 .UNSPECIFIED., .F., .F.,
 ( 4, 3, 3, 3, 3, 3, 3, 3, 3, 3, 3, 3, 3, 3, 3, 3, 3, 3, 3, 3, 3, 3, 3, 3, 3, 3, 3, 3, 3, 3, 3, 3, 3, 3, 3, 3, 3, 4 ),
 ( -1.533736992487430006, -1.476288708613070044, -1.420671477261239879, -1.384064776590339996, -1.360357240506639975, -1.351866780710969884, -1.295064170024950112, -1.237933401408560119, -1.182875636651279816, -1.170176689418420013, -1.162728782331990063, -1.127817871893999957, -1.070863257187619988, -1.013122308480070011, -0.9549592363170329445, -0.9075319312463639987, -0.8918603899297049553, -0.8833676294135619500, -0.8240633864161019950, -0.7652500160343579383, -0.7062545595011729960, -0.6468558895549011423, -0.6146511525544209320, -0.6051427578306090016, -0.5954651251075159246, -0.5353212642531580689, -0.4746770572283909306, -0.4139650854173051453, -0.3892179935510600153, -0.3405657443571770138, -0.3192803853348540333, -0.3088845139008700169, -0.2992958171375259546, -0.2386551958669829165, -0.1768310421685470590, -0.1147878079956350383, -0.05320815132276890402, 0.000000000000000000 ),
 .UNSPECIFIED. ) ;
#20015=LINE ( 'NONE', #48597, #51154 ) ;
#20016=CARTESIAN_POINT ( 'NONE',  ( 22.75210022221799733, -11.58476054589980109, -81.23899999999999011 ) ) ;
#20017=CARTESIAN_POINT ( 'NONE',  ( 17.16956915081890500, -7.705200979555163698, -73.33399818129967684 ) ) ;
#20025=EDGE_LOOP ( 'NONE', ( #25752, #5471, #18010, #43687 ) ) ;
#20031=CARTESIAN_POINT ( 'NONE',  ( 22.61700722620988202, -13.63405001173012288, -40.35842241976454403 ) ) ;
#20041=CARTESIAN_POINT ( 'NONE',  ( 21.41930692131999692, -9.815187549925822097, -59.02271152110689911 ) ) ;
#20043=CARTESIAN_POINT ( 'NONE',  ( 16.13393739769620083, -15.61618894467929941, -32.14999999999999858 ) ) ;
#20048=EDGE_CURVE ( 'NONE', #10051, #27800, #27677, .T. ) ;
#20060=CARTESIAN_POINT ( 'NONE',  ( 22.94551214130139982, -13.78743987096419943, -80.76368641361828793 ) ) ;
#20079=CARTESIAN_POINT ( 'NONE',  ( 20.99563212089781672, -9.290037028488647763, -79.50066649059343149 ) ) ;
#20097=CARTESIAN_POINT ( 'NONE',  ( 21.20676518767113805, -11.08013655934608011, -34.22047514491094233 ) ) ;
#20100=CARTESIAN_POINT ( 'NONE',  ( 21.83940206608119894, -10.22782922122060079, -49.77159047720319762 ) ) ;
#20107=CARTESIAN_POINT ( 'NONE',  ( 23.01451526111969770, -17.16544923262910061, -48.91767612604338922 ) ) ;
#20108=CARTESIAN_POINT ( 'NONE',  ( 15.09849613828851389, -7.705176109998896905, -41.25066457774981643 ) ) ;
#20112=CARTESIAN_POINT ( 'NONE',  ( 8.428840728337423371, -13.54549715867946347, -36.59100207277058558 ) ) ;
#20113=CYLINDRICAL_SURFACE ( 'NONE', #15425, 6.766999999999998572 ) ;
#20117=CARTESIAN_POINT ( 'NONE',  ( 22.90093741582260378, -14.73038773615894215, -76.41114510696804984 ) ) ;
#20118=AXIS2_PLACEMENT_3D ( 'NONE', #2654, #18624, #30666 ) ;
#20121=CARTESIAN_POINT ( 'NONE',  ( 9.807799258745877324, -20.47790172817659737, -52.58399763662833948 ) ) ;
#20122=DIRECTION ( 'NONE',  ( 1.000000000000000000, 0.000000000000000000, 0.000000000000000000 ) ) ;
#20128=CARTESIAN_POINT ( 'NONE',  ( 22.90093739792275684, -16.50198059704664999, -74.49448689417269520 ) ) ;
#20133=CARTESIAN_POINT ( 'NONE',  ( 19.26073116756969839, -21.93803356609359767, -54.80661428419509917 ) ) ;
#20136=CARTESIAN_POINT ( 'NONE',  ( 20.06281976506910070, -10.10654536788180025, -32.14999999999999858 ) ) ;
#20137=EDGE_CURVE ( 'NONE', #1216, #17773, #43581, .T. ) ;
#20139=CARTESIAN_POINT ( 'NONE',  ( 10.72003978276549852, -9.934951333187338918, -42.54517385987399791 ) ) ;
#20140=ORIENTED_EDGE ( 'NONE', *, *, #35536, .T. ) ;
#20153=CARTESIAN_POINT ( 'NONE',  ( 24.04485979958176145, -15.65237997675253467, -43.79378099706513439 ) ) ;
#20156=CARTESIAN_POINT ( 'NONE',  ( 12.76029016835228980, -8.414235847234261101, -48.86834743904469036 ) ) ;
#20164=EDGE_CURVE ( 'NONE', #36469, #26214, #48121, .T. ) ;
#20165=CARTESIAN_POINT ( 'NONE',  ( 8.367277499166009491, -18.38416908848419951, -72.68335544512909507 ) ) ;
#20170=CARTESIAN_POINT ( 'NONE',  ( 10.81560779913390036, -10.39871215161140050, -69.47961042150450339 ) ) ;
#20172=CYLINDRICAL_SURFACE ( 'NONE', #28689, 6.766999999999998572 ) ;
#20177=CARTESIAN_POINT ( 'NONE',  ( 8.167756527346648809, -13.48952887549759971, -68.59070828926491004 ) ) ;
#20183=CARTESIAN_POINT ( 'NONE',  ( 24.04507396969289346, -15.61618901627517531, -67.50767071486835391 ) ) ;
#20189=CARTESIAN_POINT ( 'NONE',  ( 23.56462136197711388, -18.43314625579564137, -65.90774450879612800 ) ) ;
#20191=CARTESIAN_POINT ( 'NONE',  ( 8.772777754335070455, -16.76511127020750180, -75.18337345808529903 ) ) ;
#20198=EDGE_LOOP ( 'NONE', ( #41811, #36149, #26503, #5414 ) ) ;
#20199=CARTESIAN_POINT ( 'NONE',  ( 16.13393739769620083, -15.61618894467929941, -81.23899999999999011 ) ) ;
#20218=CARTESIAN_POINT ( 'NONE',  ( 18.70788766945040038, -21.92435149714031439, -80.82966465033948111 ) ) ;
#20220=CARTESIAN_POINT ( 'NONE',  ( 24.04369184426532513, -15.76790706435441614, -65.51376952231562711 ) ) ;
#20222=CARTESIAN_POINT ( 'NONE',  ( 23.43186596475139893, -19.45323972439200233, -41.94641019244489399 ) ) ;
#20229=CARTESIAN_POINT ( 'NONE',  ( 22.25441655865059687, -19.86429777632060123, -38.42578944456580103 ) ) ;
#20235=CARTESIAN_POINT ( 'NONE',  ( 24.18319539530660123, -13.82952546296830043, -39.43814165785290271 ) ) ;
#20239=CARTESIAN_POINT ( 'NONE',  ( 23.98346616282663035, -16.73315592963927756, -39.55263113089927884 ) ) ;
#20251=CARTESIAN_POINT ( 'NONE',  ( 19.54197537461858403, -21.52907253456916692, -64.78615502841283558 ) ) ;
#20259=CARTESIAN_POINT ( 'NONE',  ( 20.99566198266418482, -9.290060858646725706, -73.21600132271542805 ) ) ;
#20264=CARTESIAN_POINT ( 'NONE',  ( 10.44460050029429965, -10.68230576789959940, -81.23899999999999011 ) ) ;
#20268=ORIENTED_EDGE ( 'NONE', *, *, #24149, .F. ) ;
#20271=CARTESIAN_POINT ( 'NONE',  ( 18.64696929856319940, -21.92391060386649926, -81.23899999999999011 ) ) ;
#20272=CARTESIAN_POINT ( 'NONE',  ( 8.223487313465298598, -15.61606829411550024, -62.50766849176299189 ) ) ;
#20273=CARTESIAN_POINT ( 'NONE',  ( 22.46012461926354220, -10.75454118387916580, -73.58399818425169769 ) ) ;
#20274=CARTESIAN_POINT ( 'NONE',  ( 9.366420286904855175, -15.72757149194933035, -69.84194449815306882 ) ) ;
#20276=VERTEX_POINT ( 'NONE', #5398 ) ;
#20288=B_SPLINE_CURVE_WITH_KNOTS ( 'NONE', 3,
 ( #47109, #21486, #51285, #21741, #7009, #7261, #19042, #17824, #10939, #35018, #11198, #15123, #25926, #21998, #49561, #37485, #23211, #33798 ),
 .UNSPECIFIED., .F., .F.,
 ( 4, 2, 2, 2, 2, 2, 2, 2, 4 ),
 ( 0.4999995031043945604, 0.5624995652163452542, 0.6249996273282960590, 0.6874996894402467529, 0.7499997515521974467, 0.8124998136641481405, 0.8749998757760988344, 0.9374999378880493062, 1.000000000000000000 ),
 .UNSPECIFIED. ) ;
#20295=CARTESIAN_POINT ( 'NONE',  ( 8.286499081069370831, -15.54940533950840020, -60.29021441812479765 ) ) ;
#20307=CARTESIAN_POINT ( 'NONE',  ( 12.91854708852280176, -27.61618894467928698, -22.14999999999998792 ) ) ;
#20311=ADVANCED_FACE ( 'NONE', ( #17446 ), #37358, .T. ) ;
#20312=CARTESIAN_POINT ( 'NONE',  ( 14.64089083101909949, -22.91533316082380267, -39.63156730105999515 ) ) ;
#20321=EDGE_CURVE ( 'NONE', #33243, #40988, #7279, .T. ) ;
#20323=CARTESIAN_POINT ( 'NONE',  ( 8.223605785152290792, -15.61620117245469963, -52.50766849176299900 ) ) ;
#20329=CARTESIAN_POINT ( 'NONE',  ( 16.13393739769620083, -15.61618894467929941, -28.45282021618999835 ) ) ;
#20337=CARTESIAN_POINT ( 'NONE',  ( 9.221328447382354909, -19.60017377966054397, -56.34096481581358518 ) ) ;
#20338=CARTESIAN_POINT ( 'NONE',  ( 14.88857959731166503, -8.720501068069950179, -32.29061302249797905 ) ) ;
#20341=CARTESIAN_POINT ( 'NONE',  ( 24.01953165718990846, -14.96959786440184104, -59.76628937629125460 ) ) ;
#20344=EDGE_LOOP ( 'NONE', ( #43071, #14458, #24280, #51614 ) ) ;
#20349=CARTESIAN_POINT ( 'NONE',  ( 19.05258302078599897, -8.331392769191539927, -55.63379137591120127 ) ) ;
#20358=CARTESIAN_POINT ( 'NONE',  ( 18.57770503654679928, -22.23212114670179673, -49.23455185029789760 ) ) ;
#20360=VERTEX_POINT ( 'NONE', #26064 ) ;
#20365=CARTESIAN_POINT ( 'NONE',  ( 15.24812203796652277, -8.849191014885372297, -37.91115498390873739 ) ) ;
#20372=CARTESIAN_POINT ( 'NONE',  ( 18.20469047841077170, -23.32126825782679092, -73.92433474470422539 ) ) ;
#20377=VERTEX_POINT ( 'NONE', #1457 ) ;
#20379=CARTESIAN_POINT ( 'NONE',  ( 9.366958054073847961, -16.50213838875509609, -75.41115355001534226 ) ) ;
#20383=CARTESIAN_POINT ( 'NONE',  ( 23.12781470739479772, -14.70611264375299854, -62.41163166630270354 ) ) ;
#20389=B_SPLINE_CURVE_WITH_KNOTS ( 'NONE', 3,
 ( #2025, #14077, #49223, #17495, #5453, #33462, #29533, #38186, #1766, #30038, #46061, #42118, #9633, #25589, #41594, #5703, #33717, #49731, #13820, #19296, #19550, #11189, #51534, #26627, #51276, #10671, #42643, #10929, #42903, #43410, #38443, #47604, #14591, #3062, #50759, #23202 ),
 .UNSPECIFIED., .F., .F.,
 ( 4, 2, 2, 2, 2, 2, 2, 2, 2, 2, 2, 2, 2, 1, 1, 1, 1, 1, 1, 2, 4 ),
 ( 0.000000000000000000, 0.06250066402867544835, 0.1250013280573508967, 0.1875019920860263312, 0.2500026561147017934, 0.3125033201433771723, 0.3437536521577148063, 0.3750039841720524403, 0.4062543161863901298, 0.4375046482007277637, 0.4687549802150655087, 0.4843801462222342979, 0.4921927292258187481, 0.4960990207276109731, 0.4980521664785070857, 0.4990287393539551419, 0.4995170257916792256, 0.4997611690105412396, 0.4998832406199723022, 0.4999442764246878057, 0.5000053122294032537 ),
 .UNSPECIFIED. ) ;
#20391=B_SPLINE_CURVE_WITH_KNOTS ( 'NONE', 3,
 ( #25682, #2638, #22784, #49574, #9976, #29621, #30393, #29869, #30134, #22529, #34323, #45623, #9723, #14424, #46416, #42475, #41684, #5792 ),
 .UNSPECIFIED., .F., .F.,
 ( 4, 2, 2, 2, 2, 2, 2, 2, 4 ),
 ( 0.4999961870157385579, 0.5624966636387712660, 0.6249971402618039740, 0.6874976168848365710, 0.7499980935078692790, 0.8124985701309019870, 0.8749990467539345840, 0.9374995233769672920, 1.000000000000000000 ),
 .UNSPECIFIED. ) ;
#20398=CYLINDRICAL_SURFACE ( 'NONE', #32598, 7.910999999999997812 ) ;
#20400=CARTESIAN_POINT ( 'NONE',  ( 9.807693316221877566, -10.75461209725539469, -74.71598022707215137 ) ) ;
#20407=CARTESIAN_POINT ( 'NONE',  ( 8.222936768550598075, -16.65173181358981580, -36.46600169915504353 ) ) ;
#20411=CARTESIAN_POINT ( 'NONE',  ( 11.42785662796539903, -8.845995162762550379, -71.09897682385680184 ) ) ;
#20412=CARTESIAN_POINT ( 'NONE',  ( 16.13393739769620083, -15.61618894467929941, -28.45282021618999835 ) ) ;
#20413=DIRECTION ( 'NONE',  ( -0.000000000000000000, 1.000000000000000000, 0.000000000000000000 ) ) ;
#20417=CARTESIAN_POINT ( 'NONE',  ( 22.87580916398269792, -12.44540688151340113, -64.09272310917850746 ) ) ;
#20421=EDGE_CURVE ( 'NONE', #12364, #33243, #14199, .T. ) ;
#20429=B_SPLINE_CURVE_WITH_KNOTS ( 'NONE', 3,
 ( #44513, #49497, #41102, #13584, #9403, #44251, #1008, #12818, #32688, #20911, #4420, #24565, #40579, #25091, #20648, #36634, #736, #45294 ),
 .UNSPECIFIED., .F., .F.,
 ( 4, 2, 2, 2, 2, 2, 2, 2, 4 ),
 ( 0.000000000000000000, 0.06249985449796188752, 0.1249997089959237750, 0.1874995634938856626, 0.2499994179918475501, 0.3124992724898094654, 0.3749991269877713251, 0.4374989814857331849, 0.4999988359836951002 ),
 .UNSPECIFIED. ) ;
#20430=CARTESIAN_POINT ( 'NONE',  ( 16.91175549567909897, -23.82458219277760492, -73.97759560159089176 ) ) ;
#20438=ORIENTED_EDGE ( 'NONE', *, *, #20048, .F. ) ;
#20441=CARTESIAN_POINT ( 'NONE',  ( 24.04496217889941789, -15.61618911842929869, -37.79232902657031445 ) ) ;
#20443=CARTESIAN_POINT ( 'NONE',  ( 9.272726169787338435, -17.24908183236129844, -37.37844945019890019 ) ) ;
#20446=ADVANCED_FACE ( 'NONE', ( #42335 ), #45503, .F. ) ;
#20464=CARTESIAN_POINT ( 'NONE',  ( 8.222937397696199469, -15.61618894467929941, -32.14999999999999858 ) ) ;
#20467=CARTESIAN_POINT ( 'NONE',  ( 16.13393739769620083, -15.61618894467929941, -28.45282021618999835 ) ) ;
#20469=CARTESIAN_POINT ( 'NONE',  ( 20.24159734950449518, -10.16604498721250138, -50.15866389318657070 ) ) ;
#20472=CARTESIAN_POINT ( 'NONE',  ( 14.31997823940066183, -9.037193765400974854, -71.86747918995368423 ) ) ;
#20474=CARTESIAN_POINT ( 'NONE',  ( 23.95032869375090101, -12.99192768426819988, -43.68922667584449471 ) ) ;
#20480=CARTESIAN_POINT ( 'NONE',  ( 8.691576068919250275, -15.95962985236369924, -39.21797875520199739 ) ) ;
#20486=CARTESIAN_POINT ( 'NONE',  ( 20.74197122344288502, -22.13452925154505024, -60.09665985822703504 ) ) ;
#20489=CARTESIAN_POINT ( 'NONE',  ( 12.09455160279810038, -22.80410123608560014, -38.17063876083498997 ) ) ;
#20493=CARTESIAN_POINT ( 'NONE',  ( 23.76540053402172248, -17.76641857869638841, -39.59512095345433380 ) ) ;
#20494=FACE_OUTER_BOUND ( 'NONE', #38155, .T. ) ;
#20495=CARTESIAN_POINT ( 'NONE',  ( 19.82873695480376242, -9.608609115219810093, -56.52269350815382154 ) ) ;
#20496=CARTESIAN_POINT ( 'NONE',  ( 8.222872596472118545, -15.61638977992110000, -80.50766849176289952 ) ) ;
#20500=CARTESIAN_POINT ( 'NONE',  ( 22.90093741960866325, -16.50197990757633448, -48.49448879811394875 ) ) ;
#20504=CARTESIAN_POINT ( 'NONE',  ( 16.13393739769620083, -15.61618894467929941, -28.45282021618999835 ) ) ;
#20505=CARTESIAN_POINT ( 'NONE',  ( 14.36278465922390701, -22.20708669663512325, -65.03615447382929915 ) ) ;
#20509=CARTESIAN_POINT ( 'NONE',  ( 24.04424242478976836, -15.50292783389250317, -75.78776975939635463 ) ) ;
#20513=CARTESIAN_POINT ( 'NONE',  ( 23.83903859056454522, -13.54551801267896671, -73.42433450828966102 ) ) ;
#20514=CARTESIAN_POINT ( 'NONE',  ( 9.367442997458502063, -15.61610373232760018, -47.45282021618999835 ) ) ;
#20516=DIRECTION ( 'NONE',  ( 0.000000000000000000, 0.000000000000000000, 1.000000000000000000 ) ) ;
#20527=CARTESIAN_POINT ( 'NONE',  ( 21.63843781001559918, -20.05973176279620063, -81.23899999999999011 ) ) ;
#20535=CARTESIAN_POINT ( 'NONE',  ( 22.89998542976507778, -14.84672387926992343, -42.81098146774382940 ) ) ;
#20544=EDGE_CURVE ( 'NONE', #27800, #9084, #44828, .T. ) ;
#20550=CARTESIAN_POINT ( 'NONE',  ( 18.00830954542770002, -7.995593348861908645, -58.86427365897959163 ) ) ;
#20565=CARTESIAN_POINT ( 'NONE',  ( 11.49584328075813922, -22.05115804159764181, -34.20649648869382276 ) ) ;
#20567=EDGE_CURVE ( 'NONE', #26995, #41285, #42274, .T. ) ;
#20570=CARTESIAN_POINT ( 'NONE',  ( 21.11303220515950230, -10.07404953497180067, -42.80032454360480187 ) ) ;
#20578=CARTESIAN_POINT ( 'NONE',  ( 8.428822758898967038, -17.68681539623817400, -78.70899791345021868 ) ) ;
#20583=VERTEX_POINT ( 'NONE', #2093 ) ;
#20584=VERTEX_POINT ( 'NONE', #29596 ) ;
#20593=CARTESIAN_POINT ( 'NONE',  ( 12.14969237204626573, -22.52864793124346932, -56.17427643643699042 ) ) ;
#20605=CARTESIAN_POINT ( 'NONE',  ( 14.77119402760449951, -7.887691154108790847, -65.45693882779990247 ) ) ;
#20611=DIRECTION ( 'NONE',  ( 0.000000000000000000, 0.000000000000000000, -1.000000000000000000 ) ) ;
#20617=CARTESIAN_POINT ( 'NONE',  ( 9.807869143058068673, -10.75438648984616385, -41.00066472165191556 ) ) ;
#20626=CARTESIAN_POINT ( 'NONE',  ( 22.56027083402119970, -12.69968737826519956, -32.14999999999999858 ) ) ;
#20631=CARTESIAN_POINT ( 'NONE',  ( 22.46012192026008591, -20.47784040582451226, -73.71600126361178695 ) ) ;
#20637=CARTESIAN_POINT ( 'NONE',  ( 20.44176770788429920, -21.20055615977860342, -67.13803027067579876 ) ) ;
#20645=CARTESIAN_POINT ( 'NONE',  ( 9.852363362552399195, -18.82311681066459741, -61.30256663141189932 ) ) ;
#20648=CARTESIAN_POINT ( 'NONE',  ( 23.04647616065052773, -19.60029129190153441, -79.95900011493084492 ) ) ;
#20656=CARTESIAN_POINT ( 'NONE',  ( 11.27237402512278130, -21.94244088919472446, -64.21600230519077002 ) ) ;
#20658=VERTEX_POINT ( 'NONE', #43732 ) ;
#20671=CARTESIAN_POINT ( 'NONE',  ( 22.51625110737120039, -20.83622647014099982, -76.01055054980119507 ) ) ;
#20672=CARTESIAN_POINT ( 'NONE',  ( 22.71567673004141596, -17.77000726670902253, -64.94847198785556941 ) ) ;
#20676=CARTESIAN_POINT ( 'NONE',  ( 10.22103832233932863, -19.02420151566214912, -37.28615309265127564 ) ) ;
#20678=CARTESIAN_POINT ( 'NONE',  ( 19.34704915299079886, -8.894388095715280329, -61.87459303939719746 ) ) ;
#20686=CARTESIAN_POINT ( 'NONE',  ( 24.36963727833509807, -16.01111688394609800, -79.52292077604440124 ) ) ;
#20692=CARTESIAN_POINT ( 'NONE',  ( 22.46011490975228497, -10.75452786398427918, -79.29933665554652578 ) ) ;
#20701=CARTESIAN_POINT ( 'NONE',  ( 16.12703488906409888, -8.563351852316490209, -35.95250869105369418 ) ) ;
#20708=CARTESIAN_POINT ( 'NONE',  ( 22.90092414372679386, -15.63002194425144964, -40.45347516367851171 ) ) ;
#20709=CARTESIAN_POINT ( 'NONE',  ( 9.557636492705340103, -19.11746881714849877, -59.91161365334649958 ) ) ;
#20712=CARTESIAN_POINT ( 'NONE',  ( 22.90097009252848892, -15.61618913824531418, -68.84717732178738459 ) ) ;
#20726=CARTESIAN_POINT ( 'NONE',  ( 8.222373579151801337, -15.61629175287649929, -54.79233150823699816 ) ) ;
#20728=CARTESIAN_POINT ( 'NONE',  ( 16.13393739769620083, -15.61618894467929941, -28.45282021618999835 ) ) ;
#20737=CARTESIAN_POINT ( 'NONE',  ( 24.04486012107927806, -15.65397104612058143, -65.50918627229970070 ) ) ;
#20738=CARTESIAN_POINT ( 'NONE',  ( 13.82518338685379966, -23.53151426795909984, -46.38267033200749978 ) ) ;
#20743=CARTESIAN_POINT ( 'NONE',  ( 11.27235364543490803, -21.94242546894149370, -42.50066467368454681 ) ) ;
#20744=CARTESIAN_POINT ( 'NONE',  ( 22.93909306572350104, -18.64877037624530232, -36.36609723691169904 ) ) ;
#20752=CARTESIAN_POINT ( 'NONE',  ( 8.153091836570281359, -13.54524113306460009, -52.58848421441390286 ) ) ;
#20768=CARTESIAN_POINT ( 'NONE',  ( 8.222313118464692039, -15.61611924975770016, -60.79233150823699816 ) ) ;
#20769=DIRECTION ( 'NONE',  ( 0.000000000000000000, 0.000000000000000000, 1.000000000000000000 ) ) ;
#20774=CARTESIAN_POINT ( 'NONE',  ( 14.36265541453573924, -22.20705323002841780, -61.03617101396910982 ) ) ;
#20780=EDGE_CURVE ( 'NONE', #7094, #47210, #5383, .T. ) ;
#20785=EDGE_CURVE ( 'NONE', #11267, #19523, #12247, .T. ) ;
#20790=CARTESIAN_POINT ( 'NONE',  ( 20.76034935557600036, -20.84156012990780127, -81.23899999999999011 ) ) ;
#20791=EDGE_CURVE ( 'NONE', #2233, #6769, #662, .T. ) ;
#20794=VECTOR ( 'NONE', #30482, 1000.000000000000000 ) ;
#20797=CARTESIAN_POINT ( 'NONE',  ( 9.577107432962000289, -17.87109166221290835, -35.74113635354945728 ) ) ;
#20798=ORIENTED_EDGE ( 'NONE', *, *, #16426, .T. ) ;
#20804=B_SPLINE_CURVE_WITH_KNOTS ( 'NONE', 3,
 ( #21266, #40941, #32016, #37271, #5052, #28094, #44100, #40167, #36736, #16314, #8200, #32270, #20486, #21010, #16567, #32521, #36220, #37009, #1107, #24145, #4262, #48291, #12653, #32787, #28611, #44612, #8718, #842 ),
 .UNSPECIFIED., .F., .F.,
 ( 4, 2, 2, 2, 2, 2, 2, 2, 2, 2, 1, 1, 1, 1, 2, 4 ),
 ( 0.000000000000000000, 0.06250045878239399166, 0.1250009175647879833, 0.1875013763471820027, 0.2500018351295759667, 0.3125022939119698195, 0.3750027526943637279, 0.4375032114767576363, 0.4687534408679544518, 0.4843785555635529705, 0.4921911129113520911, 0.4960973915852517346, 0.4980505309222015842, 0.4990271005906765645, 0.4995153854249139713, 0.5000036702591513782 ),
 .UNSPECIFIED. ) ;
#20814=CARTESIAN_POINT ( 'NONE',  ( 23.89748173806130183, -14.46983495992219915, -61.24084159088819490 ) ) ;
#20831=EDGE_LOOP ( 'NONE', ( #32890, #39436, #32369, #12399 ) ) ;
#20832=CARTESIAN_POINT ( 'NONE',  ( 23.15495034093260074, -13.12378617039730067, -42.95876240573199567 ) ) ;
#20834=ORIENTED_EDGE ( 'NONE', *, *, #45538, .T. ) ;
#20840=CARTESIAN_POINT ( 'NONE',  ( 9.221384164938969619, -19.60026892670780896, -78.62566431866341077 ) ) ;
#20841=CARTESIAN_POINT ( 'NONE',  ( 15.64736352786460039, -8.580152770550549590, -60.32520219920449733 ) ) ;
#20843=ORIENTED_EDGE ( 'NONE', *, *, #20780, .F. ) ;
#20851=B_SPLINE_CURVE_WITH_KNOTS ( 'NONE', 3,
 ( #22421, #38424, #34476, #50485, #14575, #6122, #13476, #22078, #33875, #33361, #33622, #10047, #9796, #1407, #26274, #38088, #13730, #5860 ),
 .UNSPECIFIED., .F., .F.,
 ( 4, 2, 2, 2, 2, 2, 2, 2, 4 ),
 ( 0.5000009455475087350, 0.5625008273540701431, 0.6250007091606315512, 0.6875005909671929594, 0.7500004727737543675, 0.8125003545803157756, 0.8750002363868771837, 0.9375001181934385919, 1.000000000000000000 ),
 .UNSPECIFIED. ) ;
#20853=EDGE_LOOP ( 'NONE', ( #38611, #174, #28908 ) ) ;
#20855=CARTESIAN_POINT ( 'NONE',  ( 8.428790385332487034, -17.68669786356424112, -56.42431456789199018 ) ) ;
#20856=CARTESIAN_POINT ( 'NONE',  ( 14.21059016770981032, -7.922947056480517780, -76.92968709617039735 ) ) ;
#20867=CARTESIAN_POINT ( 'NONE',  ( 16.13816125998162931, -22.38318796325360438, -46.95262491913606340 ) ) ;
#20870=VECTOR ( 'NONE', #51478, 1000.000000000000000 ) ;
#20872=CARTESIAN_POINT ( 'NONE',  ( 10.85903228057479986, -9.805670585965609476, -59.27786220483749702 ) ) ;
#20875=CARTESIAN_POINT ( 'NONE',  ( 22.90093739769620029, -15.61618894467913243, -28.45282021618999835 ) ) ;
#20883=CARTESIAN_POINT ( 'NONE',  ( 8.223148984577919762, -15.61599292915740023, -40.79233150823699816 ) ) ;
#20888=CARTESIAN_POINT ( 'NONE',  ( 19.54191788466946633, -9.703270981965982145, -38.11948896923542662 ) ) ;
#20889=CARTESIAN_POINT ( 'NONE',  ( 22.90085274204890808, -15.61618877333890332, -76.84718755697707593 ) ) ;
#20891=CARTESIAN_POINT ( 'NONE',  ( 23.37921890642729750, -15.16088557610839871, -32.14999999999999858 ) ) ;
#20895=CARTESIAN_POINT ( 'NONE',  ( 8.223551834036749497, -15.61610457483330094, -62.79233150823698395 ) ) ;
#20900=CARTESIAN_POINT ( 'NONE',  ( 9.965766340832269421, -12.19621453136610079, -60.00832647495010264 ) ) ;
#20908=CARTESIAN_POINT ( 'NONE',  ( 20.34507489674630065, -21.27382799827049809, -68.74914615139218199 ) ) ;
#20911=CARTESIAN_POINT ( 'NONE',  ( 17.16956960005933297, -23.52717684783756269, -80.25066610258798505 ) ) ;
#20934=CARTESIAN_POINT ( 'NONE',  ( 8.564672508253739380, -12.34675523859029944, -80.92212427574548883 ) ) ;
#20937=EDGE_CURVE ( 'NONE', #41285, #37252, #4591, .T. ) ;
#20940=AXIS2_PLACEMENT_3D ( 'NONE', #26546, #22357, #18694 ) ;
#20945=CARTESIAN_POINT ( 'NONE',  ( 18.16448196509429991, -8.861961676679291244, -32.44013846481049512 ) ) ;
#20953=DIRECTION ( 'NONE',  ( 0.000000000000000000, 0.000000000000000000, -1.000000000000000000 ) ) ;
#20964=CARTESIAN_POINT ( 'NONE',  ( 15.26394330896870244, -8.617212663664730599, -39.91345524423469726 ) ) ;
#20972=CARTESIAN_POINT ( 'NONE',  ( 17.73920358962980259, -22.89147689717010081, -77.49821634947008420 ) ) ;
#20988=ORIENTED_EDGE ( 'NONE', *, *, #6203, .T. ) ;
#20993=CARTESIAN_POINT ( 'NONE',  ( 19.87062220799639789, -9.634571621335810576, -72.52491758300199365 ) ) ;
#20994=CARTESIAN_POINT ( 'NONE',  ( 23.04644962015954235, -11.63203690814193791, -59.34097683662206180 ) ) ;
#20995=CARTESIAN_POINT ( 'NONE',  ( 16.13393739769620083, -15.61618894467929941, -81.65000000000000568 ) ) ;
#21000=CARTESIAN_POINT ( 'NONE',  ( 23.99755426256392710, -16.50001052160837034, -65.54328182147770576 ) ) ;
#21001=CARTESIAN_POINT ( 'NONE',  ( 22.12835029666389985, -9.954940491146789583, -49.55142757455229940 ) ) ;
#21002=CARTESIAN_POINT ( 'NONE',  ( 14.60579227114195788, -8.963325624781994350, -55.88125799276141947 ) ) ;
#21004=EDGE_CURVE ( 'NONE', #51178, #1216, #28636, .T. ) ;
#21007=CARTESIAN_POINT ( 'NONE',  ( 8.941982268396820643, -13.67133028058830035, -37.31672440967518867 ) ) ;
#21010=CARTESIAN_POINT ( 'NONE',  ( 22.30441927812678671, -20.68056348242964049, -60.01079243619062709 ) ) ;
#21014=CARTESIAN_POINT ( 'NONE',  ( 11.26548663221610092, -8.961798825887671072, -54.80661428419509917 ) ) ;
#21015=ORIENTED_EDGE ( 'NONE', *, *, #1408, .F. ) ;
#21031=LINE ( 'NONE', #40191, #9039 ) ;
#21033=CARTESIAN_POINT ( 'NONE',  ( 22.80556477356921263, -16.78781406865223502, -66.50815379053354093 ) ) ;
#21035=CARTESIAN_POINT ( 'NONE',  ( 22.04684512462105772, -19.02418749289184063, -60.61949336887142437 ) ) ;
#21047=ORIENTED_EDGE ( 'NONE', *, *, #28669, .F. ) ;
#21050=CARTESIAN_POINT ( 'NONE',  ( 20.86987029233329949, -20.75753920121769980, -81.23899999999999011 ) ) ;
#21070=CARTESIAN_POINT ( 'NONE',  ( 8.223569788570660677, -15.61625877447020017, -68.79233150823709764 ) ) ;
#21075=CARTESIAN_POINT ( 'NONE',  ( 23.56545591261919981, -13.09442750760010021, -75.18337345808529903 ) ) ;
#21092=CARTESIAN_POINT ( 'NONE',  ( 11.27231692120963302, -21.94239768697393700, -54.50066575920858725 ) ) ;
#21094=CARTESIAN_POINT ( 'NONE',  ( 8.812167609467170593, -16.99400660551760112, -42.00813523296859842 ) ) ;
#21096=ORIENTED_EDGE ( 'NONE', *, *, #913, .T. ) ;
#21104=CARTESIAN_POINT ( 'NONE',  ( 16.13393739769620083, -15.61618894467929941, -32.14999999999999858 ) ) ;
#21108=B_SPLINE_CURVE_WITH_KNOTS ( 'NONE', 3,
 ( #23017, #26177, #50047, #34038, #50567, #39037, #42188, #34300, #30627, #50314, #3131, #2873, #26434, #14399, #19100, #18839, #30367, #42452, #6539, #38514, #18584, #34562, #10734, #26688, #42713, #12534, #43474, #44500, #40565 ),
 .UNSPECIFIED., .F., .F.,
 ( 4, 2, 2, 2, 2, 2, 2, 2, 2, 2, 1, 1, 1, 1, 1, 2, 4 ),
 ( 0.000000000000000000, 0.06250045477388861681, 0.1250009095477772336, 0.1875013643216658643, 0.2500018190955544672, 0.3125022738694428481, 0.3750027286433312290, 0.4375031834172196654, 0.4687534108041638836, 0.4843785244976359650, 0.4921910813443720611, 0.4960973597677399427, 0.4980504989794240500, 0.4990270685852660204, 0.4995153533881869778, 0.4997594957896475121, 0.5000036381911079353 ),
 .UNSPECIFIED. ) ;
#21120=B_SPLINE_CURVE_WITH_KNOTS ( 'NONE', 3,
 ( #43182, #51553, #26919, #14616, #3860, #38737, #38995, #30586, #31608, #7792 ),
 .UNSPECIFIED., .F., .F.,
 ( 4, 1, 1, 1, 1, 1, 1, 4 ),
 ( 0.000000000000000000, 0.03120051833342932235, 0.1104194493971391161, 0.1896383804606883161, 0.2688573115242375855, 0.3480762425879473376, 0.4272951736514943311, 0.4999978458836923934 ),
 .UNSPECIFIED. ) ;
#21123=CARTESIAN_POINT ( 'NONE',  ( 22.90105422030644533, -15.61618894250064571, -66.84718200393152188 ) ) ;
#21129=CARTESIAN_POINT ( 'NONE',  ( 22.53299121009855455, -17.91495151342063252, -46.56247258658390109 ) ) ;
#21131=CARTESIAN_POINT ( 'NONE',  ( 19.51845506803190133, -8.535808465441810711, -61.65443013674619976 ) ) ;
#21141=ADVANCED_FACE ( 'NONE', ( #26261 ), #2949, .T. ) ;
#21146=CARTESIAN_POINT ( 'NONE',  ( 24.04490883580620064, -15.59321700223370044, -55.50674799533643977 ) ) ;
#21147=CARTESIAN_POINT ( 'NONE',  ( 23.44752169114309837, -16.31888570327519972, -32.14999999999999858 ) ) ;
#21150=CARTESIAN_POINT ( 'NONE',  ( 8.222937397696199469, -15.61618894467929941, -32.14999999999999858 ) ) ;
#21155=CARTESIAN_POINT ( 'NONE',  ( 13.79233564180089999, -22.26896734105170239, -67.45490599493020056 ) ) ;
#21157=ORIENTED_EDGE ( 'NONE', *, *, #12022, .F. ) ;
#21160=CARTESIAN_POINT ( 'NONE',  ( 8.223013028489239318, -15.61598591435789984, -40.50766849176299189 ) ) ;
#21163=CARTESIAN_POINT ( 'NONE',  ( 15.40691027875000074, -22.63145731195810129, -60.98569090715739804 ) ) ;
#21175=DIRECTION ( 'NONE',  ( 0.000000000000000000, 0.000000000000000000, -1.000000000000000000 ) ) ;
#21184=CARTESIAN_POINT ( 'NONE',  ( 22.04686275369982695, -12.20822338258555639, -68.28615154681510546 ) ) ;
#21187=CARTESIAN_POINT ( 'NONE',  ( 22.46012685026492761, -10.75454424016532506, -57.29933437167828458 ) ) ;
#21188=CARTESIAN_POINT ( 'NONE',  ( 29.99034385824719706, -15.61618894467929941, -32.14999999999999858 ) ) ;
#21189=CARTESIAN_POINT ( 'NONE',  ( 13.50455111243270068, -23.01031332518880035, -36.62124792064238932 ) ) ;
#21190=CARTESIAN_POINT ( 'NONE',  ( 18.53141933435923860, -22.24903445305599092, -65.23677592515561230 ) ) ;
#21199=CARTESIAN_POINT ( 'NONE',  ( 9.301828245743150703, -17.36685844811330171, -35.76733356948250275 ) ) ;
#21200=CARTESIAN_POINT ( 'NONE',  ( 9.205734167420699166, -27.61618894467930119, -32.14999999999999858 ) ) ;
#21211=CARTESIAN_POINT ( 'NONE',  ( 24.04493737213824289, -14.58064571430853995, -79.46600363739567285 ) ) ;
#21216=CARTESIAN_POINT ( 'NONE',  ( 24.04491733993996760, -15.63677092532139312, -65.79315946755016853 ) ) ;
#21222=DIRECTION ( 'NONE',  ( 1.000000000000000000, 0.000000000000000000, 0.000000000000000000 ) ) ;
#21225=CARTESIAN_POINT ( 'NONE',  ( 15.44167508794500066, -23.03423904108869991, -75.59696200394320442 ) ) ;
#21230=CARTESIAN_POINT ( 'NONE',  ( 16.25075000454472374, -7.683118076734416491, -49.29699827634726006 ) ) ;
#21231=FACE_OUTER_BOUND ( 'NONE', #28654, .T. ) ;
#21237=CARTESIAN_POINT ( 'NONE',  ( 24.01953174018752435, -16.26277903687216408, -71.53370740282881002 ) ) ;
#21239=EDGE_LOOP ( 'NONE', ( #41846, #22716, #66, #25120, #48394, #13955 ) ) ;
#21252=CARTESIAN_POINT ( 'NONE',  ( 9.550928694122980289, -10.65164299720190044, -56.99800709453249681 ) ) ;
#21259=CARTESIAN_POINT ( 'NONE',  ( 8.723884074801979693, -16.38936651614000084, -49.19956406921809133 ) ) ;
#21260=CARTESIAN_POINT ( 'NONE',  ( 8.223031589278729570, -15.61632747405269939, -32.50766849176289952 ) ) ;
#21264=EDGE_CURVE ( 'NONE', #40071, #23870, #4998, .T. ) ;
#21265=VECTOR ( 'NONE', #296, 1000.000000000000000 ) ;
#21266=CARTESIAN_POINT ( 'NONE',  ( 8.222313118464692039, -15.61611924975770016, -60.79233150823699816 ) ) ;
#21268=CARTESIAN_POINT ( 'NONE',  ( 8.223201290577328848, -15.61599831009169925, -56.79233150823699816 ) ) ;
#21269=EDGE_CURVE ( 'NONE', #34347, #15986, #7660, .T. ) ;
#21270=CARTESIAN_POINT ( 'NONE',  ( 24.04346245338579990, -17.94473658267029847, -55.59880359483129553 ) ) ;
#21271=ORIENTED_EDGE ( 'NONE', *, *, #4832, .F. ) ;
#21275=CARTESIAN_POINT ( 'NONE',  ( 10.98133074358459993, -10.80025665254149914, -52.08643336858800410 ) ) ;
#21289=CARTESIAN_POINT ( 'NONE',  ( 9.448242879478044642, -16.81408130491302089, -67.39644184705419150 ) ) ;
#21295=VERTEX_POINT ( 'NONE', #11591 ) ;
#21298=DIRECTION ( 'NONE',  ( 0.000000000000000000, 0.000000000000000000, -1.000000000000000000 ) ) ;
#21300=ORIENTED_EDGE ( 'NONE', *, *, #37088, .T. ) ;
#21306=B_SPLINE_CURVE_WITH_KNOTS ( 'NONE', 3,
 ( #26790, #7154, #22848, #42801, #18930, #23869, #7407, #27561, #35942, #23107, #19708, #27308, #11864, #35435, #39125, #35172, #23613, #39633, #11342, #16037, #23353, #39893, #6897, #51431 ),
 .UNSPECIFIED., .F., .F.,
 ( 4, 2, 2, 2, 2, 2, 2, 2, 2, 2, 2, 4 ),
 ( 0.000000000000000000, 0.03124999605426864377, 0.06249999210853728754, 0.09374998816280592784, 0.1249999842170745751, 0.1562499802713432084, 0.1874999763256118557, 0.2499999684341491502, 0.3124999605426864169, 0.3749999526512237114, 0.4374999447597610058, 0.4999999368682983003 ),
 .UNSPECIFIED. ) ;
#21310=CARTESIAN_POINT ( 'NONE',  ( 23.44593531291890187, -16.58422985608489952, -81.23899999999999011 ) ) ;
#21316=CARTESIAN_POINT ( 'NONE',  ( 15.93498023681340037, -22.66622264832809819, -69.35616034045719402 ) ) ;
#21328=CARTESIAN_POINT ( 'NONE',  ( 22.90015496201974088, -16.26211237549280852, -54.87756051468720386 ) ) ;
#21330=EDGE_CURVE ( 'NONE', #26214, #31550, #47897, .T. ) ;
#21331=CARTESIAN_POINT ( 'NONE',  ( 23.38644729089550012, -12.61821489005030017, -69.16273469725000211 ) ) ;
#21341=CARTESIAN_POINT ( 'NONE',  ( 17.01970876327451165, -22.38319278097903720, -78.91115185007626565 ) ) ;
#21344=CARTESIAN_POINT ( 'NONE',  ( 24.04492240731919850, -15.63209485227305073, -33.50830522199780859 ) ) ;
#21349=CARTESIAN_POINT ( 'NONE',  ( 22.04518293870870238, -20.15092934432739824, -43.27563812998649695 ) ) ;
#21359=AXIS2_PLACEMENT_3D ( 'NONE', #16775, #32458, #32210 ) ;
#21360=CARTESIAN_POINT ( 'NONE',  ( 12.34706755911540021, -9.666216171624100184, -60.16676433707719696 ) ) ;
#21363=ORIENTED_EDGE ( 'NONE', *, *, #2523, .T. ) ;
#21371=EDGE_CURVE ( 'NONE', #8034, #41415, #48544, .T. ) ;
#21377=CARTESIAN_POINT ( 'NONE',  ( 9.366491660071980974, -15.45061801826404313, -65.85496231377463516 ) ) ;
#21382=CARTESIAN_POINT ( 'NONE',  ( 15.24808072932934522, -22.38318161335044820, -46.99448119687986747 ) ) ;
#21385=CARTESIAN_POINT ( 'NONE',  ( 9.605521497733009895, -11.26113057208659995, -67.19975531119949608 ) ) ;
#21401=B_SPLINE_CURVE_WITH_KNOTS ( 'NONE', 3,
 ( #28207, #439, #36592, #44207, #8305, #24261, #16684, #32642, #20341, #12499, #28724, #16428, #44727, #24782, #40791, #9574, #13255, #22118, #25530, #6160, #33659, #37872, #13763, #6422, #46266, #49674, #33911, #29722 ),
 .UNSPECIFIED., .F., .F.,
 ( 4, 2, 1, 1, 1, 1, 2, 2, 2, 2, 2, 2, 2, 2, 2, 4 ),
 ( 0.5000036702591513782, 0.5004919479249139158, 0.5009802255906764534, 0.5019567809222015287, 0.5039098915852517901, 0.5078161129113522021, 0.5156285555635529150, 0.5312534408679545628, 0.5625032114767575253, 0.6250027526943636724, 0.6875022939119698195, 0.7500018351295759667, 0.8125013763471820027, 0.8750009175647879278, 0.9375004587823939639, 1.000000000000000000 ),
 .UNSPECIFIED. ) ;
#21403=CARTESIAN_POINT ( 'NONE',  ( 14.18091115246270029, -22.39322721071389921, -77.43649130894630161 ) ) ;
#21404=CARTESIAN_POINT ( 'NONE',  ( 23.34951741632489686, -14.96832030630810095, -32.14999999999999858 ) ) ;
#21412=CARTESIAN_POINT ( 'NONE',  ( 17.70165363224570143, -22.49258516525739893, -61.27582937196799406 ) ) ;
#21420=CARTESIAN_POINT ( 'NONE',  ( 9.491729301919979989, -13.24476947334350108, -75.56197422286339815 ) ) ;
#21421=DIRECTION ( 'NONE',  ( 0.000000000000000000, -1.000000000000000000, 0.000000000000000000 ) ) ;
#21425=ORIENTED_EDGE ( 'NONE', *, *, #34004, .F. ) ;
#21429=CARTESIAN_POINT ( 'NONE',  ( 12.33464918225277174, -8.580518978903178606, -38.85044401595073538 ) ) ;
#21439=CARTESIAN_POINT ( 'NONE',  ( 9.221403253415356716, -19.60030155675170604, -60.34101711567728188 ) ) ;
#21443=CARTESIAN_POINT ( 'NONE',  ( 24.04477596867337041, -15.61618922203197357, -43.50766101656756746 ) ) ;
#21447=EDGE_LOOP ( 'NONE', ( #4560, #39023, #13475, #4239 ) ) ;
#21448=CARTESIAN_POINT ( 'NONE',  ( 9.221390525194372856, -11.63209808988130334, -52.95899869926838477 ) ) ;
#21450=CARTESIAN_POINT ( 'NONE',  ( 12.61940550337589961, -22.63295351940629985, -32.66030136746149992 ) ) ;
#21458=VECTOR ( 'NONE', #12021, 1000.000000000000000 ) ;
#21459=CARTESIAN_POINT ( 'NONE',  ( 12.65447590535320010, -9.481377877827920742, -34.18295494821010294 ) ) ;
#21474=CARTESIAN_POINT ( 'NONE',  ( 14.06323322820019683, -7.911095412653208037, -68.92433645535102471 ) ) ;
#21480=LINE ( 'NONE', #33276, #51116 ) ;
#21483=CARTESIAN_POINT ( 'NONE',  ( 14.94185921909920012, -8.567953771208047797, -81.67932580530198550 ) ) ;
#21486=CARTESIAN_POINT ( 'NONE',  ( 24.04493737933958286, -16.65173024076593222, -57.54933420604645278 ) ) ;
#21490=CARTESIAN_POINT ( 'NONE',  ( 15.19106124924670098, -8.225811491055798896, -70.52695041587159608 ) ) ;
#21493=CARTESIAN_POINT ( 'NONE',  ( 11.81035279570149221, -8.951068426379952925, -49.10926437117617382 ) ) ;
#21497=CARTESIAN_POINT ( 'NONE',  ( 9.214865060109733719, -19.58814555416793013, -76.62618144234603790 ) ) ;
#21502=B_SPLINE_CURVE_WITH_KNOTS ( 'NONE', 3,
 ( #49754, #33739, #13845, #2304, #45300, #13590, #29299, #50271, #42144, #21429, #9409, #9908, #29555, #46089, #2570, #14359, #49244, #5982, #17768, #37689, #25866, #45558, #37951, #26387, #42405, #46348, #29802, #22458, #26132, #38466, #38209, #1787, #10171, #18278 ),
 .UNSPECIFIED., .F., .F.,
 ( 4, 2, 2, 2, 2, 2, 2, 2, 2, 2, 2, 2, 1, 1, 1, 1, 1, 1, 2, 4 ),
 ( 0.000000000000000000, 0.03125032255746391235, 0.06250064511492782471, 0.09375096767239174400, 0.1250012902298556494, 0.1875019353447834880, 0.2500025804597112988, 0.3125032255746391097, 0.3750038706895669760, 0.4375045158044947868, 0.4687548383619586922, 0.4843799996406906172, 0.4921925802800565797, 0.4960988705997395609, 0.4980520157595809683, 0.4990285883395016442, 0.4995168746294618711, 0.4997610177744420401, 0.4998830893469320413, 0.5000051609194220426 ),
 .UNSPECIFIED. ) ;
#21504=ADVANCED_FACE ( 'NONE', ( #44841 ), #48776, .T. ) ;
#21508=CARTESIAN_POINT ( 'NONE',  ( 15.24810682503254711, -8.849192852612759452, -69.91115498661820027 ) ) ;
#21510=CARTESIAN_POINT ( 'NONE',  ( 14.06332153136815322, -23.32130534079293938, -70.09100312201769611 ) ) ;
#21517=CARTESIAN_POINT ( 'NONE',  ( 12.23782554533866929, -22.52769441490526248, -66.17096938631890168 ) ) ;
#21518=CARTESIAN_POINT ( 'NONE',  ( 8.386807182601900834, -18.43836779909439727, -56.68113137027810211 ) ) ;
#21523=CARTESIAN_POINT ( 'NONE',  ( 15.21491748573319924, -8.222807025248849655, -39.69329234158369957 ) ) ;
#21524=DIRECTION ( 'NONE',  ( 0.000000000000000000, 0.000000000000000000, 1.000000000000000000 ) ) ;
#21525=EDGE_CURVE ( 'NONE', #3978, #29027, #3537, .T. ) ;
#21530=CARTESIAN_POINT ( 'NONE',  ( 9.418179351659979659, -20.39963065291350119, -48.31066193697829902 ) ) ;
#21535=CARTESIAN_POINT ( 'NONE',  ( 11.97520752817116652, -21.02746473356409140, -57.16110635108449856 ) ) ;
#21545=CARTESIAN_POINT ( 'NONE',  ( 9.501539899509779730, -17.54678703817369012, -57.75637824400988052 ) ) ;
#21547=DIRECTION ( 'NONE',  ( 0.000000000000000000, 0.000000000000000000, 1.000000000000000000 ) ) ;
#21549=CARTESIAN_POINT ( 'NONE',  ( 9.366922913046613175, -16.22029336621082507, -67.42439374615231884 ) ) ;
#21560=CARTESIAN_POINT ( 'NONE',  ( 12.20262750478389258, -8.709504227742451477, -80.84286210128752259 ) ) ;
#21561=ORIENTED_EDGE ( 'NONE', *, *, #25928, .T. ) ;
#21570=DIRECTION ( 'NONE',  ( 0.000000000000000000, 0.000000000000000000, -1.000000000000000000 ) ) ;
#21582=EDGE_CURVE ( 'NONE', #21743, #27935, #27273, .T. ) ;
#21586=CARTESIAN_POINT ( 'NONE',  ( 22.96503088535069992, -11.75317070163309907, -73.12368125043110467 ) ) ;
#21588=CARTESIAN_POINT ( 'NONE',  ( 24.04493739769619864, -15.61618894467929941, -32.14999999999999858 ) ) ;
#21592=B_SPLINE_CURVE_WITH_KNOTS ( 'NONE', 3,
 ( #36461, #4503, #32508, #39906, #16827, #20737, #28081, #20220, #8189, #48801, #40926, #21000, #7932, #75, #44087, #24131, #40154, #4250, #36210, #16300, #28337, #48279, #46172, #41971, #17348, #21517, #38037, #45387, #33314, #10260, #6327, #25184, #1613, #13426, #49069 ),
 .UNSPECIFIED., .F., .F.,
 ( 4, 2, 1, 1, 1, 1, 1, 2, 2, 2, 2, 2, 2, 2, 2, 2, 2, 2, 2, 4 ),
 ( 0.4999984552117135994, 0.5002425965910047845, 0.5004867379702959695, 0.5009750207288782287, 0.5019515862460430800, 0.5039047172803724495, 0.5078109793490309665, 0.5156235034863478894, 0.5312485517609818464, 0.5624986483102496493, 0.6249988414087853661, 0.6874990345073210829, 0.7499992276058569107, 0.8124994207043927386, 0.8437495172536605414, 0.8749996138029284554, 0.9062497103521963693, 0.9374998069014641722, 0.9687499034507320861, 1.000000000000000000 ),
 .UNSPECIFIED. ) ;
#21596=CARTESIAN_POINT ( 'NONE',  ( 22.90093740122328825, -16.50198959089620487, -78.49448387614262401 ) ) ;
#21598=CARTESIAN_POINT ( 'NONE',  ( 8.222912444960085665, -16.65155373173890396, -56.75066771667979992 ) ) ;
#21599=CARTESIAN_POINT ( 'NONE',  ( 24.04462826173309153, -15.61618628916268392, -33.50766512250601181 ) ) ;
#21603=CARTESIAN_POINT ( 'NONE',  ( 22.96971382812329665, -18.57910219544439556, -51.19753123634840364 ) ) ;
#21606=CARTESIAN_POINT ( 'NONE',  ( 9.366446932119513846, -15.48215974695313335, -33.85347959719207722 ) ) ;
#21609=CARTESIAN_POINT ( 'NONE',  ( 8.223487313465298598, -15.61606829411550024, -62.50766849176299189 ) ) ;
#21614=VERTEX_POINT ( 'NONE', #43175 ) ;
#21634=ADVANCED_FACE ( 'NONE', ( #31088 ), #40008, .T. ) ;
#21635=CARTESIAN_POINT ( 'NONE',  ( 20.77912286130639785, -9.290922183486799213, -63.71412234440029465 ) ) ;
#21645=VECTOR ( 'NONE', #6861, 1000.000000000000000 ) ;
#21654=CARTESIAN_POINT ( 'NONE',  ( 23.09005290148149925, -13.91445552956680132, -32.14999999999999858 ) ) ;
#21657=CARTESIAN_POINT ( 'NONE',  ( 22.84381469196726755, -14.09322211363766719, -50.77553680422087723 ) ) ;
#21661=CARTESIAN_POINT ( 'NONE',  ( 18.95614455194280268, -22.07975653177619790, -59.21613716431369312 ) ) ;
#21669=CARTESIAN_POINT ( 'NONE',  ( 19.22002932807319553, -9.274375695040369294, -78.09698001689929470 ) ) ;
#21672=DIRECTION ( 'NONE',  ( 1.000000000000000000, 0.000000000000000000, 0.000000000000000000 ) ) ;
#21674=VERTEX_POINT ( 'NONE', #27684 ) ;
#21695=CARTESIAN_POINT ( 'NONE',  ( 18.01462889419880042, -7.907399074006033146, -33.36857024937042837 ) ) ;
#21700=CARTESIAN_POINT ( 'NONE',  ( 19.87406119966940210, -8.717042509227168168, -35.67062074787909864 ) ) ;
#21706=CARTESIAN_POINT ( 'NONE',  ( 16.13393739769620083, -15.61618894467929941, -32.14999999999999858 ) ) ;
#21709=CARTESIAN_POINT ( 'NONE',  ( 12.19555056211440203, -21.23241274584290039, -31.54232391275609615 ) ) ;
#21724=CARTESIAN_POINT ( 'NONE',  ( 16.13393739769620083, -15.61618894467929941, -28.45282021618999835 ) ) ;
#21737=CARTESIAN_POINT ( 'NONE',  ( 14.60189429842830044, -22.50062084851940014, -41.02252027912539489 ) ) ;
#21741=CARTESIAN_POINT ( 'NONE',  ( 23.04647341738391830, -19.60029640582816413, -57.67433433027032663 ) ) ;
#21743=VERTEX_POINT ( 'NONE', #33153 ) ;
#21744=CARTESIAN_POINT ( 'NONE',  ( 21.01798797078739867, -21.24226611600790093, -77.33977848734279803 ) ) ;
#21747=CARTESIAN_POINT ( 'NONE',  ( 16.13393739769620083, -15.61618894467929941, -32.14999999999999858 ) ) ;
#21751=CARTESIAN_POINT ( 'NONE',  ( 12.13079090422609418, -22.51756641863451236, -76.45982039034187494 ) ) ;
#21753=CARTESIAN_POINT ( 'NONE',  ( 23.99010335988727860, -16.68233456288250238, -45.55063181585114762 ) ) ;
#21757=ORIENTED_EDGE ( 'NONE', *, *, #32786, .T. ) ;
#21760=ORIENTED_EDGE ( 'NONE', *, *, #40915, .T. ) ;
#21762=CARTESIAN_POINT ( 'NONE',  ( 9.367478339302499180, -15.61624867646989756, -69.45282021618999124 ) ) ;
#21763=CARTESIAN_POINT ( 'NONE',  ( 22.90093700018227452, -15.31200357956842062, -50.43851515688148623 ) ) ;
#21766=ORIENTED_EDGE ( 'NONE', *, *, #11184, .F. ) ;
#21774=CARTESIAN_POINT ( 'NONE',  ( 19.20039525651199597, -7.962460686108711272, -55.41362847326020358 ) ) ;
#21775=B_SPLINE_CURVE_WITH_KNOTS ( 'NONE', 3,
 ( #50077, #38547, #14688, #26726, #30657, #42218, #38285, #9982, #1863, #38810, #14172, #50853, #6057, #42743, #6841, #25688, #9728, #41691 ),
 .UNSPECIFIED., .F., .F.,
 ( 4, 2, 2, 2, 2, 2, 2, 2, 4 ),
 ( 0.4999990007379375156, 0.5624991256456953748, 0.6249992505534531784, 0.6874993754612110930, 0.7499995003689690076, 0.8124996252767267002, 0.8749997501844843928, 0.9374998750922421964, 1.000000000000000000 ),
 .UNSPECIFIED. ) ;
#21780=CARTESIAN_POINT ( 'NONE',  ( 18.18411367297410308, -22.77883308252629746, -40.64391951434709682 ) ) ;
#21782=CARTESIAN_POINT ( 'NONE',  ( 9.079715832018310451, -18.09592210593110195, -32.14999999999999858 ) ) ;
#21788=CARTESIAN_POINT ( 'NONE',  ( 9.122356773365169147, -19.95444410747009911, -54.33130069781350358 ) ) ;
#21795=CARTESIAN_POINT ( 'NONE',  ( 12.72585340994692515, -21.52904809432142486, -57.11943624023800226 ) ) ;
#21809=CARTESIAN_POINT ( 'NONE',  ( 24.04468322966528859, -15.61618861995729013, -71.79233702014498419 ) ) ;
#21820=EDGE_CURVE ( 'NONE', #40071, #37443, #11052, .T. ) ;
#21821=CARTESIAN_POINT ( 'NONE',  ( 13.03996251179858845, -21.95416011689881941, -47.49173536689809794 ) ) ;
#21822=B_SPLINE_CURVE_WITH_KNOTS ( 'NONE', 3,
 ( #36717, #17085, #819, #16821, #28856, #5029, #20993, #1086, #33037, #13169, #26210 ),
 .UNSPECIFIED., .F., .F.,
 ( 4, 1, 1, 1, 1, 1, 1, 1, 4 ),
 ( 0.000000000000000000, 0.02199317534151036882, 0.1012121064050618968, 0.1804310374687717322, 0.2596499685323187534, 0.3388688995958658023, 0.4180878306595756100, 0.4973067617231270998, 0.5000009373669883628 ),
 .UNSPECIFIED. ) ;
#21837=CARTESIAN_POINT ( 'NONE',  ( 8.931659033063507280, -18.95453092549626817, -34.65421127275790525 ) ) ;
#21842=CARTESIAN_POINT ( 'NONE',  ( 28.13393739769620439, -18.83157925385280862, -22.14999999999998792 ) ) ;
#21851=CARTESIAN_POINT ( 'NONE',  ( 9.062045689195219467, -12.21396969154209877, -70.43023759426799302 ) ) ;
#21854=ADVANCED_FACE ( 'NONE', ( #1204 ), #17197, .T. ) ;
#21856=B_SPLINE_CURVE_WITH_KNOTS ( 'NONE', 3,
 ( #19934, #24622, #3462, #31463, #35925, #35412, #15509, #11583, #51666, #15760, #16018, #11845, #27803, #43800, #47994, #12094, #8157, #24101, #40122, #4215, #20189, #49555, #5771, #45606, #790, #24880, #37480, #36962, #33009, #1580, #21216, #29851, #9704 ),
 .UNSPECIFIED., .F., .F.,
 ( 4, 2, 2, 2, 2, 2, 2, 2, 2, 2, 2, 2, 2, 1, 1, 1, 2, 4 ),
 ( 0.000000000000000000, 0.03125000081801168617, 0.06250000163602337233, 0.09375000245403505850, 0.1250000032720467447, 0.1562500040900584308, 0.1875000049080701170, 0.2500000065440936003, 0.3125000081801173057, 0.3750000098161410111, 0.4375000114521647165, 0.4687500122701767080, 0.4843750126791828148, 0.4921875128836860624, 0.4960937629859378251, 0.4980468880370637619, 0.4990234505626266470, 0.5000000130881896432 ),
 .UNSPECIFIED. ) ;
#21858=CARTESIAN_POINT ( 'NONE',  ( 20.99562489116508601, -21.94234663276146691, -36.08399623320025995 ) ) ;
#21862=B_SPLINE_CURVE_WITH_KNOTS ( 'NONE', 3,
 ( #34012, #41632, #29314, #25375, #5739, #33244, #21958, #25113, #45576, #14112, #5490, #5236, #6260, #1291, #21448, #49260, #37968, #10191 ),
 .UNSPECIFIED., .F., .F.,
 ( 4, 2, 2, 2, 2, 2, 2, 2, 4 ),
 ( 0.4999984269058530550, 0.5624986235426214787, 0.6249988201793900133, 0.6874990168161585480, 0.7499992134529269716, 0.8124994100896951732, 0.8749996067264634858, 0.9374998033632317984, 1.000000000000000000 ),
 .UNSPECIFIED. ) ;
#21869=CARTESIAN_POINT ( 'NONE',  ( 22.01335404994659939, -20.19212099919920078, -59.27786220483759649 ) ) ;
#21872=CARTESIAN_POINT ( 'NONE',  ( 14.36272346516433274, -22.20707084970106138, -69.03615254816922686 ) ) ;
#21876=CARTESIAN_POINT ( 'NONE',  ( 22.52170170608374988, -20.28853306323505734, -61.70867510901859987 ) ) ;
#21878=CARTESIAN_POINT ( 'NONE',  ( 9.807858107459463071, -10.75440064878946167, -35.00066427048108864 ) ) ;
#21880=CARTESIAN_POINT ( 'NONE',  ( 9.815298770958309049, -18.40745523507650461, -81.23899999999999011 ) ) ;
#21897=CARTESIAN_POINT ( 'NONE',  ( 22.52031032320270043, -11.05537887965270016, -77.81509207372459969 ) ) ;
#21898=CARTESIAN_POINT ( 'NONE',  ( 16.13393739769620083, -15.61618894467929941, -40.14999999999999858 ) ) ;
#21909=EDGE_CURVE ( 'NONE', #36898, #40749, #39819, .T. ) ;
#21915=CARTESIAN_POINT ( 'NONE',  ( 21.64619207794780209, -11.41351007145500063, -32.14999999999999858 ) ) ;
#21923=CARTESIAN_POINT ( 'NONE',  ( 10.60479889110639995, -19.99468030008900143, -73.63398261789269839 ) ) ;
#21930=CARTESIAN_POINT ( 'NONE',  ( 22.85072513555170204, -13.46506803194099788, -76.35416353349970109 ) ) ;
#21939=LINE ( 'NONE', #18797, #41572 ) ;
#21944=VERTEX_POINT ( 'NONE', #29997 ) ;
#21952=B_SPLINE_CURVE_WITH_KNOTS ( 'NONE', 3,
 ( #12667, #23650, #852, #23901, #8470, #40690, #20495, #35977, #12397, #16576, #28620 ),
 .UNSPECIFIED., .F., .F.,
 ( 4, 1, 1, 1, 1, 1, 1, 1, 4 ),
 ( 0.000000000000000000, 0.02088113791589244622, 0.1001000689795119303, 0.1793190000431291453, 0.2585379311067463881, 0.3377568621703658791, 0.4169757932339808182, 0.4961947242976002537, 0.5000013100879009409 ),
 .UNSPECIFIED. ) ;
#21955=CARTESIAN_POINT ( 'NONE',  ( 24.04460909154476056, -15.61619055174803172, -33.79232989763376338 ) ) ;
#21958=CARTESIAN_POINT ( 'NONE',  ( 20.11805166124982946, -8.703655564017157786, -53.45900027236253749 ) ) ;
#21961=CARTESIAN_POINT ( 'NONE',  ( 11.37287907419960042, -21.85470408961259636, -34.71999357511560191 ) ) ;
#21986=CARTESIAN_POINT ( 'NONE',  ( 23.04645919661562914, -11.63205485126550087, -69.34100441893906464 ) ) ;
#21990=ORIENTED_EDGE ( 'NONE', *, *, #8675, .F. ) ;
#21994=CARTESIAN_POINT ( 'NONE',  ( 9.230581035993791872, -14.17181031012109926, -47.51847262634220215 ) ) ;
#21995=CARTESIAN_POINT ( 'NONE',  ( 16.13393739769620083, -15.61618894467929941, -28.45282021618999835 ) ) ;
#21998=CARTESIAN_POINT ( 'NONE',  ( 9.807847332228750048, -20.47796341179069657, -58.29933495138985222 ) ) ;
#22002=CARTESIAN_POINT ( 'NONE',  ( 22.84307013152569965, -12.37670867548260034, -78.92415710861509126 ) ) ;
#22013=ORIENTED_EDGE ( 'NONE', *, *, #35169, .T. ) ;
#22019=CARTESIAN_POINT ( 'NONE',  ( 22.60131651358703664, -13.53789388470488397, -50.35393761413898517 ) ) ;
#22026=CARTESIAN_POINT ( 'NONE',  ( 24.04487538420616843, -15.58383734352081440, -43.79102361582464198 ) ) ;
#22028=CARTESIAN_POINT ( 'NONE',  ( 21.10308478659139908, -22.19572496809090367, -52.08643336858809647 ) ) ;
#22033=ORIENTED_EDGE ( 'NONE', *, *, #24618, .T. ) ;
#22035=CARTESIAN_POINT ( 'NONE',  ( 20.50180696762360100, -9.580593760668989489, -47.93206117220019991 ) ) ;
#22036=CARTESIAN_POINT ( 'NONE',  ( 10.79172117177870049, -11.23010277562130099, -32.14999999999999858 ) ) ;
#22038=CARTESIAN_POINT ( 'NONE',  ( 17.16956853822826901, -7.705200890051467688, -51.33399677538780992 ) ) ;
#22041=CARTESIAN_POINT ( 'NONE',  ( 8.856000844739879696, -19.49102574641920071, -60.35193945864850207 ) ) ;
#22048=CARTESIAN_POINT ( 'NONE',  ( 22.90099491887654182, -15.61618908163285546, -52.84717737022585027 ) ) ;
#22055=CARTESIAN_POINT ( 'NONE',  ( 22.06776932978649697, -10.30416640759050928, -65.56010685651600056 ) ) ;
#22077=AXIS2_PLACEMENT_3D ( 'NONE', #13502, #8523, #16907 ) ;
#22078=CARTESIAN_POINT ( 'NONE',  ( 18.20470610557513069, -23.32126384531657237, -79.92433626156834237 ) ) ;
#22084=CARTESIAN_POINT ( 'NONE',  ( 18.20467351747694096, -7.911104839119652787, -63.09100278528516270 ) ) ;
#22092=CARTESIAN_POINT ( 'NONE',  ( 24.00136113245211789, -16.46404240851678580, -33.82649071835572130 ) ) ;
#22105=CARTESIAN_POINT ( 'NONE',  ( 18.31782017144560015, -23.15392097850119768, -71.69774049128601234 ) ) ;
#22106=EDGE_CURVE ( 'NONE', #7516, #31721, #25308, .T. ) ;
#22115=CARTESIAN_POINT ( 'NONE',  ( 24.03895263636016111, -15.10140185694807968, -65.48698662191623043 ) ) ;
#22118=CARTESIAN_POINT ( 'NONE',  ( 18.20455775428947831, -7.911072023573607837, -59.37571045720464724 ) ) ;
#22122=CARTESIAN_POINT ( 'NONE',  ( 22.89142744636506421, -16.00358783246685945, -62.47105660056999454 ) ) ;
#22124=DIRECTION ( 'NONE',  ( 1.000000000000000000, 0.000000000000000000, 0.000000000000000000 ) ) ;
#22125=ORIENTED_EDGE ( 'NONE', *, *, #41450, .F. ) ;
#22126=AXIS2_PLACEMENT_3D ( 'NONE', #50902, #3209, #34639 ) ;
#22127=CARTESIAN_POINT ( 'NONE',  ( 22.29748881350769807, -19.80155969086050050, -53.25722344400249852 ) ) ;
#22132=CARTESIAN_POINT ( 'NONE',  ( 22.59648755964504829, -13.01690795190288519, -74.72494365400706329 ) ) ;
#22133=CARTESIAN_POINT ( 'NONE',  ( 24.04493739453105761, -15.62695325930471490, -61.50809781073701288 ) ) ;
#22135=CARTESIAN_POINT ( 'NONE',  ( 22.73379249883699060, -13.53922887446369572, -54.74949983865565173 ) ) ;
#22138=ORIENTED_EDGE ( 'NONE', *, *, #15800, .F. ) ;
#22145=CARTESIAN_POINT ( 'NONE',  ( 24.03886748631395776, -15.28162044291991961, -77.49421311239169086 ) ) ;
#22154=CARTESIAN_POINT ( 'NONE',  ( 18.19207604292220282, -8.043156995148798671, -75.59696200394320442 ) ) ;
#22155=DIRECTION ( 'NONE',  ( 0.000000000000000000, 0.000000000000000000, -1.000000000000000000 ) ) ;
#22164=CARTESIAN_POINT ( 'NONE',  ( 12.91854708852281597, -3.616188944679342931, -22.15000000000000924 ) ) ;
#22169=EDGE_CURVE ( 'NONE', #9734, #21743, #21592, .T. ) ;
#22171=CARTESIAN_POINT ( 'NONE',  ( 8.222937397696192363, -15.61618894467929941, -81.23899999999999011 ) ) ;
#22172=CARTESIAN_POINT ( 'NONE',  ( 20.83772691662250054, -10.64658677815640075, -32.14999999999999858 ) ) ;
#22175=CONICAL_SURFACE ( 'NONE', #4609, 12.92820323027549989, 0.7481802937784480800 ) ;
#22178=CARTESIAN_POINT ( 'NONE',  ( 11.27220150064897553, -21.94231036716944061, -46.50070531515176953 ) ) ;
#22181=CARTESIAN_POINT ( 'NONE',  ( 11.51802410812859989, -20.94872152101149965, -71.57429041023839034 ) ) ;
#22189=CARTESIAN_POINT ( 'NONE',  ( 9.251438566469660785, -14.07548506148300049, -79.52292077604440124 ) ) ;
#22192=CARTESIAN_POINT ( 'NONE',  ( 17.01966294822905112, -22.38319941436395411, -40.91109367937480812 ) ) ;
#22194=VERTEX_POINT ( 'NONE', #49837 ) ;
#22213=ORIENTED_EDGE ( 'NONE', *, *, #8979, .T. ) ;
#22219=CARTESIAN_POINT ( 'NONE',  ( 23.83903760508270864, -17.68686475598193297, -53.59100462632350315 ) ) ;
#22221=CARTESIAN_POINT ( 'NONE',  ( 23.98092394894220192, -15.50871961813850142, -42.00813523296849894 ) ) ;
#22230=CARTESIAN_POINT ( 'NONE',  ( 15.57679709041789984, -22.64698931536659998, -43.37235095159000053 ) ) ;
#22236=CYLINDRICAL_SURFACE ( 'NONE', #14681, 6.766999999999998572 ) ;
#22252=CARTESIAN_POINT ( 'NONE',  ( 14.06335507478330449, -23.32131402515702234, -74.37566484649038046 ) ) ;
#22255=CARTESIAN_POINT ( 'NONE',  ( 23.18611651039899968, -15.51960499682390093, -42.44846103827049433 ) ) ;
#22259=DIRECTION ( 'NONE',  ( -1.000000000000000000, 0.000000000000000000, 0.000000000000000000 ) ) ;
#22262=CARTESIAN_POINT ( 'NONE',  ( 12.28926181007750174, -22.45762284475839721, -37.95047585818409885 ) ) ;
#22264=CARTESIAN_POINT ( 'NONE',  ( 12.89372882336123638, -8.399748356796177262, -81.15800232914327239 ) ) ;
#22268=CARTESIAN_POINT ( 'NONE',  ( 24.04468182044177738, -15.61618932230105017, -75.79232603942232060 ) ) ;
#22269=CARTESIAN_POINT ( 'NONE',  ( 22.90091300232175442, -15.59650344546338907, -62.45190239597013004 ) ) ;
#22270=CARTESIAN_POINT ( 'NONE',  ( 10.72267184746520030, -11.45744867721397142, -57.66115349055309025 ) ) ;
#22274=EDGE_CURVE ( 'NONE', #37798, #8663, #9745, .T. ) ;
#22287=CARTESIAN_POINT ( 'NONE',  ( 8.428798744621994743, -13.54564960420282205, -42.87567841755609521 ) ) ;
#22289=CARTESIAN_POINT ( 'NONE',  ( 24.11850265849220065, -13.55962928057420136, -65.71208951153069222 ) ) ;
#22294=CARTESIAN_POINT ( 'NONE',  ( 12.75093326110940062, -22.25410855981340319, -48.88268834496359716 ) ) ;
#22295=CIRCLE ( 'NONE', #49925, 12.00000000000000000 ) ;
#22296=CARTESIAN_POINT ( 'NONE',  ( 9.233376442599690037, -18.60157552794879976, -32.14999999999999858 ) ) ;
#22300=CARTESIAN_POINT ( 'NONE',  ( 8.222678474964419948, -15.61600660124389961, -50.79233150823699816 ) ) ;
#22302=CARTESIAN_POINT ( 'NONE',  ( 19.23238759590467239, -8.313067289789655590, -61.13547072799036641 ) ) ;
#22303=CARTESIAN_POINT ( 'NONE',  ( 24.26898003732519626, -16.95924589075189814, -59.55975014801229861 ) ) ;
#22317=CARTESIAN_POINT ( 'NONE',  ( 16.13393739769620083, -15.61618894467929941, -28.45282021618999835 ) ) ;
#22330=CARTESIAN_POINT ( 'NONE',  ( 22.36082438643301273, -18.90756276022864668, -73.00202728647948902 ) ) ;
#22345=FACE_OUTER_BOUND ( 'NONE', #3219, .T. ) ;
#22357=DIRECTION ( 'NONE',  ( 0.000000000000000000, 0.000000000000000000, 1.000000000000000000 ) ) ;
#22358=CARTESIAN_POINT ( 'NONE',  ( 21.28448762020170193, -20.00650175921066065, -46.67749910197144914 ) ) ;
#22367=CARTESIAN_POINT ( 'NONE',  ( 23.76520713869530255, -17.44668068275500161, -81.36245008104741316 ) ) ;
#22383=EDGE_CURVE ( 'NONE', #37252, #30218, #3437, .T. ) ;
#22386=EDGE_CURVE ( 'NONE', #13106, #41523, #12338, .T. ) ;
#22387=ORIENTED_EDGE ( 'NONE', *, *, #44461, .F. ) ;
#22388=CARTESIAN_POINT ( 'NONE',  ( 9.837961696380780552, -11.63280039888219974, -50.24690406358499217 ) ) ;
#22390=VERTEX_POINT ( 'NONE', #19656 ) ;
#22393=DIRECTION ( 'NONE',  ( 0.000000000000000000, 0.000000000000000000, 1.000000000000000000 ) ) ;
#22396=DIRECTION ( 'NONE',  ( 1.000000000000000000, 0.000000000000000000, 0.000000000000000000 ) ) ;
#22409=CARTESIAN_POINT ( 'NONE',  ( 24.01053399803918253, -14.85515835932281625, -77.47701762277769433 ) ) ;
#22410=B_SPLINE_CURVE_WITH_KNOTS ( 'NONE', 3,
 ( #8436, #32760, #16287, #811, #12893, #41427, #16813, #28848, #44851, #21237, #12360, #32493, #32242, #49313, #45108, #24380, #28324, #8956, #48520, #49053, #5544, #24899, #13160, #36448, #44324, #555, #13408, #12627, #40912 ),
 .UNSPECIFIED., .F., .F.,
 ( 4, 2, 1, 1, 1, 1, 1, 2, 2, 2, 2, 2, 2, 2, 2, 2, 4 ),
 ( 0.5000036381911079353, 0.5002477770396474011, 0.5004919158881868668, 0.5009801935852656873, 0.5019567489794234394, 0.5039098597677392766, 0.5078160813443711730, 0.5156285244976349658, 0.5312534108041627734, 0.5625031834172187217, 0.6250027286433301743, 0.6875022738694417379, 0.7500018190955533015, 0.8125013643216649761, 0.8750009095477766508, 0.9375004547738883254, 1.000000000000000000 ),
 .UNSPECIFIED. ) ;
#22413=EDGE_LOOP ( 'NONE', ( #48286, #3617, #21990, #40858 ) ) ;
#22417=CARTESIAN_POINT ( 'NONE',  ( 13.83141090584470057, -23.11852987216700228, -78.60728138436070367 ) ) ;
#22421=CARTESIAN_POINT ( 'NONE',  ( 24.04519454997480210, -15.61618869140488997, -79.50766696426083513 ) ) ;
#22425=CARTESIAN_POINT ( 'NONE',  ( 8.303488653731021074, -15.09578462944280020, -50.30862910410869659 ) ) ;
#22426=ORIENTED_EDGE ( 'NONE', *, *, #3923, .F. ) ;
#22434=DIRECTION ( 'NONE',  ( 0.000000000000000000, 0.000000000000000000, 1.000000000000000000 ) ) ;
#22439=VERTEX_POINT ( 'NONE', #31943 ) ;
#22440=CARTESIAN_POINT ( 'NONE',  ( 17.01654511880040133, -8.618792084267338893, -78.38711848170969176 ) ) ;
#22443=DIRECTION ( 'NONE',  ( 0.000000000000000000, 0.000000000000000000, -1.000000000000000000 ) ) ;
#22448=CARTESIAN_POINT ( 'NONE',  ( 14.50584207537670167, -22.47854016842669722, -73.02696842882760109 ) ) ;
#22450=CARTESIAN_POINT ( 'NONE',  ( 18.20468117247153472, -23.32127088709334828, -41.92433441774539915 ) ) ;
#22458=CARTESIAN_POINT ( 'NONE',  ( 24.04483892795884969, -15.57353102523303434, -39.50595550450194082 ) ) ;
#22463=ORIENTED_EDGE ( 'NONE', *, *, #38766, .F. ) ;
#22465=CARTESIAN_POINT ( 'NONE',  ( 24.04215779552914256, -15.84268908224270511, -55.51678385230713531 ) ) ;
#22466=DIRECTION ( 'NONE',  ( 0.000000000000000000, 0.000000000000000000, -1.000000000000000000 ) ) ;
#22473=CARTESIAN_POINT ( 'NONE',  ( 8.380192598090266287, -13.82703671535675305, -32.86439260443115273 ) ) ;
#22475=ORIENTED_EDGE ( 'NONE', *, *, #47243, .F. ) ;
#22480=CARTESIAN_POINT ( 'NONE',  ( 23.97139847576909943, -16.01737648346080078, -48.02877399380358980 ) ) ;
#22486=CARTESIAN_POINT ( 'NONE',  ( 17.01654511880040133, -8.618792084267338893, -78.38711848170969176 ) ) ;
#22488=CARTESIAN_POINT ( 'NONE',  ( 9.567436321604839478, -18.18982893351659769, -39.72828012266349873 ) ) ;
#22493=CARTESIAN_POINT ( 'NONE',  ( 24.04493741226235315, -14.58064815428408245, -51.46599901981314673 ) ) ;
#22503=CARTESIAN_POINT ( 'NONE',  ( 16.34469624625884521, -23.55230478456017806, -32.28382467401409173 ) ) ;
#22511=CARTESIAN_POINT ( 'NONE',  ( 17.01981251849182186, -8.849199924388678085, -41.99448657106753302 ) ) ;
#22515=CARTESIAN_POINT ( 'NONE',  ( 10.31980611544169868, -19.60848604401130402, -49.26128910974169628 ) ) ;
#22522=CARTESIAN_POINT ( 'NONE',  ( 9.015194180556269643, -12.31312321847780034, -38.42578944456590051 ) ) ;
#22529=CARTESIAN_POINT ( 'NONE',  ( 15.09841768666722572, -7.705185590434979304, -45.25062777107746825 ) ) ;
#22530=CARTESIAN_POINT ( 'NONE',  ( 22.90093740290240731, -14.73039754886785957, -58.41115327826027936 ) ) ;
#22533=ORIENTED_EDGE ( 'NONE', *, *, #26950, .T. ) ;
#22536=ORIENTED_EDGE ( 'NONE', *, *, #1110, .F. ) ;
#22541=ORIENTED_EDGE ( 'NONE', *, *, #35366, .F. ) ;
#22544=DIRECTION ( 'NONE',  ( 1.000000000000000000, 0.000000000000000000, 0.000000000000000000 ) ) ;
#22545=CARTESIAN_POINT ( 'NONE',  ( 24.13155739828989965, -17.62138080134500129, -65.87052737365779365 ) ) ;
#22552=CARTESIAN_POINT ( 'NONE',  ( 11.20062545640499962, -21.19912070989539998, -56.96301931345279712 ) ) ;
#22554=CARTESIAN_POINT ( 'NONE',  ( 8.829388714618341183, -15.77602776797299988, -32.14999999999999858 ) ) ;
#22560=CARTESIAN_POINT ( 'NONE',  ( 8.298958134817842947, -14.29909715232032852, -60.56060963056555124 ) ) ;
#22561=CARTESIAN_POINT ( 'NONE',  ( 23.92311594283500042, -12.91222550170799899, -59.40131228588499823 ) ) ;
#22563=CARTESIAN_POINT ( 'NONE',  ( 20.07980155385570242, -22.42390109179229896, -32.14999999999999858 ) ) ;
#22570=VERTEX_POINT ( 'NONE', #45577 ) ;
#22578=ADVANCED_FACE ( 'NONE', ( #1292 ), #4965, .T. ) ;
#22579=DIRECTION ( 'NONE',  ( 0.000000000000000000, 0.000000000000000000, -1.000000000000000000 ) ) ;
#22585=CARTESIAN_POINT ( 'NONE',  ( 18.20460997748778098, -7.911086879560232710, -37.37566666715131447 ) ) ;
#22591=DIRECTION ( 'NONE',  ( 1.000000000000000000, 0.000000000000000000, 0.000000000000000000 ) ) ;
#22610=CARTESIAN_POINT ( 'NONE',  ( 9.369669958260699261, -20.33077770372739934, -32.59857632693769602 ) ) ;
#22615=CARTESIAN_POINT ( 'NONE',  ( 16.41974898881801082, -22.37754970791813136, -46.93937931256282070 ) ) ;
#22623=VECTOR ( 'NONE', #28821, 1000.000000000000000 ) ;
#22626=AXIS2_PLACEMENT_3D ( 'NONE', #44598, #28861, #8447 ) ;
#22628=CARTESIAN_POINT ( 'NONE',  ( 18.50775712175209620, -7.720120979975890307, -33.10062717276339583 ) ) ;
#22640=EDGE_CURVE ( 'NONE', #13029, #10507, #41125, .T. ) ;
#22644=CARTESIAN_POINT ( 'NONE',  ( 22.04684669439291156, -19.02418497068438796, -62.61948962174666633 ) ) ;
#22648=CARTESIAN_POINT ( 'NONE',  ( 9.366197046019539840, -18.73137511417689893, -49.93002833933049800 ) ) ;
#22655=CARTESIAN_POINT ( 'NONE',  ( 9.700417070101229555, -18.19071222218930117, -81.23899999999999011 ) ) ;
#22682=CARTESIAN_POINT ( 'NONE',  ( 22.65728558640282131, -17.99966492201340529, -38.95926740740573990 ) ) ;
#22684=CARTESIAN_POINT ( 'NONE',  ( 12.24155400994649945, -22.43059278844679838, -53.95269993303519840 ) ) ;
#22685=EDGE_LOOP ( 'NONE', ( #15901, #50402, #36607, #41105, #50062 ) ) ;
#22694=AXIS2_PLACEMENT_3D ( 'NONE', #39571, #40084, #19646 ) ;
#22702=CARTESIAN_POINT ( 'NONE',  ( 20.25033824699210072, -9.889252315854481168, -78.54555634383710583 ) ) ;
#22709=FACE_OUTER_BOUND ( 'NONE', #1346, .T. ) ;
#22710=CARTESIAN_POINT ( 'NONE',  ( 10.33272111206849964, -19.62722883991240153, -79.65462137872758319 ) ) ;
#22713=ORIENTED_EDGE ( 'NONE', *, *, #16678, .F. ) ;
#22716=ORIENTED_EDGE ( 'NONE', *, *, #35690, .T. ) ;
#22728=VECTOR ( 'NONE', #32597, 1000.000000000000000 ) ;
#22729=ORIENTED_EDGE ( 'NONE', *, *, #27017, .F. ) ;
#22737=CARTESIAN_POINT ( 'NONE',  ( 19.46890126474820093, -8.512333400185202237, -45.65220606189509311 ) ) ;
#22743=CARTESIAN_POINT ( 'NONE',  ( 9.543082594814544350, -13.84487447432519680, -77.53615328806994000 ) ) ;
#22745=CARTESIAN_POINT ( 'NONE',  ( 11.25287529172470080, -20.70714090792739981, -45.59048102137129632 ) ) ;
#22746=CARTESIAN_POINT ( 'NONE',  ( 19.54188575374945813, -9.703251766430753378, -44.11945704888728415 ) ) ;
#22751=CARTESIAN_POINT ( 'NONE',  ( 15.09847552854969344, -7.705178599813004681, -50.96600048343916001 ) ) ;
#22758=CARTESIAN_POINT ( 'NONE',  ( 8.223605785152290792, -15.61620117245469963, -52.50766849176299900 ) ) ;
#22760=CARTESIAN_POINT ( 'NONE',  ( 8.887019836252781246, -18.85787674178415330, -32.65851392028359612 ) ) ;
#22763=AXIS2_PLACEMENT_3D ( 'NONE', #23741, #35564, #8295 ) ;
#22768=CARTESIAN_POINT ( 'NONE',  ( 15.24823002788296122, -8.849177966009543539, -41.91115328570175080 ) ) ;
#22771=CARTESIAN_POINT ( 'NONE',  ( 12.40804001521799904, -9.627846319890059235, -45.77565614294249485 ) ) ;
#22776=CARTESIAN_POINT ( 'NONE',  ( 9.028267923962127739, -18.94728626226500268, -34.14796716713029667 ) ) ;
#22784=CARTESIAN_POINT ( 'NONE',  ( 23.83903608302206223, -13.54550562940452352, -45.70899248858425779 ) ) ;
#22801=CARTESIAN_POINT ( 'NONE',  ( 22.20375567613890055, -21.19651385660140264, -66.02896523578519350 ) ) ;
#22803=CARTESIAN_POINT ( 'NONE',  ( 23.83903869581317991, -17.68685937611830283, -47.59100309625389258 ) ) ;
#22809=CARTESIAN_POINT ( 'NONE',  ( 14.46478753480960044, -22.87708644708019889, -56.80458145132549674 ) ) ;
#22812=CARTESIAN_POINT ( 'NONE',  ( 9.738742532837820320, -12.64405718765570086, -32.14999999999999858 ) ) ;
#22817=CARTESIAN_POINT ( 'NONE',  ( 10.01530563823780007, -21.14294804030860320, -68.27383256501039455 ) ) ;
#22848=CARTESIAN_POINT ( 'NONE',  ( 9.458985575556051018, -14.34378805948378499, -65.51270995478979842 ) ) ;
#22853=ORIENTED_EDGE ( 'NONE', *, *, #44786, .T. ) ;
#22856=CARTESIAN_POINT ( 'NONE',  ( 21.09675763201389387, -21.77905901208185568, -77.79186885214345182 ) ) ;
#22868=CARTESIAN_POINT ( 'NONE',  ( 21.60877393982859473, -19.65386968817948343, -50.65516752091996722 ) ) ;
#22875=EDGE_CURVE ( 'NONE', #32305, #6769, #9092, .T. ) ;
#22877=DIRECTION ( 'NONE',  ( 1.000000000000000000, 0.000000000000000000, 0.000000000000000000 ) ) ;
#22878=AXIS2_PLACEMENT_3D ( 'NONE', #6434, #22393, #10628 ) ;
#22882=CARTESIAN_POINT ( 'NONE',  ( 23.71320255129930032, -13.58133288703929864, -81.20401221892029753 ) ) ;
#22883=EDGE_LOOP ( 'NONE', ( #47695, #7167, #33520, #1893, #50011, #33623 ) ) ;
#22891=CARTESIAN_POINT ( 'NONE',  ( 12.14987702140462744, -22.52875230863022793, -38.45899921809279220 ) ) ;
#22902=CARTESIAN_POINT ( 'NONE',  ( 22.36782798052980326, -11.53632343959220030, -66.88287958694509427 ) ) ;
#22907=DIRECTION ( 'NONE',  ( 0.000000000000000000, 0.000000000000000000, -1.000000000000000000 ) ) ;
#22911=VERTEX_POINT ( 'NONE', #43705 ) ;
#22912=ORIENTED_EDGE ( 'NONE', *, *, #28559, .T. ) ;
#22915=CARTESIAN_POINT ( 'NONE',  ( 21.82498608452069888, -10.18542486436930083, -81.23899999999999011 ) ) ;
#22919=ORIENTED_EDGE ( 'NONE', *, *, #6981, .F. ) ;
#22920=CARTESIAN_POINT ( 'NONE',  ( 9.366944253490801842, -14.82503573980447342, -79.49003206933410581 ) ) ;
#22922=CARTESIAN_POINT ( 'NONE',  ( 24.04513930477782679, -15.61618913701998146, -67.79233342760500136 ) ) ;
#22930=CARTESIAN_POINT ( 'NONE',  ( 22.90081829478373976, -15.57281448673799495, -40.45078489836800628 ) ) ;
#22935=B_SPLINE_CURVE_WITH_KNOTS ( 'NONE', 3,
 ( #4762, #28333, #32503, #36719, #19958, #16296, #35950, #16044, #31999, #1088, #12121, #48020, #40147, #8445, #24390, #4499, #48794, #20469, #28858, #44861, #29879, #22019, #9732, #15145, #21763, #29379 ),
 .UNSPECIFIED., .F., .F.,
 ( 4, 2, 2, 2, 2, 2, 2, 2, 2, 2, 2, 2, 4 ),
 ( 0.000000000000000000, 0.03124996214440351264, 0.06249992428880702527, 0.09374988643321054138, 0.1249998485776140505, 0.1562498107220175736, 0.1874997728664210828, 0.2187497350108245919, 0.2499996971552281011, 0.3124996214440353692, 0.3749995457328426096, 0.4374994700216498500, 0.4999993943104570904 ),
 .UNSPECIFIED. ) ;
#22936=CARTESIAN_POINT ( 'NONE',  ( 8.222937397696199469, -15.61618894467929941, -32.14999999999999858 ) ) ;
#22939=CARTESIAN_POINT ( 'NONE',  ( 18.37043360245199963, -23.13847801844509888, -55.69551641643489859 ) ) ;
#22949=CARTESIAN_POINT ( 'NONE',  ( 9.366809454094768839, -15.61635577034980038, -65.45282021618999124 ) ) ;
#22951=CARTESIAN_POINT ( 'NONE',  ( 9.367282414267279478, -15.61633198492950036, -43.45282021618999835 ) ) ;
#22952=CARTESIAN_POINT ( 'NONE',  ( 22.90015373937838916, -14.70062920033102749, -36.80410166171807873 ) ) ;
#22954=ORIENTED_EDGE ( 'NONE', *, *, #49637, .F. ) ;
#22955=CARTESIAN_POINT ( 'NONE',  ( 9.989812541601329698, -12.15320050589289913, -76.01055054980109560 ) ) ;
#22968=CYLINDRICAL_SURFACE ( 'NONE', #19745, 7.910999999999997812 ) ;
#22974=CARTESIAN_POINT ( 'NONE',  ( 24.04493737870865289, -14.58063638308804144, -39.75066769201711736 ) ) ;
#22979=CARTESIAN_POINT ( 'NONE',  ( 23.94343571634030354, -16.90563865392866205, -55.55974166775742873 ) ) ;
#22982=CARTESIAN_POINT ( 'NONE',  ( 24.04493739769619864, -15.61618894467929941, -32.14999999999999858 ) ) ;
#22986=EDGE_CURVE ( 'NONE', #35817, #12296, #4380, .T. ) ;
#22990=CARTESIAN_POINT ( 'NONE',  ( 10.22109116384483229, -12.20808603923138769, -51.61948645223564824 ) ) ;
#22991=CARTESIAN_POINT ( 'NONE',  ( 22.46011918284800757, -20.47784417130683821, -53.71600424433798082 ) ) ;
#22993=CARTESIAN_POINT ( 'NONE',  ( 14.42922720758920008, -23.27652253789360159, -40.58219447382339951 ) ) ;
#23000=CARTESIAN_POINT ( 'NONE',  ( 22.91342759294889930, -17.56068678909149838, -38.93609081202739475 ) ) ;
#23001=CARTESIAN_POINT ( 'NONE',  ( 9.367282414267279478, -15.61633198492950036, -43.45282021618999835 ) ) ;
#23003=AXIS2_PLACEMENT_3D ( 'NONE', #12192, #3041, #11169 ) ;
#23007=VECTOR ( 'NONE', #31433, 1000.000000000000000 ) ;
#23015=DIRECTION ( 'NONE',  ( 0.000000000000000000, 0.000000000000000000, -1.000000000000000000 ) ) ;
#23017=CARTESIAN_POINT ( 'NONE',  ( 8.222431652840050731, -15.61631456792169992, -70.50766849176299900 ) ) ;
#23026=CARTESIAN_POINT ( 'NONE',  ( 15.00250949113439880, -22.57768516236690104, -51.00410559314149594 ) ) ;
#23032=CARTESIAN_POINT ( 'NONE',  ( 8.816156803201931069, -12.78140736318490056, -32.40515068373079544 ) ) ;
#23033=VERTEX_POINT ( 'NONE', #39774 ) ;
#23038=( BOUNDED_CURVE ( )  B_SPLINE_CURVE ( 2, ( #49465, #29518, #49970 ),
 .UNSPECIFIED., .F., .T. ) 
 B_SPLINE_CURVE_WITH_KNOTS ( ( 3, 3 ),
 ( 2.168627590050209886, 3.232274745523169734 ),
 .UNSPECIFIED. ) 
 CURVE ( )  GEOMETRIC_REPRESENTATION_ITEM ( )  RATIONAL_B_SPLINE_CURVE ( ( 1.425426480542939967, 1.425426480542939967, 1.323085463760209857 ) ) 
 REPRESENTATION_ITEM ( '' )  );
#23044=ORIENTED_EDGE ( 'NONE', *, *, #17499, .T. ) ;
#23060=CARTESIAN_POINT ( 'NONE',  ( 7.891499209906831069, -15.40421541707130082, -60.80051578558619241 ) ) ;
#23066=CARTESIAN_POINT ( 'NONE',  ( 9.731824066760630387, -19.42665331309980203, -55.06176496792579655 ) ) ;
#23069=CARTESIAN_POINT ( 'NONE',  ( 9.859321938117989959, -19.95003254321919783, -32.14999999999999858 ) ) ;
#23070=AXIS2_PLACEMENT_3D ( 'NONE', #23083, #27027, #39101 ) ;
#23071=DIRECTION ( 'NONE',  ( 0.000000000000000000, 0.000000000000000000, -1.000000000000000000 ) ) ;
#23076=CARTESIAN_POINT ( 'NONE',  ( 21.58244677357819796, -21.80460281980919746, -61.77788021779359440 ) ) ;
#23083=CARTESIAN_POINT ( 'NONE',  ( 16.13393739769620083, -15.61618894467929941, -22.14999999999999858 ) ) ;
#23085=DIRECTION ( 'NONE',  ( 0.000000000000000000, 0.000000000000000000, -1.000000000000000000 ) ) ;
#23090=CARTESIAN_POINT ( 'NONE',  ( 17.19328695544820107, -8.241606262222608947, -79.77807145977529046 ) ) ;
#23107=CARTESIAN_POINT ( 'NONE',  ( 13.24540460468610270, -9.472626712212976585, -65.81300538149071144 ) ) ;
#23111=CARTESIAN_POINT ( 'NONE',  ( 9.366957159598959137, -16.50213183952788754, -59.41115353772929097 ) ) ;
#23112=ORIENTED_EDGE ( 'NONE', *, *, #32206, .T. ) ;
#23115=EDGE_CURVE ( 'NONE', #51612, #40071, #37758, .T. ) ;
#23117=CARTESIAN_POINT ( 'NONE',  ( 22.78356519185971862, -14.13275206067546463, -80.38311699616438943 ) ) ;
#23123=CARTESIAN_POINT ( 'NONE',  ( 23.54534064816039773, -12.00274526973129952, -31.64794915417429166 ) ) ;
#23137=CARTESIAN_POINT ( 'NONE',  ( 14.44977587363500149, -7.544888499689109906, -32.94218931063619493 ) ) ;
#23145=CARTESIAN_POINT ( 'NONE',  ( 24.04496217889941789, -15.61618911842929869, -37.79232902657031445 ) ) ;
#23149=CARTESIAN_POINT ( 'NONE',  ( 8.222937397696199469, -15.61618894467929941, -32.14999999999999858 ) ) ;
#23156=CARTESIAN_POINT ( 'NONE',  ( 11.63313639469540028, -21.55331658940179906, -65.77381455205440375 ) ) ;
#23163=CARTESIAN_POINT ( 'NONE',  ( 9.115768759226799745, -13.63938762484340117, -81.23899999999999011 ) ) ;
#23171=CARTESIAN_POINT ( 'NONE',  ( 23.58224949043920304, -15.59470245701460023, -81.23899999999999011 ) ) ;
#23173=ORIENTED_EDGE ( 'NONE', *, *, #18742, .T. ) ;
#23174=CARTESIAN_POINT ( 'NONE',  ( 12.09245220501500739, -10.13125348064280473, -79.75051504134326308 ) ) ;
#23184=CARTESIAN_POINT ( 'NONE',  ( 12.34850528888871857, -9.930145591977167285, -39.76618442199777803 ) ) ;
#23188=CARTESIAN_POINT ( 'NONE',  ( 9.367846250551377096, -16.45859118363538798, -39.80754656342805475 ) ) ;
#23189=CARTESIAN_POINT ( 'NONE',  ( 9.005166737681101097, -18.89755711361290125, -50.15019124198139622 ) ) ;
#23197=B_SPLINE_CURVE_WITH_KNOTS ( 'NONE', 3,
 ( #31195, #19425, #39604, #47226, #46975, #42773, #31455, #11058, #15245, #31965, #35673, #7129, #31705, #3963, #11316, #47987, #47730, #26760 ),
 .UNSPECIFIED., .F., .F.,
 ( 4, 2, 2, 2, 2, 2, 2, 2, 4 ),
 ( 0.000000000000000000, 0.06250000041432862696, 0.1250000008286572539, 0.1875000012429858809, 0.2500000016573145079, 0.3125000020716431348, 0.3750000024859717618, 0.4375000029003003887, 0.5000000033146290157 ),
 .UNSPECIFIED. ) ;
#23199=CARTESIAN_POINT ( 'NONE',  ( 8.223031589278729570, -15.61632747405269939, -32.50766849176289952 ) ) ;
#23202=CARTESIAN_POINT ( 'NONE',  ( 24.04478666521990959, -15.61618936535764668, -45.50767606031119783 ) ) ;
#23207=CARTESIAN_POINT ( 'NONE',  ( 10.67550186159990133, -20.68690643203139956, -35.82905861000619296 ) ) ;
#23211=CARTESIAN_POINT ( 'NONE',  ( 8.222957243667082139, -16.65188170221874131, -58.46600178368837675 ) ) ;
#23220=CARTESIAN_POINT ( 'NONE',  ( 17.16956237237686267, -7.705200009872939404, -67.04933363861024986 ) ) ;
#23227=CARTESIAN_POINT ( 'NONE',  ( 24.04465145034966156, -15.61618865458276595, -39.79233592887338489 ) ) ;
#23231=ORIENTED_EDGE ( 'NONE', *, *, #10497, .T. ) ;
#23232=CARTESIAN_POINT ( 'NONE',  ( 24.04424253783098209, -15.72944217639657083, -55.51222777783377893 ) ) ;
#23235=CARTESIAN_POINT ( 'NONE',  ( 22.42300288295763622, -13.03544233720007206, -46.32879295383082763 ) ) ;
#23240=ORIENTED_EDGE ( 'NONE', *, *, #16192, .F. ) ;
#23244=CARTESIAN_POINT ( 'NONE',  ( 24.04500464303940888, -15.61618902416171295, -53.50766607493442706 ) ) ;
#23245=CARTESIAN_POINT ( 'NONE',  ( 9.418507324180998452, -19.67694583463340052, -38.83937799042379879 ) ) ;
#23254=CARTESIAN_POINT ( 'NONE',  ( 20.83141696938240273, -20.87701063411540048, -45.11516743498959414 ) ) ;
#23255=CARTESIAN_POINT ( 'NONE',  ( 22.90093741598583676, -14.73038902033105479, -44.41114283429698162 ) ) ;
#23265=CARTESIAN_POINT ( 'NONE',  ( 17.16956573677604680, -23.52717739683416198, -58.25066468824845600 ) ) ;
#23266=CARTESIAN_POINT ( 'NONE',  ( 8.222954481030059881, -16.28154840277095872, -32.76556799064630354 ) ) ;
#23276=CARTESIAN_POINT ( 'NONE',  ( 11.06493085870990001, -10.71234031280460108, -53.69754924930450102 ) ) ;
#23282=CARTESIAN_POINT ( 'NONE',  ( 11.05757125146939934, -9.631379859604059845, -32.56358854585789686 ) ) ;
#23283=ORIENTED_EDGE ( 'NONE', *, *, #8811, .F. ) ;
#23300=ORIENTED_EDGE ( 'NONE', *, *, #38169, .F. ) ;
#23301=CARTESIAN_POINT ( 'NONE',  ( 22.46010115032094845, -20.47786891796735986, -35.71599943221371376 ) ) ;
#23305=CARTESIAN_POINT ( 'NONE',  ( 11.04065704516700031, -22.10010869329390104, -66.50427882216679620 ) ) ;
#23307=LINE ( 'NONE', #51384, #23007 ) ;
#23311=CARTESIAN_POINT ( 'NONE',  ( 16.17870178787689994, -8.166041969315839921, -51.73456986325379603 ) ) ;
#23315=ADVANCED_FACE ( 'NONE', ( #24984 ), #17672, .T. ) ;
#23323=CARTESIAN_POINT ( 'NONE',  ( 7.898808619120661234, -16.02285183855100215, -70.49196263479178981 ) ) ;
#23325=CARTESIAN_POINT ( 'NONE',  ( 21.19542947997879878, -21.50580551610960001, -32.14999999999999858 ) ) ;
#23334=CARTESIAN_POINT ( 'NONE',  ( 20.18583041119828891, -8.779548377150556249, -81.17805570793466075 ) ) ;
#23336=CARTESIAN_POINT ( 'NONE',  ( 8.222918874503296394, -14.86491039005461090, -64.82257030091628280 ) ) ;
#23337=CYLINDRICAL_SURFACE ( 'NONE', #36885, 6.766999999999998572 ) ;
#23339=CARTESIAN_POINT ( 'NONE',  ( 10.81269192673220125, -20.83069183200840158, -78.98588214913890226 ) ) ;
#23353=CARTESIAN_POINT ( 'NONE',  ( 22.57287615846372475, -13.45385276121991325, -66.34964033311129583 ) ) ;
#23360=CARTESIAN_POINT ( 'NONE',  ( 15.90741866609855037, -23.52440880927948186, -78.01678402928762068 ) ) ;
#23370=CARTESIAN_POINT ( 'NONE',  ( 22.08864837242989765, -9.913195135824970805, -33.54920349970110038 ) ) ;
#23373=CARTESIAN_POINT ( 'NONE',  ( 23.95250516387262252, -16.86464842754593008, -49.84272613458953316 ) ) ;
#23377=CARTESIAN_POINT ( 'NONE',  ( 16.74414179616239906, -7.792225870656369402, -73.53726979628919480 ) ) ;
#23382=EDGE_CURVE ( 'NONE', #22911, #50303, #17167, .T. ) ;
#23385=CARTESIAN_POINT ( 'NONE',  ( 20.71427229670339898, -9.243804751362528549, -78.98588214913890226 ) ) ;
#23400=CIRCLE ( 'NONE', #25087, 2.999999999999960920 ) ;
#23412=CARTESIAN_POINT ( 'NONE',  ( 12.13367023409020184, -9.330923878024021789, -60.38692723972829413 ) ) ;
#23417=CARTESIAN_POINT ( 'NONE',  ( 13.34937765935505638, -21.87182001026540945, -35.08569598604245954 ) ) ;
#23420=CARTESIAN_POINT ( 'NONE',  ( 11.89976507272660022, -9.206373029106490691, -81.23899999999999011 ) ) ;
#23426=CARTESIAN_POINT ( 'NONE',  ( 23.34584626182279976, -13.12694180994139970, -81.23899999999999011 ) ) ;
#23429=CARTESIAN_POINT ( 'NONE',  ( 20.11806357404540435, -8.703662688652663348, -53.17433719568577999 ) ) ;
#23430=ORIENTED_EDGE ( 'NONE', *, *, #20048, .T. ) ;
#23442=CYLINDRICAL_SURFACE ( 'NONE', #15019, 7.910999999999997812 ) ;
#23444=CYLINDRICAL_SURFACE ( 'NONE', #27068, 7.910999999999997812 ) ;
#23446=CARTESIAN_POINT ( 'NONE',  ( 11.50016019542810142, -9.282559888370199630, -54.58645138154409437 ) ) ;
#23460=CARTESIAN_POINT ( 'NONE',  ( 14.06333702061520086, -23.32130935170018304, -38.09100306346796572 ) ) ;
#23465=CARTESIAN_POINT ( 'NONE',  ( 9.375716657886298933, -12.48040407158219978, -38.20562654191490282 ) ) ;
#23467=ORIENTED_EDGE ( 'NONE', *, *, #36042, .F. ) ;
#23476=CARTESIAN_POINT ( 'NONE',  ( 8.222598545279129922, -15.61602001634830117, -66.50766849176299900 ) ) ;
#23489=CARTESIAN_POINT ( 'NONE',  ( 12.58751561127507124, -9.785251382443901136, -45.77867976294210450 ) ) ;
#23495=CARTESIAN_POINT ( 'NONE',  ( 9.569202567055908659, -17.83954696311837651, -51.74261907013472950 ) ) ;
#23496=CARTESIAN_POINT ( 'NONE',  ( 9.366957815752284588, -14.73024123919837969, -51.49448677520141615 ) ) ;
#23498=CARTESIAN_POINT ( 'NONE',  ( 8.886842905012061422, -12.60514776168469808, -49.13783902869429454 ) ) ;
#23501=CARTESIAN_POINT ( 'NONE',  ( 9.367814992753320524, -14.75118133266921916, -63.88787753192362828 ) ) ;
#23505=VECTOR ( 'NONE', #42196, 1000.000000000000000 ) ;
#23509=CARTESIAN_POINT ( 'NONE',  ( 10.63552672802899934, -20.03320595643510060, -57.63175854304149937 ) ) ;
#23520=CARTESIAN_POINT ( 'NONE',  ( 22.90071877914020249, -15.61618922162072565, -76.45281474520940890 ) ) ;
#23521=CARTESIAN_POINT ( 'NONE',  ( 9.366937397696199596, -15.61618894467949836, -28.45282021618999835 ) ) ;
#23524=CARTESIAN_POINT ( 'NONE',  ( 11.27235892926153937, -21.94242946667067073, -58.50066475901247998 ) ) ;
#23536=CARTESIAN_POINT ( 'NONE',  ( 20.63031468509390365, -10.18248394845440075, -54.17286283568619609 ) ) ;
#23541=CARTESIAN_POINT ( 'NONE',  ( 10.05032457551389946, -20.57364829529049999, -42.06986027349229573 ) ) ;
#23552=VECTOR ( 'NONE', #31104, 1000.000000000000000 ) ;
#23554=CARTESIAN_POINT ( 'NONE',  ( 8.428799735006899496, -13.54564620887036952, -74.59099179580000794 ) ) ;
#23556=CARTESIAN_POINT ( 'NONE',  ( 8.222373579151801337, -15.61629175287649929, -54.79233150823699816 ) ) ;
#23558=CARTESIAN_POINT ( 'NONE',  ( 23.73307481796224394, -17.88869294176529223, -43.88484386199081655 ) ) ;
#23559=CARTESIAN_POINT ( 'NONE',  ( 13.69578881323610275, -8.072486773562250306, -76.90822709060780937 ) ) ;
#23562=SURFACE_STYLE_FILL_AREA ( #7616 ) ;
#23566=CARTESIAN_POINT ( 'NONE',  ( 17.77171699767420066, -23.69705511221659933, -78.22868061958260455 ) ) ;
#23571=ORIENTED_EDGE ( 'NONE', *, *, #14256, .T. ) ;
#23572=CARTESIAN_POINT ( 'NONE',  ( 13.58872809970029927, -22.61823174907150147, -52.84363489814459314 ) ) ;
#23574=CARTESIAN_POINT ( 'NONE',  ( 10.99494701313530065, -21.43108936971439960, -32.14999999999999858 ) ) ;
#23577=DIRECTION ( 'NONE',  ( 0.000000000000000000, 0.000000000000000000, -1.000000000000000000 ) ) ;
#23579=AXIS2_PLACEMENT_3D ( 'NONE', #24610, #16512, #4723 ) ;
#23582=CARTESIAN_POINT ( 'NONE',  ( 24.25939741457850118, -17.01605330347319978, -75.56197422286328447 ) ) ;
#23589=EDGE_CURVE ( 'NONE', #14719, #36315, #45782, .T. ) ;
#23594=CARTESIAN_POINT ( 'NONE',  ( 2.277530937145189949, -15.61618894467929941, -32.14999999999999858 ) ) ;
#23595=CARTESIAN_POINT ( 'NONE',  ( 20.11801407433656408, -22.52874480314362771, -72.12568687505527976 ) ) ;
#23597=CARTESIAN_POINT ( 'NONE',  ( 19.39393648379719792, -8.917002444580459652, -77.87681711424829700 ) ) ;
#23600=CARTESIAN_POINT ( 'NONE',  ( 20.99563619527035030, -21.94233761205614286, -70.08400039586911134 ) ) ;
#23603=CARTESIAN_POINT ( 'NONE',  ( 22.90069280194860113, -15.61618434420927670, -40.45282443214609458 ) ) ;
#23606=CARTESIAN_POINT ( 'NONE',  ( 22.72481172681589712, -17.38743078316283075, -70.53615642371306649 ) ) ;
#23609=CYLINDRICAL_SURFACE ( 'NONE', #26750, 6.766999999999998572 ) ;
#23611=ADVANCED_FACE ( 'NONE', ( #9102 ), #36875, .T. ) ;
#23613=CARTESIAN_POINT ( 'NONE',  ( 20.03328359842011608, -10.03004935987004487, -66.14666764028179102 ) ) ;
#23614=EDGE_LOOP ( 'NONE', ( #40724, #7225, #6846, #10676 ) ) ;
#23617=CARTESIAN_POINT ( 'NONE',  ( 12.14974750058458675, -8.703698850530118492, -55.12565519788404345 ) ) ;
#23618=CARTESIAN_POINT ( 'NONE',  ( 21.54530164568834039, -19.77480089234691008, -58.66115332543646588 ) ) ;
#23619=ORIENTED_EDGE ( 'NONE', *, *, #14140, .F. ) ;
#23621=CARTESIAN_POINT ( 'NONE',  ( 21.72480972862922854, -21.21315989654026879, -77.75783541609207816 ) ) ;
#23622=EDGE_CURVE ( 'NONE', #41523, #14553, #23038, .T. ) ;
#23629=CARTESIAN_POINT ( 'NONE',  ( 20.52487568859579881, -8.637479824688210073, -41.47109660606309944 ) ) ;
#23630=DIRECTION ( 'NONE',  ( 0.000000000000000000, 0.000000000000000000, -1.000000000000000000 ) ) ;
#23632=( NAMED_UNIT ( * ) PLANE_ANGLE_UNIT ( ) SI_UNIT ( $, .RADIAN. ) );
#23635=CARTESIAN_POINT ( 'NONE',  ( 9.367462981151710721, -15.61611677545310073, -63.45282021618999124 ) ) ;
#23637=CARTESIAN_POINT ( 'NONE',  ( 12.07787674043479953, -22.33445654400859937, -70.68538827799879698 ) ) ;
#23638=CARTESIAN_POINT ( 'NONE',  ( 9.543072035750400417, -17.38746502142067740, -37.36948665442063344 ) ) ;
#23640=ADVANCED_FACE ( 'NONE', ( #5690 ), #42962, .T. ) ;
#23641=DIRECTION ( 'NONE',  ( 0.000000000000000000, 0.000000000000000000, -1.000000000000000000 ) ) ;
#23645=CARTESIAN_POINT ( 'NONE',  ( 15.50764696403139986, -7.394845927770500538, -44.98346683230629850 ) ) ;
#23650=CARTESIAN_POINT ( 'NONE',  ( 9.366759954081400608, -15.32006465563015851, -55.86110054242375611 ) ) ;
#23653=ORIENTED_EDGE ( 'NONE', *, *, #32267, .F. ) ;
#23656=CARTESIAN_POINT ( 'NONE',  ( 15.09845420510242242, -23.52719671236787846, -38.33399960928872474 ) ) ;
#23665=CARTESIAN_POINT ( 'NONE',  ( 22.46007902905824594, -10.75447858878715479, -75.58403018435342346 ) ) ;
#23668=CARTESIAN_POINT ( 'NONE',  ( 16.10260131614859702, -8.165973351266268665, -66.56600386269059300 ) ) ;
#23669=CARTESIAN_POINT ( 'NONE',  ( 23.04647760501543274, -11.63208930286926091, -41.34100076697600912 ) ) ;
#23673=CARTESIAN_POINT ( 'NONE',  ( 9.751163809707072971, -17.93838706908490366, -35.34166202078984043 ) ) ;
#23676=CARTESIAN_POINT ( 'NONE',  ( 9.950787553869369972, -11.43239409667170037, -81.23899999999999011 ) ) ;
#23683=CARTESIAN_POINT ( 'NONE',  ( 16.13393739769620083, -15.61618894467929941, -28.45282021618999835 ) ) ;
#23684=CARTESIAN_POINT ( 'NONE',  ( 22.09174715103110032, -10.52175256428180106, -81.23899999999999011 ) ) ;
#23686=CARTESIAN_POINT ( 'NONE',  ( 15.09845518977402890, -7.705181060181322650, -62.96600257953041790 ) ) ;
#23687=CARTESIAN_POINT ( 'NONE',  ( 14.06335473615125764, -7.911063951914787395, -73.20899817982366642 ) ) ;
#23690=CARTESIAN_POINT ( 'NONE',  ( 11.47502755572986111, -10.64500410686288667, -79.71330318819909166 ) ) ;
#23691=ORIENTED_EDGE ( 'NONE', *, *, #49644, .F. ) ;
#23692=CARTESIAN_POINT ( 'NONE',  ( 22.46011217105117908, -10.75452410440155404, -63.58399993108093895 ) ) ;
#23696=CARTESIAN_POINT ( 'NONE',  ( 11.02421726237627375, -21.68417027918511764, -50.23044728260685332 ) ) ;
#23700=CARTESIAN_POINT ( 'NONE',  ( 22.90069280194860113, -15.61618434420927670, -40.45282443214609458 ) ) ;
#23702=B_SPLINE_CURVE_WITH_KNOTS ( 'NONE', 3,
 ( #3139, #38259, #2879, #6546, #11001, #34569, #2352, #34307, #22768, #22511, #15185, #30887, #26969, #38787, #50574, #18847, #46399, #50320 ),
 .UNSPECIFIED., .F., .F.,
 ( 4, 2, 2, 2, 2, 2, 2, 2, 4 ),
 ( 0.000000000000000000, 0.06249996402432939774, 0.1249999280486587955, 0.1874998920729882002, 0.2499998560973175910, 0.3124998201216468985, 0.3749997841459761783, 0.4374997481703054580, 0.4999997121946347378 ),
 .UNSPECIFIED. ) ;
#23706=CARTESIAN_POINT ( 'NONE',  ( 18.49813341320899696, -8.133052878602720526, -64.88491241981458302 ) ) ;
#23710=TOROIDAL_SURFACE ( 'NONE', #12042, 7.050000000000200551, 2.999999999999960032 ) ;
#23711=CARTESIAN_POINT ( 'NONE',  ( 12.38873293430890143, -9.639902246245529938, -76.16898841192839598 ) ) ;
#23716=CARTESIAN_POINT ( 'NONE',  ( 9.833644626755106088, -20.45756770380817002, -32.29902853823453768 ) ) ;
#23724=CARTESIAN_POINT ( 'NONE',  ( 18.27890701731350021, -8.481348111111490340, -32.66030136746149992 ) ) ;
#23732=CARTESIAN_POINT ( 'NONE',  ( 22.89999440246446838, -14.86247066410843942, -58.81172304349431101 ) ) ;
#23734=CARTESIAN_POINT ( 'NONE',  ( 15.09848148096914322, -7.705177880388851541, -66.96600053909531880 ) ) ;
#23740=ORIENTED_EDGE ( 'NONE', *, *, #34004, .T. ) ;
#23741=CARTESIAN_POINT ( 'NONE',  ( 16.13393739769620083, -15.61618894467929941, -22.64999999999999858 ) ) ;
#23758=FACE_OUTER_BOUND ( 'NONE', #40867, .T. ) ;
#23759=CARTESIAN_POINT ( 'NONE',  ( 9.807841574886825953, -20.47795602692574946, -54.29933579507218866 ) ) ;
#23760=CARTESIAN_POINT ( 'NONE',  ( 23.00413257069000039, -11.82314717367879986, -57.85192144569239758 ) ) ;
#23770=CARTESIAN_POINT ( 'NONE',  ( 17.81845769390660195, -8.767470046512547910, -58.42394785367769572 ) ) ;
#23776=CARTESIAN_POINT ( 'NONE',  ( 24.04503344477293680, -15.61618896013167479, -37.50766614148061251 ) ) ;
#23778=CARTESIAN_POINT ( 'NONE',  ( 20.99564714593912029, -9.290049021956130915, -47.21600280735441402 ) ) ;
#23780=VECTOR ( 'NONE', #41252, 1000.000000000000000 ) ;
#23791=CARTESIAN_POINT ( 'NONE',  ( 17.93601177679079939, -8.797458371556761136, -60.03506373439399368 ) ) ;
#23798=CARTESIAN_POINT ( 'NONE',  ( 17.00712189924800199, -7.817195611598919847, -46.82299613730939569 ) ) ;
#23800=EDGE_CURVE ( 'NONE', #9084, #27518, #20851, .T. ) ;
#23811=CARTESIAN_POINT ( 'NONE',  ( 9.521363875773749541, -20.06653018670903066, -44.60392643449169725 ) ) ;
#23812=CARTESIAN_POINT ( 'NONE',  ( 20.50318394250193421, -8.990010964302234342, -77.19331134062903743 ) ) ;
#23813=CARTESIAN_POINT ( 'NONE',  ( 9.366383648607859769, -15.61614502978449970, -45.45282021618989177 ) ) ;
#23814=CARTESIAN_POINT ( 'NONE',  ( 23.67876224802138196, -13.17252032151039920, -49.40793180963832754 ) ) ;
#23816=CARTESIAN_POINT ( 'NONE',  ( 8.223551834036749497, -15.61610457483330094, -62.79233150823698395 ) ) ;
#23820=CARTESIAN_POINT ( 'NONE',  ( 21.43470869307749993, -9.300767839955041083, -69.51459820258440914 ) ) ;
#23822=CARTESIAN_POINT ( 'NONE',  ( 22.90056296481078135, -15.12337164449987270, -38.82400614065659283 ) ) ;
#23826=ORIENTED_EDGE ( 'NONE', *, *, #31890, .F. ) ;
#23827=CARTESIAN_POINT ( 'NONE',  ( 9.498384706515519582, -19.00383330141319860, -61.08240372876090163 ) ) ;
#23829=CARTESIAN_POINT ( 'NONE',  ( 10.46014298659379982, -20.82286570460119890, -32.14999999999999858 ) ) ;
#23834=CARTESIAN_POINT ( 'NONE',  ( 14.36887759788570129, -23.67021182843550164, -72.07634125606408304 ) ) ;
#23835=CARTESIAN_POINT ( 'NONE',  ( 23.42310265867699925, -15.54859658462440031, -32.14999999999999858 ) ) ;
#23849=CARTESIAN_POINT ( 'NONE',  ( 11.88155033719490028, -9.498681438118609321, -71.53930262915869775 ) ) ;
#23852=CARTESIAN_POINT ( 'NONE',  ( 18.20465959255140476, -23.32127698777276592, -70.20900000393402252 ) ) ;
#23860=CARTESIAN_POINT ( 'NONE',  ( 11.01510582436389818, -10.76437253241610037, -68.08865744343920312 ) ) ;
#23861=CARTESIAN_POINT ( 'NONE',  ( 9.366947021922275241, -16.50205762954551503, -71.41115368016832576 ) ) ;
#23867=CARTESIAN_POINT ( 'NONE',  ( 13.45712100228560182, -22.14131064160670093, -41.47109660606309944 ) ) ;
#23869=CARTESIAN_POINT ( 'NONE',  ( 10.66574938343825529, -11.58597127047126563, -65.65508628724941786 ) ) ;
#23870=VERTEX_POINT ( 'NONE', #45695 ) ;
#23872=CARTESIAN_POINT ( 'NONE',  ( 14.06319120082964780, -7.911106295796193955, -55.20898789521619676 ) ) ;
#23873=CARTESIAN_POINT ( 'NONE',  ( 22.90122453025153249, -15.61618899996915211, -58.45282045073077626 ) ) ;
#23875=CARTESIAN_POINT ( 'NONE',  ( 9.221348903864539537, -11.63216924204988167, -58.67431483814366544 ) ) ;
#23876=CARTESIAN_POINT ( 'NONE',  ( 11.27221720578971720, -21.94232306595641901, -78.21596981197565412 ) ) ;
#23879=CARTESIAN_POINT ( 'NONE',  ( 14.02945871500176267, -22.09610439658294823, -81.05293847742703406 ) ) ;
#23882=CARTESIAN_POINT ( 'NONE',  ( 23.32404688451439867, -11.58071553707250168, -41.62953446819029324 ) ) ;
#23883=CARTESIAN_POINT ( 'NONE',  ( 9.366764248923921343, -15.61602670952840199, -67.45282021618999124 ) ) ;
#23887=CARTESIAN_POINT ( 'NONE',  ( 12.14990538336951431, -22.52876835109338316, -42.45899798303421591 ) ) ;
#23888=CARTESIAN_POINT ( 'NONE',  ( 21.68851505677390179, -20.58140404089619935, -34.46484289138480506 ) ) ;
#23894=CARTESIAN_POINT ( 'NONE',  ( 13.55743739769619971, -15.61618894467929941, -40.14999999999999858 ) ) ;
#23896=CARTESIAN_POINT ( 'NONE',  ( 24.05953913179460102, -17.88941525576920100, -39.59657951998030256 ) ) ;
#23900=CARTESIAN_POINT ( 'NONE',  ( 9.205734167420709824, -3.616188944679339823, -32.14999999999999858 ) ) ;
#23901=CARTESIAN_POINT ( 'NONE',  ( 10.43067722519432117, -11.46704655386096938, -56.04737992177221884 ) ) ;
#23920=CARTESIAN_POINT ( 'NONE',  ( 12.81891151941730023, -22.28831737305080196, -63.71412234440029465 ) ) ;
#23921=CARTESIAN_POINT ( 'NONE',  ( 9.221497393660930797, -11.63191539839947808, -72.67433504022238822 ) ) ;
#23923=ORIENTED_EDGE ( 'NONE', *, *, #22986, .F. ) ;
#23926=VECTOR ( 'NONE', #6537, 1000.000000000000000 ) ;
#23927=CARTESIAN_POINT ( 'NONE',  ( 10.00551172459159943, -11.34028037768539932, -81.23899999999999011 ) ) ;
#23935=CARTESIAN_POINT ( 'NONE',  ( 22.21025937705890030, -10.69142112527120148, -81.23899999999999011 ) ) ;
#23936=CARTESIAN_POINT ( 'NONE',  ( 8.428884598867867339, -13.54533765120538469, -72.87566484255432897 ) ) ;
#23938=CARTESIAN_POINT ( 'NONE',  ( 9.367509928541279507, -15.61618483373539767, -35.84717978380999881 ) ) ;
#23941=AXIS2_PLACEMENT_3D ( 'NONE', #32031, #39930, #11903 ) ;
#23945=EDGE_LOOP ( 'NONE', ( #31435, #9353, #33470 ) ) ;
#23947=CARTESIAN_POINT ( 'NONE',  ( 16.13393739769620083, -15.61618894467929941, -22.14999999999999858 ) ) ;
#23950=CARTESIAN_POINT ( 'NONE',  ( 22.89327904803542069, -15.26842831173307680, -40.43646614761534153 ) ) ;
#23955=EDGE_CURVE ( 'NONE', #3350, #39386, #4619, .T. ) ;
#23956=CARTESIAN_POINT ( 'NONE',  ( 11.92027290906500170, -8.995631584423939842, -60.60709014237929892 ) ) ;
#23969=CARTESIAN_POINT ( 'NONE',  ( 16.13393739769620083, -15.61618894467929941, -32.14999999999999858 ) ) ;
#23971=CARTESIAN_POINT ( 'NONE',  ( 9.715893490282427436, -18.36164609346412036, -71.71806615547141917 ) ) ;
#23973=CARTESIAN_POINT ( 'NONE',  ( 8.744713964810220119, -16.56817550042480036, -32.02654991895249736 ) ) ;
#23975=ORIENTED_EDGE ( 'NONE', *, *, #25928, .F. ) ;
#23992=CARTESIAN_POINT ( 'NONE',  ( 9.366365007129969555, -15.61616877484880028, -59.84717978381009118 ) ) ;
#24000=CARTESIAN_POINT ( 'NONE',  ( 24.04490680206547992, -15.61618865440000192, -77.79233401716611240 ) ) ;
#24009=CARTESIAN_POINT ( 'NONE',  ( 22.04673644639285257, -12.24748586501180370, -34.28812115404945615 ) ) ;
#24011=CARTESIAN_POINT ( 'NONE',  ( 23.71976105349749986, -13.60570963499520047, -49.93002833933059748 ) ) ;
#24017=CARTESIAN_POINT ( 'NONE',  ( 21.48628740521269975, -11.02326954940469861, -54.62143916262389354 ) ) ;
#24027=CARTESIAN_POINT ( 'NONE',  ( 24.04309491136240950, -15.43172091523828193, -55.50025134836989338 ) ) ;
#24033=CARTESIAN_POINT ( 'NONE',  ( 8.428852674553464652, -17.68692416471474615, -52.70899795959353895 ) ) ;
#24036=ORIENTED_EDGE ( 'NONE', *, *, #38086, .T. ) ;
#24044=CARTESIAN_POINT ( 'NONE',  ( 13.30008482799290093, -22.07465922097630084, -59.08443656163060353 ) ) ;
#24047=EDGE_CURVE ( 'NONE', #21674, #38448, #2703, .T. ) ;
#24049=ORIENTED_EDGE ( 'NONE', *, *, #43268, .F. ) ;
#24050=ADVANCED_BREP_SHAPE_REPRESENTATION ( '', ( #44821, #20940 ), #10115 ) ;
#24051=CARTESIAN_POINT ( 'NONE',  ( 23.52949167024300081, -12.99082702962889968, -43.17892530838289389 ) ) ;
#24059=CARTESIAN_POINT ( 'NONE',  ( 8.222963953614101484, -16.65193083243917371, -64.46600189368123779 ) ) ;
#24061=CARTESIAN_POINT ( 'NONE',  ( 11.27216563094260948, -9.290094659119313647, -74.79930795411219435 ) ) ;
#24063=DIRECTION ( 'NONE',  ( 0.000000000000000000, 0.000000000000000000, -1.000000000000000000 ) ) ;
#24070=CARTESIAN_POINT ( 'NONE',  ( 20.11804278661281487, -22.52872763293026992, -62.12566277362611089 ) ) ;
#24075=CARTESIAN_POINT ( 'NONE',  ( 10.63124583700320080, -21.75647441392359838, -72.52491758300199365 ) ) ;
#24078=PRODUCT_CONTEXT ( 'NONE', #3339, 'mechanical' ) ;
#24080=CARTESIAN_POINT ( 'NONE',  ( 23.08447553396189988, -18.29885803002349931, -62.34990662577889964 ) ) ;
#24082=CARTESIAN_POINT ( 'NONE',  ( 12.26068851955660044, -22.47136919790400000, -32.14999999999999858 ) ) ;
#24089=CARTESIAN_POINT ( 'NONE',  ( 17.91047190612059836, -23.66768854721899729, -77.93854215477199432 ) ) ;
#24101=CARTESIAN_POINT ( 'NONE',  ( 21.73328479000853264, -21.28338846926865102, -66.04403864357212228 ) ) ;
#24103=CARTESIAN_POINT ( 'NONE',  ( 13.09279613430840072, -22.41752363878649845, -74.86649773383079776 ) ) ;
#24110=EDGE_CURVE ( 'NONE', #14613, #44797, #43007, .T. ) ;
#24113=LINE ( 'NONE', #51425, #17700 ) ;
#24118=CARTESIAN_POINT ( 'NONE',  ( 22.38486747247302233, -18.84477224106433724, -40.99906234112837922 ) ) ;
#24123=CARTESIAN_POINT ( 'NONE',  ( 10.22108902069157210, -19.02428818417996581, -59.28615350234715464 ) ) ;
#24131=CARTESIAN_POINT ( 'NONE',  ( 23.18974198866444070, -19.29653021243158051, -65.66053363189716663 ) ) ;
#24133=CARTESIAN_POINT ( 'NONE',  ( 8.236591511843410984, -17.98571379475770016, -46.69954605626199395 ) ) ;
#24135=CARTESIAN_POINT ( 'NONE',  ( 23.89322328078525004, -17.19759884022353447, -49.85630258065442177 ) ) ;
#24139=CARTESIAN_POINT ( 'NONE',  ( 13.63771406388430130, -22.63584441150059945, -36.84141082329339412 ) ) ;
#24145=CARTESIAN_POINT ( 'NONE',  ( 24.01641782975098849, -16.30113512706325096, -59.81990940572667625 ) ) ;
#24149=EDGE_CURVE ( 'NONE', #9856, #41648, #67, .T. ) ;
#24150=CARTESIAN_POINT ( 'NONE',  ( 12.53949280675929856, -8.195765183757039551, -40.86408241699819399 ) ) ;
#24154=CARTESIAN_POINT ( 'NONE',  ( 17.41362677703381934, -23.45504930627769369, -39.95607996559230202 ) ) ;
#24155=CARTESIAN_POINT ( 'NONE',  ( 24.04493742283841584, -16.65172811301406597, -63.83400030080247944 ) ) ;
#24158=ORIENTED_EDGE ( 'NONE', *, *, #22106, .T. ) ;
#24161=EDGE_CURVE ( 'NONE', #15474, #2233, #27079, .T. ) ;
#24169=DIRECTION ( 'NONE',  ( 0.000000000000000000, 0.000000000000000000, -1.000000000000000000 ) ) ;
#24173=CARTESIAN_POINT ( 'NONE',  ( 8.222342146248220018, -15.61610160653870061, -76.79233150823698395 ) ) ;
#24175=CARTESIAN_POINT ( 'NONE',  ( 9.659254613363348341, -12.81954403390899877, -81.58261298369839665 ) ) ;
#24183=CARTESIAN_POINT ( 'NONE',  ( 8.995234134042298990, -14.54159774915980030, -81.23899999999999011 ) ) ;
#24189=CARTESIAN_POINT ( 'NONE',  ( 21.88702750807829744, -19.77779051261680010, -81.23899999999999011 ) ) ;
#24192=CARTESIAN_POINT ( 'NONE',  ( 19.32514136844950059, -21.90576575011689897, -69.19772247832989365 ) ) ;
#24200=CARTESIAN_POINT ( 'NONE',  ( 22.90065656494205726, -15.61616387038935017, -34.45281736178981902 ) ) ;
#24206=CIRCLE ( 'NONE', #19230, 7.910999999999997812 ) ;
#24211=CARTESIAN_POINT ( 'NONE',  ( 23.77775089882910109, -17.39350808965049922, -65.36022600619639888 ) ) ;
#24212=ORIENTED_EDGE ( 'NONE', *, *, #7221, .T. ) ;
#24214=CARTESIAN_POINT ( 'NONE',  ( 22.90093739769620029, -15.61618894467913243, -28.45282021618999835 ) ) ;
#24225=CARTESIAN_POINT ( 'NONE',  ( 24.04493320937934442, -15.61618918076996110, -53.79232900421944663 ) ) ;
#24227=CARTESIAN_POINT ( 'NONE',  ( 22.31020800752009947, -11.44961052869560092, -34.87843143724279571 ) ) ;
#24235=CARTESIAN_POINT ( 'NONE',  ( 9.807739393606267342, -20.47782491541499894, -78.58399752127002102 ) ) ;
#24237=CARTESIAN_POINT ( 'NONE',  ( 20.99561924099482013, -21.94235114381296725, -51.79933308495947841 ) ) ;
#24243=DIRECTION ( 'NONE',  ( 0.000000000000000000, 0.000000000000000000, -1.000000000000000000 ) ) ;
#24249=VECTOR ( 'NONE', #11144, 1000.000000000000000 ) ;
#24261=CARTESIAN_POINT ( 'NONE',  ( 24.04424252334385059, -15.50293471796945610, -59.78776946088952116 ) ) ;
#24269=CARTESIAN_POINT ( 'NONE',  ( 21.13707352621340263, -9.570084705492890365, -53.73253703038420070 ) ) ;
#24272=DIRECTION ( 'NONE',  ( -1.000000000000000000, 0.000000000000000000, 0.000000000000000000 ) ) ;
#24276=CARTESIAN_POINT ( 'NONE',  ( 10.72264165131508129, -19.77489046754428159, -39.24448753485003749 ) ) ;
#24277=CARTESIAN_POINT ( 'NONE',  ( 15.19249895237999937, -8.626464141217319082, -54.30456343836939936 ) ) ;
#24280=ORIENTED_EDGE ( 'NONE', *, *, #1662, .F. ) ;
#24283=VECTOR ( 'NONE', #4311, 1000.000000000000000 ) ;
#24285=CARTESIAN_POINT ( 'NONE',  ( 9.629521756913746344, -18.06914890294566689, -77.73182532936149869 ) ) ;
#24299=EDGE_LOOP ( 'NONE', ( #9347, #26337 ) ) ;
#24301=CARTESIAN_POINT ( 'NONE',  ( 8.223401571539490362, -15.61634053766229968, -58.50766849176299900 ) ) ;
#24305=CARTESIAN_POINT ( 'NONE',  ( 19.58154494863300243, -9.463420391308439150, -68.11539470288319364 ) ) ;
#24310=CARTESIAN_POINT ( 'NONE',  ( 19.34621603495309827, -8.456020361482000425, -44.92174179178260118 ) ) ;
#24317=CARTESIAN_POINT ( 'NONE',  ( 17.16957795298714018, -23.52717565502518937, -63.96600271670024540 ) ) ;
#24327=CARTESIAN_POINT ( 'NONE',  ( 24.04461900158476340, -15.61617122039998051, -49.50766513674645353 ) ) ;
#24329=CARTESIAN_POINT ( 'NONE',  ( 18.20459087906956341, -23.32129640834502737, -62.20899636545249933 ) ) ;
#24334=CARTESIAN_POINT ( 'NONE',  ( 24.23497581208709661, -14.08129589808019944, -71.73272827236569071 ) ) ;
#24340=CARTESIAN_POINT ( 'NONE',  ( 18.03756209892690165, -8.413209921940879354, -59.81490083174298888 ) ) ;
#24350=CARTESIAN_POINT ( 'NONE',  ( 7.889763993325539460, -15.48841732168549967, -76.51260139562688778 ) ) ;
#24361=CARTESIAN_POINT ( 'NONE',  ( 8.428794512446437182, -17.68671268992946466, -72.70900503751509802 ) ) ;
#24365=CARTESIAN_POINT ( 'NONE',  ( 20.97695636306220024, -10.75840879809530115, -32.20281262070909634 ) ) ;
#24375=CARTESIAN_POINT ( 'NONE',  ( 21.54529203538514182, -19.77481408501185101, -70.66115603177810556 ) ) ;
#24380=CARTESIAN_POINT ( 'NONE',  ( 22.46008150092894695, -20.47789627965039472, -71.71596240367421160 ) ) ;
#24390=CARTESIAN_POINT ( 'NONE',  ( 17.75030770215581200, -9.027613932962333720, -50.02938860704751534 ) ) ;
#24396=CARTESIAN_POINT ( 'NONE',  ( 12.87384136754439901, -23.18946392516980026, -42.42172377882649670 ) ) ;
#24400=( BOUNDED_CURVE ( )  B_SPLINE_CURVE ( 2, ( #2204, #21842, #18181 ),
 .UNSPECIFIED., .F., .T. ) 
 B_SPLINE_CURVE_WITH_KNOTS ( ( 3, 3 ),
 ( 1.104980434577240045, 2.168627590050199672 ),
 .UNSPECIFIED. ) 
 CURVE ( )  GEOMETRIC_REPRESENTATION_ITEM ( )  RATIONAL_B_SPLINE_CURVE ( ( 1.323085463760209857, 1.425426480542939967, 1.425426480542939967 ) ) 
 REPRESENTATION_ITEM ( '' )  );
#24401=B_SPLINE_CURVE_WITH_KNOTS ( 'NONE', 3,
 ( #8855, #16450, #28229, #4648, #15940, #32149, #8331, #24805, #20365, #31898, #48166, #20888, #12527, #12017, #32402, #28750, #44232, #44749 ),
 .UNSPECIFIED., .F., .F.,
 ( 4, 2, 2, 2, 2, 2, 2, 2, 4 ),
 ( 0.000000000000000000, 0.06250019559800874813, 0.1250003911960174963, 0.1875005867940262583, 0.2500007823920349925, 0.3125009779900437268, 0.3750011735880525165, 0.4375013691860612508, 0.5000015647840699851 ),
 .UNSPECIFIED. ) ;
#24403=CARTESIAN_POINT ( 'NONE',  ( 12.37279372661770083, -22.04740127911919956, -38.90110303094750321 ) ) ;
#24405=CARTESIAN_POINT ( 'NONE',  ( 20.99558314274035098, -9.289997993926764508, -33.21599877232336695 ) ) ;
#24410=CARTESIAN_POINT ( 'NONE',  ( 16.13393739769620083, -15.61618894467929941, -32.14999999999999858 ) ) ;
#24411=CARTESIAN_POINT ( 'NONE',  ( 9.152839663105250878, -20.00332868818690102, -38.32907662296240403 ) ) ;
#24416=CARTESIAN_POINT ( 'NONE',  ( 8.222787824498201559, -15.61638397318239946, -64.79233150823698395 ) ) ;
#24426=FACE_OUTER_BOUND ( 'NONE', #24982, .T. ) ;
#24427=CARTESIAN_POINT ( 'NONE',  ( 12.72604533180880182, -21.52915663163615534, -65.11948762230144894 ) ) ;
#24430=CARTESIAN_POINT ( 'NONE',  ( 24.04476365437513152, -15.55955762548125243, -75.79004789881723525 ) ) ;
#24431=CARTESIAN_POINT ( 'NONE',  ( 9.366881967297588929, -15.61636073738300112, -79.84717978380999170 ) ) ;
#24436=PLANE ( 'NONE',  #14554 ) ;
#24449=CARTESIAN_POINT ( 'NONE',  ( 18.51896206369700337, -21.96195333999060040, -81.23899999999999011 ) ) ;
#24457=CARTESIAN_POINT ( 'NONE',  ( 22.48949605721776379, -18.55301542404961523, -34.98530465220235897 ) ) ;
#24460=LINE ( 'NONE', #4834, #24283 ) ;
#24461=EDGE_LOOP ( 'NONE', ( #15343, #6706, #40254, #49065 ) ) ;
#24468=CARTESIAN_POINT ( 'NONE',  ( 20.99563241385233070, -21.94234062699898402, -68.08399647260520737 ) ) ;
#24471=CARTESIAN_POINT ( 'NONE',  ( 22.87714163486811358, -16.92332580520769625, -62.90867644139516557 ) ) ;
#24473=CARTESIAN_POINT ( 'NONE',  ( 16.92883245282440186, -23.42355021687080097, -57.75520862408900058 ) ) ;
#24476=LINE ( 'NONE', #24214, #22728 ) ;
#24480=CARTESIAN_POINT ( 'NONE',  ( 12.14982920353035567, -22.52872525748182042, -36.45899726116088146 ) ) ;
#24490=CARTESIAN_POINT ( 'NONE',  ( 18.32870867059520137, -8.496520876714420467, -48.66252544231259236 ) ) ;
#24492=CARTESIAN_POINT ( 'NONE',  ( 12.65447590535301892, -9.481377877827592116, -34.18295494821030900 ) ) ;
#24494=CARTESIAN_POINT ( 'NONE',  ( 11.55666225148396720, -9.119571253868539173, -81.09705367392385256 ) ) ;
#24497=CARTESIAN_POINT ( 'NONE',  ( 8.223571189834400386, -15.61612039429540033, -78.79233150823698395 ) ) ;
#24514=CARTESIAN_POINT ( 'NONE',  ( 8.222911052588615988, -16.65154387527992341, -56.46599083452874623 ) ) ;
#24517=CARTESIAN_POINT ( 'NONE',  ( 22.90106509282977854, -15.61618896609811458, -36.45282238757207693 ) ) ;
#24523=CARTESIAN_POINT ( 'NONE',  ( 22.90065656494205726, -15.61616387038935017, -34.45281736178981902 ) ) ;
#24524=CARTESIAN_POINT ( 'NONE',  ( 8.428873804167068329, -17.68700099338225940, -54.42433541308667344 ) ) ;
#24526=CARTESIAN_POINT ( 'NONE',  ( 12.52169745332239970, -22.58314453344630124, -64.66474951716369901 ) ) ;
#24535=CARTESIAN_POINT ( 'NONE',  ( 17.16957476740626021, -7.705201780575073656, -41.33399786311579760 ) ) ;
#24540=CARTESIAN_POINT ( 'NONE',  ( 24.04493738470190323, -14.58064157137056860, -37.46600467335122175 ) ) ;
#24542=CYLINDRICAL_SURFACE ( 'NONE', #24607, 7.910999999999997812 ) ;
#24550=CARTESIAN_POINT ( 'NONE',  ( 14.06328036766014122, -23.32129468089506830, -52.37566376501965237 ) ) ;
#24555=CARTESIAN_POINT ( 'NONE',  ( 23.18087123250600357, -15.90477637036519987, -62.86020799324039388 ) ) ;
#24562=CARTESIAN_POINT ( 'NONE',  ( 10.81957041042960022, -20.25300490191509795, -69.22445973777388417 ) ) ;
#24565=CARTESIAN_POINT ( 'NONE',  ( 20.11812065015670825, -22.52868107655917029, -80.12566639359206988 ) ) ;
#24574=CARTESIAN_POINT ( 'NONE',  ( 15.09849988506595686, -23.52720223303058944, -64.04933591286372518 ) ) ;
#24580=CARTESIAN_POINT ( 'NONE',  ( 23.83903480973297562, -17.68687855746657789, -59.59100454946410252 ) ) ;
#24583=CARTESIAN_POINT ( 'NONE',  ( 14.06324741486789875, -23.32128614899894714, -44.09103022834820962 ) ) ;
#24590=CARTESIAN_POINT ( 'NONE',  ( 23.98623646584669800, -13.10140875542660055, -75.69367482554660853 ) ) ;
#24597=CARTESIAN_POINT ( 'NONE',  ( 10.52009571295500123, -20.51429830889400208, -69.00429683512291490 ) ) ;
#24604=DIRECTION ( 'NONE',  ( 1.000000000000000000, 0.000000000000000000, 0.000000000000000000 ) ) ;
#24606=ADVANCED_FACE ( 'NONE', ( #42150 ), #10441, .T. ) ;
#24607=AXIS2_PLACEMENT_3D ( 'NONE', #33197, #9113, #44494 ) ;
#24610=CARTESIAN_POINT ( 'NONE',  ( 16.13393739769620083, -15.61618894467929941, -32.14999999999999858 ) ) ;
#24618=EDGE_CURVE ( 'NONE', #11278, #36315, #45192, .T. ) ;
#24619=ORIENTED_EDGE ( 'NONE', *, *, #157, .T. ) ;
#24622=CARTESIAN_POINT ( 'NONE',  ( 8.222920464335484070, -16.32242060214289836, -66.76390504089123112 ) ) ;
#24624=CARTESIAN_POINT ( 'NONE',  ( 18.28036160049749981, -8.897899018898199230, -34.05125434552689967 ) ) ;
#24658=CARTESIAN_POINT ( 'NONE',  ( 10.71758635354190048, -21.83276850440699945, -40.52046943329969508 ) ) ;
#24663=CARTESIAN_POINT ( 'NONE',  ( 24.04493738597581753, -16.65172954098637348, -41.83399762327896809 ) ) ;
#24664=CARTESIAN_POINT ( 'NONE',  ( 9.334730646583459190, -18.66208476771889835, -35.09859433989379340 ) ) ;
#24669=CARTESIAN_POINT ( 'NONE',  ( 10.84455767947489946, -9.291223892962099384, -48.78597552336009358 ) ) ;
#24690=FACE_OUTER_BOUND ( 'NONE', #32308, .T. ) ;
#24693=CARTESIAN_POINT ( 'NONE',  ( 24.04493741173050481, -14.58064981991307008, -73.46600114540449056 ) ) ;
#24694=CARTESIAN_POINT ( 'NONE',  ( 20.79454452025889921, -20.90970388501609989, -61.11739150984060132 ) ) ;
#24703=ORIENTED_EDGE ( 'NONE', *, *, #575, .T. ) ;
#24706=ORIENTED_EDGE ( 'NONE', *, *, #49462, .F. ) ;
#24709=CARTESIAN_POINT ( 'NONE',  ( 20.84116112335389914, -20.77990536183390091, -81.23899999999999011 ) ) ;
#24710=( BOUNDED_CURVE ( )  B_SPLINE_CURVE ( 2, ( #7752, #16629, #41001 ),
 .UNSPECIFIED., .F., .T. ) 
 B_SPLINE_CURVE_WITH_KNOTS ( ( 3, 3 ),
 ( 2.168627590050209886, 3.232274745523169734 ),
 .UNSPECIFIED. ) 
 CURVE ( )  GEOMETRIC_REPRESENTATION_ITEM ( )  RATIONAL_B_SPLINE_CURVE ( ( 1.425426480542949959, 1.425426480542949959, 1.323085463760220071 ) ) 
 REPRESENTATION_ITEM ( '' )  );
#24716=ORIENTED_EDGE ( 'NONE', *, *, #19706, .T. ) ;
#24733=CARTESIAN_POINT ( 'NONE',  ( 17.06159277801890184, -7.823486994871330147, -62.82522021216060892 ) ) ;
#24739=DIRECTION ( 'NONE',  ( -0.5720614028176835841, -0.4156269377774527984, 0.7071067811865484609 ) ) ;
#24748=AXIS2_PLACEMENT_3D ( 'NONE', #50382, #23085, #30948 ) ;
#24753=ORIENTED_EDGE ( 'NONE', *, *, #14441, .F. ) ;
#24754=CARTESIAN_POINT ( 'NONE',  ( 17.84071041520759948, -22.86833484813690021, -45.49376819976789932 ) ) ;
#24759=CARTESIAN_POINT ( 'NONE',  ( 9.080923589672684315, -11.95388292134956565, -80.94469259108042536 ) ) ;
#24764=CARTESIAN_POINT ( 'NONE',  ( 18.20462978460193071, -23.32128541091630325, -51.92433345086598706 ) ) ;
#24782=CARTESIAN_POINT ( 'NONE',  ( 23.04645064152602174, -11.63203833470640447, -59.62568821185394796 ) ) ;
#24785=B_SPLINE_CURVE_WITH_KNOTS ( 'NONE', 3,
 ( #41309, #21377, #49194, #13288, #44724, #8571, #40532, #40789, #691, #32905, #21123 ),
 .UNSPECIFIED., .F., .F.,
 ( 4, 1, 1, 1, 1, 1, 1, 1, 4 ),
 ( 0.000000000000000000, 0.01167379492393827607, 0.09089272598764548683, 0.1701116570511966297, 0.2493305881149038561, 0.3285495191784527091, 0.4077684502420016455, 0.4869873813057088441, 0.5000036202821666054 ),
 .UNSPECIFIED. ) ;
#24791=CARTESIAN_POINT ( 'NONE',  ( 23.74604872763389807, -17.52472469027490121, -66.09069027630880555 ) ) ;
#24793=LINE ( 'NONE', #4902, #51464 ) ;
#24805=CARTESIAN_POINT ( 'NONE',  ( 14.36267143126516821, -9.025320511040868965, -37.86948818684339813 ) ) ;
#24808=FACE_OUTER_BOUND ( 'NONE', #46146, .T. ) ;
#24810=CARTESIAN_POINT ( 'NONE',  ( 23.25051134834439992, -17.84844637390679978, -32.14999999999999858 ) ) ;
#24820=CARTESIAN_POINT ( 'NONE',  ( 17.41965231446239670, -8.681529881159590900, -68.40553316769369019 ) ) ;
#24821=ORIENTED_EDGE ( 'NONE', *, *, #28170, .F. ) ;
#24825=CARTESIAN_POINT ( 'NONE',  ( 22.90093738767722797, -16.50198128633406469, -42.49448633122971586 ) ) ;
#24828=CARTESIAN_POINT ( 'NONE',  ( 17.58314231216230183, -22.51853375007059910, -62.88694525268430624 ) ) ;
#24833=EDGE_CURVE ( 'NONE', #47610, #19315, #10360, .T. ) ;
#24839=CARTESIAN_POINT ( 'NONE',  ( 16.13393739769620083, -15.61618894467929941, -23.15000000000000213 ) ) ;
#24842=AXIS2_PLACEMENT_3D ( 'NONE', #1748, #18241, #34209 ) ;
#24844=CARTESIAN_POINT ( 'NONE',  ( 8.222934311419814790, -16.65171382147144996, -60.46600640966879325 ) ) ;
#24849=CARTESIAN_POINT ( 'NONE',  ( 10.72267144924497018, -11.45744918686567360, -67.66115304884627335 ) ) ;
#24855=CARTESIAN_POINT ( 'NONE',  ( 14.66333043824689852, -7.907488096807699485, -33.45249067809769628 ) ) ;
#24861=CARTESIAN_POINT ( 'NONE',  ( 13.99783841214989977, -22.75367974531040360, -62.82522021216060892 ) ) ;
#24862=CARTESIAN_POINT ( 'NONE',  ( 13.20791805462510027, -21.71788541402070294, -31.48951129204709787 ) ) ;
#24867=EDGE_CURVE ( 'NONE', #2213, #41372, #12064, .T. ) ;
#24880=CARTESIAN_POINT ( 'NONE',  ( 24.03439145476966488, -16.03333523629986956, -65.80911902704585259 ) ) ;
#24882=CARTESIAN_POINT ( 'NONE',  ( 9.088594551554871614, -15.94130873329680043, -39.43814165785299508 ) ) ;
#24889=CARTESIAN_POINT ( 'NONE',  ( 11.98394575196030054, -21.80361681728220091, -75.75539986607049059 ) ) ;
#24899=CARTESIAN_POINT ( 'NONE',  ( 14.06314050699439733, -23.32125855261902103, -72.09094108337404805 ) ) ;
#24905=B_SPLINE_CURVE_WITH_KNOTS ( 'NONE', 3,
 ( #38399, #22133, #31471, #47244, #43306, #2497, #14291, #18477, #10105, #21876, #5911, #25797, #11334, #19441, #33925, #14033, #35424, #5662, #17703, #15518, #29734, #42336, #49686, #46014, #6435, #26065, #39369, #15261, #42072, #46280, #38140, #47495, #3470, #6174, #31217, #51423, #2240, #27298, #7398, #41805, #45750, #18216, #11592, #41546, #33671, #34181, #21609 ),
 .UNSPECIFIED., .F., .F.,
 ( 4, 2, 2, 2, 2, 2, 2, 1, 1, 1, 1, 2, 2, 2, 2, 2, 2, 2, 1, 1, 1, 2, 2, 2, 2, 2, 4 ),
 ( 0.5000060683415493701, 0.5312556890702444523, 0.5625053097989395345, 0.5937549305276346168, 0.6093797408919819913, 0.6171921460741557341, 0.6210983486652426055, 0.6230514499607860968, 0.6240280006085577869, 0.6245162759324436319, 0.6247604135943864989, 0.6248824824253578214, 0.6250045512563292549, 0.6562541719849754873, 0.6875037927136217197, 0.7187534134422679521, 0.7343782238065911239, 0.7421906289887525432, 0.7460968315798330863, 0.7480499328753733579, 0.7490264835231437157, 0.7495147588470287836, 0.7500030341709139625, 0.8125022756281854441, 0.8750015170854569257, 0.9375007585427284074, 1.000000000000000000 ),
 .UNSPECIFIED. ) ;
#24908=CARTESIAN_POINT ( 'NONE',  ( 21.54527551665228913, -11.45754112647657053, -70.24448936511146258 ) ) ;
#24909=DIRECTION ( 'NONE',  ( 0.000000000000000000, 0.000000000000000000, 1.000000000000000000 ) ) ;
#24916=CARTESIAN_POINT ( 'NONE',  ( 22.48256449764289755, -10.35523332789670192, -55.57206633538729790 ) ) ;
#24924=CARTESIAN_POINT ( 'NONE',  ( 23.57696182004550067, -15.94525348384249952, -32.24671282160349506 ) ) ;
#24925=CARTESIAN_POINT ( 'NONE',  ( 10.96238827582470066, -11.05823734394309987, -32.14999999999999858 ) ) ;
#24930=CARTESIAN_POINT ( 'NONE',  ( 17.49881693170749841, -23.74759869739819962, -51.95473276590490030 ) ) ;
#24936=CARTESIAN_POINT ( 'NONE',  ( 9.367540081427694787, -15.04338014694595316, -51.87411835802699045 ) ) ;
#24946=CARTESIAN_POINT ( 'NONE',  ( 21.54530371564770519, -19.77479805983715977, -64.66115530570463932 ) ) ;
#24949=CARTESIAN_POINT ( 'NONE',  ( 20.92357090894525840, -20.46386084668973027, -66.70452729442683903 ) ) ;
#24953=CARTESIAN_POINT ( 'NONE',  ( 24.04473007462266310, -15.61618926727986789, -75.50766188105974663 ) ) ;
#24954=ORIENTED_EDGE ( 'NONE', *, *, #20791, .T. ) ;
#24957=CYLINDRICAL_SURFACE ( 'NONE', #32591, 7.910999999999997812 ) ;
#24963=ORIENTED_EDGE ( 'NONE', *, *, #20937, .F. ) ;
#24966=CARTESIAN_POINT ( 'NONE',  ( 23.12137736902419860, -17.69276842965039975, -81.23899999999999011 ) ) ;
#24977=CARTESIAN_POINT ( 'NONE',  ( 24.04493618318231185, -15.62127662466025235, -33.79253448095708023 ) ) ;
#24978=AXIS2_PLACEMENT_3D ( 'NONE', #353, #37292, #12678 ) ;
#24982=EDGE_LOOP ( 'NONE', ( #13220, #29493, #1402, #43894 ) ) ;
#24984=FACE_OUTER_BOUND ( 'NONE', #3195, .T. ) ;
#24990=CARTESIAN_POINT ( 'NONE',  ( 20.51459614682930166, -22.12745434449419690, -73.59899483681280685 ) ) ;
#25000=VECTOR ( 'NONE', #12024, 1000.000000000000000 ) ;
#25007=CARTESIAN_POINT ( 'NONE',  ( 12.14986774143145887, -22.52874705890221918, -54.45899922363309997 ) ) ;
#25009=CARTESIAN_POINT ( 'NONE',  ( 16.45875955084829911, -23.05938616812849773, -47.55346040742190183 ) ) ;
#25019=CARTESIAN_POINT ( 'NONE',  ( 19.06574088075160134, -9.201589384987739706, -60.48364006133169823 ) ) ;
#25020=CARTESIAN_POINT ( 'NONE',  ( 16.13393739769620083, -15.61618894467929941, -22.14999999999999858 ) ) ;
#25032=ORIENTED_EDGE ( 'NONE', *, *, #1805, .F. ) ;
#25033=CARTESIAN_POINT ( 'NONE',  ( 16.13393739769620083, -15.61618894467929941, -24.90346750000000142 ) ) ;
#25035=CARTESIAN_POINT ( 'NONE',  ( 23.06214062797170072, -27.61618894467930119, -24.14999999999999858 ) ) ;
#25039=CYLINDRICAL_SURFACE ( 'NONE', #5032, 7.910999999999997812 ) ;
#25045=VECTOR ( 'NONE', #23577, 1000.000000000000000 ) ;
#25048=CARTESIAN_POINT ( 'NONE',  ( 11.24659819205199973, -9.476102375211780782, -65.29850096567270157 ) ) ;
#25064=CARTESIAN_POINT ( 'NONE',  ( 15.18614069519726151, -7.687728170468655975, -54.97012589771951951 ) ) ;
#25065=CARTESIAN_POINT ( 'NONE',  ( 23.20356372514779864, -14.30628808687479925, -32.14999999999999858 ) ) ;
#25069=CARTESIAN_POINT ( 'NONE',  ( 8.428879373767653505, -17.68702123896981249, -74.42433509932602931 ) ) ;
#25077=CARTESIAN_POINT ( 'NONE',  ( 9.100060599342889134, -15.09933658661340239, -65.87052737365789312 ) ) ;
#25086=CARTESIAN_POINT ( 'NONE',  ( 17.53874363813559967, -8.704671157431098649, -70.01664904841010184 ) ) ;
#25087=AXIS2_PLACEMENT_3D ( 'NONE', #29291, #4936, #28771 ) ;
#25091=CARTESIAN_POINT ( 'NONE',  ( 22.46012480422232471, -20.47783645966823585, -80.00066668459615471 ) ) ;
#25098=CARTESIAN_POINT ( 'NONE',  ( 9.221499452342687420, -19.60046601118327914, -64.34100209943599680 ) ) ;
#25101=EDGE_CURVE ( 'NONE', #26370, #49152, #16181, .T. ) ;
#25102=CARTESIAN_POINT ( 'NONE',  ( 11.27224481477622575, -21.94234313428745153, -60.21602416443509753 ) ) ;
#25103=CARTESIAN_POINT ( 'NONE',  ( 29.06214062797170072, -15.61618894467929941, -23.15000000000000213 ) ) ;
#25105=B_SPLINE_CURVE_WITH_KNOTS ( 'NONE', 3,
 ( #35023, #14089, #38985, #19048, #38456, #34766, #10426, #22710, #26638, #49998, #51027 ),
 .UNSPECIFIED., .F., .F.,
 ( 4, 1, 1, 1, 1, 1, 1, 1, 4 ),
 ( 0.4999975329053952255, 0.5076261421407139984, 0.5868450732042660434, 0.6660640042678135364, 0.7452829353315238992, 0.8245018663950713922, 0.9037207974587817549, 0.9829397285223337999, 1.000000000000000000 ),
 .UNSPECIFIED. ) ;
#25106=EDGE_CURVE ( 'NONE', #48357, #13535, #47651, .T. ) ;
#25109=EDGE_CURVE ( 'NONE', #33352, #18872, #49570, .T. ) ;
#25110=CARTESIAN_POINT ( 'NONE',  ( 11.97539229837822106, -10.20477340020057611, -67.74448618190876914 ) ) ;
#25113=CARTESIAN_POINT ( 'NONE',  ( 18.20460328303584419, -7.911084987229377141, -53.37566667684684774 ) ) ;
#25116=CARTESIAN_POINT ( 'NONE',  ( 8.087912829374468870, -13.81502027023469914, -78.86243206809139394 ) ) ;
#25120=ORIENTED_EDGE ( 'NONE', *, *, #18092, .T. ) ;
#25128=CARTESIAN_POINT ( 'NONE',  ( 21.98073010695399887, -11.67187985524660121, -34.65826853459179802 ) ) ;
#25143=ORIENTED_EDGE ( 'NONE', *, *, #39989, .F. ) ;
#25147=CARTESIAN_POINT ( 'NONE',  ( 12.14991548571375368, -22.52877406651395376, -74.45899817883974947 ) ) ;
#25149=CARTESIAN_POINT ( 'NONE',  ( 19.77219298086049903, -22.11770738490020349, -80.57026077041129497 ) ) ;
#25153=DIRECTION ( 'NONE',  ( 0.000000000000000000, 0.000000000000000000, 1.000000000000000000 ) ) ;
#25156=CARTESIAN_POINT ( 'NONE',  ( 16.58539016039730285, -8.179598009217608379, -72.58664262352569096 ) ) ;
#25157=EDGE_LOOP ( 'NONE', ( #22426, #15393, #35759, #39928 ) ) ;
#25160=CARTESIAN_POINT ( 'NONE',  ( 17.45133669559110956, -7.792397174005662563, -49.34550584340571788 ) ) ;
#25162=CARTESIAN_POINT ( 'NONE',  ( 8.222313118464692039, -15.61611924975770016, -60.79233150823699816 ) ) ;
#25163=B_SPLINE_CURVE_WITH_KNOTS ( 'NONE', 3,
 ( #24497, #674, #20578, #20840, #24235, #13013, #36837, #32882, #36062, #40515, #48124, #48916, #4604, #8287, #44967, #12748, #36571, #28703 ),
 .UNSPECIFIED., .F., .F.,
 ( 4, 2, 2, 2, 2, 2, 2, 2, 4 ),
 ( 0.000000000000000000, 0.06250019609009530019, 0.1250003921801906004, 0.1875005882702859006, 0.2500007843603812008, 0.3125009804504764732, 0.3750011765405718012, 0.4375013726306671291, 0.5000015687207624016 ),
 .UNSPECIFIED. ) ;
#25168=CARTESIAN_POINT ( 'NONE',  ( 24.04493739769619864, -15.61618894467929941, -32.14999999999999858 ) ) ;
#25176=FACE_OUTER_BOUND ( 'NONE', #17843, .T. ) ;
#25184=CARTESIAN_POINT ( 'NONE',  ( 8.654140298178170099, -18.27765407811988752, -66.39876892714730161 ) ) ;
#25186=CARTESIAN_POINT ( 'NONE',  ( 15.17406030731610045, -7.427089114582080320, -55.25519061113279662 ) ) ;
#25191=CARTESIAN_POINT ( 'NONE',  ( 15.69588917291320129, -8.178796420554320434, -45.71393110241879754 ) ) ;
#25193=DIRECTION ( 'NONE',  ( 1.000000000000000000, 0.000000000000000000, 0.000000000000000000 ) ) ;
#25199=CARTESIAN_POINT ( 'NONE',  ( 13.45088311011700100, -23.41259455232169984, -52.11317062803209410 ) ) ;
#25218=CARTESIAN_POINT ( 'NONE',  ( 22.21960090659290188, -18.66279415813841069, -66.60040840573597620 ) ) ;
#25222=CARTESIAN_POINT ( 'NONE',  ( 12.72599752907515658, -9.703248301412761734, -47.78615421569977428 ) ) ;
#25231=VERTEX_POINT ( 'NONE', #43125 ) ;
#25233=EDGE_LOOP ( 'NONE', ( #32416, #21363, #17089, #13738 ) ) ;
#25236=CARTESIAN_POINT ( 'NONE',  ( 21.36642042239409989, -20.32905245748499823, -81.23899999999999011 ) ) ;
#25244=CARTESIAN_POINT ( 'NONE',  ( 22.90125369822447610, -15.85481226531381616, -68.85839675053532005 ) ) ;
#25249=CARTESIAN_POINT ( 'NONE',  ( 22.90093739769620029, -15.61618894467913243, -28.45282021618999835 ) ) ;
#25251=EDGE_LOOP ( 'NONE', ( #2752, #47813, #44264, #38679 ) ) ;
#25258=CARTESIAN_POINT ( 'NONE',  ( 9.367050196127319595, -15.61601677469269944, -55.84717978380999881 ) ) ;
#25260=CARTESIAN_POINT ( 'NONE',  ( 22.29316687837529898, -20.47938135168080009, -75.50024918233970084 ) ) ;
#25263=LINE ( 'NONE', #37862, #15237 ) ;
#25267=AXIS2_PLACEMENT_3D ( 'NONE', #7527, #31599, #50776 ) ;
#25270=CARTESIAN_POINT ( 'NONE',  ( 22.48834434154391104, -10.88577583731355425, -65.30397204142286682 ) ) ;
#25271=CARTESIAN_POINT ( 'NONE',  ( 9.367479537931210132, -15.61613030728229923, -79.45282021618999124 ) ) ;
#25275=CARTESIAN_POINT ( 'NONE',  ( 8.713805725719740991, -18.46962709096431254, -34.39090680685740153 ) ) ;
#25278=ORIENTED_EDGE ( 'NONE', *, *, #49418, .T. ) ;
#25279=CARTESIAN_POINT ( 'NONE',  ( 23.49651994093389717, -14.47642026974889795, -45.01845461338599819 ) ) ;
#25300=CARTESIAN_POINT ( 'NONE',  ( 23.06214062797170072, -3.616188944679349593, -24.15000000000000213 ) ) ;
#25302=CARTESIAN_POINT ( 'NONE',  ( 22.90071998467804804, -15.61618839864605057, -72.45282571548244732 ) ) ;
#25303=CARTESIAN_POINT ( 'NONE',  ( 9.511343591802949859, -13.64028796437523461, -45.94011037906290085 ) ) ;
#25308=B_SPLINE_CURVE_WITH_KNOTS ( 'NONE', 3,
 ( #3750, #43070, #19201, #28863, #51695, #32004, #47771, #15789, #11877, #32774, #32256, #570, #44867, #48024, #28598, #318, #36724, #8449 ),
 .UNSPECIFIED., .F., .F.,
 ( 4, 2, 2, 2, 2, 2, 2, 2, 4 ),
 ( 0.000000000000000000, 0.06249981108821953124, 0.1249996221764390625, 0.1874994332646585937, 0.2499992443528781250, 0.3124990554410977950, 0.3749988665293174095, 0.4374986776175370795, 0.4999984887057566940 ),
 .UNSPECIFIED. ) ;
#25312=CARTESIAN_POINT ( 'NONE',  ( 20.98630067873081728, -20.33298601347895129, -46.69830337009432952 ) ) ;
#25314=CARTESIAN_POINT ( 'NONE',  ( 10.22062101548030100, -20.77559171587279963, -68.78413393247190299 ) ) ;
#25330=CARTESIAN_POINT ( 'NONE',  ( 23.28706766060589928, -17.69237313545239942, -32.14999999999999858 ) ) ;
#25335=EDGE_CURVE ( 'NONE', #40528, #47610, #20015, .T. ) ;
#25341=CARTESIAN_POINT ( 'NONE',  ( 9.319736165278609263, -13.79706257782909873, -67.93021958131210170 ) ) ;
#25349=CARTESIAN_POINT ( 'NONE',  ( 18.37403219540230026, -8.928548554084470013, -66.05570249522909876 ) ) ;
#25350=PLANE ( 'NONE',  #32889 ) ;
#25357=ADVANCED_FACE ( 'NONE', ( #32312 ), #7982, .T. ) ;
#25359=CARTESIAN_POINT ( 'NONE',  ( 19.54195246423347854, -21.52908623084648099, -54.78615564698215223 ) ) ;
#25366=CARTESIAN_POINT ( 'NONE',  ( 22.46009878491385336, -20.47787216187520087, -59.71601578695964463 ) ) ;
#25375=CARTESIAN_POINT ( 'NONE',  ( 23.04645729084084493, -11.63205128005230193, -53.62566746339389567 ) ) ;
#25377=CARTESIAN_POINT ( 'NONE',  ( 11.04448286797610024, -9.129022697162250566, -81.08056213787290289 ) ) ;
#25378=CARTESIAN_POINT ( 'NONE',  ( 9.366647546311250849, -15.61604444486649967, -65.84717978381009118 ) ) ;
#25385=CARTESIAN_POINT ( 'NONE',  ( 22.62449386613170077, -18.37576063303379925, -34.97514425884629929 ) ) ;
#25392=CARTESIAN_POINT ( 'NONE',  ( 22.11006429370840110, -9.935574188519110450, -81.26573725944388116 ) ) ;
#25407=CARTESIAN_POINT ( 'NONE',  ( 9.697439554173731935, -18.49959911504659971, -35.31875724254479820 ) ) ;
#25412=ORIENTED_EDGE ( 'NONE', *, *, #34899, .F. ) ;
#25414=CARTESIAN_POINT ( 'NONE',  ( 17.96388931505610387, -8.394141429016420020, -74.64633483117968638 ) ) ;
#25418=CARTESIAN_POINT ( 'NONE',  ( 19.58480251134974282, -8.478714239322904689, -49.43568005544015875 ) ) ;
#25430=ORIENTED_EDGE ( 'NONE', *, *, #45689, .F. ) ;
#25433=CARTESIAN_POINT ( 'NONE',  ( 10.72256258572000220, -11.45758887280185156, -69.66115420274824999 ) ) ;
#25434=CARTESIAN_POINT ( 'NONE',  ( 15.98424424538390198, -22.66744068707240345, -53.35393626560600211 ) ) ;
#25439=CARTESIAN_POINT ( 'NONE',  ( 24.04493740453103712, -15.60937728281429848, -43.79205105475155335 ) ) ;
#25440=CARTESIAN_POINT ( 'NONE',  ( 7.917544350917670393, -14.92799903136709894, -50.81893047157019794 ) ) ;
#25442=CARTESIAN_POINT ( 'NONE',  ( 20.45795268026760638, -10.33956678657632722, -56.17117403034256995 ) ) ;
#25444=B_SPLINE_CURVE_WITH_KNOTS ( 'NONE', 3,
 ( #21599, #40759, #928, #21344, #32869, #17691, #37350, #9578, #33404, #40500, #1189, #16926, #4861, #44692, #48902, #13001, #12466, #28954, #45219, #48635, #8542, #41020, #28434, #8796, #4590, #49164, #20565, #36560, #9327, #661, #13258, #44955, #25275, #16650, #37093, #5389, #12735, #1449, #9056 ),
 .UNSPECIFIED., .F., .F.,
 ( 4, 2, 1, 1, 1, 1, 1, 2, 2, 2, 2, 2, 2, 2, 2, 2, 2, 2, 2, 2, 2, 4 ),
 ( 0.4999999442541762096, 0.5001220145802860451, 0.5002440849063958250, 0.5004882255586154960, 0.5009765068630547269, 0.5019530694719332997, 0.5039061946896904454, 0.5078124451252047367, 0.5156249459962332082, 0.5312499477382901514, 0.5624999512224040377, 0.5937499547065180350, 0.6249999581906319213, 0.6562499616747458075, 0.6874999651588598049, 0.7187499686429736911, 0.7499999721270875774, 0.7812499756112015747, 0.8124999790953154610, 0.8749999860635435667, 0.9374999930317717833, 1.000000000000000000 ),
 .UNSPECIFIED. ) ;
#25447=CARTESIAN_POINT ( 'NONE',  ( 20.99980520150160146, -21.25799932088259681, -46.50612041305500099 ) ) ;
#25448=CARTESIAN_POINT ( 'NONE',  ( 11.10779186475480174, -10.92055609319979936, -32.14999999999999858 ) ) ;
#25452=CARTESIAN_POINT ( 'NONE',  ( 9.367478339302499180, -15.61624867646989756, -69.45282021618999124 ) ) ;
#25454=CARTESIAN_POINT ( 'NONE',  ( 19.98923256093490153, -8.327881876965719243, -51.16254345526869685 ) ) ;
#25475=CARTESIAN_POINT ( 'NONE',  ( 12.03708665661662636, -21.02749597990143116, -67.15911188335698512 ) ) ;
#25478=B_SPLINE_CURVE_WITH_KNOTS ( 'NONE', 3,
 ( #27508, #36148, #47960, #7866, #15985, #35113, #28014, #20156, #40089, #3939, #12063, #47704, #47453, #48209, #19899, #27768, #43763, #47198, #15216, #35644, #250, #8123, #23814, #51115, #11286, #43510, #31939, #24327 ),
 .UNSPECIFIED., .F., .F.,
 ( 4, 2, 2, 2, 2, 2, 2, 2, 2, 2, 2, 2, 2, 4 ),
 ( 0.000000000000000000, 0.03124971541833476002, 0.06249943083666952004, 0.09374914625500427312, 0.1249988616733390401, 0.1562485770916738070, 0.1874982925100085462, 0.2187480079283433132, 0.2499977233466780802, 0.2812474387650128471, 0.3124971541833476141, 0.3749965850200170925, 0.4374960158566866264, 0.4999954466933561603 ),
 .UNSPECIFIED. ) ;
#25481=CARTESIAN_POINT ( 'NONE',  ( 22.56376508447987561, -18.32376100367250515, -60.97451088762495885 ) ) ;
#25497=CARTESIAN_POINT ( 'NONE',  ( 24.04483537888494382, -15.65978551039709110, -77.50942050008035267 ) ) ;
#25505=CARTESIAN_POINT ( 'NONE',  ( 9.824348392058000812, -18.68523042451224114, -49.70282426501482576 ) ) ;
#25510=EDGE_CURVE ( 'NONE', #41523, #8412, #12657, .T. ) ;
#25516=CARTESIAN_POINT ( 'NONE',  ( 13.05426711372570026, -22.83438672010860060, -73.91587056106729392 ) ) ;
#25522=DIRECTION ( 'NONE',  ( 0.000000000000000000, 0.000000000000000000, -1.000000000000000000 ) ) ;
#25526=B_SPLINE_CURVE_WITH_KNOTS ( 'NONE', 3,
 ( #8893, #33235, #24580, #12566, #25366, #37438, #36389, #32700, #44528, #497, #13347, #32969, #25102, #41114, #21439, #16485, #24844, #5227 ),
 .UNSPECIFIED., .F., .F.,
 ( 4, 2, 2, 2, 2, 2, 2, 2, 4 ),
 ( 0.5000000030890958680, 0.5625000027029588567, 0.6250000023168218455, 0.6875000019306849453, 0.7500000015445479340, 0.8125000011584109227, 0.8750000007722740225, 0.9375000003861370113, 1.000000000000000000 ),
 .UNSPECIFIED. ) ;
#25528=CARTESIAN_POINT ( 'NONE',  ( 21.57906565130501875, -9.858451563110987692, -65.24878181863623183 ) ) ;
#25529=EDGE_CURVE ( 'NONE', #10190, #40528, #40403, .T. ) ;
#25530=CARTESIAN_POINT ( 'NONE',  ( 17.16940787898279197, -7.705177864455698966, -59.33404506873640827 ) ) ;
#25532=CARTESIAN_POINT ( 'NONE',  ( 9.807679542830243236, -20.47774811832251629, -56.58400988324318348 ) ) ;
#25536=CARTESIAN_POINT ( 'NONE',  ( 21.44577556945500163, -20.84027446995419908, -39.31469157680550097 ) ) ;
#25539=CARTESIAN_POINT ( 'NONE',  ( 9.402977987163499307, -14.22576715605993769, -33.91259203128302602 ) ) ;
#25544=CARTESIAN_POINT ( 'NONE',  ( 22.90090927591486292, -15.61618926791037687, -70.45281771081829447 ) ) ;
#25557=ORIENTED_EDGE ( 'NONE', *, *, #4300, .T. ) ;
#25559=CARTESIAN_POINT ( 'NONE',  ( 9.366916810851629194, -16.50183646529157144, -73.41114475139522710 ) ) ;
#25566=EDGE_CURVE ( 'NONE', #16548, #32624, #40075, .T. ) ;
#25567=CARTESIAN_POINT ( 'NONE',  ( 8.463963385727261368, -13.95539207350469901, -63.08037089589139867 ) ) ;
#25569=CARTESIAN_POINT ( 'NONE',  ( 22.14946380439831941, -18.71488146266838370, -32.99858898373786076 ) ) ;
#25574=CYLINDRICAL_SURFACE ( 'NONE', #24842, 7.910999999999997812 ) ;
#25585=CARTESIAN_POINT ( 'NONE',  ( 23.22693331446999920, -14.39611290704790036, -32.14999999999999858 ) ) ;
#25589=CARTESIAN_POINT ( 'NONE',  ( 19.60264381368218878, -8.482739570013125174, -45.15181677121430681 ) ) ;
#25593=CARTESIAN_POINT ( 'NONE',  ( 23.00352250046740110, -17.21348656573650260, -64.91990020089450297 ) ) ;
#25600=CARTESIAN_POINT ( 'NONE',  ( 11.42992024409580054, -10.36121213071920089, -75.72041208499069853 ) ) ;
#25601=CYLINDRICAL_SURFACE ( 'NONE', #47720, 6.766999999999998572 ) ;
#25605=VECTOR ( 'NONE', #22259, 1000.000000000000000 ) ;
#25625=CARTESIAN_POINT ( 'NONE',  ( 22.90111010729205177, -15.61618905465553553, -68.45282213299155671 ) ) ;
#25628=CARTESIAN_POINT ( 'NONE',  ( 23.04647745593273811, -11.63208902550109336, -57.34100099693699093 ) ) ;
#25630=CARTESIAN_POINT ( 'NONE',  ( 22.85730003971410085, -19.66369351922019959, -32.18498778107969116 ) ) ;
#25638=CARTESIAN_POINT ( 'NONE',  ( 20.29259217163623319, -10.20485708858880436, -78.16115132716946334 ) ) ;
#25642=CARTESIAN_POINT ( 'NONE',  ( 18.62387150434389937, -22.21488518936680023, -33.23232777544669148 ) ) ;
#25645=VERTEX_POINT ( 'NONE', #5801 ) ;
#25657=ADVANCED_FACE ( 'NONE', ( #49062 ), #29119, .T. ) ;
#25667=CARTESIAN_POINT ( 'NONE',  ( 17.03912355353180175, -8.621677044631578468, -47.99378621272389722 ) ) ;
#25674=CARTESIAN_POINT ( 'NONE',  ( 13.21023430151019973, -22.46882745431149786, -73.69570765841629623 ) ) ;
#25677=CARTESIAN_POINT ( 'NONE',  ( 8.222915784689270424, -14.75862311762373835, -48.82684667488993568 ) ) ;
#25681=CARTESIAN_POINT ( 'NONE',  ( 8.222926011208455677, -16.64759936946806462, -76.75081796745894280 ) ) ;
#25682=CARTESIAN_POINT ( 'NONE',  ( 24.04485091158800003, -15.61618876680915236, -45.79233931912149558 ) ) ;
#25684=CARTESIAN_POINT ( 'NONE',  ( 8.222919918104569348, -16.64776285459041816, -46.46616330941802175 ) ) ;
#25688=CARTESIAN_POINT ( 'NONE',  ( 8.428863955492316151, -13.54541270948961262, -46.87566500811402648 ) ) ;
#25689=ORIENTED_EDGE ( 'NONE', *, *, #26077, .F. ) ;
#25691=CARTESIAN_POINT ( 'NONE',  ( 23.06214062797170072, -27.61618894467930119, -32.14999999999999858 ) ) ;
#25692=CARTESIAN_POINT ( 'NONE',  ( 9.807834611244294010, -20.47794709156341852, -70.29933580689034045 ) ) ;
#25698=CARTESIAN_POINT ( 'NONE',  ( 16.82787181412869870, -23.83209882013590075, -58.26550999155039534 ) ) ;
#25700=CARTESIAN_POINT ( 'NONE',  ( 22.89230595604955099, -15.24705981027367052, -56.43546068824361583 ) ) ;
#25702=ORIENTED_EDGE ( 'NONE', *, *, #23955, .T. ) ;
#25704=CARTESIAN_POINT ( 'NONE',  ( 11.45349785648839891, -9.819622762339609068, -49.51643979347259261 ) ) ;
#25706=CARTESIAN_POINT ( 'NONE',  ( 8.988681696069670934, -17.72250670475619927, -32.14999999999999858 ) ) ;
#25711=CARTESIAN_POINT ( 'NONE',  ( 8.132716167238188021, -17.60696254563019991, -52.43004635228650301 ) ) ;
#25717=CARTESIAN_POINT ( 'NONE',  ( 15.24135970174500088, -8.620056853935023966, -70.30678751322059838 ) ) ;
#25718=EDGE_CURVE ( 'NONE', #39379, #39152, #10099, .T. ) ;
#25732=CARTESIAN_POINT ( 'NONE',  ( 19.65243233025719860, -21.45234396756585582, -66.78026749941459173 ) ) ;
#25739=DIRECTION ( 'NONE',  ( 0.000000000000000000, 0.000000000000000000, -1.000000000000000000 ) ) ;
#25752=ORIENTED_EDGE ( 'NONE', *, *, #3853, .F. ) ;
#25758=CARTESIAN_POINT ( 'NONE',  ( 24.01797834635617335, -16.29077936918112002, -33.81949288947817678 ) ) ;
#25759=CARTESIAN_POINT ( 'NONE',  ( 24.91854708852270406, -24.40079863550579020, -22.15000000000000924 ) ) ;
#25760=CARTESIAN_POINT ( 'NONE',  ( 11.91260932085662638, -21.26622862968680039, -49.55142757455319469 ) ) ;
#25769=EDGE_CURVE ( 'NONE', #28199, #21295, #26985, .T. ) ;
#25774=CARTESIAN_POINT ( 'NONE',  ( 8.788063236854998905, -18.37750765070880021, -72.17305407766760084 ) ) ;
#25782=DIRECTION ( 'NONE',  ( 1.000000000000000000, 0.000000000000000000, 0.000000000000000000 ) ) ;
#25783=CARTESIAN_POINT ( 'NONE',  ( 22.21722746122567571, -10.53735606139580838, -65.28627145430250778 ) ) ;
#25784=CARTESIAN_POINT ( 'NONE',  ( 12.72591348253150123, -21.52908204588105434, -79.11948583704311488 ) ) ;
#25787=CARTESIAN_POINT ( 'NONE',  ( 22.90088705258820667, -15.61618575905976414, -62.45282818884277276 ) ) ;
#25789=ORIENTED_EDGE ( 'NONE', *, *, #10245, .F. ) ;
#25790=CARTESIAN_POINT ( 'NONE',  ( 23.55489827341749987, -14.95586022399930037, -51.03909337422119563 ) ) ;
#25795=CARTESIAN_POINT ( 'NONE',  ( 14.39186542499959920, -8.781882511953600812, -74.26773406640160147 ) ) ;
#25796=( GEOMETRIC_REPRESENTATION_CONTEXT ( 3 ) GLOBAL_UNCERTAINTY_ASSIGNED_CONTEXT ( ( #3310 ) ) GLOBAL_UNIT_ASSIGNED_CONTEXT ( ( #12066, #4961, #9422 ) ) REPRESENTATION_CONTEXT ( 'NONE', 'WORKASPACE' ) );
#25797=CARTESIAN_POINT ( 'NONE',  ( 22.15209459710153084, -20.75234990211308173, -61.73254012881733388 ) ) ;
#25799=CARTESIAN_POINT ( 'NONE',  ( 12.14990911837581145, -8.703607423280148581, -35.12566392782755287 ) ) ;
#25804=ORIENTED_EDGE ( 'NONE', *, *, #45599, .T. ) ;
#25806=ORIENTED_EDGE ( 'NONE', *, *, #35062, .T. ) ;
#25813=CARTESIAN_POINT ( 'NONE',  ( 23.90924003817241683, -14.10962612633021607, -77.44674804159603809 ) ) ;
#25816=ORIENTED_EDGE ( 'NONE', *, *, #15091, .T. ) ;
#25821=CARTESIAN_POINT ( 'NONE',  ( 19.56784363952110084, -8.559629194120539353, -77.65665421159729931 ) ) ;
#25825=CARTESIAN_POINT ( 'NONE',  ( 22.14971581627796482, -18.71501114327763915, -28.45282021618999835 ) ) ;
#25829=CARTESIAN_POINT ( 'NONE',  ( 9.366560669795820360, -15.61606439180730099, -33.84717978380999881 ) ) ;
#25838=PLANE ( 'NONE',  #14222 ) ;
#25843=CARTESIAN_POINT ( 'NONE',  ( 24.04493737574808776, -16.65173435148965808, -51.83399569883714975 ) ) ;
#25847=CARTESIAN_POINT ( 'NONE',  ( 19.11048863820259669, -9.222230711542339421, -76.48586413618289725 ) ) ;
#25851=CARTESIAN_POINT ( 'NONE',  ( 9.367282414267279478, -15.61633198492950036, -43.45282021618999835 ) ) ;
#25855=CARTESIAN_POINT ( 'NONE',  ( 12.10839719180959939, -9.825024575796660997, -71.75946553180959597 ) ) ;
#25860=EDGE_CURVE ( 'NONE', #35517, #37146, #48908, .T. ) ;
#25861=VERTEX_POINT ( 'NONE', #22922 ) ;
#25864=DIRECTION ( 'NONE',  ( 1.000000000000000000, 0.000000000000000000, 0.000000000000000000 ) ) ;
#25866=CARTESIAN_POINT ( 'NONE',  ( 23.89338532170834384, -14.02234939633399335, -39.44318785247980230 ) ) ;
#25868=CARTESIAN_POINT ( 'NONE',  ( 8.222262383277058717, -15.61618471288229948, -44.50766849176299900 ) ) ;
#25889=CARTESIAN_POINT ( 'NONE',  ( 13.26742230928919852, -7.885353774765291313, -79.17930779234588101 ) ) ;
#25898=CARTESIAN_POINT ( 'NONE',  ( 22.90099047617777472, -15.26966479008347299, -44.83088873439039190 ) ) ;
#25901=CONICAL_SURFACE ( 'NONE', #6712, 12.92820323027549989, 0.7481802937784480800 ) ;
#25909=CARTESIAN_POINT ( 'NONE',  ( 24.04503344477293680, -15.61618896013167479, -37.50766614148061251 ) ) ;
#25920=CARTESIAN_POINT ( 'NONE',  ( 19.78667132190540201, -9.582939898486838359, -40.52046943329969508 ) ) ;
#25922=CARTESIAN_POINT ( 'NONE',  ( 13.16891555493870136, -9.216876155902941292, -41.81470958976149177 ) ) ;
#25926=CARTESIAN_POINT ( 'NONE',  ( 11.27234472087837780, -21.94241871684008771, -58.21600153524056509 ) ) ;
#25928=EDGE_CURVE ( 'NONE', #8909, #40766, #14454, .T. ) ;
#25930=CARTESIAN_POINT ( 'NONE',  ( 18.20721935276529990, -22.77217918175530187, -71.47757758863500044 ) ) ;
#25933=CARTESIAN_POINT ( 'NONE',  ( 21.61678711427710553, -9.893587190645865448, -49.53557109157861049 ) ) ;
#25939=CARTESIAN_POINT ( 'NONE',  ( 17.48127988501421370, -23.44392173378956556, -45.95340561908123078 ) ) ;
#25946=CARTESIAN_POINT ( 'NONE',  ( 9.366929578439700421, -14.73044796243286747, -69.49448701350169699 ) ) ;
#25952=DIRECTION ( 'NONE',  ( 0.000000000000000000, 0.000000000000000000, -1.000000000000000000 ) ) ;
#25955=CARTESIAN_POINT ( 'NONE',  ( 22.89852080129521283, -15.42085789721739708, -72.44363893989624614 ) ) ;
#25956=CARTESIAN_POINT ( 'NONE',  ( 24.04472027134544021, -15.61619704117925522, -43.79232540400376905 ) ) ;
#25960=CARTESIAN_POINT ( 'NONE',  ( 14.64547964051690165, -7.506490210384190398, -49.23455185029779813 ) ) ;
#25962=CARTESIAN_POINT ( 'NONE',  ( 10.82647640503957120, -11.32133379854484900, -55.66916738645966944 ) ) ;
#25967=CARTESIAN_POINT ( 'NONE',  ( 17.71571533420349809, -22.89661972621449948, -46.66455827518219479 ) ) ;
#25968=CARTESIAN_POINT ( 'NONE',  ( 9.116705508467720875, -14.11849739422179972, -32.14999999999999858 ) ) ;
#25972=CARTESIAN_POINT ( 'NONE',  ( 24.04481203031673076, -15.61619115162449312, -61.50767625960597229 ) ) ;
#25973=CARTESIAN_POINT ( 'NONE',  ( 24.37219564613430123, -15.95356372295639957, -63.52069670119330169 ) ) ;
#25977=CARTESIAN_POINT ( 'NONE',  ( 10.83502951711263940, -21.55863658954535822, -40.23930580441716387 ) ) ;
#25980=CARTESIAN_POINT ( 'NONE',  ( 13.90590011285059902, -8.924521810714191261, -52.24487123071539685 ) ) ;
#25993=CARTESIAN_POINT ( 'NONE',  ( 22.90100109812010842, -16.68472418553394476, -56.89745730083780018 ) ) ;
#25997=CARTESIAN_POINT ( 'NONE',  ( 22.86391141925847492, -16.33902761098219614, -66.48686977775619766 ) ) ;
#26002=LINE ( 'NONE', #45684, #45854 ) ;
#26008=CARTESIAN_POINT ( 'NONE',  ( 9.366705026548178381, -15.88967530897099678, -47.83432355292423210 ) ) ;
#26016=CARTESIAN_POINT ( 'NONE',  ( 24.04493736746855959, -15.61700137643269315, -77.50770766772195941 ) ) ;
#26023=CARTESIAN_POINT ( 'NONE',  ( 16.25866331035335222, -23.60640883099551601, -34.28700762286280934 ) ) ;
#26027=AXIS2_PLACEMENT_3D ( 'NONE', #51604, #35616, #3400 ) ;
#26037=CARTESIAN_POINT ( 'NONE',  ( 17.37891786306619935, -23.36452888456510024, -67.73679393810499505 ) ) ;
#26041=DIRECTION ( 'NONE',  ( 0.000000000000000000, 0.000000000000000000, 1.000000000000000000 ) ) ;
#26046=CARTESIAN_POINT ( 'NONE',  ( 24.04493741622511749, -14.58065722670617248, -43.46598914385031520 ) ) ;
#26057=CARTESIAN_POINT ( 'NONE',  ( 12.50377125389449873, -9.110146514235310633, -50.40534192571220018 ) ) ;
#26061=CARTESIAN_POINT ( 'NONE',  ( 22.04685453431686071, -19.02416987423216455, -68.61948488014840564 ) ) ;
#26064=CARTESIAN_POINT ( 'NONE',  ( 22.90122453025153249, -15.61618899996915211, -58.45282045073077626 ) ) ;
#26065=CARTESIAN_POINT ( 'NONE',  ( 18.27335346058083232, -23.24998756582152382, -61.92073563639246458 ) ) ;
#26069=CARTESIAN_POINT ( 'NONE',  ( 10.00711282696240012, -18.74238904653320148, -81.23899999999999011 ) ) ;
#26077=EDGE_CURVE ( 'NONE', #13824, #39880, #37010, .T. ) ;
#26080=CARTESIAN_POINT ( 'NONE',  ( 21.54526366514968316, -19.77485305479494215, -72.66112179359276979 ) ) ;
#26085=CARTESIAN_POINT ( 'NONE',  ( 23.07061256195587617, -19.52359038917101941, -49.67076867670061802 ) ) ;
#26088=CARTESIAN_POINT ( 'NONE',  ( 16.73976790070870280, -23.44049191639519947, -74.48789696905249968 ) ) ;
#26108=CARTESIAN_POINT ( 'NONE',  ( 9.407816849586122743, -14.19422756809612274, -49.91407474786834086 ) ) ;
#26112=ADVANCED_FACE ( 'NONE', ( #897 ), #11885, .T. ) ;
#26113=CARTESIAN_POINT ( 'NONE',  ( 21.09281434348019602, -20.63137574190060164, -71.09897682385668816 ) ) ;
#26122=CARTESIAN_POINT ( 'NONE',  ( 17.53487969994000295, -22.52849097422360103, -78.88916932753549816 ) ) ;
#26124=ADVANCED_FACE ( 'NONE', ( #2974 ), #45207, .F. ) ;
#26132=CARTESIAN_POINT ( 'NONE',  ( 24.04491295644446680, -15.59492720088391948, -39.50681616597011470 ) ) ;
#26147=CARTESIAN_POINT ( 'NONE',  ( 22.02282920616732653, -10.31289947776867955, -33.55901135124811674 ) ) ;
#26150=CARTESIAN_POINT ( 'NONE',  ( 20.99566274868214322, -9.290061469335373801, -57.21600112116089321 ) ) ;
#26152=CARTESIAN_POINT ( 'NONE',  ( 13.93647208143119975, -23.14997244139559740, -46.60283323465849747 ) ) ;
#26159=FACE_OUTER_BOUND ( 'NONE', #26180, .T. ) ;
#26162=CARTESIAN_POINT ( 'NONE',  ( 19.00123712817629951, -22.05987976827099928, -43.21391308946270016 ) ) ;
#26163=CARTESIAN_POINT ( 'NONE',  ( 9.366359964801500126, -15.61275108346748119, -43.84734136853051467 ) ) ;
#26177=CARTESIAN_POINT ( 'NONE',  ( 8.222918819271470170, -14.44621895267512990, -70.55475847918624765 ) ) ;
#26180=EDGE_LOOP ( 'NONE', ( #26900, #47628, #44992, #27171 ) ) ;
#26185=CARTESIAN_POINT ( 'NONE',  ( 9.366937397696199596, -15.61618894467949836, -28.45282021618999835 ) ) ;
#26188=CARTESIAN_POINT ( 'NONE',  ( 10.47335541784519997, -11.40900813729630059, -41.65627172763429797 ) ) ;
#26195=CARTESIAN_POINT ( 'NONE',  ( 10.36331059341320149, -10.29767275415630046, -36.52453509903889994 ) ) ;
#26197=CARTESIAN_POINT ( 'NONE',  ( 24.04485446177871921, -15.57701860679610562, -49.79075491074868864 ) ) ;
#26201=CARTESIAN_POINT ( 'NONE',  ( 24.04493739753763748, -15.62200579106754184, -75.79256001894520978 ) ) ;
#26202=CARTESIAN_POINT ( 'NONE',  ( 14.52552095220001327, -9.025673756071128651, -61.87668528295537129 ) ) ;
#26203=CARTESIAN_POINT ( 'NONE',  ( 23.09841952678586807, -19.38864957793463617, -45.66577835145771047 ) ) ;
#26210=CARTESIAN_POINT ( 'NONE',  ( 22.90121638405171467, -15.61618906730874734, -72.84718036870921765 ) ) ;
#26214=VERTEX_POINT ( 'NONE', #6891 ) ;
#26220=CARTESIAN_POINT ( 'NONE',  ( 23.96847382039350194, -13.04660549645949885, -59.69145075069550188 ) ) ;
#26226=CARTESIAN_POINT ( 'NONE',  ( 9.083108146633041002, -13.20942749461869958, -43.33736317051029374 ) ) ;
#26229=CARTESIAN_POINT ( 'NONE',  ( 8.831522587211491526, -16.55713555864529951, -32.14999999999999858 ) ) ;
#26235=CARTESIAN_POINT ( 'NONE',  ( 23.83903834229127128, -13.54551676074863309, -51.70899580649221861 ) ) ;
#26238=CARTESIAN_POINT ( 'NONE',  ( 14.56272227730649860, -7.522116807958889595, -64.94663746033839402 ) ) ;
#26245=DIRECTION ( 'NONE',  ( -0.6803061734058448717, -3.854301087740865499E-16, -0.7329280390501489162 ) ) ;
#26247=EDGE_LOOP ( 'NONE', ( #24821, #40341, #38462, #8868 ) ) ;
#26248=CARTESIAN_POINT ( 'NONE',  ( 12.89365889624202133, -8.399591182479161589, -80.87333339708158064 ) ) ;
#26251=CARTESIAN_POINT ( 'NONE',  ( 16.79572468873124791, -7.713964170122347142, -65.31892447852293060 ) ) ;
#26252=CARTESIAN_POINT ( 'NONE',  ( 8.223606718150689332, -15.61618413875730127, -36.50766849176289952 ) ) ;
#26255=CARTESIAN_POINT ( 'NONE',  ( 22.37291293269603898, -18.87617199571374016, -57.00054481839593734 ) ) ;
#26261=FACE_OUTER_BOUND ( 'NONE', #3694, .T. ) ;
#26264=CARTESIAN_POINT ( 'NONE',  ( 23.04645808148667996, -19.60032511754615925, -75.67434416289975729 ) ) ;
#26271=ORIENTED_EDGE ( 'NONE', *, *, #23800, .T. ) ;
#26272=ORIENTED_EDGE ( 'NONE', *, *, #9190, .F. ) ;
#26274=CARTESIAN_POINT ( 'NONE',  ( 9.221498594704018004, -19.60046454519304504, -80.34100214027874642 ) ) ;
#26291=CARTESIAN_POINT ( 'NONE',  ( 22.90362342996845513, -15.73105605196614754, -46.45820667783088709 ) ) ;
#26298=CARTESIAN_POINT ( 'NONE',  ( 17.52357721215789610, -7.488974053030859501, -37.06157372594439181 ) ) ;
#26306=CARTESIAN_POINT ( 'NONE',  ( 14.06331050438567409, -7.911075405847579844, -78.92433594638590932 ) ) ;
#26314=CARTESIAN_POINT ( 'NONE',  ( 24.04493739769619864, -15.61618894467929941, -32.14999999999999858 ) ) ;
#26317=EDGE_CURVE ( 'NONE', #39152, #20377, #29479, .T. ) ;
#26318=B_SPLINE_CURVE_WITH_KNOTS ( 'NONE', 3,
 ( #34630, #26767, #24361, #36429, #32471, #44306, #8415, #47738, #51414, #27544, #7900, #23595, #42, #36179, #4472, #28049, #48502, #43550 ),
 .UNSPECIFIED., .F., .F.,
 ( 4, 2, 2, 2, 2, 2, 2, 2, 4 ),
 ( 0.000000000000000000, 0.06250000040831246717, 0.1250000008166249343, 0.1875000012249374015, 0.2500000016332498687, 0.3125000020415623636, 0.3750000024498748030, 0.4375000028581872424, 0.5000000032664997374 ),
 .UNSPECIFIED. ) ;
#26321=CARTESIAN_POINT ( 'NONE',  ( 10.32568081865999865, -20.28211327437259826, -57.85192144569249706 ) ) ;
#26324=CARTESIAN_POINT ( 'NONE',  ( 10.22105026692229046, -19.02422193446483689, -69.28615314898171107 ) ) ;
#26329=CARTESIAN_POINT ( 'NONE',  ( 10.13877654970559838, -18.94649479092700162, -81.23899999999999011 ) ) ;
#26337=ORIENTED_EDGE ( 'NONE', *, *, #41887, .T. ) ;
#26338=CARTESIAN_POINT ( 'NONE',  ( 23.82939211681739522, -13.74556092313518718, -77.43178944251761209 ) ) ;
#26341=CARTESIAN_POINT ( 'NONE',  ( 24.04493545821624068, -15.62192134604925897, -49.50789643335303936 ) ) ;
#26344=CARTESIAN_POINT ( 'NONE',  ( 9.364637171664139004, -11.64588391339660056, -77.18134062521558292 ) ) ;
#26352=CARTESIAN_POINT ( 'NONE',  ( 20.97406584291865173, -20.57336686969118489, -33.10160192024077475 ) ) ;
#26353=CARTESIAN_POINT ( 'NONE',  ( 23.95077513244409673, -14.92063448110079982, -51.25925627687220043 ) ) ;
#26358=CARTESIAN_POINT ( 'NONE',  ( 22.90093739769620029, -15.61618894467913243, -28.45282021618999835 ) ) ;
#26359=CARTESIAN_POINT ( 'NONE',  ( 21.52140218880130007, -11.27449214404849975, -32.14999999999999858 ) ) ;
#26363=CARTESIAN_POINT ( 'NONE',  ( 24.04511355972104170, -15.61618909363076924, -51.79233356384455078 ) ) ;
#26364=CARTESIAN_POINT ( 'NONE',  ( 9.572633603277138192, -13.37907996729690829, -35.95238683638561383 ) ) ;
#26369=CARTESIAN_POINT ( 'NONE',  ( 13.56856140308030056, -9.046454919155269891, -78.22868061958250507 ) ) ;
#26370=VERTEX_POINT ( 'NONE', #32236 ) ;
#26377=CARTESIAN_POINT ( 'NONE',  ( 23.13352024345619995, -16.48128933305549992, -70.49196263479178981 ) ) ;
#26378=CARTESIAN_POINT ( 'NONE',  ( 16.13393739769620083, -15.61618894467929941, -22.14999999999999858 ) ) ;
#26379=CARTESIAN_POINT ( 'NONE',  ( 8.222734977135019108, -15.61599928274970139, -66.79233150823698395 ) ) ;
#26380=CARTESIAN_POINT ( 'NONE',  ( 11.97520588862272817, -21.02746353419226821, -41.16110300765930674 ) ) ;
#26387=CARTESIAN_POINT ( 'NONE',  ( 24.03024257791251372, -15.12402444006626467, -39.48786302714248109 ) ) ;
#26388=CARTESIAN_POINT ( 'NONE',  ( 17.01977592779661919, -22.38318318947497687, -54.91115525370862827 ) ) ;
#26394=CARTESIAN_POINT ( 'NONE',  ( 16.13393739769620083, -15.61618894467929941, -32.14999999999999858 ) ) ;
#26402=CARTESIAN_POINT ( 'NONE',  ( 14.15298794937745619, -7.924134237888455168, -33.21219548599496107 ) ) ;
#26407=CARTESIAN_POINT ( 'NONE',  ( 20.73481432542239844, -9.258620298766089718, -47.71189826954910274 ) ) ;
#26411=EDGE_CURVE ( 'NONE', #22570, #6190, #24113, .T. ) ;
#26412=B_SPLINE_CURVE_WITH_KNOTS ( 'NONE', 3,
 ( #11489, #43198, #14631, #7291, #34792, #35317, #43449, #23495, #30851, #46619 ),
 .UNSPECIFIED., .F., .F.,
 ( 4, 1, 1, 1, 1, 1, 1, 4 ),
 ( 0.5000037738926587094, 0.5650942749437076751, 0.6443132060073258893, 0.7235321370709463240, 0.8027510681345644272, 0.8819699991981826415, 0.9611889302618030761, 1.000000000000000000 ),
 .UNSPECIFIED. ) ;
#26418=CARTESIAN_POINT ( 'NONE',  ( 13.03996251179859911, -21.95416011689880165, -47.49173536689809794 ) ) ;
#26419=LINE ( 'NONE', #38495, #18926 ) ;
#26425=LINE ( 'NONE', #42443, #42338 ) ;
#26434=CARTESIAN_POINT ( 'NONE',  ( 21.50885149835741572, -9.731310480211288194, -71.24312159355089591 ) ) ;
#26435=CARTESIAN_POINT ( 'NONE',  ( 23.83903474352796437, -13.54549896641242945, -69.42433801165668683 ) ) ;
#26443=CARTESIAN_POINT ( 'NONE',  ( 18.20469938706415292, -23.32126574151624254, -74.20899818179171348 ) ) ;
#26446=CARTESIAN_POINT ( 'NONE',  ( 21.53292167905440024, -11.07817975272370070, -40.23033096848919854 ) ) ;
#26451=CIRCLE ( 'NONE', #38178, 2.576499999999998902 ) ;
#26453=CARTESIAN_POINT ( 'NONE',  ( 23.67750195217940146, -17.77983910020999758, -39.37641661732929776 ) ) ;
#26460=CARTESIAN_POINT ( 'NONE',  ( 15.01509412889560124, -8.922449039472333254, -61.90007767931285798 ) ) ;
#26462=CARTESIAN_POINT ( 'NONE',  ( 18.14859056469791554, -23.29360679183883676, -45.92611244253869529 ) ) ;
#26475=AXIS2_PLACEMENT_3D ( 'NONE', #17237, #16452, #13063 ) ;
#26477=CARTESIAN_POINT ( 'NONE',  ( 9.221383621697642141, -11.63210989131640360, -68.95899869748384958 ) ) ;
#26478=CARTESIAN_POINT ( 'NONE',  ( 17.82813868014650183, -23.68541456244950183, -62.22645654473139842 ) ) ;
#26484=CARTESIAN_POINT ( 'NONE',  ( 22.91773806209070230, -18.69624452062379660, -52.36832131176279859 ) ) ;
#26487=CARTESIAN_POINT ( 'NONE',  ( 8.870425115289640061, -15.32709397560249975, -32.14999999999999858 ) ) ;
#26489=CARTESIAN_POINT ( 'NONE',  ( 9.366940089669899550, -15.31057181698914071, -61.46719675360134971 ) ) ;
#26494=CARTESIAN_POINT ( 'NONE',  ( 9.197206178375568086, -11.15923026191389944, -66.68945394373800184 ) ) ;
#26497=AXIS2_PLACEMENT_3D ( 'NONE', #21706, #42169, #30862 ) ;
#26503=ORIENTED_EDGE ( 'NONE', *, *, #28121, .T. ) ;
#26504=CARTESIAN_POINT ( 'NONE',  ( 14.32008737414983024, -7.878783737859143876, -80.93427853967327223 ) ) ;
#26507=CARTESIAN_POINT ( 'NONE',  ( 19.85100399889286749, -8.556464285641796508, -65.44686368286718903 ) ) ;
#26546=CARTESIAN_POINT ( 'NONE',  ( 0.000000000000000000, 0.000000000000000000, 0.000000000000000000 ) ) ;
#26547=CARTESIAN_POINT ( 'NONE',  ( 9.366926243097925209, -16.50190438893503853, -47.41114289273251359 ) ) ;
#26557=CARTESIAN_POINT ( 'NONE',  ( 24.34438809016150174, -16.37198001076230014, -37.53688731232609399 ) ) ;
#26565=CARTESIAN_POINT ( 'NONE',  ( 18.20463974528131601, -23.32128259539753046, -36.20899657585380993 ) ) ;
#26577=CARTESIAN_POINT ( 'NONE',  ( 18.25716822292040220, -22.75751831680320336, -55.47535351378389379 ) ) ;
#26580=CARTESIAN_POINT ( 'NONE',  ( 17.90520935967482785, -22.20705525476682141, -68.86948548096090406 ) ) ;
#26584=CARTESIAN_POINT ( 'NONE',  ( 9.341559668391759885, -17.31601013018309843, -81.23899999999999011 ) ) ;
#26586=ORIENTED_EDGE ( 'NONE', *, *, #5319, .T. ) ;
#26598=CARTESIAN_POINT ( 'NONE',  ( 8.428860219786908914, -13.54542629176921587, -62.87566502643110766 ) ) ;
#26600=DIRECTION ( 'NONE',  ( 0.000000000000000000, 0.000000000000000000, -1.000000000000000000 ) ) ;
#26602=CARTESIAN_POINT ( 'NONE',  ( 24.04345669879266723, -15.78160371113625260, -49.51431991849604231 ) ) ;
#26610=B_SPLINE_CURVE_WITH_KNOTS ( 'NONE', 3,
 ( #26672, #30089, #30349, #6789, #41908, #22486, #38492, #49778, #33766, #18302 ),
 .UNSPECIFIED., .F., .F.,
 ( 4, 1, 1, 1, 1, 1, 1, 4 ),
 ( 0.000000000000000000, 0.03231255575895254639, 0.1115314868226600781, 0.1907504178862047817, 0.2699693489497539400, 0.3491882800134615272, 0.4284072110770061892, 0.4999975329053952255 ),
 .UNSPECIFIED. ) ;
#26616=CARTESIAN_POINT ( 'NONE',  ( 19.73361416582759986, -22.58964399566790249, -53.63582420878069001 ) ) ;
#26627=CARTESIAN_POINT ( 'NONE',  ( 24.00183349690676948, -14.77473046282855584, -45.47376742038415642 ) ) ;
#26631=CARTESIAN_POINT ( 'NONE',  ( 9.385193573649580401, -17.66485093986310062, -77.75336703320080289 ) ) ;
#26634=CYLINDRICAL_SURFACE ( 'NONE', #40474, 6.766999999999998572 ) ;
#26636=CARTESIAN_POINT ( 'NONE',  ( 11.30419729876839874, -10.47652263729510125, -58.10707212942319444 ) ) ;
#26637=CARTESIAN_POINT ( 'NONE',  ( 21.00581555762000008, -20.71593030003079861, -72.71009270457319928 ) ) ;
#26638=CARTESIAN_POINT ( 'NONE',  ( 9.438349570632869501, -17.22248095868435769, -79.77162013446428546 ) ) ;
#26639=CARTESIAN_POINT ( 'NONE',  ( 14.06335810825438060, -7.911063077082181927, -67.20899717355162295 ) ) ;
#26640=DIRECTION ( 'NONE',  ( 0.000000000000000000, 0.000000000000000000, -1.000000000000000000 ) ) ;
#26652=ORIENTED_EDGE ( 'NONE', *, *, #43137, .F. ) ;
#26660=CARTESIAN_POINT ( 'NONE',  ( 23.37058690749169187, -12.35555072797064646, -33.65753852466926332 ) ) ;
#26667=CARTESIAN_POINT ( 'NONE',  ( 22.14140776524460108, -10.56672883743910063, -39.79000516318719605 ) ) ;
#26672=CARTESIAN_POINT ( 'NONE',  ( 9.367432603602109609, -15.61609789975089946, -77.84717978380999170 ) ) ;
#26674=CARTESIAN_POINT ( 'NONE',  ( 19.02084999298380197, -9.181261218463509621, -44.48141598648069106 ) ) ;
#26680=CARTESIAN_POINT ( 'NONE',  ( 8.223201290577328848, -15.61599831009169925, -56.79233150823699816 ) ) ;
#26688=CARTESIAN_POINT ( 'NONE',  ( 24.04480613576765791, -15.56695444769906977, -71.50569215503726639 ) ) ;
#26689=CARTESIAN_POINT ( 'NONE',  ( 24.04497561966918440, -15.61618908881887080, -69.50766602643473391 ) ) ;
#26697=CARTESIAN_POINT ( 'NONE',  ( 22.90149177939719749, -15.54649009578485241, -40.84390380044833080 ) ) ;
#26700=CARTESIAN_POINT ( 'NONE',  ( 16.58402498330990227, -8.577724633346759830, -41.97314745188879215 ) ) ;
#26706=ORIENTED_EDGE ( 'NONE', *, *, #35132, .F. ) ;
#26709=CARTESIAN_POINT ( 'NONE',  ( 23.32935734630029856, -13.68438637900169930, -80.98384931626929983 ) ) ;
#26719=CARTESIAN_POINT ( 'NONE',  ( 22.34690280317739663, -12.84547917103817305, -62.31919153057756944 ) ) ;
#26720=CARTESIAN_POINT ( 'NONE',  ( 24.04805248749356394, -15.76022397032248179, -45.51348880828970067 ) ) ;
#26722=ORIENTED_EDGE ( 'NONE', *, *, #43202, .F. ) ;
#26726=CARTESIAN_POINT ( 'NONE',  ( 23.04646929297832258, -11.63207376528382753, -47.62566650700710369 ) ) ;
#26734=CARTESIAN_POINT ( 'NONE',  ( 16.13393739769620083, -15.61618894467929941, -32.14999999999999858 ) ) ;
#26735=CARTESIAN_POINT ( 'NONE',  ( 12.14976682726940460, -8.703687915727341462, -69.12566588673060153 ) ) ;
#26736=CARTESIAN_POINT ( 'NONE',  ( 21.05699174304649901, -22.23028419411919998, -68.08865744343930260 ) ) ;
#26739=ORIENTED_EDGE ( 'NONE', *, *, #7620, .F. ) ;
#26745=CARTESIAN_POINT ( 'NONE',  ( 12.61621733769010056, -9.048667388979911408, -51.57613200112670171 ) ) ;
#26748=CARTESIAN_POINT ( 'NONE',  ( 8.873811137001389682, -15.29904210822119914, -32.14999999999999858 ) ) ;
#26750=AXIS2_PLACEMENT_3D ( 'NONE', #39629, #3733, #19704 ) ;
#26754=CARTESIAN_POINT ( 'NONE',  ( 17.53709516631539955, -7.809917705144554745, -61.06435815452337579 ) ) ;
#26756=CARTESIAN_POINT ( 'NONE',  ( 17.44196880168159680, -23.75693673312990128, -67.95695684075599274 ) ) ;
#26757=CARTESIAN_POINT ( 'NONE',  ( 21.14377605645180225, -21.55665859497039705, -32.14999999999999858 ) ) ;
#26760=CARTESIAN_POINT ( 'NONE',  ( 22.90073451867936072, -15.61618922653637931, -60.45281425156898791 ) ) ;
#26766=CARTESIAN_POINT ( 'NONE',  ( 18.39424314599772359, -8.017305291866634320, -65.38436368376463292 ) ) ;
#26767=CARTESIAN_POINT ( 'NONE',  ( 8.222913330528481168, -16.65156021647412388, -72.75066848630076777 ) ) ;
#26773=CARTESIAN_POINT ( 'NONE',  ( 14.04950511168915206, -17.13061764721085467, -22.64999999999999858 ) ) ;
#26781=CARTESIAN_POINT ( 'NONE',  ( 20.99560662150501145, -21.94236121597040068, -75.79935198058029755 ) ) ;
#26785=CONICAL_SURFACE ( 'NONE', #45246, 0.3230324999999999447, 0.7853981633974469467 ) ;
#26790=CARTESIAN_POINT ( 'NONE',  ( 9.366809454094768839, -15.61635577034980038, -65.45282021618999124 ) ) ;
#26798=CARTESIAN_POINT ( 'NONE',  ( 21.51003971160372785, -21.42087352377891563, -77.76985987278362700 ) ) ;
#26805=ORIENTED_EDGE ( 'NONE', *, *, #32909, .T. ) ;
#26806=CARTESIAN_POINT ( 'NONE',  ( 21.34594057796939737, -9.227312446831069437, -37.51015005288210347 ) ) ;
#26823=CARTESIAN_POINT ( 'NONE',  ( 8.624584447526789432, -17.89574294739870197, -78.19369283850269881 ) ) ;
#26845=CARTESIAN_POINT ( 'NONE',  ( 22.99909601152119976, -12.72200658253170147, -52.94034771974799725 ) ) ;
#26849=CARTESIAN_POINT ( 'NONE',  ( 9.367299438200719308, -15.61632798465739924, -73.84717978381010539 ) ) ;
#26851=CARTESIAN_POINT ( 'NONE',  ( 11.97538944125683713, -10.20477556317503876, -73.74448688630067750 ) ) ;
#26852=CARTESIAN_POINT ( 'NONE',  ( 9.945350952399207856, -18.63771621449150118, -81.23899999999999011 ) ) ;
#26857=EDGE_LOOP ( 'NONE', ( #8038, #34760, #46296, #38548, #22475, #17033 ) ) ;
#26859=CARTESIAN_POINT ( 'NONE',  ( 23.59011241424889960, -14.63756608872980003, -81.23899999999999011 ) ) ;
#26861=CARTESIAN_POINT ( 'NONE',  ( 16.13393739769620083, -15.61618894467929941, -28.45282021618999835 ) ) ;
#26865=CARTESIAN_POINT ( 'NONE',  ( 8.428836555654854124, -13.54551232982551667, -52.59100207975336616 ) ) ;
#26867=CARTESIAN_POINT ( 'NONE',  ( 8.222948442953439852, -14.58056061358565358, -62.83399826733404581 ) ) ;
#26868=CARTESIAN_POINT ( 'NONE',  ( 22.90093739769620029, -15.61618894467913243, -28.45282021618999835 ) ) ;
#26869=ORIENTED_EDGE ( 'NONE', *, *, #11186, .T. ) ;
#26874=DIRECTION ( 'NONE',  ( 1.000000000000000000, 0.000000000000000000, 0.000000000000000000 ) ) ;
#26879=CARTESIAN_POINT ( 'NONE',  ( 9.735928820737651535, -18.42464518422739772, -39.71510072233680688 ) ) ;
#26881=CARTESIAN_POINT ( 'NONE',  ( 22.08951763117189770, -10.50563004512479992, -55.06176496792589603 ) ) ;
#26883=DIRECTION ( 'NONE',  ( 1.000000000000000000, 0.000000000000000000, 0.000000000000000000 ) ) ;
#26892=CARTESIAN_POINT ( 'NONE',  ( 21.77064918506680158, -11.55215727437349926, -32.14999999999999858 ) ) ;
#26894=CARTESIAN_POINT ( 'NONE',  ( 9.044388546175500920, -19.20379739193470670, -32.35863995352835332 ) ) ;
#26898=CARTESIAN_POINT ( 'NONE',  ( 9.367509928541279507, -15.61618483373539767, -35.84717978380999881 ) ) ;
#26900=ORIENTED_EDGE ( 'NONE', *, *, #33836, .T. ) ;
#26901=CARTESIAN_POINT ( 'NONE',  ( 21.94086349853619922, -19.61895903973029931, -69.03928461620259327 ) ) ;
#26910=CARTESIAN_POINT ( 'NONE',  ( 8.222962225833626349, -14.58045970421460957, -66.83399807476841659 ) ) ;
#26915=VERTEX_POINT ( 'NONE', #19610 ) ;
#26918=CARTESIAN_POINT ( 'NONE',  ( 23.83903321696472588, -13.54549142372404447, -39.70899962327502664 ) ) ;
#26919=CARTESIAN_POINT ( 'NONE',  ( 9.518314214286407449, -13.60873826579939205, -61.94159309563030291 ) ) ;
#26922=ORIENTED_EDGE ( 'NONE', *, *, #31513, .T. ) ;
#26924=CARTESIAN_POINT ( 'NONE',  ( 24.03381970956576552, -16.06908057521573241, -55.52589602977201366 ) ) ;
#26926=CARTESIAN_POINT ( 'NONE',  ( 22.46011740567508852, -20.47784660952951796, -69.71600428924691073 ) ) ;
#26927=CARTESIAN_POINT ( 'NONE',  ( 22.88833302732390251, -15.19494145161055165, -46.43300353811684289 ) ) ;
#26933=CARTESIAN_POINT ( 'NONE',  ( 12.81008685434317407, -8.402044234839515013, -33.15484140419596315 ) ) ;
#26938=CARTESIAN_POINT ( 'NONE',  ( 23.04647257630374213, -19.60029799513142734, -53.67433770499982870 ) ) ;
#26939=CARTESIAN_POINT ( 'NONE',  ( 9.664531381497580398, -20.05843312855249749, -48.82096330443980037 ) ) ;
#26946=CARTESIAN_POINT ( 'NONE',  ( 13.45712100228560182, -22.14131064160670093, -41.47109660606309944 ) ) ;
#26950=EDGE_CURVE ( 'NONE', #50433, #17972, #31208, .T. ) ;
#26954=CARTESIAN_POINT ( 'NONE',  ( 15.09846244433525797, -7.705180183529160232, -46.96600246067505680 ) ) ;
#26962=EDGE_CURVE ( 'NONE', #6769, #39697, #3766, .T. ) ;
#26967=ORIENTED_EDGE ( 'NONE', *, *, #24867, .F. ) ;
#26969=CARTESIAN_POINT ( 'NONE',  ( 20.29261355638415409, -10.20487415642876350, -42.16115314179906903 ) ) ;
#26972=CARTESIAN_POINT ( 'NONE',  ( 18.75695854933399787, -9.069256935357190130, -56.07411718121309008 ) ) ;
#26975=ADVANCED_FACE ( 'NONE', ( #8857 ), #44751, .T. ) ;
#26978=CARTESIAN_POINT ( 'NONE',  ( 11.45601973047439870, -9.315091065588880781, -38.58422730669299483 ) ) ;
#26979=ADVANCED_FACE ( 'NONE', ( #24808 ), #9114, .T. ) ;
#26985=B_SPLINE_CURVE_WITH_KNOTS ( 'NONE', 3,
 ( #13286, #29239, #3937, #40087, #27507, #47451, #7350, #11804, #19394, #23559, #20856, #35375, #51373, #7611, #39574, #43762, #7864, #23812, #39831, #19897, #958, #16955, #48932, #26338, #25813, #46029, #22409, #41563, #22145, #45767, #30274, #1994, #5678, #37630, #45510, #18229 ),
 .UNSPECIFIED., .F., .F.,
 ( 4, 2, 2, 2, 2, 2, 2, 2, 2, 2, 2, 2, 2, 2, 1, 1, 1, 1, 2, 4 ),
 ( 0.000000000000000000, 0.06250043248147645059, 0.1250008649629529012, 0.1875012974444293379, 0.2500017299259058023, 0.2812519461666440068, 0.3125021624073822668, 0.3437523786481204713, 0.3750025948888586758, 0.4062528111295969357, 0.4375030273703351402, 0.4687532436110734002, 0.4843783517314425580, 0.4921909057916271646, 0.4960971828217194401, 0.4980503213367655224, 0.4990268905942885080, 0.4995151752230500564, 0.4997593175374308583, 0.5000034598518116047 ),
 .UNSPECIFIED. ) ;
#26988=DIRECTION ( 'NONE',  ( 0.000000000000000000, 0.000000000000000000, -1.000000000000000000 ) ) ;
#26995=VERTEX_POINT ( 'NONE', #37151 ) ;
#26996=CARTESIAN_POINT ( 'NONE',  ( 13.36500334305701365, -23.09455901958340007, -44.40493357439147815 ) ) ;
#27003=CARTESIAN_POINT ( 'NONE',  ( 22.46009313275346742, -10.75449796053407603, -69.58400065715915161 ) ) ;
#27004=CARTESIAN_POINT ( 'NONE',  ( 17.24925778731569892, -7.446808277551939526, -63.33552157962218843 ) ) ;
#27009=AXIS2_PLACEMENT_3D ( 'NONE', #20995, #24909, #36457 ) ;
#27011=CARTESIAN_POINT ( 'NONE',  ( 18.59482207321979885, -22.64831098705879953, -50.62550482836319787 ) ) ;
#27012=AXIS2_PLACEMENT_3D ( 'NONE', #21188, #41633, #34013 ) ;
#27017=EDGE_CURVE ( 'NONE', #49799, #17454, #12270, .T. ) ;
#27020=CARTESIAN_POINT ( 'NONE',  ( 23.53364714576019878, -11.97929241695389990, -63.36225883906600131 ) ) ;
#27025=CARTESIAN_POINT ( 'NONE',  ( 8.223487313465298598, -15.61606829411550024, -62.50766849176299189 ) ) ;
#27027=DIRECTION ( 'NONE',  ( 0.000000000000000000, 0.000000000000000000, 1.000000000000000000 ) ) ;
#27046=CARTESIAN_POINT ( 'NONE',  ( 24.04493739429386068, -14.58063990169072177, -37.75066784073908366 ) ) ;
#27067=CARTESIAN_POINT ( 'NONE',  ( 20.72701976924740208, -9.175108652667299580, -31.48951129204709787 ) ) ;
#27068=AXIS2_PLACEMENT_3D ( 'NONE', #12195, #11948, #19536 ) ;
#27070=CARTESIAN_POINT ( 'NONE',  ( 23.36114490013733658, -18.93483993365045137, -49.92920886125001090 ) ) ;
#27077=DIRECTION ( 'NONE',  ( 0.000000000000000000, 0.000000000000000000, -1.000000000000000000 ) ) ;
#27079=B_SPLINE_CURVE_WITH_KNOTS ( 'NONE', 3,
 ( #3741, #31734, #40142, #7922, #15780, #8695, #39896, #48789, #4757, #27564, #23872, #23617, #43572, #39636, #40658, #8179, #28328, #20726 ),
 .UNSPECIFIED., .F., .F.,
 ( 4, 2, 2, 2, 2, 2, 2, 2, 4 ),
 ( 0.5000000031318456717, 0.5625000027403649350, 0.6250000023488841983, 0.6875000019574033505, 0.7500000015659226138, 0.8125000011744419881, 0.8750000007829612514, 0.9375000003914806257, 1.000000000000000000 ),
 .UNSPECIFIED. ) ;
#27084=ADVANCED_FACE ( 'NONE', ( #34687 ), #33198, .T. ) ;
#27085=CARTESIAN_POINT ( 'NONE',  ( 13.27943376031980094, -8.306020878940559626, -78.66900642488428730 ) ) ;
#27100=LINE ( 'NONE', #7964, #20870 ) ;
#27107=CARTESIAN_POINT ( 'NONE',  ( 19.66348914187359753, -9.055018407075850817, -66.72444172481779390 ) ) ;
#27114=CARTESIAN_POINT ( 'NONE',  ( 10.58153729635829876, -19.54390142674099806, -81.23899999999999011 ) ) ;
#27118=VERTEX_POINT ( 'NONE', #42054 ) ;
#27119=ORIENTED_EDGE ( 'NONE', *, *, #26411, .T. ) ;
#27122=CARTESIAN_POINT ( 'NONE',  ( 23.08642316010210038, -12.32642676488089961, -81.23899999999999011 ) ) ;
#27135=CARTESIAN_POINT ( 'NONE',  ( 10.95257998347446282, -11.16488345018802875, -39.67851141808000648 ) ) ;
#27141=FACE_OUTER_BOUND ( 'NONE', #31910, .T. ) ;
#27143=CARTESIAN_POINT ( 'NONE',  ( 12.76218697320820006, -8.529719636332050214, -56.64614358919829584 ) ) ;
#27152=CARTESIAN_POINT ( 'NONE',  ( 22.90093739769620029, -15.61618894467913243, -28.45282021618999835 ) ) ;
#27154=CARTESIAN_POINT ( 'NONE',  ( 9.221376762100923941, -11.63212162064420596, -70.95898967772608046 ) ) ;
#27156=CARTESIAN_POINT ( 'NONE',  ( 17.38960780687880003, -8.272485099762899807, -36.62124792064249590 ) ) ;
#27165=CARTESIAN_POINT ( 'NONE',  ( 22.46012542801484102, -10.75454228593980943, -67.58399627233477247 ) ) ;
#27166=CARTESIAN_POINT ( 'NONE',  ( 11.27235466147499743, -9.289951649597259831, -66.79933434006539983 ) ) ;
#27171=ORIENTED_EDGE ( 'NONE', *, *, #34899, .T. ) ;
#27173=CARTESIAN_POINT ( 'NONE',  ( 8.222937397696199469, -15.61618894467929941, -32.14999999999999858 ) ) ;
#27175=CARTESIAN_POINT ( 'NONE',  ( 22.90093739769620029, -15.61618894467913243, -28.45282021618999835 ) ) ;
#27183=CARTESIAN_POINT ( 'NONE',  ( 10.72266466894950732, -11.45745788688983424, -35.66115297843326459 ) ) ;
#27191=CARTESIAN_POINT ( 'NONE',  ( 20.99564860854162518, -21.94232770570259206, -53.79933732301430638 ) ) ;
#27192=CARTESIAN_POINT ( 'NONE',  ( 11.98811719313489910, -8.952937304298819399, -45.33533033764059894 ) ) ;
#27198=CARTESIAN_POINT ( 'NONE',  ( 23.18271560078089877, -15.85553183295759716, -46.85798391838910248 ) ) ;
#27199=CARTESIAN_POINT ( 'NONE',  ( 15.24806174914439438, -8.849198298406202312, -43.91112208262838124 ) ) ;
#27208=CARTESIAN_POINT ( 'NONE',  ( 8.428872386935585936, -13.54538205412076657, -46.59100194065602096 ) ) ;
#27215=CARTESIAN_POINT ( 'NONE',  ( 8.307302965981692822, -16.94665780510273834, -32.73880447305563735 ) ) ;
#27224=CARTESIAN_POINT ( 'NONE',  ( 23.13939390996569756, -16.43236156816429983, -54.48973855994069737 ) ) ;
#27229=CARTESIAN_POINT ( 'NONE',  ( 8.726417494668801567, -16.41327870859180038, -80.03322214350579600 ) ) ;
#27234=CARTESIAN_POINT ( 'NONE',  ( 8.222937397696199469, -15.61618894467929941, -32.14999999999999858 ) ) ;
#27242=FACE_OUTER_BOUND ( 'NONE', #45120, .T. ) ;
#27250=CARTESIAN_POINT ( 'NONE',  ( 23.04645488412634080, -19.60033111914527382, -61.95899558997343348 ) ) ;
#27252=CARTESIAN_POINT ( 'NONE',  ( 17.52689767915063968, -22.28079415070259017, -32.88709510709496442 ) ) ;
#27255=CARTESIAN_POINT ( 'NONE',  ( 13.21347626774960027, -7.905571145539870059, -63.17708371749469620 ) ) ;
#27256=CYLINDRICAL_SURFACE ( 'NONE', #35562, 7.910999999999997812 ) ;
#27257=CYLINDRICAL_SURFACE ( 'NONE', #43135, 6.766999999999998572 ) ;
#27260=ORIENTED_EDGE ( 'NONE', *, *, #16385, .F. ) ;
#27262=CARTESIAN_POINT ( 'NONE',  ( 13.04913953162400020, -8.834543426766860108, -57.59677076196169310 ) ) ;
#27266=CARTESIAN_POINT ( 'NONE',  ( 10.29526228329839910, -20.60856492654189864, -32.14999999999999858 ) ) ;
#27273=B_SPLINE_CURVE_WITH_KNOTS ( 'NONE', 3,
 ( #23476, #47876, #51798, #10947, #4095, #27166, #11720, #11979, #23734, #23220, #15645, #39750, #15900, #19826, #47368, #27421, #19050, #42918 ),
 .UNSPECIFIED., .F., .F.,
 ( 4, 2, 2, 2, 2, 2, 2, 2, 4 ),
 ( 0.000000000000000000, 0.06249982463622441586, 0.1249996492724488317, 0.1874994739086732476, 0.2499992985448976635, 0.3124991231811220516, 0.3749989478173464952, 0.4374987724535709388, 0.4999985970897953269 ),
 .UNSPECIFIED. ) ;
#27276=CARTESIAN_POINT ( 'NONE',  ( 8.119001781468568879, -17.55100877523230096, -68.43227042713769492 ) ) ;
#27277=CARTESIAN_POINT ( 'NONE',  ( 20.97675674825520176, -21.71492495383600385, -32.14999999999999858 ) ) ;
#27283=CARTESIAN_POINT ( 'NONE',  ( 9.221458473665698818, -11.63198193419115789, -78.67433547361216029 ) ) ;
#27291=CARTESIAN_POINT ( 'NONE',  ( 17.61382546585139863, -22.91801235355460165, -78.66900642488448625 ) ) ;
#27298=CARTESIAN_POINT ( 'NONE',  ( 16.14193623000787881, -23.52718903762350422, -62.00734913397092640 ) ) ;
#27300=CARTESIAN_POINT ( 'NONE',  ( 15.24817897964529223, -22.38319375460040916, -70.99448831995151465 ) ) ;
#27308=CARTESIAN_POINT ( 'NONE',  ( 14.73211787852873655, -8.975754037563948629, -65.88667435850260290 ) ) ;
#27310=ORIENTED_EDGE ( 'NONE', *, *, #40507, .T. ) ;
#27311=CARTESIAN_POINT ( 'NONE',  ( 16.03351556195739747, -22.66831448449761055, -37.35171219075489546 ) ) ;
#27315=CARTESIAN_POINT ( 'NONE',  ( 22.09260590323088636, -20.84538979432554484, -77.73690341447758101 ) ) ;
#27322=CARTESIAN_POINT ( 'NONE',  ( 7.939473004570360537, -16.52913894747350199, -32.75701418906499640 ) ) ;
#27323=AXIS2_PLACEMENT_3D ( 'NONE', #9846, #29137, #8982 ) ;
#27326=CARTESIAN_POINT ( 'NONE',  ( 19.93518543153535916, -21.27024298737090646, -50.76453705344157186 ) ) ;
#27330=CARTESIAN_POINT ( 'NONE',  ( 10.22350615826409914, -10.45348132381399964, -79.24103283286969202 ) ) ;
#27340=CARTESIAN_POINT ( 'NONE',  ( 7.956346363297368995, -16.66974440877379848, -32.46687572425439328 ) ) ;
#27352=DIRECTION ( 'NONE',  ( 0.000000000000000000, 0.000000000000000000, 1.000000000000000000 ) ) ;
#27359=CARTESIAN_POINT ( 'NONE',  ( 18.66652200592500321, -22.62280792536489926, -65.45693882779990247 ) ) ;
#27360=CARTESIAN_POINT ( 'NONE',  ( 8.428889295206310805, -13.54532057320010452, -40.59100171928430711 ) ) ;
#27367=CARTESIAN_POINT ( 'NONE',  ( 10.08830361353289895, -11.20408907387949782, -81.23899999999999011 ) ) ;
#27376=CARTESIAN_POINT ( 'NONE',  ( 23.44306558266119822, -13.53261324785490061, -81.23899999999999011 ) ) ;
#27391=CARTESIAN_POINT ( 'NONE',  ( 15.80267776464130947, -8.799503143537849681, -39.93719130176964427 ) ) ;
#27396=CARTESIAN_POINT ( 'NONE',  ( 19.00123712817629951, -22.05987976827099928, -43.21391308946270016 ) ) ;
#27397=CARTESIAN_POINT ( 'NONE',  ( 16.04609829188889947, -7.768958065275190172, -50.78394269049039877 ) ) ;
#27405=DIRECTION ( 'NONE',  ( 1.000000000000000000, 2.460964292799963328E-14, 0.000000000000000000 ) ) ;
#27410=CARTESIAN_POINT ( 'NONE',  ( 18.20468663224212946, -23.32126934762677095, -37.92433689214998793 ) ) ;
#27413=CARTESIAN_POINT ( 'NONE',  ( 12.48397201735700079, -22.11114445343120138, -37.73031295553310116 ) ) ;
#27421=CARTESIAN_POINT ( 'NONE',  ( 23.83903810970707227, -13.54551561636778878, -67.42433258642762439 ) ) ;
#27424=B_SPLINE_CURVE_WITH_KNOTS ( 'NONE', 3,
 ( #35171, #63, #24118, #43313, #3478, #23867, #35433, #40138, #39891, #31991 ),
 .UNSPECIFIED., .F., .F.,
 ( 4, 1, 1, 1, 1, 1, 1, 4 ),
 ( 0.5000016690426868360, 0.5743016179356827955, 0.6535205489993028971, 0.7327394800629218885, 0.8119584111265421011, 0.8911773421901610925, 0.9703962732537800839, 1.000000000000000000 ),
 .UNSPECIFIED. ) ;
#27429=CARTESIAN_POINT ( 'NONE',  ( 18.95614455194280268, -22.07975653177619790, -59.21613716431369312 ) ) ;
#27430=CARTESIAN_POINT ( 'NONE',  ( 22.90083016047308462, -15.61618874168370752, -60.84718745454353694 ) ) ;
#27436=CARTESIAN_POINT ( 'NONE',  ( 23.98146843348427737, -16.64924324331575889, -55.54932755510194653 ) ) ;
#27441=B_SPLINE_CURVE_WITH_KNOTS ( 'NONE', 3,
 ( #46840, #3316, #51779, #35276, #3059, #15883, #19031, #15371, #35540, #35007 ),
 .UNSPECIFIED., .F., .F.,
 ( 4, 1, 1, 1, 1, 1, 1, 4 ),
 ( 0.5000037312039752324, 0.5547748945261627984, 0.6339938255897815678, 0.7132127566533992269, 0.7924316877170179962, 0.8716506187806356554, 0.9508695498442544247, 1.000000000000000000 ),
 .UNSPECIFIED. ) ;
#27444=ORIENTED_EDGE ( 'NONE', *, *, #21371, .F. ) ;
#27446=CARTESIAN_POINT ( 'NONE',  ( 24.04518460902906085, -15.61618869790763675, -47.79232989768991757 ) ) ;
#27449=CARTESIAN_POINT ( 'NONE',  ( 17.64329854752050153, -7.914982772203240202, -53.57409916825699270 ) ) ;
#27457=CARTESIAN_POINT ( 'NONE',  ( 17.37116791007819927, -8.672715762353169211, -52.40330909284259775 ) ) ;
#27458=CARTESIAN_POINT ( 'NONE',  ( 22.04683866091923150, -12.20817827527022637, -44.28613215260582336 ) ) ;
#27459=VERTEX_POINT ( 'NONE', #16850 ) ;
#27478=B_SPLINE_CURVE_WITH_KNOTS ( 'NONE', 3,
 ( #51264, #14578, #6726, #42890, #27396, #3822, #43655, #7757, #43397, #47086 ),
 .UNSPECIFIED., .F., .F.,
 ( 4, 1, 1, 1, 1, 1, 1, 4 ),
 ( 0.4999963331327971772, 0.5249287906993036490, 0.6041477217628976604, 0.6833666528264928930, 0.7625855838900870154, 0.8418045149536969030, 0.9210234460172921356, 1.000000000000000000 ),
 .UNSPECIFIED. ) ;
#27481=CARTESIAN_POINT ( 'NONE',  ( 17.90524903744462293, -22.20704404317461567, -74.86948688974470656 ) ) ;
#27484=CARTESIAN_POINT ( 'NONE',  ( 22.30826260938979999, -12.20733768994999835, -58.29224725099429349 ) ) ;
#27488=CARTESIAN_POINT ( 'NONE',  ( 23.88928256296529895, -14.41561843416390154, -45.23861751603709536 ) ) ;
#27501=CARTESIAN_POINT ( 'NONE',  ( 8.223360643215830379, -15.61635149015999957, -74.50766849176298479 ) ) ;
#27506=CARTESIAN_POINT ( 'NONE',  ( 24.01324593353028547, -16.33809533768586419, -43.82140147199449842 ) ) ;
#27507=CARTESIAN_POINT ( 'NONE',  ( 8.820368351115295269, -12.49945830288972282, -76.63581724531364614 ) ) ;
#27508=CARTESIAN_POINT ( 'NONE',  ( 8.222988179026620159, -15.61639226004780134, -48.50766849176299189 ) ) ;
#27509=ORIENTED_EDGE ( 'NONE', *, *, #45929, .T. ) ;
#27510=CARTESIAN_POINT ( 'NONE',  ( 12.14975833386557724, -22.52868516919143715, -62.45899714093157939 ) ) ;
#27512=CARTESIAN_POINT ( 'NONE',  ( 20.26128133979632651, -21.03119890602486208, -32.74566382982119706 ) ) ;
#27513=CARTESIAN_POINT ( 'NONE',  ( 11.27221847759618534, -9.290054678679373623, -69.08399908941892420 ) ) ;
#27514=CARTESIAN_POINT ( 'NONE',  ( 24.31740379465060187, -14.60941300932350018, -77.75336703320090237 ) ) ;
#27518=VERTEX_POINT ( 'NONE', #20496 ) ;
#27520=CARTESIAN_POINT ( 'NONE',  ( 22.40917576918729992, -11.60021120742629996, -52.05144558750829731 ) ) ;
#27522=CARTESIAN_POINT ( 'NONE',  ( 10.33790303897889906, -20.66510390621489890, -32.14999999999999858 ) ) ;
#27529=CARTESIAN_POINT ( 'NONE',  ( 11.31210022934189929, -8.927945002443658851, -70.80883835904629109 ) ) ;
#27531=CARTESIAN_POINT ( 'NONE',  ( 20.45445179548310222, -22.15697897774440150, -32.14999999999999858 ) ) ;
#27544=CARTESIAN_POINT ( 'NONE',  ( 17.16940068822441390, -23.52720096816359074, -72.25068831949764103 ) ) ;
#27546=CARTESIAN_POINT ( 'NONE',  ( 11.87813115486479987, -21.73131829969980089, -76.92618994148479317 ) ) ;
#27561=CARTESIAN_POINT ( 'NONE',  ( 11.85320398676953246, -10.34456170899610861, -65.73580935773964029 ) ) ;
#27564=CARTESIAN_POINT ( 'NONE',  ( 15.09833416417832375, -7.705195683357469960, -55.25065450683342760 ) ) ;
#27569=CARTESIAN_POINT ( 'NONE',  ( 16.07729529398784862, -23.52701512416443563, -78.00994996383560931 ) ) ;
#27571=AXIS2_PLACEMENT_3D ( 'NONE', #13353, #4962, #8900 ) ;
#27579=CARTESIAN_POINT ( 'NONE',  ( 24.35368793360969875, -14.96933410525219976, -35.76733356948250275 ) ) ;
#27581=CARTESIAN_POINT ( 'NONE',  ( 24.04402149975506831, -15.74633035369765466, -49.79756549422418033 ) ) ;
#27585=CARTESIAN_POINT ( 'NONE',  ( 13.83560527192710232, -8.112562019569040217, -69.41788538098089134 ) ) ;
#27591=CARTESIAN_POINT ( 'NONE',  ( 20.83159658330290043, -22.39222900395139959, -41.81470958976159835 ) ) ;
#27600=VERTEX_POINT ( 'NONE', #45408 ) ;
#27609=LINE ( 'NONE', #3259, #33400 ) ;
#27616=CARTESIAN_POINT ( 'NONE',  ( 21.70451063365279865, -20.56345163845099933, -65.29850096567270157 ) ) ;
#27619=EDGE_LOOP ( 'NONE', ( #38394, #4593, #1927, #19520 ) ) ;
#27623=DIRECTION ( 'NONE',  ( 0.000000000000000000, 0.000000000000000000, -1.000000000000000000 ) ) ;
#27624=CARTESIAN_POINT ( 'NONE',  ( 9.045058299293090798, -14.07202885548180049, -81.23899999999999011 ) ) ;
#27625=ORIENTED_EDGE ( 'NONE', *, *, #29926, .F. ) ;
#27633=CARTESIAN_POINT ( 'NONE',  ( 22.43307764042800301, -11.02875726361830111, -81.23899999999999011 ) ) ;
#27637=VERTEX_POINT ( 'NONE', #38845 ) ;
#27638=CARTESIAN_POINT ( 'NONE',  ( 20.99563574407254407, -9.290039920899717529, -63.50066641288683655 ) ) ;
#27652=CARTESIAN_POINT ( 'NONE',  ( 22.90018981389043873, -16.24635821130550539, -38.87681876136569770 ) ) ;
#27653=CARTESIAN_POINT ( 'NONE',  ( 8.856465214167128508, -12.67932892058150074, -64.40959883343289505 ) ) ;
#27656=ADVANCED_FACE ( 'NONE', ( #18137 ), #2406, .T. ) ;
#27668=CARTESIAN_POINT ( 'NONE',  ( 22.46012080236426911, -20.47784194944630443, -37.71600417800252103 ) ) ;
#27669=CARTESIAN_POINT ( 'NONE',  ( 24.04468322966528859, -15.61618861995729013, -71.79233702014498419 ) ) ;
#27671=CARTESIAN_POINT ( 'NONE',  ( 18.73669033277520057, -8.635331440240550549, -38.68094012829649841 ) ) ;
#27672=CARTESIAN_POINT ( 'NONE',  ( 9.366428224829499882, -15.61611423639980067, -77.45282021618989177 ) ) ;
#27673=VERTEX_POINT ( 'NONE', #14464 ) ;
#27677=LINE ( 'NONE', #39745, #43810 ) ;
#27682=VECTOR ( 'NONE', #33504, 1000.000000000000000 ) ;
#27684=CARTESIAN_POINT ( 'NONE',  ( 16.13393739769620083, -15.61618894467929941, -41.69811738492444420 ) ) ;
#27690=CYLINDRICAL_SURFACE ( 'NONE', #6029, 7.910999999999997812 ) ;
#27691=CARTESIAN_POINT ( 'NONE',  ( 8.222921866017912862, -14.58075518776391810, -38.83399696775236976 ) ) ;
#27698=CARTESIAN_POINT ( 'NONE',  ( 22.77734342274874280, -14.28677838390695776, -46.38995319782638660 ) ) ;
#27705=CARTESIAN_POINT ( 'NONE',  ( 9.984421472749652082, -12.69805524141423270, -33.59399944151634543 ) ) ;
#27707=CARTESIAN_POINT ( 'NONE',  ( 22.54949557071089927, -20.13585275078779802, -54.20785061676599526 ) ) ;
#27714=CARTESIAN_POINT ( 'NONE',  ( 19.54195640215267460, -21.52908387663484291, -38.78615563590209803 ) ) ;
#27715=CARTESIAN_POINT ( 'NONE',  ( 9.436316225021858628, -13.40611433014809961, -57.94863426729589406 ) ) ;
#27716=CARTESIAN_POINT ( 'NONE',  ( 16.13393739769620083, -15.61618894467929941, -28.45282021618999835 ) ) ;
#27725=EDGE_CURVE ( 'NONE', #37443, #51612, #30946, .T. ) ;
#27732=LINE ( 'NONE', #19099, #15591 ) ;
#27740=CARTESIAN_POINT ( 'NONE',  ( 10.22109192583901560, -19.02429315089245776, -75.28615355149135269 ) ) ;
#27744=CARTESIAN_POINT ( 'NONE',  ( 16.63319231246079966, -8.581041239996130443, -57.97537152673989880 ) ) ;
#27749=CARTESIAN_POINT ( 'NONE',  ( 15.53783599433159957, -7.791138702023379992, -44.76330392965529370 ) ) ;
#27755=CIRCLE ( 'NONE', #47051, 4.296700167715679086 ) ;
#27766=CARTESIAN_POINT ( 'NONE',  ( 8.222290034161709116, -15.61613760572089937, -44.79233150823699816 ) ) ;
#27768=CARTESIAN_POINT ( 'NONE',  ( 20.53874876090047863, -9.019602519203475666, -49.19511954482316440 ) ) ;
#27770=CARTESIAN_POINT ( 'NONE',  ( 8.428838373751766255, -17.68687216982602095, -36.42433490654720174 ) ) ;
#27772=CARTESIAN_POINT ( 'NONE',  ( 8.222963747489538733, -14.58044856772349895, -56.54933511702171245 ) ) ;
#27775=CARTESIAN_POINT ( 'NONE',  ( 9.921146318005629183, -21.03688512285170376, -68.56397102982089109 ) ) ;
#27781=CARTESIAN_POINT ( 'NONE',  ( 9.292831712696338897, -18.56677648139270076, -67.10304248959609197 ) ) ;
#27782=CARTESIAN_POINT ( 'NONE',  ( 10.25343679584480050, -20.55147180341439750, -32.14999999999999858 ) ) ;
#27786=EDGE_CURVE ( 'NONE', #8412, #40071, #45691, .T. ) ;
#27790=CARTESIAN_POINT ( 'NONE',  ( 23.44421149204620036, -19.42966680280959935, -73.66071987733648996 ) ) ;
#27792=CARTESIAN_POINT ( 'NONE',  ( 22.72757484624980151, -19.35329995587120067, -32.14999999999999858 ) ) ;
#27798=CARTESIAN_POINT ( 'NONE',  ( 8.428865626044137471, -13.54540663567643399, -78.59100198268760096 ) ) ;
#27800=VERTEX_POINT ( 'NONE', #28043 ) ;
#27803=CARTESIAN_POINT ( 'NONE',  ( 14.59138716251818479, -23.39588144484022436, -66.35464036535437060 ) ) ;
#27805=CARTESIAN_POINT ( 'NONE',  ( 9.116028935892819263, -18.11731961437540050, -73.12368125043110467 ) ) ;
#27827=CARTESIAN_POINT ( 'NONE',  ( 16.12583665212202533, -23.52718583135971997, -78.00799738171198783 ) ) ;
#27831=CARTESIAN_POINT ( 'NONE',  ( 21.75737274077464178, -19.46263012217717403, -80.64360312776651085 ) ) ;
#27835=CARTESIAN_POINT ( 'NONE',  ( 9.078410285617929176, -19.88259928906289886, -38.61921508777280110 ) ) ;
#27837=CARTESIAN_POINT ( 'NONE',  ( 24.04493737978153689, -16.65173533839766051, -67.54933246951844694 ) ) ;
#27842=CARTESIAN_POINT ( 'NONE',  ( 12.79739587422460012, -22.27759566055959795, -32.88046427011249051 ) ) ;
#27843=CARTESIAN_POINT ( 'NONE',  ( 19.54193610434072781, -21.52909601099131365, -36.78615172203510753 ) ) ;
#27848=CARTESIAN_POINT ( 'NONE',  ( 23.24087076968150001, -19.79640649346030301, -47.67691048846949542 ) ) ;
#27853=CARTESIAN_POINT ( 'NONE',  ( 24.04462281140675728, -15.61619016268715399, -39.50767146438039390 ) ) ;
#27854=CARTESIAN_POINT ( 'NONE',  ( 22.55531606818893664, -17.79663561174430697, -56.55696934072006599 ) ) ;
#27858=DIRECTION ( 'NONE',  ( 0.000000000000000000, 0.000000000000000000, -1.000000000000000000 ) ) ;
#27859=CARTESIAN_POINT ( 'NONE',  ( 9.807831198552406704, -20.47794271258318943, -38.58399882689687388 ) ) ;
#27864=CARTESIAN_POINT ( 'NONE',  ( 24.04493738991158480, -14.58064431297338537, -61.75066186890055064 ) ) ;
#27867=CARTESIAN_POINT ( 'NONE',  ( 23.64088593898193480, -13.06712279613562266, -75.68818038166295992 ) ) ;
#27870=CARTESIAN_POINT ( 'NONE',  ( 23.31571238671009993, -13.63406827592180015, -64.98162524141820029 ) ) ;
#27876=CARTESIAN_POINT ( 'NONE',  ( 9.082179215743179768, -13.83380170031609957, -81.23899999999999011 ) ) ;
#27885=CARTESIAN_POINT ( 'NONE',  ( 15.09848951713014387, -7.705176910871855966, -73.25066484698234603 ) ) ;
#27888=ORIENTED_EDGE ( 'NONE', *, *, #22383, .F. ) ;
#27895=CARTESIAN_POINT ( 'NONE',  ( 12.45398646450647995, -22.71722742353124858, -50.15946686457399295 ) ) ;
#27899=CARTESIAN_POINT ( 'NONE',  ( 9.366922731475222363, -14.63844643040854976, -39.49882628218075098 ) ) ;
#27905=CARTESIAN_POINT ( 'NONE',  ( 8.436531076600029877, -14.08756730701639803, -62.34990662577889964 ) ) ;
#27910=CARTESIAN_POINT ( 'NONE',  ( 9.366376358913971245, -15.61615244833809868, -75.84717978381000592 ) ) ;
#27916=FACE_OUTER_BOUND ( 'NONE', #26247, .T. ) ;
#27922=CARTESIAN_POINT ( 'NONE',  ( 24.04493739712419043, -16.65173214393696810, -53.83400119000078377 ) ) ;
#27923=EDGE_LOOP ( 'NONE', ( #14322, #5917, #29442, #15889 ) ) ;
#27924=CARTESIAN_POINT ( 'NONE',  ( 21.24586391840339772, -10.75704091599320122, -80.60524855149108703 ) ) ;
#27925=CARTESIAN_POINT ( 'NONE',  ( 9.543045992446268500, -17.38737032729065390, -77.36949155694581748 ) ) ;
#27932=CARTESIAN_POINT ( 'NONE',  ( 23.04647526746508390, -11.63208492753508416, -35.62566255721337427 ) ) ;
#27935=VERTEX_POINT ( 'NONE', #20183 ) ;
#27938=CARTESIAN_POINT ( 'NONE',  ( 22.78093346138021502, -17.47720641827233834, -58.93471117284045135 ) ) ;
#27943=CARTESIAN_POINT ( 'NONE',  ( 20.99557505903451471, -21.94238661114907529, -55.79928181614338456 ) ) ;
#27956=CARTESIAN_POINT ( 'NONE',  ( 22.74393318103090067, -11.38597578978039948, -51.83128268485739909 ) ) ;
#27960=CARTESIAN_POINT ( 'NONE',  ( 22.90065884458136480, -15.61618680935524317, -64.84717769963093303 ) ) ;
#27964=CARTESIAN_POINT ( 'NONE',  ( 9.549614380104699762, -18.14388544039750073, -55.73050419751459827 ) ) ;
#27965=CARTESIAN_POINT ( 'NONE',  ( 10.72252174668208546, -11.45764127470922489, -43.66113319608867016 ) ) ;
#27967=B_SPLINE_CURVE_WITH_KNOTS ( 'NONE', 3,
 ( #30879, #23266, #27215, #47164, #22760, #14657, #42971, #38252, #10480, #46651, #43227, #38781, #18319, #22503, #39285, #7066, #3393, #6287 ),
 .UNSPECIFIED., .F., .F.,
 ( 4, 2, 2, 2, 2, 2, 2, 2, 4 ),
 ( 0.000000000000000000, 0.1250000000000000000, 0.2500000000000000000, 0.3750000000000000000, 0.5000000000000000000, 0.6250000000000000000, 0.7500000000000000000, 0.8750000000000000000, 1.000000000000000000 ),
 .UNSPECIFIED. ) ;
#27977=CARTESIAN_POINT ( 'NONE',  ( 20.37502878971641351, -8.918043044671964736, -65.18732621157280960 ) ) ;
#27978=CARTESIAN_POINT ( 'NONE',  ( 2.277530937145189949, -15.61618894467929941, -32.14999999999999858 ) ) ;
#27981=B_SPLINE_CURVE_WITH_KNOTS ( 'NONE', 3,
 ( #28637, #1134, #17129, #21035, #40448, #49111, #875, #13210, #12945, #12415, #20774, #28901, #5081, #9009, #28122, #40196, #16595, #45159 ),
 .UNSPECIFIED., .F., .F.,
 ( 4, 2, 2, 2, 2, 2, 2, 2, 4 ),
 ( 0.5000000033146290157, 0.5625000029003004443, 0.6250000024859717618, 0.6875000020716430793, 0.7500000016573145079, 0.8125000012429859364, 0.8750000008286572539, 0.9375000004143285715, 1.000000000000000000 ),
 .UNSPECIFIED. ) ;
#27988=CARTESIAN_POINT ( 'NONE',  ( 9.543102950792974326, -17.38757742493531566, -75.36948688384066486 ) ) ;
#27992=CARTESIAN_POINT ( 'NONE',  ( 15.86297936323760283, -22.66382262132480108, -54.96505214632229297 ) ) ;
#27997=CARTESIAN_POINT ( 'NONE',  ( 20.19834834365759590, -8.902969758213549412, -40.96079523860159810 ) ) ;
#28014=CARTESIAN_POINT ( 'NONE',  ( 11.36138452961498935, -9.254399639206521755, -48.80268936686415771 ) ) ;
#28022=CARTESIAN_POINT ( 'NONE',  ( 19.24953057887579888, -23.25004767963920216, -76.16898841192839598 ) ) ;
#28028=CARTESIAN_POINT ( 'NONE',  ( 20.58238051217970366, -21.59264673022000025, -68.52898324874119851 ) ) ;
#28031=CARTESIAN_POINT ( 'NONE',  ( 10.71761651803740101, -21.13360478435039624, -32.14999999999999858 ) ) ;
#28034=EDGE_CURVE ( 'NONE', #5352, #28199, #39799, .T. ) ;
#28037=CARTESIAN_POINT ( 'NONE',  ( 20.50233011740730049, -8.623345048570200788, -73.18540629095480199 ) ) ;
#28043=CARTESIAN_POINT ( 'NONE',  ( 8.223516320988901285, -15.61608250808600040, -78.50766849176299900 ) ) ;
#28048=AXIS2_PLACEMENT_3D ( 'NONE', #45010, #6214, #13565 ) ;
#28049=CARTESIAN_POINT ( 'NONE',  ( 23.83903219839593390, -17.68689162105726709, -71.87567630288067733 ) ) ;
#28051=CARTESIAN_POINT ( 'NONE',  ( 16.70908614872999820, -23.04423698702060008, -74.70805987170351159 ) ) ;
#28059=DIRECTION ( 'NONE',  ( 1.000000000000000000, 0.000000000000000000, 0.000000000000000000 ) ) ;
#28074=ORIENTED_EDGE ( 'NONE', *, *, #47573, .F. ) ;
#28081=CARTESIAN_POINT ( 'NONE',  ( 24.04462728581425068, -15.69187742550130693, -65.51071106015494649 ) ) ;
#28083=CARTESIAN_POINT ( 'NONE',  ( 24.30253626735589734, -14.49515702607499890, -45.74891888349849722 ) ) ;
#28086=CARTESIAN_POINT ( 'NONE',  ( 9.700071671388441175, -20.26994223601302636, -50.59290778570318992 ) ) ;
#28090=CARTESIAN_POINT ( 'NONE',  ( 19.90766354386979842, -22.04007435515010016, -32.56358854585799634 ) ) ;
#28094=CARTESIAN_POINT ( 'NONE',  ( 11.02646362629858245, -21.74036658064323646, -60.51332976940924624 ) ) ;
#28096=DIRECTION ( 'NONE',  ( 0.000000000000000000, 0.000000000000000000, 1.000000000000000000 ) ) ;
#28097=CARTESIAN_POINT ( 'NONE',  ( 19.50889905593779972, -8.093399932991250267, -45.14190469443359888 ) ) ;
#28102=CARTESIAN_POINT ( 'NONE',  ( 24.04516176800591865, -15.61618872104648226, -63.79232972929064971 ) ) ;
#28103=CARTESIAN_POINT ( 'NONE',  ( 22.84664618675378378, -16.49985765395500437, -56.49448217489652535 ) ) ;
#28117=CARTESIAN_POINT ( 'NONE',  ( 23.98146751630273243, -14.58312774351319341, -75.75066832808212780 ) ) ;
#28121=EDGE_CURVE ( 'NONE', #4148, #20658, #6177, .T. ) ;
#28122=CARTESIAN_POINT ( 'NONE',  ( 10.22099957837624018, -19.02413528178931656, -61.28616401637014377 ) ) ;
#28123=CARTESIAN_POINT ( 'NONE',  ( 9.109677719005789598, -16.24994667744640253, -81.42417512157139470 ) ) ;
#28127=CARTESIAN_POINT ( 'NONE',  ( 16.24075058801180660, -22.45095174809149796, -34.94749056287888322 ) ) ;
#28129=CARTESIAN_POINT ( 'NONE',  ( 12.28182699806689904, -8.928754245619188623, -81.23899999999999011 ) ) ;
#28136=CARTESIAN_POINT ( 'NONE',  ( 20.94776370346930250, -20.69586690337569834, -81.23899999999999011 ) ) ;
#28140=EDGE_CURVE ( 'NONE', #2233, #6987, #46191, .T. ) ;
#28143=CARTESIAN_POINT ( 'NONE',  ( 22.57761993255723709, -12.95386672222832480, -42.72197786470339764 ) ) ;
#28148=CARTESIAN_POINT ( 'NONE',  ( 7.349327706869664745, -24.40079863550579375, -22.14999999999998792 ) ) ;
#28158=CARTESIAN_POINT ( 'NONE',  ( 23.17695949768430097, -12.15460146459719937, -63.14209593641499652 ) ) ;
#28161=FACE_OUTER_BOUND ( 'NONE', #16737, .T. ) ;
#28170=EDGE_CURVE ( 'NONE', #17698, #1081, #4342, .T. ) ;
#28171=AXIS2_PLACEMENT_3D ( 'NONE', #14968, #41260, #35133 ) ;
#28173=CARTESIAN_POINT ( 'NONE',  ( 8.222524523195870572, -15.61634168869099959, -38.50766849176289952 ) ) ;
#28177=CARTESIAN_POINT ( 'NONE',  ( 15.99849640639799908, -8.167138661756609963, -34.56155571298840101 ) ) ;
#28182=AXIS2_PLACEMENT_3D ( 'NONE', #34101, #34888, #42518 ) ;
#28188=CARTESIAN_POINT ( 'NONE',  ( 14.06325681293461116, -23.32128858265275539, -52.09100060540798438 ) ) ;
#28195=CARTESIAN_POINT ( 'NONE',  ( 9.807806602964351583, -10.75446673786055385, -79.00066532657710638 ) ) ;
#28199=VERTEX_POINT ( 'NONE', #17184 ) ;
#28207=CARTESIAN_POINT ( 'NONE',  ( 24.04470022272198193, -15.61619473591594698, -59.79232576333501470 ) ) ;
#28214=CARTESIAN_POINT ( 'NONE',  ( 8.388736160725070334, -16.88054862072210227, -58.96098648058310232 ) ) ;
#28218=FACE_OUTER_BOUND ( 'NONE', #48015, .T. ) ;
#28222=DIRECTION ( 'NONE',  ( 0.000000000000000000, 0.000000000000000000, -1.000000000000000000 ) ) ;
#28223=CARTESIAN_POINT ( 'NONE',  ( 13.10370563145900036, -9.247495623648822161, -56.20581778389630045 ) ) ;
#28229=CARTESIAN_POINT ( 'NONE',  ( 9.543056551245093999, -13.84496916688426182, -37.53615381032067688 ) ) ;
#28230=CARTESIAN_POINT ( 'NONE',  ( 22.55396266313498188, -18.35526875653752299, -76.97599367191068609 ) ) ;
#28231=CARTESIAN_POINT ( 'NONE',  ( 24.04493539499120658, -15.60966883180437570, -55.50740977386095665 ) ) ;
#28236=CARTESIAN_POINT ( 'NONE',  ( 12.14983891641476177, -22.52873075169600625, -52.45899731366314001 ) ) ;
#28249=CARTESIAN_POINT ( 'NONE',  ( 22.96386447642289852, -13.85702584936900017, -66.37257821948358583 ) ) ;
#28254=CARTESIAN_POINT ( 'NONE',  ( 20.60515567366930156, -22.06560405860919971, -41.59454668711060066 ) ) ;
#28261=CARTESIAN_POINT ( 'NONE',  ( 20.99566313739885715, -21.94231611088021339, -63.79933632437322188 ) ) ;
#28267=ADVANCED_FACE ( 'NONE', ( #37095 ), #19789, .T. ) ;
#28270=B_SPLINE_CURVE_WITH_KNOTS ( 'NONE', 3,
 ( #29208, #21596, #42323, #33134, #49159, #34168, #5896, #45216, #21341, #30245, #9324, #25784, #42059, #17688, #10089, #38128, #37348, #25271 ),
 .UNSPECIFIED., .F., .F.,
 ( 4, 2, 2, 2, 2, 2, 2, 2, 4 ),
 ( 0.4999984312796272867, 0.5624986273696739314, 0.6249988234597205761, 0.6874990195497672207, 0.7499992156398138654, 0.8124994117298603991, 0.8749996078199069327, 0.9374998039099534664, 1.000000000000000000 ),
 .UNSPECIFIED. ) ;
#28273=CARTESIAN_POINT ( 'NONE',  ( 20.99559717909331624, -21.94236875847741075, -62.08399597771296641 ) ) ;
#28277=CARTESIAN_POINT ( 'NONE',  ( 21.83276634445940090, -9.657492049260909539, -75.53523696341960658 ) ) ;
#28278=CARTESIAN_POINT ( 'NONE',  ( 11.92983776680180341, -9.953318164944898072, -38.14390150139128366 ) ) ;
#28279=EDGE_CURVE ( 'NONE', #35815, #38000, #33059, .T. ) ;
#28283=CARTESIAN_POINT ( 'NONE',  ( 23.52193300906940010, -14.65482811154960174, -62.19146876365169874 ) ) ;
#28290=CARTESIAN_POINT ( 'NONE',  ( 18.15912969681970068, -7.623610082976019164, -75.08666063648169597 ) ) ;
#28297=CARTESIAN_POINT ( 'NONE',  ( 18.20466777478382880, -7.911103216214283584, -79.09100292823505640 ) ) ;
#28308=CARTESIAN_POINT ( 'NONE',  ( 22.17630248670440096, -19.25372891403399933, -32.62531358638169365 ) ) ;
#28324=CARTESIAN_POINT ( 'NONE',  ( 20.99557608044584001, -21.94238580726353049, -71.79928481050744438 ) ) ;
#28328=CARTESIAN_POINT ( 'NONE',  ( 8.222923941706072881, -14.58073999030537848, -54.83399627919607155 ) ) ;
#28333=CARTESIAN_POINT ( 'NONE',  ( 9.366918910324010028, -14.88264276746137682, -49.48733500142635222 ) ) ;
#28336=CARTESIAN_POINT ( 'NONE',  ( 12.69092708031987016, -9.723879944688558652, -71.78431635714069614 ) ) ;
#28337=CARTESIAN_POINT ( 'NONE',  ( 17.17653815174671550, -23.52626367551765796, -65.96613581823291383 ) ) ;
#28338=CARTESIAN_POINT ( 'NONE',  ( 24.37832766821379948, -15.50327692879579899, -41.78797233031760072 ) ) ;
#28343=CARTESIAN_POINT ( 'NONE',  ( 9.234060601172799920, -12.80577920849349915, -33.35577785649419980 ) ) ;
#28347=CARTESIAN_POINT ( 'NONE',  ( 12.14972585590047238, -8.703711119338285229, -32.84099998782102858 ) ) ;
#28354=CARTESIAN_POINT ( 'NONE',  ( 22.67586280804129828, -20.63474776514319586, -43.71596393528839286 ) ) ;
#28363=CARTESIAN_POINT ( 'NONE',  ( 16.13393739769620083, -15.61618894467929941, -22.14999999999999858 ) ) ;
#28364=EDGE_CURVE ( 'NONE', #31550, #14613, #15496, .T. ) ;
#28372=CARTESIAN_POINT ( 'NONE',  ( 11.27229802542173331, -9.289994498170599968, -61.08399727017809511 ) ) ;
#28375=CARTESIAN_POINT ( 'NONE',  ( 24.04493739777547390, -15.61328088927116475, -75.79220904166886896 ) ) ;
#28380=DIRECTION ( 'NONE',  ( 0.000000000000000000, 0.000000000000000000, -1.000000000000000000 ) ) ;
#28384=CARTESIAN_POINT ( 'NONE',  ( 22.21599079217217465, -18.67024064526685123, -34.60078485984914920 ) ) ;
#28385=VECTOR ( 'NONE', #48059, 1000.000000000000000 ) ;
#28386=CARTESIAN_POINT ( 'NONE',  ( 9.068231266001319568, -13.91742136908450078, -81.23899999999999011 ) ) ;
#28390=EDGE_LOOP ( 'NONE', ( #14887, #28718, #14111, #9903 ) ) ;
#28395=CARTESIAN_POINT ( 'NONE',  ( 19.45428832600709868, -21.61900137026959712, -81.23899999999999011 ) ) ;
#28398=ORIENTED_EDGE ( 'NONE', *, *, #25109, .F. ) ;
#28420=CARTESIAN_POINT ( 'NONE',  ( 9.710243317568311383, -20.12428195038719991, -64.09272310917839377 ) ) ;
#28424=VECTOR ( 'NONE', #6832, 1000.000000000000000 ) ;
#28434=CARTESIAN_POINT ( 'NONE',  ( 14.92658367925920615, -23.46628484408796922, -34.05631316871021141 ) ) ;
#28438=CARTESIAN_POINT ( 'NONE',  ( 10.37278528681540024, -10.89222655134519968, -46.28595751040398909 ) ) ;
#28440=ORIENTED_EDGE ( 'NONE', *, *, #51526, .F. ) ;
#28453=EDGE_LOOP ( 'NONE', ( #15857, #6441, #6323, #37283 ) ) ;
#28475=CARTESIAN_POINT ( 'NONE',  ( 13.29067414848886308, -9.445305870462737730, -33.81532646017170407 ) ) ;
#28476=CARTESIAN_POINT ( 'NONE',  ( 12.42856185862050111, -8.698317906129821253, -51.35596909847569691 ) ) ;
#28485=CARTESIAN_POINT ( 'NONE',  ( 21.54529553476142922, -19.77480928362585999, -38.66115602709810872 ) ) ;
#28486=CARTESIAN_POINT ( 'NONE',  ( 18.14390284338869819, -22.37655861516129718, -55.25519061113289609 ) ) ;
#28494=FACE_BOUND ( 'NONE', #29430, .T. ) ;
#28505=CARTESIAN_POINT ( 'NONE',  ( 12.74054237724960004, -9.433355499594508586, -66.18740309791249388 ) ) ;
#28510=DIRECTION ( 'NONE',  ( -1.000000000000000000, 1.330268894940021809E-33, -1.060511545910580040E-15 ) ) ;
#28513=CARTESIAN_POINT ( 'NONE',  ( 22.53532168237200395, -18.57673584289430124, -68.59070828926491004 ) ) ;
#28529=LINE ( 'NONE', #32701, #3276 ) ;
#28531=CARTESIAN_POINT ( 'NONE',  ( 8.428838513752189954, -17.68687267757047721, -44.42434460177876332 ) ) ;
#28534=CARTESIAN_POINT ( 'NONE',  ( 19.54197404232941793, -9.703304558279992165, -68.11948528069008546 ) ) ;
#28539=CARTESIAN_POINT ( 'NONE',  ( 23.37753514989420012, -19.55484501754060034, -73.95085834214698650 ) ) ;
#28546=CARTESIAN_POINT ( 'NONE',  ( 11.49411317949089906, -9.787061648994210827, -65.51866386832369926 ) ) ;
#28551=ADVANCED_FACE ( 'NONE', ( #48510 ), #13147, .T. ) ;
#28559=EDGE_CURVE ( 'NONE', #9084, #17470, #17320, .T. ) ;
#28569=CARTESIAN_POINT ( 'NONE',  ( 11.66494716225189876, -10.15993774188009979, -33.73437862127239839 ) ) ;
#28574=DIRECTION ( 'NONE',  ( 1.000000000000000000, 2.460964292799963328E-14, 0.000000000000000000 ) ) ;
#28575=ORIENTED_EDGE ( 'NONE', *, *, #25860, .T. ) ;
#28579=CARTESIAN_POINT ( 'NONE',  ( 16.13393739769620083, -15.61618894467929941, -32.14999999999999858 ) ) ;
#28594=FACE_OUTER_BOUND ( 'NONE', #20853, .T. ) ;
#28597=CARTESIAN_POINT ( 'NONE',  ( 19.50681848041033106, -9.682899184164803330, -72.11765224560839727 ) ) ;
#28598=CARTESIAN_POINT ( 'NONE',  ( 23.04647303881236553, -11.63208075929189356, -35.34099930627255759 ) ) ;
#28599=CARTESIAN_POINT ( 'NONE',  ( 22.44565080833970327, -10.31100337979670023, -39.56984226053619835 ) ) ;
#28601=DIRECTION ( 'NONE',  ( -1.224646799147357151E-16, 1.000000000000000000, 3.740764114965448302E-16 ) ) ;
#28607=CARTESIAN_POINT ( 'NONE',  ( 14.87826689285460091, -8.191960251112410774, -81.45916290265100201 ) ) ;
#28609=CARTESIAN_POINT ( 'NONE',  ( 14.06316976997283064, -7.911111869945884223, -32.92433297370318712 ) ) ;
#28611=CARTESIAN_POINT ( 'NONE',  ( 24.04486774516310277, -15.65047751723203362, -59.79370488822283392 ) ) ;
#28614=CARTESIAN_POINT ( 'NONE',  ( 24.27816550820259778, -16.90237291014140197, -43.55752607316119906 ) ) ;
#28619=CARTESIAN_POINT ( 'NONE',  ( 24.04493739769619864, -15.61618894467929941, -32.14999999999999858 ) ) ;
#28620=CARTESIAN_POINT ( 'NONE',  ( 22.90120720387987774, -15.61618909956830770, -56.84718059981966576 ) ) ;
#28630=PLANE ( 'NONE',  #9378 ) ;
#28634=CARTESIAN_POINT ( 'NONE',  ( 23.04644708940202591, -11.63203215977157257, -75.62569094467853859 ) ) ;
#28636=LINE ( 'NONE', #40195, #32931 ) ;
#28637=CARTESIAN_POINT ( 'NONE',  ( 22.90073451867936072, -15.61618922653637931, -60.45281425156898791 ) ) ;
#28638=CARTESIAN_POINT ( 'NONE',  ( 17.90521964142824274, -9.025325540544024250, -48.03615471533210268 ) ) ;
#28644=CARTESIAN_POINT ( 'NONE',  ( 14.30294810761210123, -7.958315104980580479, -81.23899999999999011 ) ) ;
#28652=CARTESIAN_POINT ( 'NONE',  ( 23.18878377121089684, -17.50908265191390001, -81.23899999999999011 ) ) ;
#28654=EDGE_LOOP ( 'NONE', ( #45175, #30882, #6601, #39083 ) ) ;
#28655=CARTESIAN_POINT ( 'NONE',  ( 22.90097009252848892, -15.61618913824531418, -68.84717732178738459 ) ) ;
#28662=CARTESIAN_POINT ( 'NONE',  ( 2.277530937145189949, -15.61618894467929941, -24.15000000000000213 ) ) ;
#28669=EDGE_CURVE ( 'NONE', #40528, #9856, #42726, .T. ) ;
#28674=CARTESIAN_POINT ( 'NONE',  ( 8.223596773276058869, -15.61622589296290009, -36.79233150823699816 ) ) ;
#28677=CARTESIAN_POINT ( 'NONE',  ( 20.66963613231810015, -9.211957127206400031, -62.98365807428779561 ) ) ;
#28689=AXIS2_PLACEMENT_3D ( 'NONE', #50875, #19666, #11045 ) ;
#28691=CARTESIAN_POINT ( 'NONE',  ( 8.428876971878688451, -17.68701251098292815, -38.42433540610390708 ) ) ;
#28692=CARTESIAN_POINT ( 'NONE',  ( 8.222950854910955343, -16.65183494035026612, -54.75066497266151799 ) ) ;
#28694=CARTESIAN_POINT ( 'NONE',  ( 8.683664543233660993, -15.60484291453579964, -44.06782744062269330 ) ) ;
#28697=ORIENTED_EDGE ( 'NONE', *, *, #16192, .T. ) ;
#28698=CARTESIAN_POINT ( 'NONE',  ( 8.222268241235530795, -15.61616536502389962, -60.50766849176299900 ) ) ;
#28700=CARTESIAN_POINT ( 'NONE',  ( 8.222732946675209931, -15.61637358666110131, -80.79233150823698395 ) ) ;
#28703=CARTESIAN_POINT ( 'NONE',  ( 24.04490680206547992, -15.61618865440000192, -77.79233401716611240 ) ) ;
#28706=CARTESIAN_POINT ( 'NONE',  ( 20.11807062262020551, -22.52871098524190785, -51.84099987359497419 ) ) ;
#28713=CARTESIAN_POINT ( 'NONE',  ( 23.04646684753098995, -11.63206918574938875, -79.62566678159748790 ) ) ;
#28718=ORIENTED_EDGE ( 'NONE', *, *, #43773, .T. ) ;
#28720=CARTESIAN_POINT ( 'NONE',  ( 14.06313845534990037, -23.32125801677240062, -56.09093780913883620 ) ) ;
#28724=CARTESIAN_POINT ( 'NONE',  ( 23.94343574623035664, -14.32673947065577202, -59.74025267311575504 ) ) ;
#28725=B_SPLINE_CURVE_WITH_KNOTS ( 'NONE', 3,
 ( #30634, #18593, #19107, #14923, #31146, #7073, #25920, #39045, #38522, #26697, #46658 ),
 .UNSPECIFIED., .F., .F.,
 ( 4, 1, 1, 1, 1, 1, 1, 1, 4 ),
 ( 0.000000000000000000, 0.01976910049033019090, 0.09898803155395019537, 0.1782069626175702137, 0.2574258936811890663, 0.3366448247448090569, 0.4158637558084279373, 0.4950826868720638041, 0.5000016690426868360 ),
 .UNSPECIFIED. ) ;
#28726=B_SPLINE_CURVE_WITH_KNOTS ( 'NONE', 3,
 ( #24953, #40965, #9274, #26264, #34642, #26781, #30713, #41744, #34906, #6113, #42536, #42796, #2695, #2175, #46476, #18668, #46735, #50647 ),
 .UNSPECIFIED., .F., .F.,
 ( 4, 2, 2, 2, 2, 2, 2, 2, 4 ),
 ( 0.5000000032451481502, 0.5625000028395046314, 0.6250000024338611126, 0.6875000020282175939, 0.7500000016225740751, 0.8125000012169305563, 0.8750000008112870375, 0.9375000004056435188, 1.000000000000000000 ),
 .UNSPECIFIED. ) ;
#28734=CARTESIAN_POINT ( 'NONE',  ( 13.40148368168809867, -22.97284880370879989, -68.62569607034480157 ) ) ;
#28750=CARTESIAN_POINT ( 'NONE',  ( 22.72480996509791851, -13.84493836002453016, -38.36948975162746223 ) ) ;
#28753=CARTESIAN_POINT ( 'NONE',  ( 19.28335304380221160, -8.292279851470313545, -55.13679355289837503 ) ) ;
#28754=CARTESIAN_POINT ( 'NONE',  ( 23.34518454799010101, -17.37660377373440213, -32.14999999999999858 ) ) ;
#28762=CARTESIAN_POINT ( 'NONE',  ( 12.24635195013770073, -21.50085024014760293, -59.53301288856830098 ) ) ;
#28770=CARTESIAN_POINT ( 'NONE',  ( 20.30862021219660107, -9.931597306316877649, -64.15444814970220477 ) ) ;
#28771=DIRECTION ( 'NONE',  ( 0.000000000000000000, 5.782411586589432581E-16, -1.000000000000000000 ) ) ;
#28784=CARTESIAN_POINT ( 'NONE',  ( 14.06336563596984313, -23.32131676130726561, -64.09100251094548639 ) ) ;
#28800=CARTESIAN_POINT ( 'NONE',  ( 23.10711481198539730, -20.01590724778190022, -79.97149710298219816 ) ) ;
#28806=CARTESIAN_POINT ( 'NONE',  ( 23.34874387044599686, -13.75789365977069956, -66.15241531683260234 ) ) ;
#28821=DIRECTION ( 'NONE',  ( 0.000000000000000000, 0.000000000000000000, 1.000000000000000000 ) ) ;
#28822=CARTESIAN_POINT ( 'NONE',  ( 8.223600577592289795, -15.61621812327629932, -68.50766849176299900 ) ) ;
#28829=CARTESIAN_POINT ( 'NONE',  ( 22.93861538555659862, -13.76175748592850034, -34.36813006978140095 ) ) ;
#28838=CARTESIAN_POINT ( 'NONE',  ( 12.17768353250039937, -9.303127112852680014, -76.38915131457939367 ) ) ;
#28846=DIRECTION ( 'NONE',  ( -1.224646799147353700E-16, 1.000000000000000000, 5.351958659602136763E-17 ) ) ;
#28848=CARTESIAN_POINT ( 'NONE',  ( 24.04215780991690110, -15.84268857627947646, -71.51678454628235215 ) ) ;
#28854=DIRECTION ( 'NONE',  ( 0.000000000000000000, 0.000000000000000000, 1.000000000000000000 ) ) ;
#28856=CARTESIAN_POINT ( 'NONE',  ( 13.14827817127709864, -9.226478610231410471, -72.20804185874739289 ) ) ;
#28857=CARTESIAN_POINT ( 'NONE',  ( 19.54190978043818916, -9.703266135105563350, -70.11948897317647322 ) ) ;
#28858=CARTESIAN_POINT ( 'NONE',  ( 20.85900685591025550, -10.71576073910020099, -50.19691013058185547 ) ) ;
#28861=DIRECTION ( 'NONE',  ( 1.060511545910580040E-15, 5.351958659602149705E-17, -1.000000000000000000 ) ) ;
#28862=CARTESIAN_POINT ( 'NONE',  ( 22.55005608494040104, -13.41974511834900774, -72.34789028957942492 ) ) ;
#28863=CARTESIAN_POINT ( 'NONE',  ( 9.221475126720598325, -11.63195346281944786, -34.67433465466491072 ) ) ;
#28866=CARTESIAN_POINT ( 'NONE',  ( 7.971080360336099346, -14.45408523004980061, -40.83734515755419636 ) ) ;
#28867=CARTESIAN_POINT ( 'NONE',  ( 22.90093739619960900, -15.61165398910431179, -56.45261194681012284 ) ) ;
#28872=CARTESIAN_POINT ( 'NONE',  ( 23.25862214412349971, -12.32596019608740079, -79.87478428137859510 ) ) ;
#28873=CARTESIAN_POINT ( 'NONE',  ( 11.29067012326649966, -10.76071234358520101, -32.14999999999999858 ) ) ;
#28875=CARTESIAN_POINT ( 'NONE',  ( 24.04493741964421361, -14.58064922431956667, -51.75066236550382115 ) ) ;
#28876=B_SPLINE_CURVE_WITH_KNOTS ( 'NONE', 3,
 ( #15898, #11977, #12223, #27932, #43934, #8031, #49688, #17450, #14035, #41807, #17705, #25799, #2242, #21878, #49944, #17959, #13782, #5913 ),
 .UNSPECIFIED., .F., .F.,
 ( 4, 2, 2, 2, 2, 2, 2, 2, 4 ),
 ( 0.5000013706141720471, 0.5625011992874004996, 0.6250010279606290631, 0.6875008566338575156, 0.7500006853070859680, 0.8125005139803145315, 0.8750003426535429840, 0.9375001713267714365, 1.000000000000000000 ),
 .UNSPECIFIED. ) ;
#28878=CARTESIAN_POINT ( 'NONE',  ( 22.39113274415149846, -10.24681029298479906, -55.28192787057689372 ) ) ;
#28891=CARTESIAN_POINT ( 'NONE',  ( 24.04481203031673076, -15.61619115162449312, -61.50767625960597229 ) ) ;
#28893=DIRECTION ( 'NONE',  ( 1.000000000000000000, 0.000000000000000000, 0.000000000000000000 ) ) ;
#28894=CARTESIAN_POINT ( 'NONE',  ( 10.72267370182032309, -19.77493159281586088, -65.24448734500967362 ) ) ;
#28897=CARTESIAN_POINT ( 'NONE',  ( 22.89703504567739856, -15.86470445441918642, -66.46450912331485483 ) ) ;
#28901=CARTESIAN_POINT ( 'NONE',  ( 12.72591286716733805, -21.52908169620734924, -61.11950314682426466 ) ) ;
#28902=CARTESIAN_POINT ( 'NONE',  ( 14.22831053668800116, -22.40670773495260093, -61.43426723409519496 ) ) ;
#28908=ORIENTED_EDGE ( 'NONE', *, *, #4010, .F. ) ;
#28912=VERTEX_POINT ( 'NONE', #20136 ) ;
#28915=CARTESIAN_POINT ( 'NONE',  ( 21.41354075005730095, -20.28432539553539726, -81.23899999999999011 ) ) ;
#28923=CARTESIAN_POINT ( 'NONE',  ( 22.90079931266048874, -15.61618915558698184, -42.84717230777439312 ) ) ;
#28925=CARTESIAN_POINT ( 'NONE',  ( 24.04379852435330989, -15.76128024319491772, -33.79816624355701293 ) ) ;
#28929=ORIENTED_EDGE ( 'NONE', *, *, #5353, .T. ) ;
#28934=CARTESIAN_POINT ( 'NONE',  ( 22.46011036989908760, -20.47785625781408214, -68.00066293900144387 ) ) ;
#28939=CARTESIAN_POINT ( 'NONE',  ( 9.981643928145130573, -20.48815294779980078, -74.07430842319449482 ) ) ;
#28946=AXIS2_PLACEMENT_3D ( 'NONE', #43921, #660, #8016 ) ;
#28954=CARTESIAN_POINT ( 'NONE',  ( 20.77870735952862091, -22.07375217990394489, -33.80906069049880358 ) ) ;
#28957=ORIENTED_EDGE ( 'NONE', *, *, #6557, .F. ) ;
#28959=CARTESIAN_POINT ( 'NONE',  ( 11.33709965304220013, -21.31680662961520056, -39.79000516318719605 ) ) ;
#28970=CARTESIAN_POINT ( 'NONE',  ( 9.366361720925400647, -15.59697802929608024, -59.84808272681433294 ) ) ;
#28975=EDGE_LOOP ( 'NONE', ( #23240, #41494, #14703, #9701 ) ) ;
#28979=CARTESIAN_POINT ( 'NONE',  ( 24.04493737386696139, -14.58064414827727084, -79.75066707260157273 ) ) ;
#28983=ORIENTED_EDGE ( 'NONE', *, *, #29136, .T. ) ;
#28989=CARTESIAN_POINT ( 'NONE',  ( 22.90093741420372098, -14.73039702075610968, -36.41115092250901597 ) ) ;
#28991=CARTESIAN_POINT ( 'NONE',  ( 11.97527360937055363, -10.20486319393767793, -53.74448780049490182 ) ) ;
#28998=CARTESIAN_POINT ( 'NONE',  ( 17.74647322415179929, -23.29645429165649873, -62.44661944738230375 ) ) ;
#29008=CARTESIAN_POINT ( 'NONE',  ( 23.04647701948986338, -11.63208821185457253, -41.62566436189668195 ) ) ;
#29014=FACE_OUTER_BOUND ( 'NONE', #45910, .T. ) ;
#29017=CARTESIAN_POINT ( 'NONE',  ( 21.72146850305579591, -9.937738037311971695, -55.25497476500451910 ) ) ;
#29019=CARTESIAN_POINT ( 'NONE',  ( 23.44917627852430186, -16.12890410639889893, -32.14999999999999858 ) ) ;
#29027=VERTEX_POINT ( 'NONE', #33482 ) ;
#29028=CARTESIAN_POINT ( 'NONE',  ( 10.36088797006879858, -19.66766515473189969, -63.65239730387659023 ) ) ;
#29031=AXIS2_PLACEMENT_3D ( 'NONE', #10743, #7842, #30636 ) ;
#29033=CARTESIAN_POINT ( 'NONE',  ( 17.01980114826354296, -22.38317958693441057, -42.91115323773419021 ) ) ;
#29036=CARTESIAN_POINT ( 'NONE',  ( 11.09931817734580051, -10.67704245943470021, -69.69977332415560056 ) ) ;
#29037=CARTESIAN_POINT ( 'NONE',  ( 16.13393739769620083, -15.61618894467929941, -28.45282021618999835 ) ) ;
#29047=CARTESIAN_POINT ( 'NONE',  ( 8.428889251930748117, -17.68705715933444722, -64.42433529559949079 ) ) ;
#29054=ADVANCED_FACE ( 'NONE', ( #36375 ), #4938, .T. ) ;
#29056=CARTESIAN_POINT ( 'NONE',  ( 12.14980512970851301, -22.52871163933854248, -44.17436150934778993 ) ) ;
#29057=ORIENTED_EDGE ( 'NONE', *, *, #23589, .F. ) ;
#29061=CARTESIAN_POINT ( 'NONE',  ( 14.06336471865839144, -7.911061366011778340, -56.92433474434999852 ) ) ;
#29063=CARTESIAN_POINT ( 'NONE',  ( 17.35390478220470101, -23.36850648025069788, -36.46281005851519552 ) ) ;
#29064=CARTESIAN_POINT ( 'NONE',  ( 15.07367541409510814, -22.58887879155687273, -65.39521378728271372 ) ) ;
#29067=ORIENTED_EDGE ( 'NONE', *, *, #36672, .T. ) ;
#29070=AXIS2_PLACEMENT_3D ( 'NONE', #29143, #13194, #40689 ) ;
#29072=CARTESIAN_POINT ( 'NONE',  ( 10.14762331803439821, -11.88703313963030084, -34.02451708608289493 ) ) ;
#29080=CARTESIAN_POINT ( 'NONE',  ( 23.18176326819819977, -19.89530930007790133, -79.68135863817160214 ) ) ;
#29089=CARTESIAN_POINT ( 'NONE',  ( 9.221491627360364873, -19.60045263248064629, -74.62566484353840224 ) ) ;
#29091=CARTESIAN_POINT ( 'NONE',  ( 19.70635122345840173, -21.69738725281480285, -32.78375144850900114 ) ) ;
#29097=DIRECTION ( 'NONE',  ( 0.000000000000000000, 0.000000000000000000, -1.000000000000000000 ) ) ;
#29099=CARTESIAN_POINT ( 'NONE',  ( 13.42399758170009960, -8.676237899047920976, -78.44884352223340329 ) ) ;
#29103=CARTESIAN_POINT ( 'NONE',  ( 24.03071935106534696, -15.12947789652383079, -49.77274206133255063 ) ) ;
#29119=PLANE ( 'NONE',  #10145 ) ;
#29124=CARTESIAN_POINT ( 'NONE',  ( 9.540065987903542322, -13.85895121319336809, -71.53551241591725329 ) ) ;
#29125=CARTESIAN_POINT ( 'NONE',  ( 17.16941332651105867, -7.705178615749455950, -43.33403995393874197 ) ) ;
#29126=CARTESIAN_POINT ( 'NONE',  ( 12.24090637955089989, -8.347968423279731098, -51.13580619582459974 ) ) ;
#29127=CARTESIAN_POINT ( 'NONE',  ( 22.90092786074403719, -15.60305501299737507, -56.45220756279023533 ) ) ;
#29132=CARTESIAN_POINT ( 'NONE',  ( 9.655419314464330327, -11.93712693781080070, -45.39705537816439573 ) ) ;
#29133=CARTESIAN_POINT ( 'NONE',  ( 12.20479792536879948, -10.10644435241950134, -32.14999999999999858 ) ) ;
#29136=EDGE_CURVE ( 'NONE', #17773, #17470, #20429, .T. ) ;
#29137=DIRECTION ( 'NONE',  ( 0.000000000000000000, 0.000000000000000000, -1.000000000000000000 ) ) ;
#29139=CARTESIAN_POINT ( 'NONE',  ( 20.45336392292970018, -8.592993432514999697, -57.18318221610369534 ) ) ;
#29143=CARTESIAN_POINT ( 'NONE',  ( 16.13393739769620083, -15.61618894467929941, -28.45282021618999835 ) ) ;
#29144=CARTESIAN_POINT ( 'NONE',  ( 10.72251233321565778, -19.77472457186372168, -57.24444900321750396 ) ) ;
#29153=CARTESIAN_POINT ( 'NONE',  ( 22.90121965235462653, -15.61618904849089340, -42.45282069170939110 ) ) ;
#29161=CARTESIAN_POINT ( 'NONE',  ( 8.222948829813766736, -14.58055777486210225, -76.83399804417695123 ) ) ;
#29162=CARTESIAN_POINT ( 'NONE',  ( 16.13393739769620083, -15.61618894467929941, -28.45282021618999835 ) ) ;
#29164=CYLINDRICAL_SURFACE ( 'NONE', #34667, 6.766999999999998572 ) ;
#29176=CARTESIAN_POINT ( 'NONE',  ( 22.63681060059330008, -18.70819294529809795, -81.23899999999999011 ) ) ;
#29185=CARTESIAN_POINT ( 'NONE',  ( 9.366937397696199596, -15.61618894467949836, -28.45282021618999835 ) ) ;
#29195=CARTESIAN_POINT ( 'NONE',  ( 9.725847485215973975, -18.39314784772030720, -55.71658343890410237 ) ) ;
#29197=CARTESIAN_POINT ( 'NONE',  ( 14.19552728039930045, -8.011630154036440743, -74.70805987170351159 ) ) ;
#29208=CARTESIAN_POINT ( 'NONE',  ( 22.90091122653545241, -15.61618862529044804, -78.45282272177526295 ) ) ;
#29211=CARTESIAN_POINT ( 'NONE',  ( 24.04497561966918440, -15.61618908881887080, -69.50766602643473391 ) ) ;
#29215=CARTESIAN_POINT ( 'NONE',  ( 16.13393739769620083, -15.61618894467929941, -81.23899999999999011 ) ) ;
#29217=CARTESIAN_POINT ( 'NONE',  ( 14.19299298219679883, -8.423176424581528821, -42.48344881935029349 ) ) ;
#29220=CARTESIAN_POINT ( 'NONE',  ( 20.43063756541187814, -15.61618894467929941, -22.14999999999999858 ) ) ;
#29228=EDGE_LOOP ( 'NONE', ( #27310, #14362, #1575, #25143 ) ) ;
#29229=EDGE_LOOP ( 'NONE', ( #18351, #45447, #29797, #29782 ) ) ;
#29239=CARTESIAN_POINT ( 'NONE',  ( 8.222940294821349028, -15.07895016470535943, -76.52928890672468754 ) ) ;
#29249=CARTESIAN_POINT ( 'NONE',  ( 19.11395969596977906, -21.71459350761253759, -46.80819746545874693 ) ) ;
#29254=CARTESIAN_POINT ( 'NONE',  ( 8.601692148444030295, -17.81892113373459807, -62.92193303376410540 ) ) ;
#29265=EDGE_LOOP ( 'NONE', ( #42398, #7280, #29445, #22729 ) ) ;
#29271=CARTESIAN_POINT ( 'NONE',  ( 23.31866335234750309, -17.53501162367199839, -32.14999999999999858 ) ) ;
#29282=CARTESIAN_POINT ( 'NONE',  ( 15.52768592298719952, -22.64292490982440142, -59.37457502644110008 ) ) ;
#29287=CARTESIAN_POINT ( 'NONE',  ( 15.24821661813249030, -22.38319830166902946, -42.99448661903509361 ) ) ;
#29290=CARTESIAN_POINT ( 'NONE',  ( 16.27092104377510040, -22.66769900829920203, -64.94663746033859297 ) ) ;
#29291=CARTESIAN_POINT ( 'NONE',  ( 9.183937397696297467, -15.61618894467929941, -20.75000000000000711 ) ) ;
#29299=CARTESIAN_POINT ( 'NONE',  ( 9.728155433668721486, -10.93576152856158856, -38.70851398578017921 ) ) ;
#29302=ORIENTED_EDGE ( 'NONE', *, *, #43773, .F. ) ;
#29310=ORIENTED_EDGE ( 'NONE', *, *, #25860, .F. ) ;
#29314=CARTESIAN_POINT ( 'NONE',  ( 23.83903434524771470, -13.54549697515503759, -53.70900105890960674 ) ) ;
#29316=CARTESIAN_POINT ( 'NONE',  ( 23.70552850492139996, -13.55275599941940001, -33.92780426447939846 ) ) ;
#29327=EDGE_CURVE ( 'NONE', #25231, #41523, #47414, .T. ) ;
#29330=CARTESIAN_POINT ( 'NONE',  ( 10.16236763787109965, -19.36890979467510121, -37.66858791500939674 ) ) ;
#29332=CONICAL_SURFACE ( 'NONE', #20118, 0.2705324999999987323, 1.029744258676660307 ) ;
#29350=CARTESIAN_POINT ( 'NONE',  ( 9.933815087369589847, -19.74726581762220334, -81.04557435679309663 ) ) ;
#29357=CARTESIAN_POINT ( 'NONE',  ( 9.075377375428610449, -13.23219549871780032, -74.17102124479808367 ) ) ;
#29360=CARTESIAN_POINT ( 'NONE',  ( 24.04493006531424726, -15.60506294570754982, -49.79188297642375005 ) ) ;
#29375=FACE_OUTER_BOUND ( 'NONE', #12122, .T. ) ;
#29379=CARTESIAN_POINT ( 'NONE',  ( 22.90065299155850198, -15.61618013372109637, -50.45281880338879432 ) ) ;
#29385=CARTESIAN_POINT ( 'NONE',  ( 24.22405364513110015, -14.02473075832179994, -55.73050419751459827 ) ) ;
#29392=CARTESIAN_POINT ( 'NONE',  ( 23.19678285945379770, -13.24492181749289976, -44.12955248114639772 ) ) ;
#29394=CARTESIAN_POINT ( 'NONE',  ( 23.04644940922143093, -11.63203671537942974, -33.34099856603324952 ) ) ;
#29397=CARTESIAN_POINT ( 'NONE',  ( 16.13393739769620083, -15.61618894467929941, -32.14999999999999858 ) ) ;
#29401=VECTOR ( 'NONE', #15652, 1000.000000000000000 ) ;
#29402=CARTESIAN_POINT ( 'NONE',  ( 24.37674430018200056, -15.41907203188980091, -57.50005794035820372 ) ) ;
#29409=ORIENTED_EDGE ( 'NONE', *, *, #46100, .T. ) ;
#29415=CARTESIAN_POINT ( 'NONE',  ( 16.13393739769620083, -15.61618894467929941, -81.23899999999999011 ) ) ;
#29422=CARTESIAN_POINT ( 'NONE',  ( 14.36273799164256815, -9.025303278630660841, -47.86948771557721471 ) ) ;
#29430=EDGE_LOOP ( 'NONE', ( #16038, #379, #43319, #33867 ) ) ;
#29437=CARTESIAN_POINT ( 'NONE',  ( 24.04493712615994028, -15.61869300327582977, -77.50777460550092712 ) ) ;
#29439=CARTESIAN_POINT ( 'NONE',  ( 16.13393739769620083, -15.61618894467929941, -32.14999999999999858 ) ) ;
#29442=ORIENTED_EDGE ( 'NONE', *, *, #17154, .F. ) ;
#29445=ORIENTED_EDGE ( 'NONE', *, *, #38949, .F. ) ;
#29447=CARTESIAN_POINT ( 'NONE',  ( 9.582536624350547427, -20.09909968766171318, -34.60122671728029786 ) ) ;
#29448=CARTESIAN_POINT ( 'NONE',  ( 9.367479025678566273, -16.58895892350905399, -49.80140833476744433 ) ) ;
#29460=CARTESIAN_POINT ( 'NONE',  ( 10.79995697763059859, -9.859853212502130759, -74.54962200957619700 ) ) ;
#29463=DIRECTION ( 'NONE',  ( 0.000000000000000000, 0.000000000000000000, 1.000000000000000000 ) ) ;
#29473=CARTESIAN_POINT ( 'NONE',  ( 24.04466642925503095, -15.61618863334376250, -55.79233649161735542 ) ) ;
#29478=CARTESIAN_POINT ( 'NONE',  ( 16.94034526300609755, -23.02269964089170173, -41.53282164658679676 ) ) ;
#29479=B_SPLINE_CURVE_WITH_KNOTS ( 'NONE', 3,
 ( #51677, #16282, #23606, #11595, #24375, #36443, #19443, #31725, #43562, #27300, #48259, #31986, #35936, #56, #40390, #35426, #23861, #47497 ),
 .UNSPECIFIED., .F., .F.,
 ( 4, 2, 2, 2, 2, 2, 2, 2, 4 ),
 ( 0.5000015677398489400, 0.5625013717723678086, 0.6250011758048866772, 0.6875009798374056569, 0.7500007838699245255, 0.8125005879024433941, 0.8750003919349622628, 0.9375001959674811314, 1.000000000000000000 ),
 .UNSPECIFIED. ) ;
#29487=CARTESIAN_POINT ( 'NONE',  ( 9.840592242581751137, -12.50199903054207695, -53.99366435805588083 ) ) ;
#29493=ORIENTED_EDGE ( 'NONE', *, *, #4832, .T. ) ;
#29494=EDGE_LOOP ( 'NONE', ( #46879, #37224, #12645, #32020, #34025, #30831 ) ) ;
#29495=FACE_OUTER_BOUND ( 'NONE', #22413, .T. ) ;
#29503=CARTESIAN_POINT ( 'NONE',  ( 22.90093739799785766, -15.62120111656948218, -72.45306145236200734 ) ) ;
#29507=EDGE_LOOP ( 'NONE', ( #51357, #33973, #27625, #40522 ) ) ;
#29508=CARTESIAN_POINT ( 'NONE',  ( 16.13393739769620083, -15.61618894467929941, -23.74958330439410048 ) ) ;
#29512=CARTESIAN_POINT ( 'NONE',  ( 9.337061569587699950, -11.69327847299420142, -61.17911655036439811 ) ) ;
#29518=CARTESIAN_POINT ( 'NONE',  ( 28.13393739769620439, -12.40079863550581862, -22.14999999999998792 ) ) ;
#29529=DIRECTION ( 'NONE',  ( 0.000000000000000000, 0.000000000000000000, -1.000000000000000000 ) ) ;
#29530=CARTESIAN_POINT ( 'NONE',  ( 23.35725391028839937, -17.30451495249259963, -32.14999999999999858 ) ) ;
#29533=CARTESIAN_POINT ( 'NONE',  ( 10.75327222894697776, -9.738703401990544961, -44.77156291098159357 ) ) ;
#29534=CARTESIAN_POINT ( 'NONE',  ( 8.222924357332910716, -16.65164095223361684, -46.75067280918717216 ) ) ;
#29536=ORIENTED_EDGE ( 'NONE', *, *, #20164, .T. ) ;
#29538=CARTESIAN_POINT ( 'NONE',  ( 12.34706755911540021, -9.666216171624100184, -60.16676433707719696 ) ) ;
#29539=AXIS2_PLACEMENT_3D ( 'NONE', #41515, #40740, #44936 ) ;
#29546=CARTESIAN_POINT ( 'NONE',  ( 9.084739283574659652, -15.84282663900890142, -71.44258980755509469 ) ) ;
#29547=DIRECTION ( 'NONE',  ( 0.000000000000000000, 0.000000000000000000, -1.000000000000000000 ) ) ;
#29555=CARTESIAN_POINT ( 'NONE',  ( 16.63095995406284899, -7.653195049244535753, -39.02733329801645823 ) ) ;
#29572=CARTESIAN_POINT ( 'NONE',  ( 20.50561976785459706, -9.485587557738790920, -31.70967419469809201 ) ) ;
#29575=ADVANCED_FACE ( 'NONE', ( #42920 ), #22968, .T. ) ;
#29579=CARTESIAN_POINT ( 'NONE',  ( 22.90091122653545241, -15.61618862529044804, -78.45282272177526295 ) ) ;
#29583=CARTESIAN_POINT ( 'NONE',  ( 15.14368416393440064, -8.633212666080371633, -38.30233936351839219 ) ) ;
#29596=CARTESIAN_POINT ( 'NONE',  ( 9.133937397696200833, -15.61618894467929941, -82.15000000000000568 ) ) ;
#29600=ORIENTED_EDGE ( 'NONE', *, *, #41852, .F. ) ;
#29605=CARTESIAN_POINT ( 'NONE',  ( 9.378617007155710894, -17.64305971455430111, -47.36003476421489466 ) ) ;
#29612=CARTESIAN_POINT ( 'NONE',  ( 8.793629121247519720, -16.89155898707499759, -74.01258338267071224 ) ) ;
#29615=CARTESIAN_POINT ( 'NONE',  ( 8.871876924530811337, -12.37411265878318289, -48.92611659854718198 ) ) ;
#29620=CARTESIAN_POINT ( 'NONE',  ( 23.98099588838510599, -16.65306419375328417, -75.83413829860595001 ) ) ;
#29621=CARTESIAN_POINT ( 'NONE',  ( 20.99562822605996004, -9.290033917162169530, -45.50063643852418238 ) ) ;
#29629=CARTESIAN_POINT ( 'NONE',  ( 8.222937397696199469, -15.61618894467929941, -32.14999999999999858 ) ) ;
#29631=CARTESIAN_POINT ( 'NONE',  ( 9.366438350291463877, -15.74334315553391939, -53.84120313986934292 ) ) ;
#29636=CARTESIAN_POINT ( 'NONE',  ( 23.40487804057610077, -19.50413727556700039, -57.94863426729589406 ) ) ;
#29643=CARTESIAN_POINT ( 'NONE',  ( 9.253865619591300273, -12.75763928912490108, -49.35800193134529934 ) ) ;
#29644=CARTESIAN_POINT ( 'NONE',  ( 8.864140624387911060, -15.38326400578280051, -32.14999999999999858 ) ) ;
#29650=CARTESIAN_POINT ( 'NONE',  ( 24.03277050005166515, -15.16864035720454140, -61.48966201727984071 ) ) ;
#29652=CARTESIAN_POINT ( 'NONE',  ( 14.42519478801719934, -23.68234784485250088, -56.07411718121299771 ) ) ;
#29658=CARTESIAN_POINT ( 'NONE',  ( 9.543024404835053431, -17.38729190938108360, -57.36946905751702275 ) ) ;
#29670=CARTESIAN_POINT ( 'NONE',  ( 22.90085138535262743, -15.65142864927533317, -66.45447747818334960 ) ) ;
#29678=CARTESIAN_POINT ( 'NONE',  ( 16.13393739769620083, -15.61618894467929941, -28.45282021618999835 ) ) ;
#29682=CARTESIAN_POINT ( 'NONE',  ( 22.21314585784342199, -19.19191036455051247, -47.01642178051652365 ) ) ;
#29690=CARTESIAN_POINT ( 'NONE',  ( 22.90075166721855737, -15.61618922411645727, -44.45281379938008115 ) ) ;
#29694=VERTEX_POINT ( 'NONE', #21268 ) ;
#29696=CARTESIAN_POINT ( 'NONE',  ( 14.57822604302202585, -23.39323822619865823, -34.35516676250910706 ) ) ;
#29698=CARTESIAN_POINT ( 'NONE',  ( 22.90088880405416205, -15.64389692910371821, -50.45412216600715993 ) ) ;
#29711=CARTESIAN_POINT ( 'NONE',  ( 8.402054737090029590, -16.95959458178240098, -74.23274628532179520 ) ) ;
#29721=CARTESIAN_POINT ( 'NONE',  ( 11.27217872414320077, -9.290084753452736877, -42.79930174472833926 ) ) ;
#29722=CARTESIAN_POINT ( 'NONE',  ( 8.223295469878840080, -15.61636541503349918, -58.79233150823709764 ) ) ;
#29728=CARTESIAN_POINT ( 'NONE',  ( 9.178575242519139366, -18.28632595027880114, -55.95066710016559597 ) ) ;
#29733=CARTESIAN_POINT ( 'NONE',  ( 9.669467020143732938, -13.02337471114221756, -73.96911144341058275 ) ) ;
#29734=CARTESIAN_POINT ( 'NONE',  ( 21.72939861980660581, -21.20857138557213872, -61.75757471702103629 ) ) ;
#29740=EDGE_CURVE ( 'NONE', #4643, #42078, #40495, .T. ) ;
#29748=ORIENTED_EDGE ( 'NONE', *, *, #3600, .T. ) ;
#29757=CARTESIAN_POINT ( 'NONE',  ( 13.35425103422070059, -8.277245470834399654, -63.39724662014580048 ) ) ;
#29782=ORIENTED_EDGE ( 'NONE', *, *, #10177, .T. ) ;
#29783=CARTESIAN_POINT ( 'NONE',  ( 22.27312146484720046, -12.14444901143390076, -72.68335544512909507 ) ) ;
#29787=CARTESIAN_POINT ( 'NONE',  ( 22.04686114124215379, -19.02415750966752483, -42.61948640318105674 ) ) ;
#29790=CARTESIAN_POINT ( 'NONE',  ( 10.53269849474080111, -11.33031896897490043, -73.66071987733648996 ) ) ;
#29791=FACE_OUTER_BOUND ( 'NONE', #43676, .T. ) ;
#29797=ORIENTED_EDGE ( 'NONE', *, *, #21269, .F. ) ;
#29798=ADVANCED_FACE ( 'NONE', ( #10011 ), #1890, .T. ) ;
#29802=CARTESIAN_POINT ( 'NONE',  ( 24.04454178464035152, -15.53069869766736311, -39.50423254393393080 ) ) ;
#29803=CARTESIAN_POINT ( 'NONE',  ( 9.366455112259469473, -15.61627688590920116, -55.45282021618999835 ) ) ;
#29819=CARTESIAN_POINT ( 'NONE',  ( 9.366937397696199596, -15.61618894467949836, -28.45282021618999835 ) ) ;
#29820=CARTESIAN_POINT ( 'NONE',  ( 8.309212758712860136, -15.01582912232649925, -35.03686929937009609 ) ) ;
#29827=DIRECTION ( 'NONE',  ( 1.000000000000000000, 0.000000000000000000, 0.000000000000000000 ) ) ;
#29831=CARTESIAN_POINT ( 'NONE',  ( 20.49757756391890240, -10.07532225487519817, -36.55952288011869911 ) ) ;
#29851=CARTESIAN_POINT ( 'NONE',  ( 24.04493739809674580, -15.62506615101500529, -65.79268861494041687 ) ) ;
#29854=CARTESIAN_POINT ( 'NONE',  ( 15.71925719199229832, -8.575549838488520038, -45.93409400506989471 ) ) ;
#29861=CARTESIAN_POINT ( 'NONE',  ( 14.53903968535739999, -22.89375691932010071, -71.63601545076220134 ) ) ;
#29864=CARTESIAN_POINT ( 'NONE',  ( 13.50570672964423125, -8.124416908735485165, -81.18499873804080380 ) ) ;
#29869=CARTESIAN_POINT ( 'NONE',  ( 18.20464558802392219, -7.911096944365791472, -45.37562956944282888 ) ) ;
#29870=CARTESIAN_POINT ( 'NONE',  ( 14.36278247063658320, -9.025291760554305043, -57.86948676491621057 ) ) ;
#29873=ORIENTED_EDGE ( 'NONE', *, *, #40742, .T. ) ;
#29875=CARTESIAN_POINT ( 'NONE',  ( 20.71801037028389914, -10.57375650054692073, -32.18785271271227799 ) ) ;
#29879=CARTESIAN_POINT ( 'NONE',  ( 22.13942092184361954, -12.44121325561192570, -50.29796736139999069 ) ) ;
#29881=ORIENTED_EDGE ( 'NONE', *, *, #18450, .F. ) ;
#29882=CARTESIAN_POINT ( 'NONE',  ( 24.04493739769619864, -15.61618894467929941, -32.14999999999999858 ) ) ;
#29885=CARTESIAN_POINT ( 'NONE',  ( 22.90033352662897670, -15.51853657338904391, -72.44823326450749335 ) ) ;
#29887=CARTESIAN_POINT ( 'NONE',  ( 22.46008563728267049, -10.75448725963247476, -43.58402342215438097 ) ) ;
#29888=CARTESIAN_POINT ( 'NONE',  ( 24.10393840806110077, -13.50389068195270070, -49.70986543667950031 ) ) ;
#29893=CARTESIAN_POINT ( 'NONE',  ( 13.18813369118609913, -22.45935592553379934, -42.86204958412849919 ) ) ;
#29895=CARTESIAN_POINT ( 'NONE',  ( 9.114425618932170181, -18.21946245242060058, -32.14999999999999858 ) ) ;
#29902=DIRECTION ( 'NONE',  ( 0.000000000000000000, 0.000000000000000000, -1.000000000000000000 ) ) ;
#29904=CARTESIAN_POINT ( 'NONE',  ( 7.949225475402950103, -16.61278889352830035, -48.46909979910559230 ) ) ;
#29910=CARTESIAN_POINT ( 'NONE',  ( 9.366916053341348913, -16.50183103721897737, -57.41114402924350202 ) ) ;
#29926=EDGE_CURVE ( 'NONE', #3031, #36842, #4857, .T. ) ;
#29938=ORIENTED_EDGE ( 'NONE', *, *, #39124, .T. ) ;
#29946=CARTESIAN_POINT ( 'NONE',  ( 17.01971542465727438, -22.38319182777647143, -44.91117421213777305 ) ) ;
#29947=CARTESIAN_POINT ( 'NONE',  ( 24.04521450903870061, -15.61618868716203501, -63.50766715510244609 ) ) ;
#29948=CYLINDRICAL_SURFACE ( 'NONE', #11727, 7.910999999999997812 ) ;
#29950=EDGE_CURVE ( 'NONE', #12868, #48498, #26419, .T. ) ;
#29954=CARTESIAN_POINT ( 'NONE',  ( 8.222623404330700936, -15.61601543569009820, -34.79233150823699816 ) ) ;
#29968=CARTESIAN_POINT ( 'NONE',  ( 23.90530189779430259, -14.52410745055090047, -77.24306566573919497 ) ) ;
#29976=CARTESIAN_POINT ( 'NONE',  ( 18.20456863547079962, -7.911075193718300369, -43.09096072954493906 ) ) ;
#29981=CARTESIAN_POINT ( 'NONE',  ( 22.90093474979461519, -15.62310337989116249, -62.45315357117970478 ) ) ;
#29985=CARTESIAN_POINT ( 'NONE',  ( 9.798314152055999315, -19.53621093793969976, -53.89097489251149398 ) ) ;
#29990=CARTESIAN_POINT ( 'NONE',  ( 9.366376358913971245, -15.61615244833809868, -75.84717978381000592 ) ) ;
#29996=CARTESIAN_POINT ( 'NONE',  ( 9.231727895759359370, -16.96735512897419795, -81.23899999999999011 ) ) ;
#29997=CARTESIAN_POINT ( 'NONE',  ( 22.90111010729205177, -15.61618905465553553, -68.45282213299155671 ) ) ;
#30008=CARTESIAN_POINT ( 'NONE',  ( 12.72585596997502577, -21.52904951597577465, -73.11944019431979314 ) ) ;
#30016=CARTESIAN_POINT ( 'NONE',  ( 9.121612794133520552, -12.09283099439219988, -71.16070186438049916 ) ) ;
#30022=ADVANCED_FACE ( 'NONE', ( #43717 ), #42953, .T. ) ;
#30025=CARTESIAN_POINT ( 'NONE',  ( 16.13393739769620083, -15.61618894467929941, -28.45282021618999835 ) ) ;
#30035=CARTESIAN_POINT ( 'NONE',  ( 9.205734167420699166, -27.61618894467930119, -32.14999999999999858 ) ) ;
#30038=CARTESIAN_POINT ( 'NONE',  ( 15.23033464293179584, -7.689033395369536450, -44.97182431223551191 ) ) ;
#30042=CARTESIAN_POINT ( 'NONE',  ( 12.59310188071810011, -21.71578262099550116, -69.51459820258429545 ) ) ;
#30046=CARTESIAN_POINT ( 'NONE',  ( 22.46011261673628923, -10.75452470914569680, -77.58399569109577953 ) ) ;
#30049=CARTESIAN_POINT ( 'NONE',  ( 14.50967856369199893, -8.752928645318320378, -75.87884994711791364 ) ) ;
#30051=CARTESIAN_POINT ( 'NONE',  ( 24.04460909154476056, -15.61619055174803172, -33.79232989763376338 ) ) ;
#30052=CARTESIAN_POINT ( 'NONE',  ( 22.04683993050034374, -19.02419775999589646, -40.61945535750037095 ) ) ;
#30053=ORIENTED_EDGE ( 'NONE', *, *, #6557, .T. ) ;
#30060=CARTESIAN_POINT ( 'NONE',  ( 22.04685682393931145, -19.02416559795394946, -54.61948950468019603 ) ) ;
#30065=VECTOR ( 'NONE', #8221, 1000.000000000000000 ) ;
#30069=EDGE_CURVE ( 'NONE', #40977, #33168, #51740, .T. ) ;
#30079=CARTESIAN_POINT ( 'NONE',  ( 8.222963495597628736, -16.65192748015167723, -48.75066492484217662 ) ) ;
#30083=CARTESIAN_POINT ( 'NONE',  ( 10.97867031235510105, -21.53311119111619831, -40.74063233595069988 ) ) ;
#30089=CARTESIAN_POINT ( 'NONE',  ( 9.367214120893741836, -15.15805200183645951, -77.86872148764932433 ) ) ;
#30091=CARTESIAN_POINT ( 'NONE',  ( 16.46289132105319908, -8.571024043077699162, -40.36203157117240181 ) ) ;
#30092=CARTESIAN_POINT ( 'NONE',  ( 19.02084999298380197, -9.181261218463509621, -44.48141598648069106 ) ) ;
#30120=CARTESIAN_POINT ( 'NONE',  ( 11.50083822998139915, -20.93379656453479853, -41.18095814125259579 ) ) ;
#30127=CARTESIAN_POINT ( 'NONE',  ( 23.35600429417859658, -18.68677486991650483, -35.41547006414829468 ) ) ;
#30133=CARTESIAN_POINT ( 'NONE',  ( 22.90105422030644533, -15.61618894250064571, -66.84718200393152188 ) ) ;
#30134=CARTESIAN_POINT ( 'NONE',  ( 17.16950835854344248, -7.705192299006624168, -45.33396173990814049 ) ) ;
#30137=VERTEX_POINT ( 'NONE', #51328 ) ;
#30144=CARTESIAN_POINT ( 'NONE',  ( 23.04647144370960632, -19.60030011359189928, -69.67433775227239323 ) ) ;
#30153=CARTESIAN_POINT ( 'NONE',  ( 23.94343616722941093, -14.32674203509526301, -43.74025135623552529 ) ) ;
#30156=CARTESIAN_POINT ( 'NONE',  ( 9.959172811698669747, -21.08016207450399904, -52.56174695496979865 ) ) ;
#30157=CARTESIAN_POINT ( 'NONE',  ( 9.807872731394935428, -20.47799600457528513, -48.29933544732911344 ) ) ;
#30160=VERTEX_POINT ( 'NONE', #11759 ) ;
#30163=CARTESIAN_POINT ( 'NONE',  ( 11.08775496079699963, -10.13506345636259987, -43.49580103263740227 ) ) ;
#30164=CARTESIAN_POINT ( 'NONE',  ( 10.53549630783540181, -11.50741195615269952, -32.14999999999999858 ) ) ;
#30169=CARTESIAN_POINT ( 'NONE',  ( 12.14991428949967123, -8.703604497957496022, -51.12566398032977588 ) ) ;
#30171=CARTESIAN_POINT ( 'NONE',  ( 24.04491700689571942, -15.59675040521408818, -61.50689416717609959 ) ) ;
#30172=CARTESIAN_POINT ( 'NONE',  ( 10.38625880047930039, -21.52778022385869860, -62.25319380417529658 ) ) ;
#30186=FACE_OUTER_BOUND ( 'NONE', #29265, .T. ) ;
#30191=CARTESIAN_POINT ( 'NONE',  ( 16.39527617993162423, -15.42631520516813204, -24.90346750000000142 ) ) ;
#30200=CARTESIAN_POINT ( 'NONE',  ( 10.60479889110639995, -19.99468030008900143, -73.63398261789269839 ) ) ;
#30206=ORIENTED_EDGE ( 'NONE', *, *, #40869, .F. ) ;
#30213=CARTESIAN_POINT ( 'NONE',  ( 17.90516752299720338, -22.20706707859404005, -44.86950677487307360 ) ) ;
#30218=VERTEX_POINT ( 'NONE', #36346 ) ;
#30223=CARTESIAN_POINT ( 'NONE',  ( 16.89924507312233715, -22.34215272261101859, -46.91676882640332735 ) ) ;
#30234=CARTESIAN_POINT ( 'NONE',  ( 19.04480908643419923, -23.33043247825739996, -33.89281648339959929 ) ) ;
#30242=CARTESIAN_POINT ( 'NONE',  ( 9.807704576006088359, -10.75459764923981965, -42.71597528472769056 ) ) ;
#30245=CARTESIAN_POINT ( 'NONE',  ( 15.24810741696761518, -22.38318510825263274, -78.99448544486300250 ) ) ;
#30247=CARTESIAN_POINT ( 'NONE',  ( 22.90090026390140565, -15.64040415753374269, -62.45396734492114632 ) ) ;
#30252=CARTESIAN_POINT ( 'NONE',  ( 8.904080688170550317, -17.41504032766459886, -51.98972054698469947 ) ) ;
#30256=AXIS2_PLACEMENT_3D ( 'NONE', #12708, #40216, #7989 ) ;
#30258=CARTESIAN_POINT ( 'NONE',  ( 20.92027185089429864, -10.43607681494890116, -74.58460979065598906 ) ) ;
#30260=CARTESIAN_POINT ( 'NONE',  ( 22.04686229628420335, -12.20822253710021954, -74.28615355936335618 ) ) ;
#30270=EDGE_CURVE ( 'NONE', #31804, #7417, #16255, .T. ) ;
#30274=CARTESIAN_POINT ( 'NONE',  ( 24.04455721578320038, -15.53241555943019669, -77.50430590993917690 ) ) ;
#30275=CARTESIAN_POINT ( 'NONE',  ( 22.72481123428762118, -17.38743319054560743, -52.53615118110773352 ) ) ;
#30278=CARTESIAN_POINT ( 'NONE',  ( 19.74986264806196701, -22.71836713299729027, -49.85790434740009403 ) ) ;
#30282=CARTESIAN_POINT ( 'NONE',  ( 23.43694177994569827, -12.74340726407310065, -69.89319896736259352 ) ) ;
#30285=ADVANCED_FACE ( 'NONE', ( #32924 ), #13055, .T. ) ;
#30289=AXIS2_PLACEMENT_3D ( 'NONE', #20329, #24243, #36318 ) ;
#30303=CARTESIAN_POINT ( 'NONE',  ( 22.90132873572047600, -15.41596929237549674, -50.83776837827166872 ) ) ;
#30305=CARTESIAN_POINT ( 'NONE',  ( 20.11803839206749345, -22.52873026110887267, -46.12571104359029306 ) ) ;
#30308=CARTESIAN_POINT ( 'NONE',  ( 15.47860435268529855, -22.63851745982070085, -75.37679910129230620 ) ) ;
#30316=CARTESIAN_POINT ( 'NONE',  ( 23.13400276341360140, -14.75500164161349836, -78.41385574115379598 ) ) ;
#30317=CARTESIAN_POINT ( 'NONE',  ( 22.46011903968922141, -20.47784435745758458, -41.71600081988199804 ) ) ;
#30318=CARTESIAN_POINT ( 'NONE',  ( 15.24805187626227543, -22.38317847404922034, -40.99442667353930858 ) ) ;
#30324=CARTESIAN_POINT ( 'NONE',  ( 9.366937397696199596, -15.61618894467949836, -28.45282021618999835 ) ) ;
#30330=EDGE_CURVE ( 'NONE', #20584, #31550, #2009, .T. ) ;
#30339=CARTESIAN_POINT ( 'NONE',  ( 16.80019542733428750, -7.709322181342847635, -33.31905990858218303 ) ) ;
#30344=CARTESIAN_POINT ( 'NONE',  ( 8.287590648356600198, -15.46925262952789915, -45.01845461338609766 ) ) ;
#30349=CARTESIAN_POINT ( 'NONE',  ( 9.525402744584583914, -13.57718879627017117, -77.94307581219771919 ) ) ;
#30350=CARTESIAN_POINT ( 'NONE',  ( 9.206757876277350761, -14.29076710523099969, -45.90735674562569812 ) ) ;
#30363=EDGE_CURVE ( 'NONE', #36315, #367, #10056, .T. ) ;
#30365=DIRECTION ( 'NONE',  ( 1.000000000000000000, 2.460964292799963328E-14, 0.000000000000000000 ) ) ;
#30367=CARTESIAN_POINT ( 'NONE',  ( 23.84888678603816814, -13.80674682629403804, -71.43433972173403390 ) ) ;
#30377=CARTESIAN_POINT ( 'NONE',  ( 16.32018716749529830, -22.66656976559070102, -48.94441338548719500 ) ) ;
#30384=B_SPLINE_CURVE_WITH_KNOTS ( 'NONE', 3,
 ( #36864, #963, #16960, #44990, #32908, #28991, #13038, #5681, #17720, #38158, #49706, #2511, #18231, #46295, #34196, #5421, #33943, #33689 ),
 .UNSPECIFIED., .F., .F.,
 ( 4, 2, 2, 2, 2, 2, 2, 2, 4 ),
 ( 0.000000000000000000, 0.06250019663676391335, 0.1250003932735278267, 0.1875005899102917262, 0.2500007865470556534, 0.3125009831838195806, 0.3750011798205834523, 0.4375013764573473796, 0.5000015730941113068 ),
 .UNSPECIFIED. ) ;
#30385=CARTESIAN_POINT ( 'NONE',  ( 23.34384601745220067, -12.51716234299430042, -37.15828654754790250 ) ) ;
#30392=CARTESIAN_POINT ( 'NONE',  ( 20.97958295125081563, -21.95497548660398479, -76.08475998165809528 ) ) ;
#30393=CARTESIAN_POINT ( 'NONE',  ( 20.11808194642809866, -8.703673674707349761, -45.45896691875083206 ) ) ;
#30394=CARTESIAN_POINT ( 'NONE',  ( 9.543104245580357414, -13.84479575616211733, -57.53615352593524079 ) ) ;
#30401=CARTESIAN_POINT ( 'NONE',  ( 22.75768029318954788, -17.21802539889342754, -32.52852712712287797 ) ) ;
#30411=CARTESIAN_POINT ( 'NONE',  ( 11.47147311421140081, -22.41649385410530115, -60.48364006133179771 ) ) ;
#30414=ORIENTED_EDGE ( 'NONE', *, *, #271, .T. ) ;
#30416=CARTESIAN_POINT ( 'NONE',  ( 8.780985052446480310, -16.81651623905879589, -59.18114938323400054 ) ) ;
#30418=CARTESIAN_POINT ( 'NONE',  ( 9.574329378931039969, -12.95124520122079836, -32.14999999999999858 ) ) ;
#30425=CARTESIAN_POINT ( 'NONE',  ( 24.08194699500409897, -13.42259277626600067, -65.42195104672009620 ) ) ;
#30440=CARTESIAN_POINT ( 'NONE',  ( 15.08138911710155128, -7.754377985150386898, -65.24995822591438355 ) ) ;
#30469=CARTESIAN_POINT ( 'NONE',  ( 22.90093737940656027, -16.50198913682855562, -44.49448475077488041 ) ) ;
#30472=DIRECTION ( 'NONE',  ( 1.000000000000000000, 0.000000000000000000, 0.000000000000000000 ) ) ;
#30480=CARTESIAN_POINT ( 'NONE',  ( 22.89358800639388036, -15.93836948567792255, -50.46797458509442436 ) ) ;
#30482=DIRECTION ( 'NONE',  ( 0.000000000000000000, 0.000000000000000000, -1.000000000000000000 ) ) ;
#30489=CARTESIAN_POINT ( 'NONE',  ( 23.97265246126819704, -15.99208020242580019, -79.30275787339340354 ) ) ;
#30491=CARTESIAN_POINT ( 'NONE',  ( 9.367838033491670657, -14.76692425612211146, -47.88713617363420383 ) ) ;
#30512=CARTESIAN_POINT ( 'NONE',  ( 21.15163403916380247, -10.10897415383030129, -58.80254861845600090 ) ) ;
#30516=DIRECTION ( 'NONE',  ( 0.000000000000000000, 0.000000000000000000, -1.000000000000000000 ) ) ;
#30517=CARTESIAN_POINT ( 'NONE',  ( 22.90076005816202809, -15.61619656631699193, -74.84717351858182610 ) ) ;
#30518=CARTESIAN_POINT ( 'NONE',  ( 23.06214062797170072, -3.616188944679339823, -32.14999999999999858 ) ) ;
#30519=CARTESIAN_POINT ( 'NONE',  ( 9.115821549383319677, -16.48115037890739742, -81.23899999999999011 ) ) ;
#30532=LINE ( 'NONE', #26868, #45240 ) ;
#30537=DIRECTION ( 'NONE',  ( 0.000000000000000000, 0.000000000000000000, -1.000000000000000000 ) ) ;
#30540=DIRECTION ( 'NONE',  ( -1.000000000000000000, 0.000000000000000000, 0.000000000000000000 ) ) ;
#30546=CARTESIAN_POINT ( 'NONE',  ( 23.94340337760679915, -16.39013292960409984, -53.31894848452630242 ) ) ;
#30549=ADVANCED_FACE ( 'NONE', ( #27141 ), #14652, .F. ) ;
#30561=CARTESIAN_POINT ( 'NONE',  ( 22.99224927569089871, -17.26127340059479920, -80.92212427574548883 ) ) ;
#30565=EDGE_LOOP ( 'NONE', ( #49410, #50210, #7896, #23044, #31039 ) ) ;
#30566=CARTESIAN_POINT ( 'NONE',  ( 10.45980683277509904, -11.42729869705060075, -72.04960399662019199 ) ) ;
#30573=CARTESIAN_POINT ( 'NONE',  ( 15.36183068599440027, -8.605738893336619455, -71.91790339393689635 ) ) ;
#30576=CARTESIAN_POINT ( 'NONE',  ( 9.367118387258660306, -15.61602127472129986, -41.45282021618999835 ) ) ;
#30580=B_SPLINE_CURVE_WITH_KNOTS ( 'NONE', 3,
 ( #6493, #10946, #19312, #43174, #27165, #18790, #46597, #7015, #2297, #38457, #26639, #7267, #34768, #10427, #18535, #35293, #26910, #26379 ),
 .UNSPECIFIED., .F., .F.,
 ( 4, 2, 2, 2, 2, 2, 2, 2, 4 ),
 ( 0.5000012016224835154, 0.5625010514196729927, 0.6250009012168624700, 0.6875007510140520584, 0.7500006008112415357, 0.8125004506084312350, 0.8750003004056208233, 0.9375001502028104117, 1.000000000000000000 ),
 .UNSPECIFIED. ) ;
#30586=CARTESIAN_POINT ( 'NONE',  ( 22.40179979670677568, -12.43270815927585815, -62.69742595855866085 ) ) ;
#30597=CARTESIAN_POINT ( 'NONE',  ( 24.03684650753359975, -15.24774525578274087, -33.77750442297574551 ) ) ;
#30598=CARTESIAN_POINT ( 'NONE',  ( 14.06336364397819771, -23.32131624563684014, -48.37566567428872588 ) ) ;
#30604=CARTESIAN_POINT ( 'NONE',  ( 8.364553939350129141, -14.51010202731669985, -41.05750806020520116 ) ) ;
#30611=CARTESIAN_POINT ( 'NONE',  ( 22.77319179948189998, -17.99586542748549789, -44.95672957286230087 ) ) ;
#30613=ORIENTED_EDGE ( 'NONE', *, *, #20421, .T. ) ;
#30622=EDGE_CURVE ( 'NONE', #667, #38732, #50051, .T. ) ;
#30627=CARTESIAN_POINT ( 'NONE',  ( 15.90957661418855551, -7.640854637591640852, -70.99854306824902039 ) ) ;
#30629=ORIENTED_EDGE ( 'NONE', *, *, #31953, .T. ) ;
#30634=CARTESIAN_POINT ( 'NONE',  ( 9.367002091613079173, -15.61601527432330094, -39.84717978380999881 ) ) ;
#30636=DIRECTION ( 'NONE',  ( 1.000000000000000000, 0.000000000000000000, 0.000000000000000000 ) ) ;
#30637=CARTESIAN_POINT ( 'NONE',  ( 20.05198078271940076, -21.48061515102730112, -42.76533676252499561 ) ) ;
#30643=CARTESIAN_POINT ( 'NONE',  ( 9.472942927203090946, -11.46674308091629868, -34.46484289138480506 ) ) ;
#30645=FACE_OUTER_BOUND ( 'NONE', #3856, .T. ) ;
#30651=CARTESIAN_POINT ( 'NONE',  ( 24.04478666521990959, -15.61618936535764668, -45.50767606031119783 ) ) ;
#30657=CARTESIAN_POINT ( 'NONE',  ( 22.46011406273482081, -10.75452670129970123, -47.58399975706858953 ) ) ;
#30666=DIRECTION ( 'NONE',  ( 0.8090169943749457859, 0.5877852522924753575, 0.000000000000000000 ) ) ;
#30668=EDGE_CURVE ( 'NONE', #39880, #3031, #27478, .T. ) ;
#30669=CARTESIAN_POINT ( 'NONE',  ( 21.01437418586129979, -8.970584622071779535, -63.49395944174919748 ) ) ;
#30671=CARTESIAN_POINT ( 'NONE',  ( 18.20470709615282701, -23.32126356507290410, -47.92433596734809953 ) ) ;
#30673=ORIENTED_EDGE ( 'NONE', *, *, #25529, .F. ) ;
#30676=CARTESIAN_POINT ( 'NONE',  ( 21.55045383549850158, -10.50071795129430008, -49.99175337985419532 ) ) ;
#30678=CARTESIAN_POINT ( 'NONE',  ( 9.627072997565139900, -12.84800818159280134, -32.14999999999999858 ) ) ;
#30680=CARTESIAN_POINT ( 'NONE',  ( 9.536969139191834088, -14.04286193784190928, -61.52738334231096928 ) ) ;
#30682=B_SPLINE_CURVE_WITH_KNOTS ( 'NONE', 3,
 ( #9573, #9830, #49673, #13762, #30242, #29721, #37870, #41274, #1964, #46263, #29976, #5384, #45998, #10087, #41016, #17179, #26046, #42057 ),
 .UNSPECIFIED., .F., .F.,
 ( 4, 2, 2, 2, 2, 2, 2, 2, 4 ),
 ( 0.000000000000000000, 0.06249952351881701840, 0.1249990470376340368, 0.1874985705564510552, 0.2499980940752680736, 0.3124976175940852308, 0.3749971411129023324, 0.4374966646317194896, 0.4999961881505365913 ),
 .UNSPECIFIED. ) ;
#30683=B_SPLINE_CURVE_WITH_KNOTS ( 'NONE', 3,
 ( #45162, #34385, #22330, #14228, #49629, #41746, #30200, #37551, #9533, #2425 ),
 .UNSPECIFIED., .F., .F.,
 ( 4, 1, 1, 1, 1, 1, 1, 4 ),
 ( 0.5000009373669883628, 0.5765256927868320780, 0.6557446238503832348, 0.7349635549139298396, 0.8141824859776393142, 0.8934014170411903599, 0.9726203481048998345, 1.000000000000000000 ),
 .UNSPECIFIED. ) ;
#30688=CARTESIAN_POINT ( 'NONE',  ( 18.10323547118819931, -7.609655000036609884, -59.08443656163060353 ) ) ;
#30690=ORIENTED_EDGE ( 'NONE', *, *, #2523, .F. ) ;
#30691=CARTESIAN_POINT ( 'NONE',  ( 20.28858101704520323, -22.28087760341009727, -32.14999999999999858 ) ) ;
#30711=CARTESIAN_POINT ( 'NONE',  ( 11.27223721714355698, -9.290040501825846064, -37.08399908769415987 ) ) ;
#30713=CARTESIAN_POINT ( 'NONE',  ( 20.11805472015788609, -22.52872049315324432, -75.84102053616285843 ) ) ;
#30718=LINE ( 'NONE', #18673, #47716 ) ;
#30719=CARTESIAN_POINT ( 'NONE',  ( 9.366980835600751121, -15.61636285886159925, -47.84717978380999881 ) ) ;
#30720=EDGE_LOOP ( 'NONE', ( #24158, #37412, #2030, #16328 ) ) ;
#30721=ORIENTED_EDGE ( 'NONE', *, *, #6981, .T. ) ;
#30722=DIRECTION ( 'NONE',  ( 0.6934629132905126836, 0.5038302981000500891, 0.5150380749100492705 ) ) ;
#30729=ORIENTED_EDGE ( 'NONE', *, *, #14854, .T. ) ;
#30734=CARTESIAN_POINT ( 'NONE',  ( 8.112799223618010203, -17.52513170135909704, -36.71796074224590001 ) ) ;
#30738=CARTESIAN_POINT ( 'NONE',  ( 22.89776929422545493, -15.84020125202738605, -50.46335449847054377 ) ) ;
#30747=CARTESIAN_POINT ( 'NONE',  ( 13.47464181256609983, -7.811647465521459388, -36.90313586381709854 ) ) ;
#30768=CARTESIAN_POINT ( 'NONE',  ( 10.10928765634339932, -11.23323448080919995, -56.26754282442009725 ) ) ;
#30774=CARTESIAN_POINT ( 'NONE',  ( 17.01980771413989757, -8.849199239206612333, -73.99448688925269835 ) ) ;
#30775=CARTESIAN_POINT ( 'NONE',  ( 10.24083624763009936, -19.10015682395959757, -81.23899999999999011 ) ) ;
#30785=CARTESIAN_POINT ( 'NONE',  ( 20.86616962407251208, -10.71475060854243644, -80.19705727907313531 ) ) ;
#30800=CARTESIAN_POINT ( 'NONE',  ( 11.59299064767398590, -21.01270279974525934, -39.56984226053648257 ) ) ;
#30802=CARTESIAN_POINT ( 'NONE',  ( 13.58021417256130015, -23.03678500379669813, -51.89300772538110351 ) ) ;
#30811=CARTESIAN_POINT ( 'NONE',  ( 20.69643343333880381, -10.53272061581830066, -32.14999999999999858 ) ) ;
#30812=CARTESIAN_POINT ( 'NONE',  ( 8.223013028489239318, -15.61598591435789984, -40.50766849176299189 ) ) ;
#30815=CARTESIAN_POINT ( 'NONE',  ( 19.44826417394619966, -21.62186115282320031, -81.18618737929101314 ) ) ;
#30820=CARTESIAN_POINT ( 'NONE',  ( 9.885447592686571028, -18.88711149514460175, -75.69367482554670801 ) ) ;
#30829=CARTESIAN_POINT ( 'NONE',  ( 23.04647245864238769, -19.60029819911440541, -41.67433410030931640 ) ) ;
#30831=ORIENTED_EDGE ( 'NONE', *, *, #25529, .T. ) ;
#30836=CARTESIAN_POINT ( 'NONE',  ( 12.14973823253568419, -8.703704093358281213, -39.12565883727726401 ) ) ;
#30849=VERTEX_POINT ( 'NONE', #6661 ) ;
#30850=CARTESIAN_POINT ( 'NONE',  ( 24.04420212447170613, -15.49892605004181334, -33.78761283496942980 ) ) ;
#30851=CARTESIAN_POINT ( 'NONE',  ( 9.367479402551163403, -16.16638264608517161, -51.82130573733594758 ) ) ;
#30853=CARTESIAN_POINT ( 'NONE',  ( 9.501448989937911094, -14.08578117475173919, -33.52488049317692997 ) ) ;
#30857=CARTESIAN_POINT ( 'NONE',  ( 21.47828441782199960, -9.869476621963398699, -43.75095171636819913 ) ) ;
#30862=DIRECTION ( 'NONE',  ( 1.000000000000000000, 0.000000000000000000, 0.000000000000000000 ) ) ;
#30864=CARTESIAN_POINT ( 'NONE',  ( 13.05928102721579975, -9.268823555959679439, -40.20359370904520091 ) ) ;
#30866=ORIENTED_EDGE ( 'NONE', *, *, #3544, .T. ) ;
#30867=B_SPLINE_CURVE_WITH_KNOTS ( 'NONE', 3,
 ( #24416, #8209, #32530, #16068, #36485, #12666, #5318, #590, #16575, #48557, #5058, #48049, #16325, #12148, #33064, #44885, #24155, #28102 ),
 .UNSPECIFIED., .F., .F.,
 ( 4, 2, 2, 2, 2, 2, 2, 2, 4 ),
 ( 0.000000000000000000, 0.06249986135442708174, 0.1249997227088541635, 0.1874995840632812383, 0.2499994454177083270, 0.3124993067721353879, 0.3749991681265624766, 0.4374990294809895652, 0.4999988908354166539 ),
 .UNSPECIFIED. ) ;
#30872=DIRECTION ( 'NONE',  ( 0.000000000000000000, 0.000000000000000000, -1.000000000000000000 ) ) ;
#30878=CARTESIAN_POINT ( 'NONE',  ( 22.46012367902698514, -20.47783799420304618, -58.00066461748448177 ) ) ;
#30879=CARTESIAN_POINT ( 'NONE',  ( 8.222903922732800908, -15.61639209420869889, -32.79233150823699816 ) ) ;
#30882=ORIENTED_EDGE ( 'NONE', *, *, #25106, .T. ) ;
#30887=CARTESIAN_POINT ( 'NONE',  ( 19.54197556973233318, -9.703305473112902035, -42.11948649911619924 ) ) ;
#30890=CARTESIAN_POINT ( 'NONE',  ( 15.31286695519810159, -8.611304789671351045, -55.91567931908580391 ) ) ;
#30896=CARTESIAN_POINT ( 'NONE',  ( 8.524204963362700838, -13.69818986724079934, -36.36609723691169904 ) ) ;
#30918=FACE_OUTER_BOUND ( 'NONE', #38685, .T. ) ;
#30922=CARTESIAN_POINT ( 'NONE',  ( 10.28542518435660114, -21.42804105449349805, -62.54333226898589260 ) ) ;
#30923=CARTESIAN_POINT ( 'NONE',  ( 8.222988179026620159, -15.61639226004780134, -48.50766849176299189 ) ) ;
#30929=CARTESIAN_POINT ( 'NONE',  ( 18.45084779930429875, -8.535326003196420430, -49.83331551772709389 ) ) ;
#30934=CARTESIAN_POINT ( 'NONE',  ( 10.85494166744680022, -21.28090959162620166, -32.14999999999999858 ) ) ;
#30940=CARTESIAN_POINT ( 'NONE',  ( 22.64063804623240017, -20.68033422096370089, -59.71818801013959899 ) ) ;
#30941=CARTESIAN_POINT ( 'NONE',  ( 21.90854117136780133, -20.69689202967290242, -32.14999999999999858 ) ) ;
#30945=DIRECTION ( 'NONE',  ( 0.000000000000000000, 0.000000000000000000, 1.000000000000000000 ) ) ;
#30946=LINE ( 'NONE', #14210, #3865 ) ;
#30948=DIRECTION ( 'NONE',  ( 1.000000000000000000, 2.460964292799963328E-14, 0.000000000000000000 ) ) ;
#30977=CARTESIAN_POINT ( 'NONE',  ( 22.90131613704217628, -15.82328094948992359, -36.85691428242716938 ) ) ;
#30982=CARTESIAN_POINT ( 'NONE',  ( 16.02066548673491653, -23.52649381719373878, -78.01222798080634391 ) ) ;
#30990=EDGE_LOOP ( 'NONE', ( #22533, #964, #19299, #5967 ) ) ;
#30991=CARTESIAN_POINT ( 'NONE',  ( 17.66316605052760025, -7.514079356226750050, -37.35171219075489546 ) ) ;
#30993=CARTESIAN_POINT ( 'NONE',  ( 8.714124674500926204, -18.45117587401020032, -50.67606243729918702 ) ) ;
#31004=CARTESIAN_POINT ( 'NONE',  ( 8.877163880441720778, -12.62854938784190040, -80.41182290828409407 ) ) ;
#31006=VERTEX_POINT ( 'NONE', #23894 ) ;
#31012=LINE ( 'NONE', #11124, #2152 ) ;
#31027=CARTESIAN_POINT ( 'NONE',  ( 19.23095358872740235, -8.840114487382349395, -60.70380296398279540 ) ) ;
#31033=CARTESIAN_POINT ( 'NONE',  ( 15.24822436422556216, -8.849178651065907175, -73.91115355493535333 ) ) ;
#31034=CARTESIAN_POINT ( 'NONE',  ( 9.205734167420709824, -3.616188944679339823, -32.14999999999999858 ) ) ;
#31039=ORIENTED_EDGE ( 'NONE', *, *, #41038, .T. ) ;
#31050=B_SPLINE_CURVE_WITH_KNOTS ( 'NONE', 3,
 ( #16050, #27837, #31752, #35961, #572, #7935, #47773, #8708, #51448, #39648, #32006, #43835, #16558, #16304, #39908, #321, #4003, #32258 ),
 .UNSPECIFIED., .F., .F.,
 ( 4, 2, 2, 2, 2, 2, 2, 2, 4 ),
 ( 0.4999985970897953269, 0.5624987724535709388, 0.6249989478173465507, 0.6874991231811220516, 0.7499992985448976635, 0.8124994739086732753, 0.8749996492724487762, 0.9374998246362243881, 1.000000000000000000 ),
 .UNSPECIFIED. ) ;
#31061=CARTESIAN_POINT ( 'NONE',  ( 23.11702576777929607, -19.19714202993379715, -57.43833289983449930 ) ) ;
#31062=EDGE_LOOP ( 'NONE', ( #33420, #8514, #19556, #10255, #7352, #46271, #16870, #12494 ) ) ;
#31063=FACE_OUTER_BOUND ( 'NONE', #23614, .T. ) ;
#31064=B_SPLINE_CURVE_WITH_KNOTS ( 'NONE', 3,
 ( #13000, #21598, #33403, #1448, #25532, #18204, #45218, #44954, #33661, #34170, #5132, #45738, #38130, #49676, #49420, #13765, #13516, #29473 ),
 .UNSPECIFIED., .F., .F.,
 ( 4, 2, 2, 2, 2, 2, 2, 2, 4 ),
 ( 0.000000000000000000, 0.06250000039148076447, 0.1250000007829615289, 0.1875000011744422934, 0.2500000015659230579, 0.3125000019574037391, 0.3750000023488843648, 0.4375000027403650460, 0.5000000031318456717 ),
 .UNSPECIFIED. ) ;
#31072=DIRECTION ( 'NONE',  ( -1.000000000000000000, 0.000000000000000000, 0.000000000000000000 ) ) ;
#31076=EDGE_CURVE ( 'NONE', #28912, #11278, #46332, .T. ) ;
#31078=CARTESIAN_POINT ( 'NONE',  ( 20.76651019224579997, -21.45108085822009869, -35.35374502362449789 ) ) ;
#31086=FACE_BOUND ( 'NONE', #40529, .T. ) ;
#31087=CARTESIAN_POINT ( 'NONE',  ( 17.16954876375649874, -23.52717981931520086, -41.96600113731807369 ) ) ;
#31088=FACE_OUTER_BOUND ( 'NONE', #50455, .T. ) ;
#31092=ORIENTED_EDGE ( 'NONE', *, *, #21330, .T. ) ;
#31103=CARTESIAN_POINT ( 'NONE',  ( 23.83903735962793746, -17.68686596444559100, -69.59100467832332981 ) ) ;
#31104=DIRECTION ( 'NONE',  ( 0.000000000000000000, 0.000000000000000000, -1.000000000000000000 ) ) ;
#31105=ADVANCED_FACE ( 'NONE', ( #35726 ), #4264, .T. ) ;
#31112=AXIS2_PLACEMENT_3D ( 'NONE', #42658, #50264, #21672 ) ;
#31116=CARTESIAN_POINT ( 'NONE',  ( 8.706976243475381239, -13.08103695608429895, -43.11720026785919657 ) ) ;
#31123=CARTESIAN_POINT ( 'NONE',  ( 9.575305561104880070, -13.02256067399330064, -47.96704895327989959 ) ) ;
#31124=CARTESIAN_POINT ( 'NONE',  ( 20.29254231923757956, -10.20481729065597598, -44.16112523059096873 ) ) ;
#31128=CARTESIAN_POINT ( 'NONE',  ( 9.807850478269243055, -10.75441043811473918, -50.71600121525216309 ) ) ;
#31133=CARTESIAN_POINT ( 'NONE',  ( 13.00753648416289998, -8.313058068840117443, -64.87884994055072241 ) ) ;
#31136=EDGE_CURVE ( 'NONE', #43673, #29694, #19418, .T. ) ;
#31146=CARTESIAN_POINT ( 'NONE',  ( 13.05928102721579975, -9.268823555959679439, -40.20359370904520091 ) ) ;
#31149=CARTESIAN_POINT ( 'NONE',  ( 22.86441391394799894, -17.72408945485720366, -56.54943076759479936 ) ) ;
#31154=CARTESIAN_POINT ( 'NONE',  ( 15.06271142038569977, -23.39045548577020028, -33.83109144287589487 ) ) ;
#31159=CARTESIAN_POINT ( 'NONE',  ( 12.14969309051077317, -22.52864826167251522, -40.45900981262661134 ) ) ;
#31163=ORIENTED_EDGE ( 'NONE', *, *, #20567, .T. ) ;
#31169=CARTESIAN_POINT ( 'NONE',  ( 23.91899059252033766, -17.05099851077971707, -43.85032385076039674 ) ) ;
#31173=CARTESIAN_POINT ( 'NONE',  ( 24.04493738681399151, -16.65173670305258113, -35.54933226178233241 ) ) ;
#31174=CARTESIAN_POINT ( 'NONE',  ( 18.26295693003078213, -22.08338128206962736, -32.85173728777652258 ) ) ;
#31175=CARTESIAN_POINT ( 'NONE',  ( 8.223569788570660677, -15.61625877447020017, -68.79233150823709764 ) ) ;
#31176=CARTESIAN_POINT ( 'NONE',  ( 8.542109907880320208, -12.39953300709269968, -64.91990020089438929 ) ) ;
#31182=CARTESIAN_POINT ( 'NONE',  ( 21.87051971591800026, -10.86242021751020026, -56.01239214068929329 ) ) ;
#31190=CARTESIAN_POINT ( 'NONE',  ( 8.020540499375330867, -17.08435497047219798, -58.45068511312169335 ) ) ;
#31195=CARTESIAN_POINT ( 'NONE',  ( 9.367243689500000414, -15.61633989587210003, -59.45282021618999835 ) ) ;
#31200=ORIENTED_EDGE ( 'NONE', *, *, #16258, .F. ) ;
#31205=FACE_OUTER_BOUND ( 'NONE', #29228, .T. ) ;
#31207=CARTESIAN_POINT ( 'NONE',  ( 13.09659873358270055, -8.813155235764829953, -73.59899483681280685 ) ) ;
#31208=B_SPLINE_CURVE_WITH_KNOTS ( 'NONE', 3,
 ( #39278, #11245, #27208, #19861, #43219, #35602, #10990, #50817, #26954, #31641, #39029, #15434, #23778, #39790, #14908, #35068, #15173, #51587 ),
 .UNSPECIFIED., .F., .F.,
 ( 4, 2, 2, 2, 2, 2, 2, 2, 4 ),
 ( 0.000000000000000000, 0.06250008666983568328, 0.1250001733396713666, 0.1875002600095070637, 0.2500003466793427331, 0.3125004333491783193, 0.3750005200190139054, 0.4375006066888494360, 0.5000006933586850222 ),
 .UNSPECIFIED. ) ;
#31217=CARTESIAN_POINT ( 'NONE',  ( 16.17501676180923553, -23.52709765870719849, -62.00601847604462336 ) ) ;
#31234=CARTESIAN_POINT ( 'NONE',  ( 15.68102735321344099, -23.51607019824295008, -78.02589618440929087 ) ) ;
#31247=CARTESIAN_POINT ( 'NONE',  ( 21.55806612471909744, -9.944718664031841016, -75.75539986607049059 ) ) ;
#31248=CARTESIAN_POINT ( 'NONE',  ( 9.366941535224629689, -16.50201745891097005, -37.41115343530533011 ) ) ;
#31249=ADVANCED_FACE ( 'NONE', ( #51334 ), #20113, .T. ) ;
#31255=CARTESIAN_POINT ( 'NONE',  ( 16.36649570679220034, -23.46046469067789886, -79.77807145977510572 ) ) ;
#31276=CARTESIAN_POINT ( 'NONE',  ( 14.12092483504799922, -22.78936639689409915, -61.65443013674619976 ) ) ;
#31277=CARTESIAN_POINT ( 'NONE',  ( 20.99566316520265730, -9.290061801217850856, -41.21600092569405405 ) ) ;
#31281=CARTESIAN_POINT ( 'NONE',  ( 17.18180055072906498, -22.35999544095330194, -34.90393729465625938 ) ) ;
#31284=CARTESIAN_POINT ( 'NONE',  ( 11.24014119269209999, -9.776142739560269135, -81.23899999999999011 ) ) ;
#31293=CARTESIAN_POINT ( 'NONE',  ( 23.55096566107879852, -15.91424779115909871, -81.23899999999999011 ) ) ;
#31295=CARTESIAN_POINT ( 'NONE',  ( 23.04647602230480885, -11.63208635115726253, -73.62566485141034889 ) ) ;
#31299=CARTESIAN_POINT ( 'NONE',  ( 24.04516176800591865, -15.61618872104648226, -63.79232972929064971 ) ) ;
#31302=VERTEX_POINT ( 'NONE', #39537 ) ;
#31316=CARTESIAN_POINT ( 'NONE',  ( 8.518398427704360287, -17.51100143664740116, -52.20988344963559769 ) ) ;
#31326=ADVANCED_FACE ( 'NONE', ( #15685 ), #51842, .T. ) ;
#31331=CARTESIAN_POINT ( 'NONE',  ( 20.99559669166361431, -9.290008747073166262, -71.50065479947573976 ) ) ;
#31333=CARTESIAN_POINT ( 'NONE',  ( 21.77309873898569847, -20.48512569386770110, -33.29405281597039590 ) ) ;
#31348=CYLINDRICAL_SURFACE ( 'NONE', #36164, 6.766999999999998572 ) ;
#31350=CARTESIAN_POINT ( 'NONE',  ( 24.04527493495583457, -15.61618894149694192, -73.79233149842438877 ) ) ;
#31354=CARTESIAN_POINT ( 'NONE',  ( 9.366403394718119557, -15.61612932825470068, -61.45282021618999124 ) ) ;
#31368=CARTESIAN_POINT ( 'NONE',  ( 12.88457861957980199, -8.472771336652998642, -57.37660785931070251 ) ) ;
#31377=CARTESIAN_POINT ( 'NONE',  ( 10.43067722519890062, -11.46704655386430005, -56.04737992176909955 ) ) ;
#31381=CARTESIAN_POINT ( 'NONE',  ( 16.13393739769620083, -15.61618894467929941, -82.15000000000000568 ) ) ;
#31383=CARTESIAN_POINT ( 'NONE',  ( 23.04647402534414979, -11.63208260442388564, -51.34099938571964827 ) ) ;
#31386=CARTESIAN_POINT ( 'NONE',  ( 9.367202679915338948, -15.61634672871210050, -75.45282021618999124 ) ) ;
#31400=CARTESIAN_POINT ( 'NONE',  ( 22.72481314779377470, -17.38742374030793769, -74.53615356034734418 ) ) ;
#31403=CARTESIAN_POINT ( 'NONE',  ( 9.086494889888442117, -15.89207442050179964, -55.44036573270419410 ) ) ;
#31407=VERTEX_POINT ( 'NONE', #13062 ) ;
#31408=CARTESIAN_POINT ( 'NONE',  ( 19.32439272560200294, -22.78610825969399656, -43.65423889476469554 ) ) ;
#31409=ORIENTED_EDGE ( 'NONE', *, *, #44902, .F. ) ;
#31422=CARTESIAN_POINT ( 'NONE',  ( 22.14842110270483744, -20.87114761213502589, -44.02058836580484780 ) ) ;
#31426=CARTESIAN_POINT ( 'NONE',  ( 18.20462292297444762, -23.32128735048156543, -35.92433339525297953 ) ) ;
#31428=CARTESIAN_POINT ( 'NONE',  ( 13.10862549112176012, -21.71576177937856400, -33.09924202300560125 ) ) ;
#31430=CARTESIAN_POINT ( 'NONE',  ( 11.87640767932309949, -8.555299428973780707, -77.11961558469180034 ) ) ;
#31433=DIRECTION ( 'NONE',  ( 0.000000000000000000, 0.000000000000000000, -1.000000000000000000 ) ) ;
#31435=ORIENTED_EDGE ( 'NONE', *, *, #36828, .F. ) ;
#31438=CARTESIAN_POINT ( 'NONE',  ( 23.33558369893389894, -13.70752858803779972, -50.15019124198150280 ) ) ;
#31443=CARTESIAN_POINT ( 'NONE',  ( 9.366937397696199596, -15.61618894467949836, -28.45282021618999835 ) ) ;
#31449=CARTESIAN_POINT ( 'NONE',  ( 12.89829992594130026, -23.19994598590569979, -74.13603346371840530 ) ) ;
#31450=ADVANCED_FACE ( 'NONE', ( #32932 ), #24542, .T. ) ;
#31455=CARTESIAN_POINT ( 'NONE',  ( 12.72585954689345655, -9.703326353824166972, -59.78612966474727841 ) ) ;
#31463=CARTESIAN_POINT ( 'NONE',  ( 8.673554481405242100, -18.33517393658237182, -66.68099849312459071 ) ) ;
#31465=CARTESIAN_POINT ( 'NONE',  ( 23.58421856477589884, -15.61827139591260050, -74.23274628532179520 ) ) ;
#31468=CARTESIAN_POINT ( 'NONE',  ( 24.04493739326861146, -16.65173287428400428, -69.83400117973924637 ) ) ;
#31471=CARTESIAN_POINT ( 'NONE',  ( 24.04795836731096159, -15.76465008236952947, -61.51362244070021035 ) ) ;
#31484=CARTESIAN_POINT ( 'NONE',  ( 17.01980479381098377, -22.38317906675219504, -58.91115339620073144 ) ) ;
#31490=CARTESIAN_POINT ( 'NONE',  ( 20.09351995423807580, -21.16054109508102954, -80.75524004131028732 ) ) ;
#31494=CARTESIAN_POINT ( 'NONE',  ( 22.28114148176659981, -21.11115046850839860, -34.02451708608289493 ) ) ;
#31499=B_SPLINE_CURVE_WITH_KNOTS ( 'NONE', 3,
 ( #31386, #7830, #16196, #48170, #212, #19611, #32153, #31901, #12272, #43978, #43469, #35855, #40050, #36110, #4141, #11769, #20117, #23520 ),
 .UNSPECIFIED., .F., .F.,
 ( 4, 2, 2, 2, 2, 2, 2, 2, 4 ),
 ( 0.000000000000000000, 0.06250000040710312899, 0.1250000008142062580, 0.1875000012213093870, 0.2500000016284125159, 0.3125000020355155339, 0.3750000024426185519, 0.4375000028497215698, 0.5000000032568245878 ),
 .UNSPECIFIED. ) ;
#31500=CARTESIAN_POINT ( 'NONE',  ( 10.63047440947285160, -19.59698183909219082, -51.25339573762192202 ) ) ;
#31504=CARTESIAN_POINT ( 'NONE',  ( 21.54529180190751703, -11.45756348979150907, -64.24448863903798213 ) ) ;
#31506=CARTESIAN_POINT ( 'NONE',  ( 19.56389830141130304, -22.67466723610790424, -70.36851255374439518 ) ) ;
#31507=CARTESIAN_POINT ( 'NONE',  ( 22.04685232790915350, -19.02417400735164321, -36.61948459849637771 ) ) ;
#31513=EDGE_CURVE ( 'NONE', #34513, #1610, #19376, .T. ) ;
#31515=CARTESIAN_POINT ( 'NONE',  ( 21.62555272082460078, -21.76638258811500037, -45.77565614294260143 ) ) ;
#31516=ORIENTED_EDGE ( 'NONE', *, *, #5353, .F. ) ;
#31520=LINE ( 'NONE', #32531, #14583 ) ;
#31537=CARTESIAN_POINT ( 'NONE',  ( 9.618178158523400967, -12.00349246206750031, -60.22848937760100085 ) ) ;
#31540=ORIENTED_EDGE ( 'NONE', *, *, #48306, .T. ) ;
#31542=CARTESIAN_POINT ( 'NONE',  ( 22.90093207708843792, -15.62495752410452887, -34.45323087790774963 ) ) ;
#31545=ADVANCED_FACE ( 'NONE', ( #28494, #8596 ), #25838, .T. ) ;
#31546=CARTESIAN_POINT ( 'NONE',  ( 12.09138161462960070, -9.064420227699880428, -81.23899999999999011 ) ) ;
#31550=VERTEX_POINT ( 'NONE', #22171 ) ;
#31551=CARTESIAN_POINT ( 'NONE',  ( 23.57620331537150093, -14.43797626381360111, -81.23899999999999011 ) ) ;
#31560=ORIENTED_EDGE ( 'NONE', *, *, #44461, .T. ) ;
#31567=CARTESIAN_POINT ( 'NONE',  ( 17.56839097463578980, -8.943911882717593187, -40.02052517762369632 ) ) ;
#31572=CARTESIAN_POINT ( 'NONE',  ( 16.42129855753530165, -23.45864849172179945, -63.77584738492399197 ) ) ;
#31582=LINE ( 'NONE', #27152, #49079 ) ;
#31587=CARTESIAN_POINT ( 'NONE',  ( 22.16258581960079965, -19.27651095769689604, -79.02086993021860906 ) ) ;
#31599=DIRECTION ( 'NONE',  ( 0.000000000000000000, 0.000000000000000000, -1.000000000000000000 ) ) ;
#31600=ORIENTED_EDGE ( 'NONE', *, *, #36042, .T. ) ;
#31607=CARTESIAN_POINT ( 'NONE',  ( 8.222412332301150428, -15.61630761206940043, -38.79233150823699816 ) ) ;
#31608=CARTESIAN_POINT ( 'NONE',  ( 22.90070908176307896, -14.58601874559523992, -62.79870702742260136 ) ) ;
#31614=CARTESIAN_POINT ( 'NONE',  ( 10.40721350023446057, -11.95274919063715835, -45.63409041280543477 ) ) ;
#31622=CARTESIAN_POINT ( 'NONE',  ( 16.13393739769629676, -15.61618894467929941, -20.75000000000000000 ) ) ;
#31625=CARTESIAN_POINT ( 'NONE',  ( 12.12491682425339867, -22.36263257323610176, -54.68316420314769033 ) ) ;
#31633=CARTESIAN_POINT ( 'NONE',  ( 23.18476211127489961, -15.44757686670599917, -56.83956923240509695 ) ) ;
#31639=CARTESIAN_POINT ( 'NONE',  ( 16.13393739769620083, -15.61618894467929941, -32.14999999999999858 ) ) ;
#31641=CARTESIAN_POINT ( 'NONE',  ( 17.16954621662006630, -7.705197706395741086, -47.04933590956818534 ) ) ;
#31646=CARTESIAN_POINT ( 'NONE',  ( 9.807859542861747215, -20.47797908015472501, -58.58399811593378814 ) ) ;
#31657=CARTESIAN_POINT ( 'NONE',  ( 10.85209793954360080, -20.29002362670730264, -53.22223566292269226 ) ) ;
#31660=EDGE_CURVE ( 'NONE', #41906, #43383, #13566, .T. ) ;
#31662=CARTESIAN_POINT ( 'NONE',  ( 17.95501807827959695, -7.982682978349759928, -42.86204958412849919 ) ) ;
#31668=CARTESIAN_POINT ( 'NONE',  ( 14.06313816487032753, -23.32125786362827569, -40.37567779348978547 ) ) ;
#31670=CARTESIAN_POINT ( 'NONE',  ( 13.79233564179163629, -22.26896734107802445, -67.45490599494564776 ) ) ;
#31687=CARTESIAN_POINT ( 'NONE',  ( 23.80679600161530374, -12.59791776729979951, -69.67303606471159583 ) ) ;
#31691=VERTEX_POINT ( 'NONE', #9629 ) ;
#31692=CARTESIAN_POINT ( 'NONE',  ( 21.61858969539150266, -20.65853789913799687, -66.46929104108710362 ) ) ;
#31700=CARTESIAN_POINT ( 'NONE',  ( 17.63700976455559655, -7.509186158879920470, -69.06602187564659801 ) ) ;
#31702=CARTESIAN_POINT ( 'NONE',  ( 22.96155967568899925, -13.55454926668129900, -32.14999999999999858 ) ) ;
#31705=CARTESIAN_POINT ( 'NONE',  ( 20.29254050540992438, -10.20481584277917619, -60.16112895304275554 ) ) ;
#31710=EDGE_LOOP ( 'NONE', ( #46364, #37174, #13811 ) ) ;
#31715=CARTESIAN_POINT ( 'NONE',  ( 10.21705801865680030, -11.08880203620289961, -73.44055697468560595 ) ) ;
#31721=VERTEX_POINT ( 'NONE', #42639 ) ;
#31725=CARTESIAN_POINT ( 'NONE',  ( 17.90521499757843316, -22.20705366312095208, -70.86948871188650401 ) ) ;
#31734=CARTESIAN_POINT ( 'NONE',  ( 24.04493737731856839, -14.58063703369262321, -55.75066751970105372 ) ) ;
#31735=CARTESIAN_POINT ( 'NONE',  ( 19.54197066778965208, -21.52907534521731137, -58.78615336081859510 ) ) ;
#31737=DIRECTION ( 'NONE',  ( 0.000000000000000000, 0.000000000000000000, 1.000000000000000000 ) ) ;
#31738=CARTESIAN_POINT ( 'NONE',  ( 21.71994269503706221, -21.21801661426634666, -77.75811212484384782 ) ) ;
#31743=ORIENTED_EDGE ( 'NONE', *, *, #8555, .F. ) ;
#31751=CARTESIAN_POINT ( 'NONE',  ( 9.653580312505349426, -20.71400142694579927, -42.58016164095380418 ) ) ;
#31752=CARTESIAN_POINT ( 'NONE',  ( 23.83903569875588246, -17.68687415037926769, -67.59099925309431001 ) ) ;
#31754=CARTESIAN_POINT ( 'NONE',  ( 24.02301761236539690, -16.22472933103653503, -49.81682925502759929 ) ) ;
#31760=CARTESIAN_POINT ( 'NONE',  ( 21.55489477686560207, -21.29069056903449919, -72.26976689927120390 ) ) ;
#31761=CARTESIAN_POINT ( 'NONE',  ( 14.36270743733633104, -22.20706670009677097, -37.03615240734319514 ) ) ;
#31766=CARTESIAN_POINT ( 'NONE',  ( 23.50805523095529992, -11.92767882673400059, -47.36003476421500125 ) ) ;
#31770=CARTESIAN_POINT ( 'NONE',  ( 21.26855178092368703, -21.65669804013363375, -39.78344367522398528 ) ) ;
#31771=CARTESIAN_POINT ( 'NONE',  ( 22.89855964779329867, -15.80993874071388561, -56.46193748095264198 ) ) ;
#31789=EDGE_CURVE ( 'NONE', #47534, #47610, #32355, .T. ) ;
#31792=CARTESIAN_POINT ( 'NONE',  ( 10.03556564381850080, -19.89597355255950362, -63.87256020652749555 ) ) ;
#31797=CARTESIAN_POINT ( 'NONE',  ( 20.91567610440962000, -20.47173450993272681, -34.70503499978224227 ) ) ;
#31800=CARTESIAN_POINT ( 'NONE',  ( 9.588579560587598749, -12.15087335004630020, -81.23899999999999011 ) ) ;
#31804=VERTEX_POINT ( 'NONE', #51194 ) ;
#31806=CARTESIAN_POINT ( 'NONE',  ( 22.54657568291069936, -11.21650286210249980, -81.23899999999999011 ) ) ;
#31808=DIRECTION ( 'NONE',  ( 0.000000000000000000, 0.000000000000000000, 1.000000000000000000 ) ) ;
#31815=VERTEX_POINT ( 'NONE', #23883 ) ;
#31818=CARTESIAN_POINT ( 'NONE',  ( 10.57891470305085235, -21.28119600275288192, -50.25446074854212952 ) ) ;
#31820=VECTOR ( 'NONE', #41174, 1000.000000000000000 ) ;
#31824=FACE_OUTER_BOUND ( 'NONE', #32900, .T. ) ;
#31828=CARTESIAN_POINT ( 'NONE',  ( 11.39303770747540057, -21.87003722477430046, -65.99397745470540144 ) ) ;
#31836=CARTESIAN_POINT ( 'NONE',  ( 8.222950370390678998, -16.35708134086146615, -32.47786278411599170 ) ) ;
#31842=CARTESIAN_POINT ( 'NONE',  ( 8.428818494671439510, -13.54557800259576439, -70.87566006981948874 ) ) ;
#31845=CARTESIAN_POINT ( 'NONE',  ( 23.40719984908270135, -14.00177027172209954, -38.99781585255099259 ) ) ;
#31847=CARTESIAN_POINT ( 'NONE',  ( 19.54190535476944390, -21.52911439740251964, -76.78616460542943400 ) ) ;
#31856=AXIS2_PLACEMENT_3D ( 'NONE', #31622, #47899, #699 ) ;
#31864=VERTEX_POINT ( 'NONE', #7170 ) ;
#31866=CARTESIAN_POINT ( 'NONE',  ( 15.09842697026319414, -7.705184469708584949, -79.25066590858526183 ) ) ;
#31880=CARTESIAN_POINT ( 'NONE',  ( 14.43936601292799438, -9.036495058040628692, -33.87268009392107615 ) ) ;
#31882=CARTESIAN_POINT ( 'NONE',  ( 13.78323292975819925, -8.128803813941159362, -53.41566130612969943 ) ) ;
#31888=CARTESIAN_POINT ( 'NONE',  ( 17.01978215929854699, -22.38318229988689367, -38.91115524470608023 ) ) ;
#31890=EDGE_CURVE ( 'NONE', #1136, #43399, #2488, .T. ) ;
#31891=CARTESIAN_POINT ( 'NONE',  ( 9.193808866418558878, -16.87204528351649913, -57.79019640516870027 ) ) ;
#31892=CARTESIAN_POINT ( 'NONE',  ( 9.543029255252220011, -13.84506841537463373, -43.53614410085236841 ) ) ;
#31898=CARTESIAN_POINT ( 'NONE',  ( 17.01972112733642462, -8.849186874510190037, -37.99448857803940882 ) ) ;
#31901=CARTESIAN_POINT ( 'NONE',  ( 14.36259954236786918, -9.025339123761108695, -75.86946488318916693 ) ) ;
#31903=CARTESIAN_POINT ( 'NONE',  ( 18.86653953160487163, -8.170294702091634775, -65.11960522023254327 ) ) ;
#31904=DIRECTION ( 'NONE',  ( 0.000000000000000000, 0.000000000000000000, 1.000000000000000000 ) ) ;
#31910=EDGE_LOOP ( 'NONE', ( #36128, #8560, #24036, #11734, #48404 ) ) ;
#31912=CARTESIAN_POINT ( 'NONE',  ( 10.72266925234624679, -19.77492588197056378, -75.24448688531667528 ) ) ;
#31915=CARTESIAN_POINT ( 'NONE',  ( 9.158617068706689679, -14.57337304308830106, -57.50005794035820372 ) ) ;
#31921=CARTESIAN_POINT ( 'NONE',  ( 11.87411739806599797, -9.025234404255449761, -44.60486606752819938 ) ) ;
#31927=LINE ( 'NONE', #27234, #18492 ) ;
#31936=CARTESIAN_POINT ( 'NONE',  ( 11.58381202359622364, -22.16518687231168627, -44.48577634035566319 ) ) ;
#31939=CARTESIAN_POINT ( 'NONE',  ( 24.04493721399152051, -15.53462765768975196, -49.50438507894359930 ) ) ;
#31942=CARTESIAN_POINT ( 'NONE',  ( 11.27237311615841087, -9.289937688271868055, -56.79933486857391500 ) ) ;
#31943=CARTESIAN_POINT ( 'NONE',  ( 24.04487853986463008, -15.61618860033810030, -61.79233400586811342 ) ) ;
#31944=CARTESIAN_POINT ( 'NONE',  ( 8.205515328865471858, -13.35281898941070011, -68.88084675407539237 ) ) ;
#31948=CARTESIAN_POINT ( 'NONE',  ( 11.53167905867499954, -21.47502090899229898, -66.94460462746880580 ) ) ;
#31952=CARTESIAN_POINT ( 'NONE',  ( 10.21244040264410025, -20.49383822526380072, -32.14999999999999858 ) ) ;
#31953=EDGE_CURVE ( 'NONE', #14876, #4764, #23307, .T. ) ;
#31956=ADVANCED_FACE ( 'NONE', ( #2916 ), #27257, .T. ) ;
#31961=CARTESIAN_POINT ( 'NONE',  ( 24.37792036543810070, -15.47666999773330154, -73.50228201520930327 ) ) ;
#31965=CARTESIAN_POINT ( 'NONE',  ( 17.01966651355726867, -8.849179074080744556, -59.99445920821477785 ) ) ;
#31974=CARTESIAN_POINT ( 'NONE',  ( 22.90077909847273219, -15.61618896438501203, -58.84717277627543552 ) ) ;
#31976=CARTESIAN_POINT ( 'NONE',  ( 18.95302484735409720, -8.719853703674310452, -71.85617835341321324 ) ) ;
#31986=CARTESIAN_POINT ( 'NONE',  ( 12.72599073039820539, -21.52912574338567353, -71.11948792801658215 ) ) ;
#31991=CARTESIAN_POINT ( 'NONE',  ( 9.367366684597708826, -15.61630833865650025, -41.84717978380999170 ) ) ;
#31996=CARTESIAN_POINT ( 'NONE',  ( 12.72603599818342701, -21.52915135001642710, -59.11948678850429673 ) ) ;
#31998=CARTESIAN_POINT ( 'NONE',  ( 18.20456379148673065, -7.911073824624160089, -59.09096439960827496 ) ) ;
#31999=CARTESIAN_POINT ( 'NONE',  ( 12.96504724582215395, -9.608149964835362766, -49.79827915037039077 ) ) ;
#32000=EDGE_LOOP ( 'NONE', ( #40150, #35771, #48654 ) ) ;
#32004=CARTESIAN_POINT ( 'NONE',  ( 11.27234134993635983, -9.289961720576606297, -34.79933427684135694 ) ) ;
#32005=CARTESIAN_POINT ( 'NONE',  ( 14.34289366216970052, -23.66447338258069877, -40.36203157117240181 ) ) ;
#32006=CARTESIAN_POINT ( 'NONE',  ( 14.06326646941806935, -23.32129108267079687, -68.09100065600449625 ) ) ;
#32009=CARTESIAN_POINT ( 'NONE',  ( 20.99565480752007574, -21.94232275358465856, -42.08399776718106722 ) ) ;
#32010=CARTESIAN_POINT ( 'NONE',  ( 12.47311850084049922, -22.55771338299259909, -80.66697359201489803 ) ) ;
#32016=CARTESIAN_POINT ( 'NONE',  ( 8.404314066867630828, -17.56895299481232797, -60.71374772562547406 ) ) ;
#32019=CARTESIAN_POINT ( 'NONE',  ( 22.35346372623429900, -10.20322183249439973, -39.27970379572579418 ) ) ;
#32020=ORIENTED_EDGE ( 'NONE', *, *, #48464, .T. ) ;
#32023=CARTESIAN_POINT ( 'NONE',  ( 22.01208305704984625, -20.93590873092134430, -39.74177713259125966 ) ) ;
#32025=CARTESIAN_POINT ( 'NONE',  ( 22.89142722538155184, -16.00359191757463151, -56.47104994342021911 ) ) ;
#32030=VECTOR ( 'NONE', #41321, 1000.000000000000000 ) ;
#32031=CARTESIAN_POINT ( 'NONE',  ( 16.13393739769620083, -15.61618894467929941, -32.14999999999999858 ) ) ;
#32032=CARTESIAN_POINT ( 'NONE',  ( 24.04462281140675728, -15.61619016268715399, -39.50767146438039390 ) ) ;
#32036=CARTESIAN_POINT ( 'NONE',  ( 17.90525277672623616, -22.20704298856055203, -64.86948817688498536 ) ) ;
#32037=EDGE_CURVE ( 'NONE', #25645, #4148, #14959, .T. ) ;
#32040=CARTESIAN_POINT ( 'NONE',  ( 8.222913253182543514, -14.58081823353785289, -74.83400703225677830 ) ) ;
#32044=CARTESIAN_POINT ( 'NONE',  ( 9.807815828836600858, -10.75445489836692836, -77.00066418793667822 ) ) ;
#32050=CARTESIAN_POINT ( 'NONE',  ( 11.98399099476960039, -9.143003290065829347, -81.23899999999999011 ) ) ;
#32054=ORIENTED_EDGE ( 'NONE', *, *, #19462, .F. ) ;
#32058=CARTESIAN_POINT ( 'NONE',  ( 19.11635189901000231, -21.76136781846319934, -81.23899999999999011 ) ) ;
#32065=VECTOR ( 'NONE', #46596, 1000.000000000000000 ) ;
#32074=CARTESIAN_POINT ( 'NONE',  ( 22.72397170760201845, -14.02689616002885309, -40.37749311795220564 ) ) ;
#32080=CARTESIAN_POINT ( 'NONE',  ( 13.10477641622549960, -22.85572842806620031, -57.91364648621609490 ) ) ;
#32095=CARTESIAN_POINT ( 'NONE',  ( 15.09844560108056477, -23.52719567249974020, -54.33399961690664526 ) ) ;
#32097=CARTESIAN_POINT ( 'NONE',  ( 10.09604082153919968, -19.98116939500580358, -31.86811205682530002 ) ) ;
#32108=ORIENTED_EDGE ( 'NONE', *, *, #35472, .F. ) ;
#32118=ORIENTED_EDGE ( 'NONE', *, *, #39349, .F. ) ;
#32126=CARTESIAN_POINT ( 'NONE',  ( 16.13393739769620083, -15.61618894467929941, -32.14999999999999858 ) ) ;
#32127=VERTEX_POINT ( 'NONE', #37199 ) ;
#32130=DIRECTION ( 'NONE',  ( -0.6934629132905126836, -0.5038302981000498670, 0.5150380749100492705 ) ) ;
#32131=CARTESIAN_POINT ( 'NONE',  ( 4.133937397696232807, -12.40079863550581862, -22.14999999999998792 ) ) ;
#32132=CARTESIAN_POINT ( 'NONE',  ( 20.35952799517920297, -9.003237130697479884, -57.69348358356519668 ) ) ;
#32141=CARTESIAN_POINT ( 'NONE',  ( 11.97535763329322300, -21.02757826297640875, -39.16115446231404462 ) ) ;
#32142=CARTESIAN_POINT ( 'NONE',  ( 11.96950732185199939, -9.924082013335240759, -54.14612557624219846 ) ) ;
#32144=ADVANCED_FACE ( 'NONE', ( #13114 ), #48476, .T. ) ;
#32146=DIRECTION ( 'NONE',  ( 0.000000000000000000, 0.000000000000000000, 1.000000000000000000 ) ) ;
#32149=CARTESIAN_POINT ( 'NONE',  ( 11.97528171298242761, -10.20485706339848697, -37.74448779564736611 ) ) ;
#32153=CARTESIAN_POINT ( 'NONE',  ( 12.72585555203040641, -9.703328613768398725, -75.78613368438831799 ) ) ;
#32157=CARTESIAN_POINT ( 'NONE',  ( 8.222944410885272504, -16.65178775934220212, -52.75066473391525790 ) ) ;
#32159=EDGE_CURVE ( 'NONE', #27673, #34513, #33248, .T. ) ;
#32168=CARTESIAN_POINT ( 'NONE',  ( 9.639954762936479682, -12.86468967408800168, -65.58038890884739658 ) ) ;
#32174=CARTESIAN_POINT ( 'NONE',  ( 13.15543360202459944, -22.87671670251840084, -41.91142241136510194 ) ) ;
#32190=CARTESIAN_POINT ( 'NONE',  ( 22.90085274204890808, -15.61618877333890332, -76.84718755697707593 ) ) ;
#32192=CARTESIAN_POINT ( 'NONE',  ( 14.06324711021505180, -23.32128607067484083, -36.09100056568438930 ) ) ;
#32194=CARTESIAN_POINT ( 'NONE',  ( 22.90066830340121840, -15.61618925674170022, -38.84718272210749035 ) ) ;
#32196=CARTESIAN_POINT ( 'NONE',  ( 9.582977133340488507, -20.62294834280969980, -74.58460979065590379 ) ) ;
#32202=CARTESIAN_POINT ( 'NONE',  ( 14.88739902878229948, -22.96144836147129809, -66.78616676534149121 ) ) ;
#32206=EDGE_CURVE ( 'NONE', #39152, #35815, #47903, .T. ) ;
#32210=DIRECTION ( 'NONE',  ( -1.000000000000000000, 0.000000000000000000, 0.000000000000000000 ) ) ;
#32212=CARTESIAN_POINT ( 'NONE',  ( 8.244279884465401054, -18.01118895116649909, -78.41385574115369650 ) ) ;
#32226=CARTESIAN_POINT ( 'NONE',  ( 8.863596654104609840, -13.98866346440020081, -79.30275787339340354 ) ) ;
#32236=CARTESIAN_POINT ( 'NONE',  ( 22.52288591994712164, -13.38583005777697466, -80.34591106198659816 ) ) ;
#32242=CARTESIAN_POINT ( 'NONE',  ( 23.79191518862026555, -17.66738158803666536, -71.59098575566194711 ) ) ;
#32253=ORIENTED_EDGE ( 'NONE', *, *, #6666, .F. ) ;
#32256=CARTESIAN_POINT ( 'NONE',  ( 18.20468374244083520, -7.911107725230738907, -35.09100006191968646 ) ) ;
#32257=CARTESIAN_POINT ( 'NONE',  ( 7.897539103648019143, -15.99627209049759813, -38.77765294989999489 ) ) ;
#32258=CARTESIAN_POINT ( 'NONE',  ( 8.223600577592289795, -15.61621812327629932, -68.50766849176299900 ) ) ;
#32263=CARTESIAN_POINT ( 'NONE',  ( 9.807855002554534352, -20.47797325407011115, -42.58399805498525126 ) ) ;
#32264=CARTESIAN_POINT ( 'NONE',  ( 22.77098726966259790, -19.80382795992320055, -80.19166000563299690 ) ) ;
#32267=EDGE_CURVE ( 'NONE', #37443, #34841, #48893, .T. ) ;
#32270=CARTESIAN_POINT ( 'NONE',  ( 19.81837380836439166, -22.69532670800266416, -60.13927688927024207 ) ) ;
#32272=DIRECTION ( 'NONE',  ( 0.000000000000000000, 0.000000000000000000, -1.000000000000000000 ) ) ;
#32273=CARTESIAN_POINT ( 'NONE',  ( 23.89559567647939886, -18.39816332852450032, -45.61721828081520158 ) ) ;
#32277=CARTESIAN_POINT ( 'NONE',  ( 15.25515948764014595, -23.51599653976285609, -40.04283046677572599 ) ) ;
#32278=LINE ( 'NONE', #28619, #10680 ) ;
#32281=ORIENTED_EDGE ( 'NONE', *, *, #39129, .F. ) ;
#32285=CARTESIAN_POINT ( 'NONE',  ( 11.97539703212459550, -21.02760807041932267, -49.16115413242771837 ) ) ;
#32290=CARTESIAN_POINT ( 'NONE',  ( 24.04493739769619864, -15.61618894467929941, -32.14999999999999858 ) ) ;
#32297=CARTESIAN_POINT ( 'NONE',  ( 8.223124147305879816, -15.61599092713959891, -72.50766849176299900 ) ) ;
#32302=CARTESIAN_POINT ( 'NONE',  ( 22.90087708341497574, -15.64706466928298845, -34.45427045631887353 ) ) ;
#32304=CARTESIAN_POINT ( 'NONE',  ( 9.510021278886100049, -12.32986133896500114, -81.23899999999999011 ) ) ;
#32305=VERTEX_POINT ( 'NONE', #5308 ) ;
#32308=EDGE_LOOP ( 'NONE', ( #26722, #29748, #50889, #28929 ) ) ;
#32312=FACE_OUTER_BOUND ( 'NONE', #38149, .T. ) ;
#32314=EDGE_CURVE ( 'NONE', #5472, #44209, #43794, .T. ) ;
#32323=ORIENTED_EDGE ( 'NONE', *, *, #31953, .F. ) ;
#32324=ORIENTED_EDGE ( 'NONE', *, *, #18444, .T. ) ;
#32333=CARTESIAN_POINT ( 'NONE',  ( 9.367861075313296482, -16.44284879759471352, -55.80828792171165276 ) ) ;
#32336=CARTESIAN_POINT ( 'NONE',  ( 19.85177579122500191, -8.705007724165220395, -66.94460462746880580 ) ) ;
#32337=ORIENTED_EDGE ( 'NONE', *, *, #10007, .F. ) ;
#32338=AXIS2_PLACEMENT_3D ( 'NONE', #29397, #14453, #6339 ) ;
#32340=CARTESIAN_POINT ( 'NONE',  ( 15.69653675527930226, -8.576924789068980814, -76.32742627405558267 ) ) ;
#32344=CARTESIAN_POINT ( 'NONE',  ( 9.221428961875151487, -19.60034550577672974, -36.62566438469894337 ) ) ;
#32350=DIRECTION ( 'NONE',  ( 0.000000000000000000, 0.000000000000000000, -1.000000000000000000 ) ) ;
#32351=CARTESIAN_POINT ( 'NONE',  ( 8.222937397696199469, -15.61618894467929941, -32.14999999999999858 ) ) ;
#32353=ORIENTED_EDGE ( 'NONE', *, *, #46055, .F. ) ;
#32354=CARTESIAN_POINT ( 'NONE',  ( 15.54540117339269933, -23.04318830182370093, -43.59251385424099823 ) ) ;
#32355=( BOUNDED_CURVE ( )  B_SPLINE_CURVE ( 2, ( #10847, #25759, #41769 ),
 .UNSPECIFIED., .F., .T. ) 
 B_SPLINE_CURVE_WITH_KNOTS ( ( 3, 3 ),
 ( 2.168627590050199672, 3.232274745523179948 ),
 .UNSPECIFIED. ) 
 CURVE ( )  GEOMETRIC_REPRESENTATION_ITEM ( )  RATIONAL_B_SPLINE_CURVE ( ( 1.425426480542939967, 1.425426480542949959, 1.323085463760209857 ) ) 
 REPRESENTATION_ITEM ( '' )  );
#32365=CARTESIAN_POINT ( 'NONE',  ( 8.222938998452162807, -16.65174813775593776, -52.46600170312751743 ) ) ;
#32369=ORIENTED_EDGE ( 'NONE', *, *, #43141, .T. ) ;
#32379=CARTESIAN_POINT ( 'NONE',  ( 12.96511943382801313, -9.565397813277416006, -32.19390020089446125 ) ) ;
#32388=CARTESIAN_POINT ( 'NONE',  ( 23.62296424492599911, -17.96165786859479852, -56.10910496229280398 ) ) ;
#32389=EDGE_CURVE ( 'NONE', #11278, #10625, #20013, .T. ) ;
#32397=CARTESIAN_POINT ( 'NONE',  ( 11.91260932085759983, -21.26622862968550010, -49.55142757455229940 ) ) ;
#32399=ORIENTED_EDGE ( 'NONE', *, *, #50279, .F. ) ;
#32402=CARTESIAN_POINT ( 'NONE',  ( 22.04684738446895764, -12.20819461931851357, -38.28615615749678369 ) ) ;
#32404=CARTESIAN_POINT ( 'NONE',  ( 24.04493739677426234, -15.61429984773749169, -55.50759605722655010 ) ) ;
#32410=CARTESIAN_POINT ( 'NONE',  ( 8.223360643215830379, -15.61635149015999957, -74.50766849176298479 ) ) ;
#32411=VECTOR ( 'NONE', #22579, 1000.000000000000000 ) ;
#32416=ORIENTED_EDGE ( 'NONE', *, *, #34508, .T. ) ;
#32422=CARTESIAN_POINT ( 'NONE',  ( 20.70280240204410305, -20.98908679115569953, -62.72850739055710534 ) ) ;
#32435=ORIENTED_EDGE ( 'NONE', *, *, #10588, .F. ) ;
#32441=CARTESIAN_POINT ( 'NONE',  ( 22.90112932213407149, -15.61618880384378905, -64.45281843961751633 ) ) ;
#32447=CARTESIAN_POINT ( 'NONE',  ( 15.75961300321349690, -23.85285096904510027, -70.30678751322059838 ) ) ;
#32448=CARTESIAN_POINT ( 'NONE',  ( 22.90066830340121840, -15.61618925674170022, -38.84718272210749035 ) ) ;
#32450=ADVANCED_FACE ( 'NONE', ( #14966 ), #20172, .T. ) ;
#32453=CARTESIAN_POINT ( 'NONE',  ( 12.24237353118370031, -9.263046062766429500, -61.55771731514269618 ) ) ;
#32458=DIRECTION ( 'NONE',  ( 0.000000000000000000, 0.000000000000000000, -1.000000000000000000 ) ) ;
#32463=FACE_OUTER_BOUND ( 'NONE', #20344, .T. ) ;
#32469=AXIS2_PLACEMENT_3D ( 'NONE', #2582, #49766, #13858 ) ;
#32471=CARTESIAN_POINT ( 'NONE',  ( 9.807682861627638360, -20.47775237701530315, -72.58401298376038824 ) ) ;
#32474=CARTESIAN_POINT ( 'NONE',  ( 22.89779876327829911, -12.49259093177239954, -80.09494718402969227 ) ) ;
#32493=CARTESIAN_POINT ( 'NONE',  ( 23.94343581735640214, -16.90563803632168316, -71.55974283691564608 ) ) ;
#32503=CARTESIAN_POINT ( 'NONE',  ( 9.487004236308452576, -14.16812596634764354, -49.52099469407719567 ) ) ;
#32506=CARTESIAN_POINT ( 'NONE',  ( 15.20323989161956391, -8.855217236353226440, -71.90910339118616434 ) ) ;
#32508=CARTESIAN_POINT ( 'NONE',  ( 24.04493605050502936, -15.62153787553132034, -65.50788166513238764 ) ) ;
#32509=CARTESIAN_POINT ( 'NONE',  ( 16.66011486035179701, -7.387832041036370256, -41.31265874393589144 ) ) ;
#32515=CARTESIAN_POINT ( 'NONE',  ( 20.82320479922240253, -9.323532524045690550, -79.71634641925129472 ) ) ;
#32516=AXIS2_PLACEMENT_3D ( 'NONE', #29508, #42353, #10647 ) ;
#32518=CARTESIAN_POINT ( 'NONE',  ( 9.221354224360256424, -11.63216018383065986, -32.67433414864056118 ) ) ;
#32519=VECTOR ( 'NONE', #21547, 1000.000000000000000 ) ;
#32521=CARTESIAN_POINT ( 'NONE',  ( 23.59532682517835056, -18.30036212264693773, -59.90219143874516305 ) ) ;
#32524=EDGE_CURVE ( 'NONE', #37146, #12364, #1305, .T. ) ;
#32525=CARTESIAN_POINT ( 'NONE',  ( 9.742225364899180562, -20.82471445568270241, -42.29002317614339290 ) ) ;
#32526=VERTEX_POINT ( 'NONE', #4454 ) ;
#32530=CARTESIAN_POINT ( 'NONE',  ( 8.428887333864649278, -17.68705018600014256, -64.70899835976443626 ) ) ;
#32531=CARTESIAN_POINT ( 'NONE',  ( 9.366937397696199596, -15.61618894467949836, -28.45282021618999835 ) ) ;
#32540=CARTESIAN_POINT ( 'NONE',  ( 17.16951678489785138, -7.705193502012818385, -61.33399649469901505 ) ) ;
#32543=CARTESIAN_POINT ( 'NONE',  ( 24.01953109262902331, -14.96959097810077033, -75.76629004851450588 ) ) ;
#32549=CARTESIAN_POINT ( 'NONE',  ( 10.22106108903712851, -12.20813745483522617, -47.61948721594488632 ) ) ;
#32557=CARTESIAN_POINT ( 'NONE',  ( 13.16285594202260079, -8.418783507588880610, -81.23899999999999011 ) ) ;
#32558=ADVANCED_FACE ( 'NONE', ( #49273 ), #8395, .T. ) ;
#32567=CARTESIAN_POINT ( 'NONE',  ( 21.46001303057629883, -20.23894261149060014, -81.23899999999999011 ) ) ;
#32568=CARTESIAN_POINT ( 'NONE',  ( 12.14987812824804614, -8.703624956618371655, -62.84100237377567311 ) ) ;
#32573=ORIENTED_EDGE ( 'NONE', *, *, #20544, .F. ) ;
#32588=CARTESIAN_POINT ( 'NONE',  ( 9.366668631897962172, -15.87390888100710029, -63.83506491120805038 ) ) ;
#32591=AXIS2_PLACEMENT_3D ( 'NONE', #33086, #21298, #22591 ) ;
#32592=CARTESIAN_POINT ( 'NONE',  ( 8.681468816368131058, -13.15703050580209954, -58.38896007259789656 ) ) ;
#32597=DIRECTION ( 'NONE',  ( 0.000000000000000000, 0.000000000000000000, -1.000000000000000000 ) ) ;
#32598=AXIS2_PLACEMENT_3D ( 'NONE', #36641, #21175, #4170 ) ;
#32612=CARTESIAN_POINT ( 'NONE',  ( 23.57992767232060416, -15.86901926038440003, -47.07814682104019255 ) ) ;
#32622=DIRECTION ( 'NONE',  ( 0.000000000000000000, 0.000000000000000000, -1.000000000000000000 ) ) ;
#32624=VERTEX_POINT ( 'NONE', #32721 ) ;
#32642=CARTESIAN_POINT ( 'NONE',  ( 24.03381966901990552, -15.16329667443855911, -59.77410034332016409 ) ) ;
#32649=CARTESIAN_POINT ( 'NONE',  ( 23.45525733055259821, -18.44196707332659813, -62.12974372312790194 ) ) ;
#32663=CARTESIAN_POINT ( 'NONE',  ( 18.20462679473721224, -7.911091633304650372, -37.09100355881665934 ) ) ;
#32667=CARTESIAN_POINT ( 'NONE',  ( 22.16267452853670150, -12.06226307891249938, -32.14999999999999858 ) ) ;
#32672=CARTESIAN_POINT ( 'NONE',  ( 23.83903794312202251, -17.68686302044806524, -73.59100117495633242 ) ) ;
#32677=CARTESIAN_POINT ( 'NONE',  ( 23.09258150619950101, -16.76502807425499952, -58.89926144005930553 ) ) ;
#32681=DIRECTION ( 'NONE',  ( 0.000000000000000000, 0.000000000000000000, -1.000000000000000000 ) ) ;
#32684=CARTESIAN_POINT ( 'NONE',  ( 9.657775751103418571, -18.40937512247450059, -67.32320539224699019 ) ) ;
#32688=CARTESIAN_POINT ( 'NONE',  ( 15.09849001458553097, -23.52720104044158944, -80.33399924191861885 ) ) ;
#32691=VERTEX_POINT ( 'NONE', #10560 ) ;
#32697=ORIENTED_EDGE ( 'NONE', *, *, #7176, .T. ) ;
#32698=CARTESIAN_POINT ( 'NONE',  ( 15.09830194314797147, -7.705199573743128028, -74.96596846305294548 ) ) ;
#32700=CARTESIAN_POINT ( 'NONE',  ( 18.20461530425851038, -23.32128950267136247, -59.92435972222848051 ) ) ;
#32701=CARTESIAN_POINT ( 'NONE',  ( 22.90093739769620029, -15.61618894467913243, -28.45282021618999835 ) ) ;
#32708=CYLINDRICAL_SURFACE ( 'NONE', #27571, 6.766999999999998572 ) ;
#32712=CARTESIAN_POINT ( 'NONE',  ( 23.18808933907469694, -12.17692382128999817, -31.86811205682530002 ) ) ;
#32718=CARTESIAN_POINT ( 'NONE',  ( 16.23075547080119918, -8.166536599377129946, -67.73679393810499505 ) ) ;
#32721=CARTESIAN_POINT ( 'NONE',  ( 24.04475233726670780, -15.61618925176752271, -59.50766149565701113 ) ) ;
#32727=CARTESIAN_POINT ( 'NONE',  ( 20.28352806221460014, -22.74104818079599966, -79.83979650029888830 ) ) ;
#32732=CARTESIAN_POINT ( 'NONE',  ( 23.83903698041244823, -13.54551011926608162, -79.42433689193339319 ) ) ;
#32742=CARTESIAN_POINT ( 'NONE',  ( 12.57343482522869849, -21.70432331639599965, -39.12126593359850091 ) ) ;
#32750=CARTESIAN_POINT ( 'NONE',  ( 12.02727910879949924, -21.83246210764250250, -59.75317579121929867 ) ) ;
#32755=DIRECTION ( 'NONE',  ( 1.000000000000000000, 2.460964292799963328E-14, 0.000000000000000000 ) ) ;
#32760=CARTESIAN_POINT ( 'NONE',  ( 24.04493739903013960, -15.61839112611826330, -71.50776123734669909 ) ) ;
#32764=DIRECTION ( 'NONE',  ( -0.4999999999999998890, 0.8660254037844387076, 0.000000000000000000 ) ) ;
#32768=CARTESIAN_POINT ( 'NONE',  ( 17.01970826270887471, -8.849185036877550203, -69.99448858124149808 ) ) ;
#32773=CARTESIAN_POINT ( 'NONE',  ( 20.26294502443843015, -10.18158913507981822, -72.15944758614480747 ) ) ;
#32774=CARTESIAN_POINT ( 'NONE',  ( 17.16955165497868308, -7.705198479972275472, -35.04933352119421386 ) ) ;
#32775=CARTESIAN_POINT ( 'NONE',  ( 11.97151152939560070, -22.73355720456560292, -38.46077722564559309 ) ) ;
#32776=CARTESIAN_POINT ( 'NONE',  ( 22.88119099990498029, -15.08889120109404480, -56.42800610659730864 ) ) ;
#32780=CARTESIAN_POINT ( 'NONE',  ( 8.223340741289188571, -15.61635616670070092, -42.79233150823699816 ) ) ;
#32781=CARTESIAN_POINT ( 'NONE',  ( 20.28421976646189862, -9.796066462810269826, -31.92983709734899378 ) ) ;
#32783=CARTESIAN_POINT ( 'NONE',  ( 23.83903224035146096, -13.54548743036029990, -33.42433181708312162 ) ) ;
#32786=EDGE_CURVE ( 'NONE', #16071, #34347, #16218, .T. ) ;
#32787=CARTESIAN_POINT ( 'NONE',  ( 24.04474217745232068, -15.67622493691082575, -59.79474066186497794 ) ) ;
#32792=CARTESIAN_POINT ( 'NONE',  ( 15.03334340613479903, -7.444811241090149245, -54.96505214632239245 ) ) ;
#32809=LINE ( 'NONE', #32290, #30065 ) ;
#32812=CARTESIAN_POINT ( 'NONE',  ( 10.53341022709680352, -19.45603223815694349, -67.26142806095880644 ) ) ;
#32817=CARTESIAN_POINT ( 'NONE',  ( 19.54195158308641211, -9.703291134712584309, -48.11948821520955732 ) ) ;
#32826=ORIENTED_EDGE ( 'NONE', *, *, #28034, .T. ) ;
#32827=ORIENTED_EDGE ( 'NONE', *, *, #3375, .F. ) ;
#32831=CARTESIAN_POINT ( 'NONE',  ( 22.70811139964889946, -18.58208211393579745, -81.23899999999999011 ) ) ;
#32851=CARTESIAN_POINT ( 'NONE',  ( 12.99575412164399779, -21.93238755621440106, -63.49395944174919748 ) ) ;
#32855=CARTESIAN_POINT ( 'NONE',  ( 14.45395864162150090, -23.28198437387779762, -71.85617835341309956 ) ) ;
#32863=CARTESIAN_POINT ( 'NONE',  ( 11.03791300131472042, -9.515481636700208412, -64.78606741210316500 ) ) ;
#32869=CARTESIAN_POINT ( 'NONE',  ( 24.04489541832924004, -15.64402584357523374, -33.50878528010039048 ) ) ;
#32871=CARTESIAN_POINT ( 'NONE',  ( 18.09661853408499965, -22.39043738500940961, -71.25741468598400274 ) ) ;
#32874=CARTESIAN_POINT ( 'NONE',  ( 10.07881066264659964, -11.27543618037340067, -40.26531874956899770 ) ) ;
#32876=ORIENTED_EDGE ( 'NONE', *, *, #10245, .T. ) ;
#32882=CARTESIAN_POINT ( 'NONE',  ( 14.06321080411807678, -23.32127667121109837, -78.37566353430301547 ) ) ;
#32889=AXIS2_PLACEMENT_3D ( 'NONE', #41350, #5467, #21421 ) ;
#32890=ORIENTED_EDGE ( 'NONE', *, *, #25106, .F. ) ;
#32900=EDGE_LOOP ( 'NONE', ( #30690, #25804, #6124, #16149 ) ) ;
#32901=CARTESIAN_POINT ( 'NONE',  ( 8.223069265346360623, -15.61598766837350105, -56.50766849176299189 ) ) ;
#32905=CARTESIAN_POINT ( 'NONE',  ( 22.90135621376786901, -15.43173441932949252, -66.83850953173875098 ) ) ;
#32908=CARTESIAN_POINT ( 'NONE',  ( 10.72256940289631721, -11.45758012563586092, -53.66115420497921917 ) ) ;
#32909=EDGE_CURVE ( 'NONE', #3546, #32127, #41838, .T. ) ;
#32915=CARTESIAN_POINT ( 'NONE',  ( 20.01403207936019868, -22.43759736617889899, -64.34787379290919773 ) ) ;
#32924=FACE_OUTER_BOUND ( 'NONE', #12493, .T. ) ;
#32931=VECTOR ( 'NONE', #35995, 1000.000000000000000 ) ;
#32932=FACE_OUTER_BOUND ( 'NONE', #3809, .T. ) ;
#32934=CARTESIAN_POINT ( 'NONE',  ( 22.89531333654768375, -11.40322039812424748, -55.33051484484766291 ) ) ;
#32935=CARTESIAN_POINT ( 'NONE',  ( 23.36827203260559926, -17.23220949816419889, -32.14999999999999858 ) ) ;
#32944=CARTESIAN_POINT ( 'NONE',  ( 10.71149743639709939, -11.10623284283549950, -62.06801868260409094 ) ) ;
#32951=CARTESIAN_POINT ( 'NONE',  ( 12.84739398434249935, -9.375901203816159324, -67.79851897862879184 ) ) ;
#32966=ADVANCED_FACE ( 'NONE', ( #2109 ), #41947, .T. ) ;
#32969=CARTESIAN_POINT ( 'NONE',  ( 12.14979381587971830, -22.52870523912515566, -60.17435903463200475 ) ) ;
#32980=CARTESIAN_POINT ( 'NONE',  ( 21.80161389069149891, -10.18809611409700011, -33.76936640235220466 ) ) ;
#32988=CARTESIAN_POINT ( 'NONE',  ( 21.47227334498080253, -20.22538852244909791, -33.07388991331939820 ) ) ;
#32990=EDGE_CURVE ( 'NONE', #14613, #1216, #5564, .T. ) ;
#33009=CARTESIAN_POINT ( 'NONE',  ( 24.04465550003185115, -15.68834717694893932, -65.79523427362767052 ) ) ;
#33011=CARTESIAN_POINT ( 'NONE',  ( 18.51000033465340167, -22.25673738164740101, -34.84344365616309602 ) ) ;
#33018=CARTESIAN_POINT ( 'NONE',  ( 22.50231163579990223, -19.48277707182389662, -79.24103283286959254 ) ) ;
#33022=CARTESIAN_POINT ( 'NONE',  ( 24.03633545123255644, -15.23418074785793763, -49.77695913693929697 ) ) ;
#33034=EDGE_CURVE ( 'NONE', #43399, #20583, #10575, .T. ) ;
#33037=CARTESIAN_POINT ( 'NONE',  ( 22.89189869931721688, -14.41738426556256059, -72.79077680364316905 ) ) ;
#33044=CARTESIAN_POINT ( 'NONE',  ( 20.11802429440930595, -8.703639022759114496, -43.45903450409944213 ) ) ;
#33046=CARTESIAN_POINT ( 'NONE',  ( 24.00223941041499742, -18.08044207546359772, -55.88894205964189865 ) ) ;
#33052=CARTESIAN_POINT ( 'NONE',  ( 14.51556075300879911, -22.88857169320650087, -40.80235737647439720 ) ) ;
#33059=B_SPLINE_CURVE_WITH_KNOTS ( 'NONE', 3,
 ( #1191, #36827, #44436, #4592, #32871, #8798, #8544, #23971, #39995, #663 ),
 .UNSPECIFIED., .F., .F.,
 ( 4, 1, 1, 1, 1, 1, 1, 4 ),
 ( 0.5000020751347326042, 0.5466795889596607338, 0.6258985200233790902, 0.7051174510869482326, 0.7843363821506665889, 0.8635553132142266275, 0.9427742442777956589, 1.000000000000000000 ),
 .UNSPECIFIED. ) ;
#33060=CARTESIAN_POINT ( 'NONE',  ( 21.28041071868149814, -9.174408673251130963, -53.22223566292279173 ) ) ;
#33064=CARTESIAN_POINT ( 'NONE',  ( 23.04647698446151338, -19.60028975017581132, -63.95900002351130809 ) ) ;
#33065=CARTESIAN_POINT ( 'NONE',  ( 17.37116791007819927, -8.672715762353169211, -52.40330909284259775 ) ) ;
#33082=CARTESIAN_POINT ( 'NONE',  ( 12.14985869000924801, -8.703635950884679673, -77.12566379575649478 ) ) ;
#33086=CARTESIAN_POINT ( 'NONE',  ( 16.13393739769620083, -15.61618894467929941, -32.14999999999999858 ) ) ;
#33097=CARTESIAN_POINT ( 'NONE',  ( 20.89839241790010149, -20.73495673888379898, -81.23899999999999011 ) ) ;
#33101=CARTESIAN_POINT ( 'NONE',  ( 9.366668810525878186, -15.61604052661200015, -35.45282021618999835 ) ) ;
#33104=CARTESIAN_POINT ( 'NONE',  ( 17.35001377175326098, -22.56339827118826591, -35.29201998310100663 ) ) ;
#33120=CARTESIAN_POINT ( 'NONE',  ( 10.36088797006879858, -19.66766515473189969, -63.65239730387659023 ) ) ;
#33122=CARTESIAN_POINT ( 'NONE',  ( 15.40474582320469921, -23.42996062235669896, -75.81712490659418791 ) ) ;
#33126=CARTESIAN_POINT ( 'NONE',  ( 24.04493739769619864, -15.61618894467929941, -32.14999999999999858 ) ) ;
#33131=CARTESIAN_POINT ( 'NONE',  ( 8.428848602312072558, -17.68690935890205651, -36.70899794646796721 ) ) ;
#33134=CARTESIAN_POINT ( 'NONE',  ( 22.04684527241202119, -19.02418722779176363, -78.61948426832272219 ) ) ;
#33141=CARTESIAN_POINT ( 'NONE',  ( 23.04646962482851791, -19.60030351599067444, -53.95900079672725269 ) ) ;
#33143=CARTESIAN_POINT ( 'NONE',  ( 9.593095007195888257, -12.04910678120510070, -44.22626530274989420 ) ) ;
#33153=CARTESIAN_POINT ( 'NONE',  ( 8.222598545279129922, -15.61602001634830117, -66.50766849176299900 ) ) ;
#33155=ORIENTED_EDGE ( 'NONE', *, *, #31660, .F. ) ;
#33156=ORIENTED_EDGE ( 'NONE', *, *, #22274, .T. ) ;
#33168=VERTEX_POINT ( 'NONE', #14012 ) ;
#33178=CARTESIAN_POINT ( 'NONE',  ( 21.60259711254701998, -19.60660697021737775, -46.65346184971561172 ) ) ;
#33181=CARTESIAN_POINT ( 'NONE',  ( 18.62649940869980014, -8.174826017574890358, -65.61537668992708916 ) ) ;
#33197=CARTESIAN_POINT ( 'NONE',  ( 16.13393739769620083, -15.61618894467929941, -32.14999999999999858 ) ) ;
#33198=CYLINDRICAL_SURFACE ( 'NONE', #51633, 6.766999999999998572 ) ;
#33200=CARTESIAN_POINT ( 'NONE',  ( 22.46384208064960220, -12.53037029265690094, -32.14999999999999858 ) ) ;
#33210=CARTESIAN_POINT ( 'NONE',  ( 23.11112601400289890, -14.58594713474730042, -60.80051578558619241 ) ) ;
#33218=CARTESIAN_POINT ( 'NONE',  ( 10.78987444403530027, -11.01362989085549948, -63.67913456332050259 ) ) ;
#33219=FACE_OUTER_BOUND ( 'NONE', #11031, .T. ) ;
#33222=EDGE_LOOP ( 'NONE', ( #49961, #2829, #25689, #47932 ) ) ;
#33235=CARTESIAN_POINT ( 'NONE',  ( 24.04493737759684180, -16.65173755265768563, -59.54933332424322145 ) ) ;
#33238=CARTESIAN_POINT ( 'NONE',  ( 20.11806584526820174, -22.52871384128776100, -43.84102563478171533 ) ) ;
#33241=CARTESIAN_POINT ( 'NONE',  ( 20.29261235332924329, -10.20487319419143368, -68.16115184722131914 ) ) ;
#33243=VERTEX_POINT ( 'NONE', #17427 ) ;
#33244=CARTESIAN_POINT ( 'NONE',  ( 20.99560421276813571, -9.290014746710346216, -53.50066707012037881 ) ) ;
#33246=CARTESIAN_POINT ( 'NONE',  ( 23.61944552496879979, -12.15932946040240026, -79.65462137872769688 ) ) ;
#33248=LINE ( 'NONE', #764, #45581 ) ;
#33255=CARTESIAN_POINT ( 'NONE',  ( 9.747988662193298737, -18.60988528556680066, -33.70764136182839366 ) ) ;
#33256=DIRECTION ( 'NONE',  ( -0.8660254037844387076, -0.4999999999999998890, 0.000000000000000000 ) ) ;
#33262=EDGE_CURVE ( 'NONE', #34702, #3924, #2217, .T. ) ;
#33268=CARTESIAN_POINT ( 'NONE',  ( 16.13393739769620083, -15.61618894467929941, -23.15000000000000213 ) ) ;
#33269=LINE ( 'NONE', #45079, #17631 ) ;
#33270=CARTESIAN_POINT ( 'NONE',  ( 9.221400882477601257, -11.63208038433509373, -68.67433567719821497 ) ) ;
#33276=CARTESIAN_POINT ( 'NONE',  ( 24.04493739769619864, -15.61618894467929941, -32.14999999999999858 ) ) ;
#33279=CARTESIAN_POINT ( 'NONE',  ( 15.05117764281579973, -22.58542061303949922, -35.00188151829029692 ) ) ;
#33286=CARTESIAN_POINT ( 'NONE',  ( 8.692723195675709391, -15.98364715725590024, -70.05163682948979442 ) ) ;
#33288=B_SPLINE_CURVE_WITH_KNOTS ( 'NONE', 3,
 ( #7451, #3524, #106, #12938, #24946, #43864, #20251, #32036, #15820, #36756, #20505, #24427, #40441, #28894, #7962, #12407, #48576, #40190 ),
 .UNSPECIFIED., .F., .F.,
 ( 4, 2, 2, 2, 2, 2, 2, 2, 4 ),
 ( 0.5000011091671422436, 0.5625009705212494771, 0.6250008318753568215, 0.6875006932294640549, 0.7500005545835712883, 0.8125004159376785218, 0.8750002772917856442, 0.9375001386458927666, 1.000000000000000000 ),
 .UNSPECIFIED. ) ;
#33291=CARTESIAN_POINT ( 'NONE',  ( 13.69709356640602671, -8.058494653411733211, -49.19314222014786964 ) ) ;
#33306=VERTEX_POINT ( 'NONE', #23900 ) ;
#33308=CARTESIAN_POINT ( 'NONE',  ( 10.22099953874110412, -12.20824267314787548, -69.61948740543661529 ) ) ;
#33314=CARTESIAN_POINT ( 'NONE',  ( 9.910435692222698378, -20.53991556490245785, -66.29463588517631933 ) ) ;
#33315=CARTESIAN_POINT ( 'NONE',  ( 24.37891534843840091, -15.56088390232210017, -57.79019640516870027 ) ) ;
#33316=CARTESIAN_POINT ( 'NONE',  ( 12.14477763102834373, -10.07529305404503717, -55.75450440121188933 ) ) ;
#33318=ORIENTED_EDGE ( 'NONE', *, *, #37023, .F. ) ;
#33320=CARTESIAN_POINT ( 'NONE',  ( 22.72830296970559871, -19.08332558863240180, -42.38673599774679701 ) ) ;
#33327=CARTESIAN_POINT ( 'NONE',  ( 14.50620669810990115, -7.533292590116819731, -48.94441338548729448 ) ) ;
#33330=EDGE_CURVE ( 'NONE', #19102, #1209, #33654, .T. ) ;
#33332=CARTESIAN_POINT ( 'NONE',  ( 13.74532132657402173, -23.19733159729566552, -40.10491864076364976 ) ) ;
#33334=CARTESIAN_POINT ( 'NONE',  ( 9.366504787982940172, -15.61629640169840094, -69.84717978381009118 ) ) ;
#33336=VERTEX_POINT ( 'NONE', #22949 ) ;
#33343=CARTESIAN_POINT ( 'NONE',  ( 10.22104436064596023, -19.02421183790971071, -53.28615311890232675 ) ) ;
#33351=CYLINDRICAL_SURFACE ( 'NONE', #13242, 6.766999999999998572 ) ;
#33352=VERTEX_POINT ( 'NONE', #51529 ) ;
#33357=ADVANCED_FACE ( 'NONE', ( #27916 ), #34747, .T. ) ;
#33361=CARTESIAN_POINT ( 'NONE',  ( 15.09849879369435399, -23.52720210124172340, -80.04933602518147495 ) ) ;
#33363=EDGE_CURVE ( 'NONE', #10625, #5472, #19918, .T. ) ;
#33367=CARTESIAN_POINT ( 'NONE',  ( 10.22100624670438052, -19.02414668158459321, -45.28616605880424828 ) ) ;
#33369=DIRECTION ( 'NONE',  ( 1.000000000000000000, 0.000000000000000000, 0.000000000000000000 ) ) ;
#33387=CARTESIAN_POINT ( 'NONE',  ( 18.14390284338876214, -22.37655861516149614, -55.25519061113300268 ) ) ;
#33389=CARTESIAN_POINT ( 'NONE',  ( 8.505345115432438874, -17.45774480160260111, -68.21210752448658354 ) ) ;
#33391=CARTESIAN_POINT ( 'NONE',  ( 21.17745084236876707, -10.68612491792656627, -48.60080040178979743 ) ) ;
#33392=ADVANCED_FACE ( 'NONE', ( #19547 ), #3579, .T. ) ;
#33400=VECTOR ( 'NONE', #10872, 1000.000000000000000 ) ;
#33403=CARTESIAN_POINT ( 'NONE',  ( 8.428792854876448359, -17.68670666238835310, -56.70900359172159000 ) ) ;
#33404=CARTESIAN_POINT ( 'NONE',  ( 24.03425380569510139, -16.05991031410578884, -33.52552477532261577 ) ) ;
#33407=CARTESIAN_POINT ( 'NONE',  ( 12.86561113652319932, -22.31131685898150252, -47.71189826954910274 ) ) ;
#33410=CARTESIAN_POINT ( 'NONE',  ( 22.90129928757160727, -15.40020387630258725, -34.83702718343101168 ) ) ;
#33412=CARTESIAN_POINT ( 'NONE',  ( 16.13393739769620083, -15.61618894467929941, -32.14999999999999858 ) ) ;
#33416=CARTESIAN_POINT ( 'NONE',  ( 22.90083016047308462, -15.61618874168370752, -60.84718745454353694 ) ) ;
#33420=ORIENTED_EDGE ( 'NONE', *, *, #41580, .T. ) ;
#33421=EDGE_CURVE ( 'NONE', #36842, #2213, #27441, .T. ) ;
#33427=EDGE_LOOP ( 'NONE', ( #41987, #2962, #48469, #15705 ) ) ;
#33436=ORIENTED_EDGE ( 'NONE', *, *, #33421, .F. ) ;
#33441=VECTOR ( 'NONE', #15766, 1000.000000000000000 ) ;
#33442=CARTESIAN_POINT ( 'NONE',  ( 23.25678206576879958, -18.91040075118040065, -68.15038248396299991 ) ) ;
#33457=CARTESIAN_POINT ( 'NONE',  ( 23.23758385637279744, -14.43887883678110029, -32.14999999999999858 ) ) ;
#33462=CARTESIAN_POINT ( 'NONE',  ( 10.11250238224864617, -10.41121846697807030, -44.73474056346155692 ) ) ;
#33465=APPLICATION_CONTEXT ( 'automotive_design' ) ;
#33469=CARTESIAN_POINT ( 'NONE',  ( 16.96763219941080081, -8.612796041803930436, -62.38489440685859222 ) ) ;
#33470=ORIENTED_EDGE ( 'NONE', *, *, #22386, .F. ) ;
#33473=CARTESIAN_POINT ( 'NONE',  ( 22.90093739769620029, -15.61618894467913243, -28.45282021618999835 ) ) ;
#33477=CARTESIAN_POINT ( 'NONE',  ( 19.96964979656319983, -21.53479258825970177, -74.76978491222709522 ) ) ;
#33482=CARTESIAN_POINT ( 'NONE',  ( 6.430637565411768897, -15.61618894467929941, -22.14999999999999858 ) ) ;
#33484=ADVANCED_FACE ( 'NONE', ( #48442 ), #23710, .F. ) ;
#33485=ORIENTED_EDGE ( 'NONE', *, *, #50004, .F. ) ;
#33498=AXIS2_PLACEMENT_3D ( 'NONE', #27716, #3118, #11501 ) ;
#33504=DIRECTION ( 'NONE',  ( 0.000000000000000000, 0.000000000000000000, -1.000000000000000000 ) ) ;
#33507=CARTESIAN_POINT ( 'NONE',  ( 16.23647018767980299, -23.86072634112229807, -80.28837282723650048 ) ) ;
#33511=EDGE_LOOP ( 'NONE', ( #1214, #4939, #33485, #40019 ) ) ;
#33517=CARTESIAN_POINT ( 'NONE',  ( 17.35001377175319703, -22.56339827118789998, -35.29201998310079347 ) ) ;
#33518=CARTESIAN_POINT ( 'NONE',  ( 22.79012786898881160, -13.80047699738691591, -44.76177760185372279 ) ) ;
#33520=ORIENTED_EDGE ( 'NONE', *, *, #30330, .T. ) ;
#33525=CARTESIAN_POINT ( 'NONE',  ( 7.936097814644250903, -16.49832144022300184, -80.47354794880769191 ) ) ;
#33540=CARTESIAN_POINT ( 'NONE',  ( 22.57606680859020187, -18.48699499001489954, -36.58626013956269674 ) ) ;
#33547=CARTESIAN_POINT ( 'NONE',  ( 8.836677506919789593, -14.11395979259429900, -78.13196779797900149 ) ) ;
#33551=CARTESIAN_POINT ( 'NONE',  ( 9.239619369984774622, -11.66024772074672633, -48.95806641941920390 ) ) ;
#33556=CARTESIAN_POINT ( 'NONE',  ( 13.61287798883271272, -9.318081818693075391, -61.83160618788794949 ) ) ;
#33559=CARTESIAN_POINT ( 'NONE',  ( 9.142468753586408425, -19.44231997591093375, -46.34810776502081353 ) ) ;
#33564=ORIENTED_EDGE ( 'NONE', *, *, #24161, .F. ) ;
#33574=CARTESIAN_POINT ( 'NONE',  ( 8.519820190432819018, -12.45265623424450041, -48.91767612604329685 ) ) ;
#33581=CARTESIAN_POINT ( 'NONE',  ( 20.27276998682100029, -21.81108673272580134, -42.54517385987409739 ) ) ;
#33582=CARTESIAN_POINT ( 'NONE',  ( 8.428805570490940369, -13.54562505507219505, -32.59100129534225943 ) ) ;
#33585=CYLINDRICAL_SURFACE ( 'NONE', #32338, 7.910999999999997812 ) ;
#33588=CARTESIAN_POINT ( 'NONE',  ( 24.01463920420174603, -14.90188333430748280, -61.47890500563420346 ) ) ;
#33589=VECTOR ( 'NONE', #28854, 1000.000000000000000 ) ;
#33590=CARTESIAN_POINT ( 'NONE',  ( 23.69903331857869944, -18.89521996265120052, -51.63785704165039192 ) ) ;
#33613=CARTESIAN_POINT ( 'NONE',  ( 22.90093737578363786, -14.73039410641558611, -48.41115546478060594 ) ) ;
#33618=CARTESIAN_POINT ( 'NONE',  ( 13.91520078321919840, -8.088981630189278960, -81.23899999999999011 ) ) ;
#33622=CARTESIAN_POINT ( 'NONE',  ( 14.06336448650593063, -23.32131646376723211, -80.09100261305252388 ) ) ;
#33623=ORIENTED_EDGE ( 'NONE', *, *, #47243, .T. ) ;
#33647=CARTESIAN_POINT ( 'NONE',  ( 13.70687704985900091, -8.153205208187619846, -68.68742111086849889 ) ) ;
#33654=B_SPLINE_CURVE_WITH_KNOTS ( 'NONE', 3,
 ( #27853, #48819, #43854, #4021, #20239, #20493, #16574, #51715, #16067, #15809, #32023, #31770, #19982, #35976, #95, #48048, #24154, #36229, #32277, #33332, #1635, #8989, #25977, #37016, #41991, #51012, #2803, #30812 ),
 .UNSPECIFIED., .F., .F.,
 ( 4, 2, 2, 2, 2, 2, 2, 2, 2, 2, 2, 2, 2, 4 ),
 ( 0.5000051609194220426, 0.5625045158044944538, 0.6250038706895668650, 0.6875032255746391652, 0.7187529030171753153, 0.7500025804597113543, 0.7812522579022473934, 0.8125019353447835435, 0.8437516127873195826, 0.8750012902298556217, 0.9062509676723917718, 0.9375006451149278108, 0.9687503225574638499, 1.000000000000000000 ),
 .UNSPECIFIED. ) ;
#33656=AXIS2_PLACEMENT_3D ( 'NONE', #21724, #20953, #780 ) ;
#33659=CARTESIAN_POINT ( 'NONE',  ( 14.06315214856010698, -7.911116337559645828, -59.20904473871448204 ) ) ;
#33661=CARTESIAN_POINT ( 'NONE',  ( 15.09828672688668760, -23.52717647678493051, -56.33401646506906246 ) ) ;
#33665=CARTESIAN_POINT ( 'NONE',  ( 23.17219357687709902, -13.17290339146140177, -58.96098648058299574 ) ) ;
#33668=CARTESIAN_POINT ( 'NONE',  ( 19.38808262899626556, -9.358945304425906997, -34.49983067246480317 ) ) ;
#33671=CARTESIAN_POINT ( 'NONE',  ( 8.428808952652845576, -17.68676381052137003, -62.42431570012554687 ) ) ;
#33673=CARTESIAN_POINT ( 'NONE',  ( 22.90060991778284816, -15.13913409275305888, -54.82474789397813453 ) ) ;
#33686=CARTESIAN_POINT ( 'NONE',  ( 22.84664585888298660, -16.49986012204790953, -72.49448347767508949 ) ) ;
#33689=CARTESIAN_POINT ( 'NONE',  ( 22.90093381512099668, -15.61618921778096336, -54.45281771551935890 ) ) ;
#33692=CARTESIAN_POINT ( 'NONE',  ( 24.03897853505547033, -15.94809715369253844, -49.52101926789728736 ) ) ;
#33696=CARTESIAN_POINT ( 'NONE',  ( 13.88388657071990018, -23.13443467540700027, -62.60505730950970360 ) ) ;
#33704=CARTESIAN_POINT ( 'NONE',  ( 11.95218966202808275, -21.29558555530721975, -33.54920349970121407 ) ) ;
#33717=CARTESIAN_POINT ( 'NONE',  ( 21.57348933224839982, -9.838876617649450651, -45.24807099536945287 ) ) ;
#33722=CARTESIAN_POINT ( 'NONE',  ( 9.706778812668741097, -18.52035693179009712, -65.71208951153059274 ) ) ;
#33727=CARTESIAN_POINT ( 'NONE',  ( 19.54196835879244531, -21.52907672520979787, -42.78615316578282801 ) ) ;
#33730=CARTESIAN_POINT ( 'NONE',  ( 17.98361080673300094, -8.810216054891400361, -76.03728780924510033 ) ) ;
#33733=CARTESIAN_POINT ( 'NONE',  ( 9.543023349596007066, -17.38728816782158759, -41.36946782366739939 ) ) ;
#33739=CARTESIAN_POINT ( 'NONE',  ( 8.222924952385369579, -14.97165744064022519, -38.53361264593338120 ) ) ;
#33740=CARTESIAN_POINT ( 'NONE',  ( 22.72481197475541848, -17.38742956073991763, -54.53615643352921438 ) ) ;
#33745=EDGE_CURVE ( 'NONE', #3035, #40977, #34961, .T. ) ;
#33752=ORIENTED_EDGE ( 'NONE', *, *, #36399, .F. ) ;
#33754=CARTESIAN_POINT ( 'NONE',  ( 23.04639156216936868, -11.67809813557746956, -33.62763753640791009 ) ) ;
#33755=CARTESIAN_POINT ( 'NONE',  ( 8.428888394969163755, -17.68705404388839142, -48.70899834144735507 ) ) ;
#33757=CARTESIAN_POINT ( 'NONE',  ( 17.16957720519042851, -7.705202128115011817, -57.04933462012610335 ) ) ;
#33760=CARTESIAN_POINT ( 'NONE',  ( 13.73097534871769909, -8.145411141615490180, -37.41343723127859278 ) ) ;
#33766=CARTESIAN_POINT ( 'NONE',  ( 22.90060573590868032, -14.60176553067577743, -78.79944796840196375 ) ) ;
#33770=CARTESIAN_POINT ( 'NONE',  ( 10.94780721248440081, -10.83637588594240064, -36.08420929373698982 ) ) ;
#33772=ORIENTED_EDGE ( 'NONE', *, *, #18678, .T. ) ;
#33777=CARTESIAN_POINT ( 'NONE',  ( 8.222962354643469141, -14.58045876702774457, -56.83399816310966912 ) ) ;
#33782=LINE ( 'NONE', #17306, #3169 ) ;
#33790=ADVANCED_FACE ( 'NONE', ( #13578 ), #730, .T. ) ;
#33794=CARTESIAN_POINT ( 'NONE',  ( 12.18644699963370037, -21.46083420798060004, -45.14190469443359888 ) ) ;
#33798=CARTESIAN_POINT ( 'NONE',  ( 8.223401571539490362, -15.61634053766229968, -58.50766849176299900 ) ) ;
#33801=CARTESIAN_POINT ( 'NONE',  ( 19.06740212538899826, -22.46465439540060061, -75.43852414181598931 ) ) ;
#33808=CARTESIAN_POINT ( 'NONE',  ( 18.18145487699519691, -23.32761325202299929, -76.20989520122053307 ) ) ;
#33810=CARTESIAN_POINT ( 'NONE',  ( 23.60352091122579665, -18.33564502225974024, -45.61878283607229179 ) ) ;
#33818=CARTESIAN_POINT ( 'NONE',  ( 12.63580666350229897, -21.74037383255939915, -53.51237412773319591 ) ) ;
#33826=CARTESIAN_POINT ( 'NONE',  ( 12.72001770753569971, -8.110999246539140728, -57.15644495665979719 ) ) ;
#33827=AXIS2_PLACEMENT_3D ( 'NONE', #35714, #28601, #44602 ) ;
#33830=ORIENTED_EDGE ( 'NONE', *, *, #13307, .F. ) ;
#33832=CARTESIAN_POINT ( 'NONE',  ( 8.758027518364150055, -14.56611882458369855, -41.27767096285609938 ) ) ;
#33833=CARTESIAN_POINT ( 'NONE',  ( 9.096695146297609114, -18.15749579477679987, -32.14999999999999858 ) ) ;
#33836=EDGE_CURVE ( 'NONE', #1209, #3482, #48617, .T. ) ;
#33839=CARTESIAN_POINT ( 'NONE',  ( 18.10834526513780318, -7.932589976104685192, -61.08772463901920702 ) ) ;
#33840=CARTESIAN_POINT ( 'NONE',  ( 9.166234375111990573, -11.20780655449969920, -50.68722986888699467 ) ) ;
#33861=CARTESIAN_POINT ( 'NONE',  ( 8.223247527389670353, -15.61637340300369914, -74.79233150823711185 ) ) ;
#33863=AXIS2_PLACEMENT_3D ( 'NONE', #20412, #43517, #35651 ) ;
#33867=ORIENTED_EDGE ( 'NONE', *, *, #32389, .T. ) ;
#33875=CARTESIAN_POINT ( 'NONE',  ( 17.16957703054396944, -23.52717578683977351, -79.96600284943940551 ) ) ;
#33881=CARTESIAN_POINT ( 'NONE',  ( 20.29256489975345445, -21.02754256757432927, -44.74450245125017744 ) ) ;
#33882=CARTESIAN_POINT ( 'NONE',  ( 23.83903722046451179, -13.54551130856877350, -63.42433666729781550 ) ) ;
#33890=CARTESIAN_POINT ( 'NONE',  ( 14.01384274612104264, -23.26046374906674785, -34.37835804628995362 ) ) ;
#33892=CARTESIAN_POINT ( 'NONE',  ( 22.90015331880489668, -15.72754863961103844, -50.45805598341791409 ) ) ;
#33894=CARTESIAN_POINT ( 'NONE',  ( 24.04493739769619864, -15.61618894467929941, -32.14999999999999858 ) ) ;
#33898=AXIS2_PLACEMENT_3D ( 'NONE', #17727, #22155, #26874 ) ;
#33902=CARTESIAN_POINT ( 'NONE',  ( 11.76256125941080022, -22.13368991060269764, -75.97556276872140302 ) ) ;
#33908=CARTESIAN_POINT ( 'NONE',  ( 20.11807775056638192, -22.52870672239707517, -36.12566301408477187 ) ) ;
#33910=CARTESIAN_POINT ( 'NONE',  ( 24.04461175216078317, -15.61617380819018663, -65.50766589912049653 ) ) ;
#33911=CARTESIAN_POINT ( 'NONE',  ( 8.222914298532977284, -14.58081029244737792, -58.83400626709403269 ) ) ;
#33919=CARTESIAN_POINT ( 'NONE',  ( 19.55131170787279871, -22.23647950948729957, -53.41566130612969943 ) ) ;
#33921=ORIENTED_EDGE ( 'NONE', *, *, #38169, .T. ) ;
#33925=CARTESIAN_POINT ( 'NONE',  ( 21.88292891939993368, -21.05125959484767151, -61.74872814468829318 ) ) ;
#33929=CARTESIAN_POINT ( 'NONE',  ( 9.801945429253240860, -18.38258714374390124, -81.23899999999999011 ) ) ;
#33939=EDGE_CURVE ( 'NONE', #13019, #5352, #19278, .T. ) ;
#33940=ORIENTED_EDGE ( 'NONE', *, *, #5435, .F. ) ;
#33941=CARTESIAN_POINT ( 'NONE',  ( 22.90078878137445173, -15.66463057220322064, -72.45510385531270003 ) ) ;
#33943=CARTESIAN_POINT ( 'NONE',  ( 22.90093739818529528, -14.73038881013940404, -54.41115656462039141 ) ) ;
#33945=CARTESIAN_POINT ( 'NONE',  ( 24.04493739803490371, -15.61633039186437699, -49.50767153938471665 ) ) ;
#33948=CARTESIAN_POINT ( 'NONE',  ( 23.92293678423830272, -14.65794255342009933, -77.97352993585168690 ) ) ;
#33967=CARTESIAN_POINT ( 'NONE',  ( 22.90103018812914115, -15.61618888866172483, -50.84718209631233066 ) ) ;
#33971=CARTESIAN_POINT ( 'NONE',  ( 9.807724164810522893, -20.47780537512590371, -46.58403036311962353 ) ) ;
#33973=ORIENTED_EDGE ( 'NONE', *, *, #3672, .T. ) ;
#33974=CARTESIAN_POINT ( 'NONE',  ( 22.81273049926999974, -13.34985227930480001, -74.74304765278330365 ) ) ;
#33982=CARTESIAN_POINT ( 'NONE',  ( 14.06462975631870016, -22.35863098146390016, -79.04760718966259958 ) ) ;
#33989=ORIENTED_EDGE ( 'NONE', *, *, #3923, .T. ) ;
#34004=EDGE_CURVE ( 'NONE', #41906, #12868, #27981, .T. ) ;
#34005=DIRECTION ( 'NONE',  ( 0.000000000000000000, 0.000000000000000000, -1.000000000000000000 ) ) ;
#34012=CARTESIAN_POINT ( 'NONE',  ( 24.04493320937934442, -15.61618918076996110, -53.79232900421944663 ) ) ;
#34013=DIRECTION ( 'NONE',  ( 0.000000000000000000, 0.000000000000000000, -1.000000000000000000 ) ) ;
#34014=CARTESIAN_POINT ( 'NONE',  ( 19.00161232051599924, -8.311177779142791877, -39.63156730105999515 ) ) ;
#34020=CARTESIAN_POINT ( 'NONE',  ( 19.54194862422452417, -9.703289362798095397, -78.11948479122949607 ) ) ;
#34021=CARTESIAN_POINT ( 'NONE',  ( 22.39003682439990328, -12.40129601987878338, -46.69594346447604494 ) ) ;
#34023=CARTESIAN_POINT ( 'NONE',  ( 16.89732681591289776, -22.62759363779219868, -41.31265874393579907 ) ) ;
#34025=ORIENTED_EDGE ( 'NONE', *, *, #35472, .T. ) ;
#34026=B_SPLINE_CURVE_WITH_KNOTS ( 'NONE', 3,
 ( #40525, #28979, #4102, #28713, #40015, #20079, #40272, #36319, #36847, #31866, #41043, #8040, #48391, #28195, #684, #430, #952, #48926 ),
 .UNSPECIFIED., .F., .F.,
 ( 4, 2, 2, 2, 2, 2, 2, 2, 4 ),
 ( 0.4999988359836951002, 0.5624989814857331849, 0.6249991269877712696, 0.6874992724898094654, 0.7499994179918475501, 0.8124995634938856348, 0.8749997089959238306, 0.9374998544979619153, 1.000000000000000000 ),
 .UNSPECIFIED. ) ;
#34032=AXIS2_PLACEMENT_3D ( 'NONE', #9471, #27623, #32755 ) ;
#34037=EDGE_CURVE ( 'NONE', #6190, #11854, #10469, .T. ) ;
#34038=CARTESIAN_POINT ( 'NONE',  ( 9.448786886202281465, -11.23620880982031700, -70.69263903080977229 ) ) ;
#34044=LINE ( 'NONE', #26185, #23505 ) ;
#34046=CARTESIAN_POINT ( 'NONE',  ( 11.70317949953529890, -10.12884503851570095, -49.73660269612349794 ) ) ;
#34051=CARTESIAN_POINT ( 'NONE',  ( 23.06214062797170072, -27.61618894467930119, -32.14999999999999858 ) ) ;
#34054=CARTESIAN_POINT ( 'NONE',  ( 19.27822296750359854, -8.861918991986240002, -76.70602703883389495 ) ) ;
#34061=CARTESIAN_POINT ( 'NONE',  ( 20.44176770790133801, -21.20055615980069774, -67.13803027069128859 ) ) ;
#34062=CARTESIAN_POINT ( 'NONE',  ( 12.03301697448477015, -10.16097117192421528, -61.74741793951960034 ) ) ;
#34072=CARTESIAN_POINT ( 'NONE',  ( 8.222953841603198200, -16.65185680590451156, -70.46600195478848150 ) ) ;
#34076=PRODUCT ( 'Height Adjustment Lead Screw', 'Height Adjustment Lead Screw', '', ( #24078 ) ) ;
#34080=CARTESIAN_POINT ( 'NONE',  ( 24.04476371970871540, -15.55956675530847200, -43.79004723472182548 ) ) ;
#34081=CARTESIAN_POINT ( 'NONE',  ( 24.32370634531909914, -16.57034021176809802, -53.82924985198769718 ) ) ;
#34082=CARTESIAN_POINT ( 'NONE',  ( 15.09850012911266681, -23.52720226237179801, -48.04933579400842092 ) ) ;
#34086=CARTESIAN_POINT ( 'NONE',  ( 10.88607800575399942, -20.90454082475969955, -46.98143399943669607 ) ) ;
#34087=CARTESIAN_POINT ( 'NONE',  ( 9.231882466319580871, -13.75394085457820026, -32.14999999999999858 ) ) ;
#34092=CARTESIAN_POINT ( 'NONE',  ( 9.384920991318070449, -20.35259034821490332, -64.31288601182949094 ) ) ;
#34101=CARTESIAN_POINT ( 'NONE',  ( 16.13393739769620083, -15.61618894467929941, -32.14999999999999858 ) ) ;
#34102=ORIENTED_EDGE ( 'NONE', *, *, #6646, .F. ) ;
#34107=CARTESIAN_POINT ( 'NONE',  ( 13.33295398203071080, -8.192918865366621617, -65.17746492593889229 ) ) ;
#34121=DIRECTION ( 'NONE',  ( 1.000000000000000000, 2.460964292799963328E-14, 0.000000000000000000 ) ) ;
#34126=CARTESIAN_POINT ( 'NONE',  ( 8.222872596472118545, -15.61638977992110000, -80.50766849176289952 ) ) ;
#34132=EDGE_CURVE ( 'NONE', #1287, #4643, #2530, .T. ) ;
#34136=CARTESIAN_POINT ( 'NONE',  ( 24.04154727951358339, -15.88190596389101117, -77.51834605307320203 ) ) ;
#34143=CARTESIAN_POINT ( 'NONE',  ( 24.03431982466308270, -16.03474806585207446, -33.80917298512384406 ) ) ;
#34155=CARTESIAN_POINT ( 'NONE',  ( 23.72175950820210133, -18.84228198835780077, -35.63563296679920001 ) ) ;
#34156=ORIENTED_EDGE ( 'NONE', *, *, #48433, .T. ) ;
#34161=CARTESIAN_POINT ( 'NONE',  ( 16.13393739769620083, -15.61618894467929941, -28.45282021618999835 ) ) ;
#34162=ADVANCED_FACE ( 'NONE', ( #11687 ), #23444, .T. ) ;
#34168=CARTESIAN_POINT ( 'NONE',  ( 20.29256161582522822, -21.02754519288219370, -78.74448466050279194 ) ) ;
#34170=CARTESIAN_POINT ( 'NONE',  ( 17.16939758333402466, -23.52720141142701848, -56.25068354753920374 ) ) ;
#34174=CARTESIAN_POINT ( 'NONE',  ( 13.25818560489270048, -22.48908833027550358, -57.69348358356519668 ) ) ;
#34181=CARTESIAN_POINT ( 'NONE',  ( 8.222921604359401115, -16.65161820214613186, -62.46599063383079198 ) ) ;
#34184=CARTESIAN_POINT ( 'NONE',  ( 10.07160187669169993, -18.84535597674730312, -81.23899999999999011 ) ) ;
#34195=CARTESIAN_POINT ( 'NONE',  ( 14.36271553927783096, -22.20706879767622866, -53.03615247297079094 ) ) ;
#34196=CARTESIAN_POINT ( 'NONE',  ( 22.04684627355322135, -12.20819253758295275, -54.28615617134685323 ) ) ;
#34202=CARTESIAN_POINT ( 'NONE',  ( 8.290410016103750834, -15.35962354207850034, -77.02290276308829675 ) ) ;
#34209=DIRECTION ( 'NONE',  ( 1.000000000000000000, 0.000000000000000000, 0.000000000000000000 ) ) ;
#34225=CARTESIAN_POINT ( 'NONE',  ( 16.05499536011143746, -8.563790251354252092, -50.34361688520657196 ) ) ;
#34229=CARTESIAN_POINT ( 'NONE',  ( 23.18576810717789982, -15.49684566140489927, -72.84179330725640966 ) ) ;
#34230=ORIENTED_EDGE ( 'NONE', *, *, #31076, .F. ) ;
#34233=CARTESIAN_POINT ( 'NONE',  ( 20.11812595995350250, -8.703699988156179401, -41.17433431193339288 ) ) ;
#34236=CARTESIAN_POINT ( 'NONE',  ( 12.49208382618429880, -9.576365995269719988, -77.78010429264477921 ) ) ;
#34245=AXIS2_PLACEMENT_3D ( 'NONE', #23969, #32350, #44175 ) ;
#34246=DIRECTION ( 'NONE',  ( 0.000000000000000000, 0.000000000000000000, -1.000000000000000000 ) ) ;
#34251=AXIS2_PLACEMENT_3D ( 'NONE', #13146, #25153, #21222 ) ;
#34257=CARTESIAN_POINT ( 'NONE',  ( 9.366940099211698012, -15.19984693586703628, -45.47240728461869708 ) ) ;
#34262=CARTESIAN_POINT ( 'NONE',  ( 19.63536038757005997, -8.499666568143982914, -33.43793342242106092 ) ) ;
#34265=CARTESIAN_POINT ( 'NONE',  ( 22.90108808520262329, -15.61618901356150069, -52.45282226904397049 ) ) ;
#34267=CARTESIAN_POINT ( 'NONE',  ( 17.80009649341840117, -23.28499989940520010, -46.44439537253119710 ) ) ;
#34276=CARTESIAN_POINT ( 'NONE',  ( 9.931764968075150080, -18.97410739629480148, -43.68922667584449471 ) ) ;
#34293=B_SPLINE_CURVE_WITH_KNOTS ( 'NONE', 3,
 ( #42426, #23496, #6516, #22990, #15153, #51056, #3362, #47139, #38485, #2585, #6781, #42941, #7039, #43450, #11227, #7552, #19336, #34265 ),
 .UNSPECIFIED., .F., .F.,
 ( 4, 2, 2, 2, 2, 2, 2, 2, 4 ),
 ( 0.000000000000000000, 0.06249983851711840566, 0.1249996770342368113, 0.1874995155513552170, 0.2499993540684736226, 0.3124991925855918895, 0.3749990311027102119, 0.4374988696198284788, 0.4999987081369468012 ),
 .UNSPECIFIED. ) ;
#34300=CARTESIAN_POINT ( 'NONE',  ( 14.84079903770737019, -7.738696850407225547, -70.95619825573045603 ) ) ;
#34307=CARTESIAN_POINT ( 'NONE',  ( 14.36278510963897048, -9.025291076946244218, -41.86948664301885970 ) ) ;
#34310=CARTESIAN_POINT ( 'NONE',  ( 9.524139214987918933, -18.07649922602429982, -41.33939600337990328 ) ) ;
#34316=CARTESIAN_POINT ( 'NONE',  ( 19.63503279775940058, -21.96029221563379963, -81.40635028194188294 ) ) ;
#34323=CARTESIAN_POINT ( 'NONE',  ( 14.06327912329211571, -7.911083529862108499, -45.20896163178147020 ) ) ;
#34324=CARTESIAN_POINT ( 'NONE',  ( 22.04686277055845167, -12.20822342221341827, -58.28615331364241570 ) ) ;
#34328=CARTESIAN_POINT ( 'NONE',  ( 22.51821868797902582, -17.99963233150277020, -32.56637983983515028 ) ) ;
#34339=CARTESIAN_POINT ( 'NONE',  ( 8.222915508880662472, -14.58080133695443870, -42.83400543223867629 ) ) ;
#34343=CARTESIAN_POINT ( 'NONE',  ( 23.10957479117670132, -11.22037240953919834, -67.61334385705760042 ) ) ;
#34344=EDGE_CURVE ( 'NONE', #10625, #1162, #320, .T. ) ;
#34347=VERTEX_POINT ( 'NONE', #28674 ) ;
#34349=CARTESIAN_POINT ( 'NONE',  ( 23.24368907943700080, -17.84287366172600287, -56.32926786494380167 ) ) ;
#34351=CARTESIAN_POINT ( 'NONE',  ( 8.860320911730040550, -16.94687217539350144, -32.14999999999999858 ) ) ;
#34353=CARTESIAN_POINT ( 'NONE',  ( 23.04647597310426832, -11.63208624730823182, -51.62566268846900641 ) ) ;
#34356=CARTESIAN_POINT ( 'NONE',  ( 24.16486509800989779, -17.48351885160749930, -65.58038890884739658 ) ) ;
#34371=CARTESIAN_POINT ( 'NONE',  ( 9.741321230546846621, -10.90463958868946648, -64.99459759734693876 ) ) ;
#34376=CARTESIAN_POINT ( 'NONE',  ( 22.90120720387987774, -15.61618909956830770, -56.84718059981966576 ) ) ;
#34385=CARTESIAN_POINT ( 'NONE',  ( 22.90113830400267148, -16.70047761723187918, -72.89819816215725723 ) ) ;
#34389=CARTESIAN_POINT ( 'NONE',  ( 9.449690553371750568, -17.28557240283720020, -47.76865470132936053 ) ) ;
#34400=FACE_OUTER_BOUND ( 'NONE', #30565, .T. ) ;
#34405=EDGE_CURVE ( 'NONE', #12296, #22390, #42402, .T. ) ;
#34408=CARTESIAN_POINT ( 'NONE',  ( 15.12341578682209686, -22.32525615540303221, -51.00040296984943211 ) ) ;
#34409=EDGE_CURVE ( 'NONE', #13535, #50973, #18629, .T. ) ;
#34421=CARTESIAN_POINT ( 'NONE',  ( 13.96079765809810169, -23.15702522818530085, -77.87681711424819753 ) ) ;
#34423=CARTESIAN_POINT ( 'NONE',  ( 9.366980835600751121, -15.61636285886159925, -47.84717978380999881 ) ) ;
#34430=CARTESIAN_POINT ( 'NONE',  ( 15.09844748716482599, -7.705181990897977506, -78.96600269184820320 ) ) ;
#34432=CARTESIAN_POINT ( 'NONE',  ( 24.04511355972104170, -15.61618909363076924, -51.79233356384455078 ) ) ;
#34444=CARTESIAN_POINT ( 'NONE',  ( 16.53341908198030197, -8.176625199252880449, -56.58441854867459853 ) ) ;
#34450=CARTESIAN_POINT ( 'NONE',  ( 22.90088226672064664, -16.00112289232146523, -74.86527751735805225 ) ) ;
#34464=CARTESIAN_POINT ( 'NONE',  ( 22.68450300562881239, -17.37076631674719351, -72.53614194588162434 ) ) ;
#34473=CARTESIAN_POINT ( 'NONE',  ( 23.43533467884909882, -18.49305274663100462, -78.13196779797910096 ) ) ;
#34476=CARTESIAN_POINT ( 'NONE',  ( 23.83903865928639476, -17.68685956421354177, -79.59100355860006459 ) ) ;
#34478=AXIS2_PLACEMENT_3D ( 'NONE', #47373, #43688, #19574 ) ;
#34484=CARTESIAN_POINT ( 'NONE',  ( 9.502098035746389115, -11.42030347669100010, -50.46706696623599697 ) ) ;
#34494=CARTESIAN_POINT ( 'NONE',  ( 22.02274569102419832, -11.87050655181369940, -32.14999999999999858 ) ) ;
#34497=CARTESIAN_POINT ( 'NONE',  ( 16.13393739769620083, -15.61618894467929941, -22.14999999999999858 ) ) ;
#34501=CARTESIAN_POINT ( 'NONE',  ( 9.089680483953220147, -15.96404481660830221, -69.83147392683879673 ) ) ;
#34508=EDGE_CURVE ( 'NONE', #18282, #26915, #25478, .T. ) ;
#34509=CARTESIAN_POINT ( 'NONE',  ( 21.59331255549819772, -20.08136325068349848, -76.67103925775420237 ) ) ;
#34512=CARTESIAN_POINT ( 'NONE',  ( 22.87920564048909000, -16.16927619967657392, -40.47885954242595119 ) ) ;
#34513=VERTEX_POINT ( 'NONE', #32190 ) ;
#34517=ORIENTED_EDGE ( 'NONE', *, *, #10538, .T. ) ;
#34519=AXIS2_PLACEMENT_3D ( 'NONE', #19065, #39003, #1352 ) ;
#34523=ORIENTED_EDGE ( 'NONE', *, *, #12523, .F. ) ;
#34539=CARTESIAN_POINT ( 'NONE',  ( 9.169509088546389464, -19.23329910588459768, -44.86001675125889676 ) ) ;
#34547=CARTESIAN_POINT ( 'NONE',  ( 21.74289213372750140, -11.34042165171269900, -44.63985384860789907 ) ) ;
#34552=CARTESIAN_POINT ( 'NONE',  ( 9.221480375469107926, -11.63194448996753927, -50.67433467055431606 ) ) ;
#34561=CARTESIAN_POINT ( 'NONE',  ( 9.221488231078874165, -19.60044682611274069, -58.62566479439444578 ) ) ;
#34562=CARTESIAN_POINT ( 'NONE',  ( 24.04283007690743545, -15.41892889378250864, -71.49973720589011350 ) ) ;
#34569=CARTESIAN_POINT ( 'NONE',  ( 11.97539538442253537, -10.20477106632094966, -41.74448671497020058 ) ) ;
#34572=CARTESIAN_POINT ( 'NONE',  ( 21.07660274011399792, -20.64735362191730061, -40.70564455487090072 ) ) ;
#34573=CARTESIAN_POINT ( 'NONE',  ( 9.366927619519092474, -16.50191557742974524, -77.41115605758611196 ) ) ;
#34578=ORIENTED_EDGE ( 'NONE', *, *, #44902, .T. ) ;
#34579=CARTESIAN_POINT ( 'NONE',  ( 23.66891508207319816, -13.42282091850420045, -33.19733999436689942 ) ) ;
#34586=CARTESIAN_POINT ( 'NONE',  ( 15.07403858729344037, -23.52396399615719247, -76.33491533744847857 ) ) ;
#34603=CARTESIAN_POINT ( 'NONE',  ( 24.04493740212382491, -14.58063858884763775, -69.75066784640594619 ) ) ;
#34605=CARTESIAN_POINT ( 'NONE',  ( 24.31016961241860130, -14.55225904714300000, -61.75114295834970335 ) ) ;
#34606=DIRECTION ( 'NONE',  ( 0.000000000000000000, 0.000000000000000000, -1.000000000000000000 ) ) ;
#34610=CARTESIAN_POINT ( 'NONE',  ( 11.83891062116510007, -9.528542536252919248, -55.53707855430759821 ) ) ;
#34611=CARTESIAN_POINT ( 'NONE',  ( 9.453617838139571461, -19.16200623842560091, -32.14999999999999858 ) ) ;
#34618=CARTESIAN_POINT ( 'NONE',  ( 21.17003102617220378, -22.14462533283520074, -67.79851897862869237 ) ) ;
#34630=CARTESIAN_POINT ( 'NONE',  ( 8.223251455316621161, -15.61600507739779786, -72.79233150823699816 ) ) ;
#34633=LINE ( 'NONE', #17886, #32411 ) ;
#34635=CARTESIAN_POINT ( 'NONE',  ( 22.90086341797264780, -15.61618933298137790, -46.45282805145726002 ) ) ;
#34639=DIRECTION ( 'NONE',  ( 0.9441240636101839723, 0.3295902797598760925, 0.000000000000000000 ) ) ;
#34642=CARTESIAN_POINT ( 'NONE',  ( 22.46009641123071532, -20.47787541989118409, -75.71601379394873277 ) ) ;
#34656=CARTESIAN_POINT ( 'NONE',  ( 8.223516320988901285, -15.61608250808600040, -78.50766849176299900 ) ) ;
#34657=CARTESIAN_POINT ( 'NONE',  ( 18.21836968370322296, -14.10176024214776547, -40.14999999999999858 ) ) ;
#34659=VERTEX_POINT ( 'NONE', #32441 ) ;
#34664=EDGE_CURVE ( 'NONE', #637, #1577, #4894, .T. ) ;
#34665=CARTESIAN_POINT ( 'NONE',  ( 11.13175947076070038, -22.17064819186600033, -34.49983067246459001 ) ) ;
#34667=AXIS2_PLACEMENT_3D ( 'NONE', #41229, #25739, #34121 ) ;
#34672=CARTESIAN_POINT ( 'NONE',  ( 20.95264282180487569, -20.36726231655321229, -46.70056344322360076 ) ) ;
#34680=CARTESIAN_POINT ( 'NONE',  ( 8.331257654656530676, -16.45580007440739934, -80.25338504615679369 ) ) ;
#34681=ORIENTED_EDGE ( 'NONE', *, *, #20937, .T. ) ;
#34687=FACE_OUTER_BOUND ( 'NONE', #49856, .T. ) ;
#34689=CARTESIAN_POINT ( 'NONE',  ( 22.46010630395649343, -20.47786184072016624, -36.00066267143122900 ) ) ;
#34702=VERTEX_POINT ( 'NONE', #13105 ) ;
#34704=CARTESIAN_POINT ( 'NONE',  ( 20.72562825268699882, -21.48330658714520069, -51.35596909847559743 ) ) ;
#34706=ORIENTED_EDGE ( 'NONE', *, *, #16874, .T. ) ;
#34710=CARTESIAN_POINT ( 'NONE',  ( 14.36277915339450928, -9.025292619810310057, -73.86948688777668792 ) ) ;
#34718=DIRECTION ( 'NONE',  ( 1.000000000000000000, 2.460964292799963328E-14, 0.000000000000000000 ) ) ;
#34721=ORIENTED_EDGE ( 'NONE', *, *, #27786, .F. ) ;
#34722=CARTESIAN_POINT ( 'NONE',  ( 18.20465886699604852, -7.911100698668976250, -63.37566613559571493 ) ) ;
#34730=CARTESIAN_POINT ( 'NONE',  ( 16.13393739769620083, -15.61618894467929941, -23.15000000000000213 ) ) ;
#34735=CARTESIAN_POINT ( 'NONE',  ( 18.19108902640490300, -22.36234980482461410, -39.25296653628198129 ) ) ;
#34737=CARTESIAN_POINT ( 'NONE',  ( 8.807536104933550547, -18.42876646016020104, -56.17083000281660077 ) ) ;
#34747=CYLINDRICAL_SURFACE ( 'NONE', #10326, 6.766999999999998572 ) ;
#34755=CARTESIAN_POINT ( 'NONE',  ( 18.20459011730063636, -7.911081268728054283, -71.37565166824786900 ) ) ;
#34758=CARTESIAN_POINT ( 'NONE',  ( 15.93498023681340037, -22.66622264832809819, -69.35616034045719402 ) ) ;
#34760=ORIENTED_EDGE ( 'NONE', *, *, #48497, .T. ) ;
#34765=CARTESIAN_POINT ( 'NONE',  ( 9.660248756158969385, -13.05489770709887232, -57.96762872684301726 ) ) ;
#34766=CARTESIAN_POINT ( 'NONE',  ( 16.34294028551579814, -22.66593182482080238, -79.33774565447309612 ) ) ;
#34768=CARTESIAN_POINT ( 'NONE',  ( 11.27236649766430077, -9.289942694860799932, -67.08399747395723978 ) ) ;
#34771=DIRECTION ( 'NONE',  ( 0.000000000000000000, 0.000000000000000000, 1.000000000000000000 ) ) ;
#34776=CARTESIAN_POINT ( 'NONE',  ( 15.09832557892497462, -7.705196720676832811, -39.25065852084387075 ) ) ;
#34785=CARTESIAN_POINT ( 'NONE',  ( 22.90093562328744170, -15.61111289037969563, -46.45258946822546875 ) ) ;
#34792=CARTESIAN_POINT ( 'NONE',  ( 17.30144337755940143, -22.57172551362165436, -51.29424405796996211 ) ) ;
#34797=CARTESIAN_POINT ( 'NONE',  ( 22.97746258194329982, -11.77523715584399966, -41.84969737084139751 ) ) ;
#34801=CARTESIAN_POINT ( 'NONE',  ( 21.21177448403727794, -10.72148469424713468, -64.60302447664658132 ) ) ;
#34803=CARTESIAN_POINT ( 'NONE',  ( 15.24817962068161670, -8.849184057285455651, -77.91115211152967390 ) ) ;
#34806=CARTESIAN_POINT ( 'NONE',  ( 10.68011837214289983, -11.14422995437500141, -46.06579460775299140 ) ) ;
#34812=CARTESIAN_POINT ( 'NONE',  ( 11.27236702745989305, -9.289942295366476088, -57.08399809234570199 ) ) ;
#34820=CARTESIAN_POINT ( 'NONE',  ( 20.99565695329222947, -21.94232104174841780, -58.08399797440581125 ) ) ;
#34833=CARTESIAN_POINT ( 'NONE',  ( 10.59069679657289953, -19.97681302096509981, -43.24065034890669068 ) ) ;
#34840=CARTESIAN_POINT ( 'NONE',  ( 11.75167936957159931, -21.86538255309680068, -31.98264971805809509 ) ) ;
#34841=VERTEX_POINT ( 'NONE', #35043 ) ;
#34845=CARTESIAN_POINT ( 'NONE',  ( 18.20454585312310058, -23.32130913405535821, -40.20901186456822529 ) ) ;
#34853=AXIS2_PLACEMENT_3D ( 'NONE', #9829, #45996, #25782 ) ;
#34854=CARTESIAN_POINT ( 'NONE',  ( 20.06281976506910070, -10.10654536788180025, -32.14999999999999858 ) ) ;
#34855=ORIENTED_EDGE ( 'NONE', *, *, #36672, .F. ) ;
#34864=CARTESIAN_POINT ( 'NONE',  ( 8.220228225067870653, -17.93047656444329974, -62.70177013111309350 ) ) ;
#34865=LINE ( 'NONE', #10781, #41388 ) ;
#34871=CARTESIAN_POINT ( 'NONE',  ( 22.70391683925680226, -19.12931631820509892, -58.38896007259789656 ) ) ;
#34874=CARTESIAN_POINT ( 'NONE',  ( 9.718208567743850779, -12.68094353378160122, -32.14999999999999858 ) ) ;
#34882=CARTESIAN_POINT ( 'NONE',  ( 24.29065960009049974, -14.41177887250970002, -61.46100449353919259 ) ) ;
#34883=CARTESIAN_POINT ( 'NONE',  ( 19.55461702279360026, -22.74941205225439944, -32.14999999999999858 ) ) ;
#34888=DIRECTION ( 'NONE',  ( 0.000000000000000000, 0.000000000000000000, -1.000000000000000000 ) ) ;
#34899=EDGE_CURVE ( 'NONE', #7417, #1209, #12973, .T. ) ;
#34900=CARTESIAN_POINT ( 'NONE',  ( 22.46011244405145746, -20.47785341715781371, -70.00066732382580881 ) ) ;
#34906=CARTESIAN_POINT ( 'NONE',  ( 17.16946523506752342, -23.52719174747369024, -75.96602405197781138 ) ) ;
#34915=CARTESIAN_POINT ( 'NONE',  ( 21.99623050575980798, -19.53742327708051008, -37.03483646650040129 ) ) ;
#34927=CARTESIAN_POINT ( 'NONE',  ( 14.58885284465669940, -7.517087735128769488, -33.23232777544669148 ) ) ;
#34929=CARTESIAN_POINT ( 'NONE',  ( 8.222678474964419948, -15.61600660124389961, -50.79233150823699816 ) ) ;
#34930=CARTESIAN_POINT ( 'NONE',  ( 22.77115846768018415, -16.96893195659617959, -50.51679219443402502 ) ) ;
#34932=CARTESIAN_POINT ( 'NONE',  ( 22.90112932213407149, -15.61618880384378905, -64.45281843961751633 ) ) ;
#34940=CARTESIAN_POINT ( 'NONE',  ( 22.96916380865210172, -11.00507187559370159, -35.31875724254479820 ) ) ;
#34955=CARTESIAN_POINT ( 'NONE',  ( 22.90093739769620029, -15.61618894467913243, -28.45282021618999835 ) ) ;
#34961=B_SPLINE_CURVE_WITH_KNOTS ( 'NONE', 3,
 ( #45288, #24825, #37673, #29787, #1775, #9129, #33727, #45546, #29033, #29287, #5709, #5463, #45808, #9641, #9895, #41604, #1519, #25851 ),
 .UNSPECIFIED., .F., .F.,
 ( 4, 2, 2, 2, 2, 2, 2, 2, 4 ),
 ( 0.4999997121946347378, 0.5624997481703053470, 0.6249997841459757897, 0.6874998201216464544, 0.7499998560973168971, 0.8124998920729877838, 0.8749999280486584485, 0.9374999640243293353, 1.000000000000000000 ),
 .UNSPECIFIED. ) ;
#34963=CARTESIAN_POINT ( 'NONE',  ( 13.82979338249550061, -8.531161443281989776, -68.46725820821738751 ) ) ;
#34970=DIRECTION ( 'NONE',  ( 0.000000000000000000, 0.000000000000000000, -1.000000000000000000 ) ) ;
#34981=CARTESIAN_POINT ( 'NONE',  ( 15.09838326309694878, -7.705189749657031406, -52.96600322570992603 ) ) ;
#34989=CARTESIAN_POINT ( 'NONE',  ( 22.90089492651413394, -15.59142452382446109, -40.45166006685596471 ) ) ;
#34996=CARTESIAN_POINT ( 'NONE',  ( 18.92684706093190172, -8.282267497309700133, -54.90332710579859565 ) ) ;
#35004=VECTOR ( 'NONE', #25952, 1000.000000000000000 ) ;
#35007=CARTESIAN_POINT ( 'NONE',  ( 9.367379825797401693, -15.61607429561870042, -45.84717978380999881 ) ) ;
#35015=CARTESIAN_POINT ( 'NONE',  ( 11.97361496584299978, -21.54889764946979724, -31.76248681540709384 ) ) ;
#35018=CARTESIAN_POINT ( 'NONE',  ( 15.09847197271365182, -23.52719885739764294, -58.04933470294202635 ) ) ;
#35023=CARTESIAN_POINT ( 'NONE',  ( 22.90115736359569354, -15.61618877121331295, -78.84717825834033533 ) ) ;
#35030=CARTESIAN_POINT ( 'NONE',  ( 16.13393739769620083, -15.61618894467929941, -28.45282021618999835 ) ) ;
#35031=CARTESIAN_POINT ( 'NONE',  ( 20.99558919860562867, -9.290002765462324064, -39.50066101904910454 ) ) ;
#35040=CARTESIAN_POINT ( 'NONE',  ( 9.366668810525878186, -15.61604052661200015, -35.45282021618999835 ) ) ;
#35043=CARTESIAN_POINT ( 'NONE',  ( 5.741632552282950108, -21.61618894467929763, -22.14999999999999858 ) ) ;
#35046=CARTESIAN_POINT ( 'NONE',  ( 20.99566233906968904, -21.94231674831827306, -48.08399959052492534 ) ) ;
#35051=CARTESIAN_POINT ( 'NONE',  ( 15.16589166249769960, -7.828401386832981146, -39.47312943893269477 ) ) ;
#35060=CARTESIAN_POINT ( 'NONE',  ( 23.18341189490050169, -15.39831630363000059, -40.83734515755419636 ) ) ;
#35062=EDGE_CURVE ( 'NONE', #15209, #47941, #427, .T. ) ;
#35068=CARTESIAN_POINT ( 'NONE',  ( 23.83903744840162275, -13.54551243526225868, -47.42433642958721407 ) ) ;
#35072=CARTESIAN_POINT ( 'NONE',  ( 16.42857207933229091, -7.682041846050376321, -65.01956441179268609 ) ) ;
#35084=CARTESIAN_POINT ( 'NONE',  ( 20.11812049527873825, -22.52868116577465685, -74.12566484944238709 ) ) ;
#35088=CARTESIAN_POINT ( 'NONE',  ( 19.53847090439890266, -9.439481869030970529, -52.11317062803219358 ) ) ;
#35095=CARTESIAN_POINT ( 'NONE',  ( 22.07392413299059797, -20.74486286528630075, -33.51421571862140070 ) ) ;
#35096=ORIENTED_EDGE ( 'NONE', *, *, #12958, .T. ) ;
#35097=CARTESIAN_POINT ( 'NONE',  ( 16.13393739769620083, -15.61618894467929941, -32.14999999999999858 ) ) ;
#35103=LINE ( 'NONE', #17014, #9926 ) ;
#35113=CARTESIAN_POINT ( 'NONE',  ( 10.70077573641860447, -9.799726819224163776, -48.76866075350059049 ) ) ;
#35114=ORIENTED_EDGE ( 'NONE', *, *, #13488, .T. ) ;
#35117=CARTESIAN_POINT ( 'NONE',  ( 22.90065884458136480, -15.61618680935524317, -64.84717769963093303 ) ) ;
#35119=CARTESIAN_POINT ( 'NONE',  ( 23.59510982153750192, -12.10711127132339904, -63.65239730387659023 ) ) ;
#35127=CARTESIAN_POINT ( 'NONE',  ( 14.36753390939369979, -8.378336188394568396, -59.65646296961590167 ) ) ;
#35131=CARTESIAN_POINT ( 'NONE',  ( 12.09004633843789911, -22.35834692618010067, -32.14999999999999858 ) ) ;
#35132=EDGE_CURVE ( 'NONE', #16605, #22390, #45452, .T. ) ;
#35133=DIRECTION ( 'NONE',  ( -0.4096086573010331855, 0.9122613374817791776, 0.000000000000000000 ) ) ;
#35138=CARTESIAN_POINT ( 'NONE',  ( 16.43585171025809899, -23.85582294485470101, -63.99601028757499677 ) ) ;
#35139=CARTESIAN_POINT ( 'NONE',  ( 22.37881013509309724, -19.99905837446409862, -32.14999999999999858 ) ) ;
#35150=CARTESIAN_POINT ( 'NONE',  ( 17.87699378894365054, -7.880242123305163382, -65.36294250950261642 ) ) ;
#35151=DIRECTION ( 'NONE',  ( 0.000000000000000000, 0.000000000000000000, -1.000000000000000000 ) ) ;
#35153=CARTESIAN_POINT ( 'NONE',  ( 20.92049246423509601, -21.32544322209390231, -78.51056856275720008 ) ) ;
#35168=CIRCLE ( 'NONE', #46069, 9.703299832284479010 ) ;
#35169=EDGE_CURVE ( 'NONE', #4288, #41372, #9809, .T. ) ;
#35171=CARTESIAN_POINT ( 'NONE',  ( 22.90119541241246637, -15.61618911972255930, -40.84718082130915207 ) ) ;
#35172=CARTESIAN_POINT ( 'NONE',  ( 19.31348261253770460, -9.577361911703928143, -66.10735234099374225 ) ) ;
#35180=CARTESIAN_POINT ( 'NONE',  ( 8.428814911140731780, -17.68678876403731692, -78.42431588342377324 ) ) ;
#35182=DIRECTION ( 'NONE',  ( 0.000000000000000000, 0.000000000000000000, -1.000000000000000000 ) ) ;
#35183=EDGE_LOOP ( 'NONE', ( #10803, #38407, #24753 ) ) ;
#35184=CARTESIAN_POINT ( 'NONE',  ( 16.38388870865558289, -22.42468798131612928, -80.94130156388325759 ) ) ;
#35194=CARTESIAN_POINT ( 'NONE',  ( 10.72262724756561880, -11.45750590540933800, -63.66115401167630949 ) ) ;
#35196=CARTESIAN_POINT ( 'NONE',  ( 21.54528678323437063, -19.77482129041136005, -36.66115137938106727 ) ) ;
#35199=FACE_OUTER_BOUND ( 'NONE', #25233, .T. ) ;
#35205=CARTESIAN_POINT ( 'NONE',  ( 22.37474952699549746, -21.00460003670480091, -33.73437862127239839 ) ) ;
#35225=CARTESIAN_POINT ( 'NONE',  ( 22.09038143216230310, -11.14098293795579941, -60.86224082610989683 ) ) ;
#35226=CARTESIAN_POINT ( 'NONE',  ( 20.11809238705456693, -8.703679916704407660, -77.45899608327597718 ) ) ;
#35233=CARTESIAN_POINT ( 'NONE',  ( 9.754056310848479683, -11.79350258725770040, -81.23899999999999011 ) ) ;
#35242=CARTESIAN_POINT ( 'NONE',  ( 22.36170331077510198, -10.91435426618479987, -81.23899999999999011 ) ) ;
#35248=ORIENTED_EDGE ( 'NONE', *, *, #6203, .F. ) ;
#35250=CARTESIAN_POINT ( 'NONE',  ( 20.99561365428662896, -9.290022285047772499, -53.21600398968095647 ) ) ;
#35260=CYLINDRICAL_SURFACE ( 'NONE', #23003, 6.766999999999998572 ) ;
#35261=EDGE_CURVE ( 'NONE', #33306, #23870, #46498, .T. ) ;
#35265=CARTESIAN_POINT ( 'NONE',  ( 21.16241148139313921, -20.56159161423454051, -39.09452867415468802 ) ) ;
#35266=CARTESIAN_POINT ( 'NONE',  ( 23.68405699770680073, -13.47552498022369960, -49.19956406921799186 ) ) ;
#35267=ORIENTED_EDGE ( 'NONE', *, *, #23382, .T. ) ;
#35268=FACE_OUTER_BOUND ( 'NONE', #15620, .T. ) ;
#35276=CARTESIAN_POINT ( 'NONE',  ( 20.83141696938240273, -20.87701063411540048, -45.11516743498959414 ) ) ;
#35281=CARTESIAN_POINT ( 'NONE',  ( 23.04647360858802330, -19.60029606439469774, -37.67433763517301770 ) ) ;
#35282=CARTESIAN_POINT ( 'NONE',  ( 14.06320080711358855, -7.911103808508573643, -71.20898408184140749 ) ) ;
#35284=CARTESIAN_POINT ( 'NONE',  ( 19.68346084944639784, -21.71073103174810015, -79.17930779234599470 ) ) ;
#35293=CARTESIAN_POINT ( 'NONE',  ( 8.428886018646599254, -13.54533248524384881, -66.87566464129990607 ) ) ;
#35297=ORIENTED_EDGE ( 'NONE', *, *, #42745, .T. ) ;
#35300=CARTESIAN_POINT ( 'NONE',  ( 22.90092760148217010, -15.98535187056947926, -58.86453566420338035 ) ) ;
#35306=CARTESIAN_POINT ( 'NONE',  ( 24.01953169521327425, -16.26277958825795977, -55.53370651648724987 ) ) ;
#35308=DIRECTION ( 'NONE',  ( 0.000000000000000000, 0.000000000000000000, -1.000000000000000000 ) ) ;
#35309=CARTESIAN_POINT ( 'NONE',  ( 22.15000760687365045, -12.45670961578212044, -46.29898909444737853 ) ) ;
#35312=DIRECTION ( 'NONE',  ( 0.000000000000000000, 0.000000000000000000, 1.000000000000000000 ) ) ;
#35313=AXIS2_PLACEMENT_3D ( 'NONE', #35097, #18340, #38798 ) ;
#35314=EDGE_LOOP ( 'NONE', ( #41751, #29409, #32697, #49680 ) ) ;
#35317=CARTESIAN_POINT ( 'NONE',  ( 13.83887629743938952, -22.28516590677773124, -51.45268192009724828 ) ) ;
#35320=CARTESIAN_POINT ( 'NONE',  ( 21.59441065045999864, -21.25267538992449801, -56.26754282442009725 ) ) ;
#35324=CARTESIAN_POINT ( 'NONE',  ( 9.750628328246584431, -12.76251341456665500, -63.98138790073967641 ) ) ;
#35328=CARTESIAN_POINT ( 'NONE',  ( 19.43172305938700006, -9.381835016324110654, -50.50205474731569666 ) ) ;
#35329=CARTESIAN_POINT ( 'NONE',  ( 17.90512765755580205, -9.025299540750683747, -44.03612187393183319 ) ) ;
#35333=CARTESIAN_POINT ( 'NONE',  ( 8.222546438703959737, -15.61603098320130201, -50.50766849176299900 ) ) ;
#35335=CARTESIAN_POINT ( 'NONE',  ( 12.07188106636699843, -8.733914759373510250, -54.83830562705740874 ) ) ;
#35343=ORIENTED_EDGE ( 'NONE', *, *, #40931, .T. ) ;
#35346=VECTOR ( 'NONE', #5237, 1000.000000000000000 ) ;
#35352=CARTESIAN_POINT ( 'NONE',  ( 21.26150560491580066, -10.77360668136810062, -50.21191628250519301 ) ) ;
#35356=ORIENTED_EDGE ( 'NONE', *, *, #34405, .T. ) ;
#35358=CARTESIAN_POINT ( 'NONE',  ( 15.99127120266549973, -7.769763351723340428, -34.78171861563929923 ) ) ;
#35364=CARTESIAN_POINT ( 'NONE',  ( 17.16939511183450051, -23.52720176420199039, -40.25067858312961988 ) ) ;
#35366=EDGE_CURVE ( 'NONE', #27935, #26995, #31050, .T. ) ;
#35375=CARTESIAN_POINT ( 'NONE',  ( 15.29152898199282795, -7.731039397677363034, -76.97386002471692734 ) ) ;
#35378=CARTESIAN_POINT ( 'NONE',  ( 9.221377447920410475, -19.60025744400465086, -62.62566432458431365 ) ) ;
#35382=CARTESIAN_POINT ( 'NONE',  ( 9.274895627196098502, -11.04057247840179912, -66.97959240854859786 ) ) ;
#35383=CARTESIAN_POINT ( 'NONE',  ( 15.14368416393435801, -8.633212666080043007, -38.30233936351858404 ) ) ;
#35387=ORIENTED_EDGE ( 'NONE', *, *, #20780, .T. ) ;
#35390=CARTESIAN_POINT ( 'NONE',  ( 11.57272752930120063, -21.50703424409100251, -50.94238055261769915 ) ) ;
#35400=CARTESIAN_POINT ( 'NONE',  ( 16.63355634930200111, -7.386176696075330561, -73.02696842882760109 ) ) ;
#35401=CARTESIAN_POINT ( 'NONE',  ( 21.23861683953670365, -21.46253214949600263, -32.14999999999999858 ) ) ;
#35402=VECTOR ( 'NONE', #26041, 1000.000000000000000 ) ;
#35412=CARTESIAN_POINT ( 'NONE',  ( 9.586608879048261755, -20.10517931648513468, -66.60093937048264934 ) ) ;
#35415=CARTESIAN_POINT ( 'NONE',  ( 23.52796006295030296, -16.53003938695930231, -70.27179973214080633 ) ) ;
#35418=CARTESIAN_POINT ( 'NONE',  ( 14.06329888286234286, -23.32129947607171871, -70.37566614802058496 ) ) ;
#35424=CARTESIAN_POINT ( 'NONE',  ( 21.76696967735496457, -21.17076488492029540, -61.75542963454200418 ) ) ;
#35425=CARTESIAN_POINT ( 'NONE',  ( 9.221397583389689956, -11.63208602404207248, -36.95899869649823444 ) ) ;
#35426=CARTESIAN_POINT ( 'NONE',  ( 9.543082305263988374, -17.38750236223247470, -71.36948714414663186 ) ) ;
#35433=CARTESIAN_POINT ( 'NONE',  ( 10.66652299674349891, -20.07151597450609870, -41.62953446819029324 ) ) ;
#35435=CARTESIAN_POINT ( 'NONE',  ( 16.70953489029340844, -8.802035222471227272, -65.98000098515855427 ) ) ;
#35436=ORIENTED_EDGE ( 'NONE', *, *, #13707, .T. ) ;
#35439=CARTESIAN_POINT ( 'NONE',  ( 17.90524625539175929, -22.20704482888588061, -58.86948671774002406 ) ) ;
#35442=CARTESIAN_POINT ( 'NONE',  ( 20.44745845214795565, -22.25469778744673377, -77.82425224410800979 ) ) ;
#35449=CARTESIAN_POINT ( 'NONE',  ( 18.91168734512759997, -23.37936002268359914, -34.18295494821020242 ) ) ;
#35453=EDGE_CURVE ( 'NONE', #37534, #4707, #50608, .T. ) ;
#35457=CARTESIAN_POINT ( 'NONE',  ( 14.36273055480719485, -9.025305204108461155, -63.86948780716260643 ) ) ;
#35459=CARTESIAN_POINT ( 'NONE',  ( 17.69707065050570094, -7.925716785862018554, -69.57632324310809224 ) ) ;
#35462=CYLINDRICAL_SURFACE ( 'NONE', #39338, 7.910999999999997812 ) ;
#35468=ADVANCED_FACE ( 'NONE', ( #15543 ), #40670, .T. ) ;
#35469=CARTESIAN_POINT ( 'NONE',  ( 7.888783485131068751, -15.60363238914669992, -44.50815324592469580 ) ) ;
#35472=EDGE_CURVE ( 'NONE', #5521, #10190, #40928, .T. ) ;
#35493=CARTESIAN_POINT ( 'NONE',  ( 8.935742952634630143, -13.69455134371859906, -68.15038248396290044 ) ) ;
#35496=EDGE_LOOP ( 'NONE', ( #5046, #48787, #42557, #23231 ) ) ;
#35498=CARTESIAN_POINT ( 'NONE',  ( 12.03010629790625252, -21.02215419574001132, -35.15951470918400190 ) ) ;
#35501=CARTESIAN_POINT ( 'NONE',  ( 12.03971614317870120, -9.101958363581481137, -81.23899999999999011 ) ) ;
#35507=EDGE_LOOP ( 'NONE', ( #49172, #26271, #38033, #28983 ) ) ;
#35509=CARTESIAN_POINT ( 'NONE',  ( 21.67336050504559708, -10.00387830695770042, -81.23899999999999011 ) ) ;
#35517=VERTEX_POINT ( 'NONE', #45643 ) ;
#35523=DIRECTION ( 'NONE',  ( 1.071169953407190059E-15, 3.740764114965449782E-16, -1.000000000000000000 ) ) ;
#35529=CARTESIAN_POINT ( 'NONE',  ( 9.038446734346580413, -12.26346461519720066, -54.42801351941700005 ) ) ;
#35536=EDGE_CURVE ( 'NONE', #10825, #39256, #5455, .T. ) ;
#35540=CARTESIAN_POINT ( 'NONE',  ( 9.367802395840252316, -16.31250631742587132, -45.81442615037286004 ) ) ;
#35545=CARTESIAN_POINT ( 'NONE',  ( 9.221478158419834870, -19.60042960929790112, -38.34100232044492884 ) ) ;
#35548=CARTESIAN_POINT ( 'NONE',  ( 23.55285262543469926, -16.29911733182590083, -37.09656150702409860 ) ) ;
#35554=DIRECTION ( 'NONE',  ( 0.000000000000000000, 0.000000000000000000, 1.000000000000000000 ) ) ;
#35557=CARTESIAN_POINT ( 'NONE',  ( 2.277530937145189949, -15.61618894467929941, -24.14999999999999858 ) ) ;
#35562=AXIS2_PLACEMENT_3D ( 'NONE', #46175, #34606, #46434 ) ;
#35564=DIRECTION ( 'NONE',  ( 0.000000000000000000, 0.000000000000000000, -1.000000000000000000 ) ) ;
#35566=LINE ( 'NONE', #7275, #16020 ) ;
#35572=CARTESIAN_POINT ( 'NONE',  ( 18.16448196509431057, -8.861961676679264599, -32.44013846481051644 ) ) ;
#35582=CARTESIAN_POINT ( 'NONE',  ( 22.89179345042635561, -15.09430521664105207, -34.42831083698472128 ) ) ;
#35585=CARTESIAN_POINT ( 'NONE',  ( 10.49363452053940016, -10.15965789963630073, -53.25722344400259800 ) ) ;
#35592=CARTESIAN_POINT ( 'NONE',  ( 14.67229395948390014, -22.51591050674119998, -55.41362847326009700 ) ) ;
#35602=CARTESIAN_POINT ( 'NONE',  ( 11.27233469758729534, -9.289966755700637790, -46.79933556288879970 ) ) ;
#35605=CARTESIAN_POINT ( 'NONE',  ( 8.222913476524595922, -14.68340101419122767, -64.54520946242661239 ) ) ;
#35606=CARTESIAN_POINT ( 'NONE',  ( 9.367118387258660306, -15.61602127472129986, -41.45282021618999835 ) ) ;
#35616=DIRECTION ( 'NONE',  ( 5.675813951744191581E-32, -1.000000000000000000, -5.351958659602149705E-17 ) ) ;
#35619=CARTESIAN_POINT ( 'NONE',  ( 9.261484497740870125, -17.20110213931209842, -53.38067352504999263 ) ) ;
#35626=CARTESIAN_POINT ( 'NONE',  ( 11.08120865841010172, -21.62091045948539758, -40.01016806583820085 ) ) ;
#35634=CARTESIAN_POINT ( 'NONE',  ( 9.366937397696199596, -15.61618894467949836, -28.45282021618999835 ) ) ;
#35642=CARTESIAN_POINT ( 'NONE',  ( 24.04406723441278615, -15.74292296389717016, -43.79742354999311260 ) ) ;
#35644=CARTESIAN_POINT ( 'NONE',  ( 22.65454694203958041, -11.11335924479742232, -49.31532081587366889 ) ) ;
#35646=CARTESIAN_POINT ( 'NONE',  ( 17.16944623581769136, -23.52719446311581564, -62.25066316136566513 ) ) ;
#35650=CARTESIAN_POINT ( 'NONE',  ( 8.764411544466659265, -19.31386507361439797, -76.64430199831019763 ) ) ;
#35651=DIRECTION ( 'NONE',  ( 0.8889875008987390137, -0.4579314612972278375, 0.000000000000000000 ) ) ;
#35654=EDGE_LOOP ( 'NONE', ( #2287, #41187, #8562, #25806 ) ) ;
#35656=CARTESIAN_POINT ( 'NONE',  ( 21.93377459515039973, -20.29257454556510254, -60.44865228025199144 ) ) ;
#35668=CARTESIAN_POINT ( 'NONE',  ( 18.42842099012590040, -23.53566277524700112, -71.91790339393689635 ) ) ;
#35673=CARTESIAN_POINT ( 'NONE',  ( 17.90512446449194783, -9.025298638364542825, -60.03612613525060482 ) ) ;
#35683=CARTESIAN_POINT ( 'NONE',  ( 8.773421182200600299, -14.46315171779890107, -73.28211911255840505 ) ) ;
#35689=CARTESIAN_POINT ( 'NONE',  ( 22.89855976872829046, -15.80993452990232129, -40.46193658699167628 ) ) ;
#35690=EDGE_CURVE ( 'NONE', #42806, #31006, #34865, .T. ) ;
#35692=CARTESIAN_POINT ( 'NONE',  ( 9.807754884354935143, -10.75453309769691757, -37.00066549356353818 ) ) ;
#35707=CARTESIAN_POINT ( 'NONE',  ( 21.72379952060926911, -21.21416803257280037, -77.75789285207679313 ) ) ;
#35712=CARTESIAN_POINT ( 'NONE',  ( 18.18491397528629960, -7.630187746700939577, -43.37235095159000053 ) ) ;
#35714=CARTESIAN_POINT ( 'NONE',  ( 23.08393739769629960, -15.61618894467929941, -20.74999999999999289 ) ) ;
#35715=CARTESIAN_POINT ( 'NONE',  ( 24.04488077751907582, -15.64853513552632513, -49.79363160827950452 ) ) ;
#35718=CARTESIAN_POINT ( 'NONE',  ( 11.65110190134180002, -22.05753457305690191, -76.70602703883379547 ) ) ;
#35723=ADVANCED_FACE ( 'NONE', ( #14958 ), #27256, .T. ) ;
#35726=FACE_OUTER_BOUND ( 'NONE', #47895, .T. ) ;
#35728=CARTESIAN_POINT ( 'NONE',  ( 23.25356989242479955, -11.45763705141400202, -41.33939600337990328 ) ) ;
#35729=ORIENTED_EDGE ( 'NONE', *, *, #28140, .T. ) ;
#35739=CARTESIAN_POINT ( 'NONE',  ( 20.29261426253945899, -21.02750317140192493, -48.74448829848160614 ) ) ;
#35743=LINE ( 'NONE', #868, #28385 ) ;
#35746=CARTESIAN_POINT ( 'NONE',  ( 15.09829013782090179, -7.705200998933884549, -75.25071684570102093 ) ) ;
#35749=EDGE_CURVE ( 'NONE', #17972, #18282, #42957, .T. ) ;
#35750=CARTESIAN_POINT ( 'NONE',  ( 22.82027184960839961, -12.32991051224040113, -62.92193303376410540 ) ) ;
#35751=CARTESIAN_POINT ( 'NONE',  ( 23.83903868892194211, -13.54551848185154306, -41.42433399449730302 ) ) ;
#35753=ORIENTED_EDGE ( 'NONE', *, *, #37023, .T. ) ;
#35755=CARTESIAN_POINT ( 'NONE',  ( 9.366924169342379258, -16.21927461595470987, -35.42444116589499004 ) ) ;
#35758=CARTESIAN_POINT ( 'NONE',  ( 10.56495154625470079, -10.52090938289240007, -81.23899999999999011 ) ) ;
#35759=ORIENTED_EDGE ( 'NONE', *, *, #34344, .F. ) ;
#35764=CARTESIAN_POINT ( 'NONE',  ( 22.28740654554379930, -10.80186921573359982, -81.23899999999999011 ) ) ;
#35766=CARTESIAN_POINT ( 'NONE',  ( 8.222937397696199469, -15.61618894467929941, -32.14999999999999858 ) ) ;
#35771=ORIENTED_EDGE ( 'NONE', *, *, #21820, .F. ) ;
#35772=CARTESIAN_POINT ( 'NONE',  ( 9.807814359748768140, -10.75445678515254855, -63.00066530372220797 ) ) ;
#35786=CARTESIAN_POINT ( 'NONE',  ( 12.35809383743469958, -8.736526627994370742, -66.62772890321430452 ) ) ;
#35795=DIRECTION ( 'NONE',  ( 1.000000000000000000, 0.000000000000000000, 0.000000000000000000 ) ) ;
#35803=CARTESIAN_POINT ( 'NONE',  ( 22.99024908015519841, -18.53126775147510230, -35.19530716149729699 ) ) ;
#35815=VERTEX_POINT ( 'NONE', #2658 ) ;
#35817=VERTEX_POINT ( 'NONE', #50609 ) ;
#35823=VERTEX_POINT ( 'NONE', #10524 ) ;
#35827=CYLINDRICAL_SURFACE ( 'NONE', #16961, 7.910999999999997812 ) ;
#35837=CARTESIAN_POINT ( 'NONE',  ( 14.71722765695869839, -7.897401403745059945, -49.45471475294879582 ) ) ;
#35842=CARTESIAN_POINT ( 'NONE',  ( 22.90095859539430379, -15.61618916398383661, -38.45281773784812174 ) ) ;
#35844=CARTESIAN_POINT ( 'NONE',  ( 20.53618552854030099, -10.10594661162980046, -52.56174695496989102 ) ) ;
#35854=CARTESIAN_POINT ( 'NONE',  ( 8.513496274260603514, -13.18580911493815933, -54.60561559637670115 ) ) ;
#35855=CARTESIAN_POINT ( 'NONE',  ( 19.54188148977384643, -9.703249216854988646, -76.11946519189100968 ) ) ;
#35857=CARTESIAN_POINT ( 'NONE',  ( 10.43817627109141277, -10.06373200202189899, -64.75374759500355992 ) ) ;
#35869=CARTESIAN_POINT ( 'NONE',  ( 11.46379677190219937, -20.90129492582429904, -57.18318221610359586 ) ) ;
#35870=CARTESIAN_POINT ( 'NONE',  ( 8.223148984577919762, -15.61599292915740023, -40.79233150823699816 ) ) ;
#35874=CARTESIAN_POINT ( 'NONE',  ( 23.97713974386040192, -15.88250668781109809, -47.29830972369129682 ) ) ;
#35879=CARTESIAN_POINT ( 'NONE',  ( 20.99557161890594514, -21.94238916341829082, -40.08401076356010861 ) ) ;
#35882=CIRCLE ( 'NONE', #32516, 6.999999999999999112 ) ;
#35896=PRESENTATION_STYLE_ASSIGNMENT (( #43765 ) ) ;
#35900=CARTESIAN_POINT ( 'NONE',  ( 14.23508833078220093, -7.592655291916660332, -75.21836123916510530 ) ) ;
#35901=CARTESIAN_POINT ( 'NONE',  ( 21.45406565774166197, -10.98598436268488143, -38.61921508777308532 ) ) ;
#35904=CARTESIAN_POINT ( 'NONE',  ( 10.84925596614229981, -20.86774452109049705, -62.98365807428779561 ) ) ;
#35906=CARTESIAN_POINT ( 'NONE',  ( 9.901323237974340330, -20.02052287148769949, -32.14999999999999858 ) ) ;
#35909=EDGE_CURVE ( 'NONE', #39386, #667, #12882, .T. ) ;
#35914=CARTESIAN_POINT ( 'NONE',  ( 11.54117676686140115, -22.46376300392310199, -76.19572567137230124 ) ) ;
#35925=CARTESIAN_POINT ( 'NONE',  ( 8.933902816692604887, -18.95954763342607308, -66.65399573834119451 ) ) ;
#35927=CARTESIAN_POINT ( 'NONE',  ( 18.94916917498509790, -22.51409905175449921, -76.60931421723030610 ) ) ;
#35936=CARTESIAN_POINT ( 'NONE',  ( 11.97534166513855780, -21.02756618211127204, -71.16115446403824762 ) ) ;
#35942=CARTESIAN_POINT ( 'NONE',  ( 12.30296576684403931, -10.01166978920420370, -65.76193325973878245 ) ) ;
#35948=ORIENTED_EDGE ( 'NONE', *, *, #22386, .T. ) ;
#35949=CARTESIAN_POINT ( 'NONE',  ( 9.807698685860906096, -10.75460520716508839, -58.71597766615245462 ) ) ;
#35950=CARTESIAN_POINT ( 'NONE',  ( 11.45435236478304475, -10.68831163810841467, -49.71098155378554395 ) ) ;
#35960=CARTESIAN_POINT ( 'NONE',  ( 22.77612783160510190, -10.73110692943910038, -45.59048102137129632 ) ) ;
#35961=CARTESIAN_POINT ( 'NONE',  ( 23.04646376015080378, -19.60031448718766001, -67.67433282024596508 ) ) ;
#35963=CARTESIAN_POINT ( 'NONE',  ( 16.09564338120661020, -23.54783898205173287, -50.29378284779397745 ) ) ;
#35966=CARTESIAN_POINT ( 'NONE',  ( 23.32207194523900284, -13.65725674267400080, -34.14796716713039615 ) ) ;
#35972=CARTESIAN_POINT ( 'NONE',  ( 10.42770386432230012, -21.56779541449689930, -46.25096972932420414 ) ) ;
#35976=CARTESIAN_POINT ( 'NONE',  ( 19.85413879631180833, -22.62203224873998408, -39.85232524897160289 ) ) ;
#35977=CARTESIAN_POINT ( 'NONE',  ( 22.24871428180610167, -12.10163878397787407, -56.68113137028124271 ) ) ;
#35985=CARTESIAN_POINT ( 'NONE',  ( 19.54197644776506593, -21.52907189293042833, -48.78615488187620741 ) ) ;
#35990=CARTESIAN_POINT ( 'NONE',  ( 15.09842764044654118, -7.705184387498995591, -61.25066341985870366 ) ) ;
#35993=CARTESIAN_POINT ( 'NONE',  ( 18.20455060651569568, -7.911070096530949058, -75.37571502603971396 ) ) ;
#35994=CARTESIAN_POINT ( 'NONE',  ( 17.90515954968781287, -22.20706941336631601, -62.86948484627593814 ) ) ;
#35995=DIRECTION ( 'NONE',  ( 0.000000000000000000, 0.000000000000000000, -1.000000000000000000 ) ) ;
#35996=CARTESIAN_POINT ( 'NONE',  ( 15.09849723051076253, -7.705175977862010583, -72.96600150002632290 ) ) ;
#36001=CARTESIAN_POINT ( 'NONE',  ( 11.53903724180579893, -9.499211462746920631, -81.23899999999999011 ) ) ;
#36006=ADVANCED_FACE ( 'NONE', ( #19909 ), #16, .T. ) ;
#36009=CARTESIAN_POINT ( 'NONE',  ( 23.41817524370990000, -13.41780268114560037, -81.23899999999999011 ) ) ;
#36016=ORIENTED_EDGE ( 'NONE', *, *, #12958, .F. ) ;
#36017=CARTESIAN_POINT ( 'NONE',  ( 11.26840393093330128, -10.51039387845690065, -42.10484805457209490 ) ) ;
#36022=CARTESIAN_POINT ( 'NONE',  ( 9.366937397696199596, -15.61618894467949836, -28.45282021618999835 ) ) ;
#36028=CARTESIAN_POINT ( 'NONE',  ( 22.90092895423980224, -15.60382985759644292, -40.45224344630474178 ) ) ;
#36034=CARTESIAN_POINT ( 'NONE',  ( 9.270589976214530736, -11.81077039276889806, -60.44865228025189907 ) ) ;
#36042=EDGE_CURVE ( 'NONE', #586, #45208, #37846, .T. ) ;
#36052=CARTESIAN_POINT ( 'NONE',  ( 9.121577334681090221, -16.37075734277619787, -79.81305924085489778 ) ) ;
#36054=CARTESIAN_POINT ( 'NONE',  ( 20.29255783753004039, -21.02754820491093213, -76.74449668442458972 ) ) ;
#36062=CARTESIAN_POINT ( 'NONE',  ( 15.09835279927984963, -23.52718445968407224, -78.33399673690963994 ) ) ;
#36065=ORIENTED_EDGE ( 'NONE', *, *, #10588, .T. ) ;
#36068=EDGE_LOOP ( 'NONE', ( #49427, #41176, #34721 ) ) ;
#36081=CARTESIAN_POINT ( 'NONE',  ( 14.36277414553998000, -9.025293915162313496, -35.86948574067652373 ) ) ;
#36088=CARTESIAN_POINT ( 'NONE',  ( 22.90093739769620029, -15.61618894467913243, -28.45282021618999835 ) ) ;
#36089=CARTESIAN_POINT ( 'NONE',  ( 9.575251713171320844, -11.30685144534250064, -51.19753123634840364 ) ) ;
#36091=DIRECTION ( 'NONE',  ( 0.000000000000000000, 0.000000000000000000, -1.000000000000000000 ) ) ;
#36099=CARTESIAN_POINT ( 'NONE',  ( 9.092282930800720919, -16.01325511460819939, -53.82924985198780377 ) ) ;
#36100=CARTESIAN_POINT ( 'NONE',  ( 14.06336169935696034, -7.911062148213927614, -41.20899793506684006 ) ) ;
#36106=CARTESIAN_POINT ( 'NONE',  ( 11.27226101419321402, -9.290022498966679976, -36.79933602528976877 ) ) ;
#36110=CARTESIAN_POINT ( 'NONE',  ( 21.54526339463619777, -11.45752448184413019, -76.24446912191029924 ) ) ;
#36114=CARTESIAN_POINT ( 'NONE',  ( 11.27228881102597136, -21.94237641914053683, -52.50066408798487316 ) ) ;
#36117=ORIENTED_EDGE ( 'NONE', *, *, #40810, .T. ) ;
#36124=CARTESIAN_POINT ( 'NONE',  ( 22.97503138632190200, -17.33141246813480052, -66.53101608161080094 ) ) ;
#36128=ORIENTED_EDGE ( 'NONE', *, *, #39861, .T. ) ;
#36129=CARTESIAN_POINT ( 'NONE',  ( 23.97791451297860021, -15.37376122739139994, -41.27767096285609938 ) ) ;
#36138=DIRECTION ( 'NONE',  ( 0.000000000000000000, 0.000000000000000000, -1.000000000000000000 ) ) ;
#36142=CARTESIAN_POINT ( 'NONE',  ( 12.14971266001781380, -8.703718556933592865, -74.84097244948981142 ) ) ;
#36144=DIRECTION ( 'NONE',  ( 1.000000000000000000, 2.460964292799963328E-14, 0.000000000000000000 ) ) ;
#36146=CARTESIAN_POINT ( 'NONE',  ( 24.04472027134544021, -15.61619704117925522, -43.79232540400376905 ) ) ;
#36148=CARTESIAN_POINT ( 'NONE',  ( 8.222911833873924436, -14.62160878757158500, -48.54769499149303869 ) ) ;
#36149=ORIENTED_EDGE ( 'NONE', *, *, #32037, .T. ) ;
#36150=CARTESIAN_POINT ( 'NONE',  ( 9.807731639197928786, -20.47781496564226700, -62.58399752867111232 ) ) ;
#36154=CARTESIAN_POINT ( 'NONE',  ( 22.84106276893500009, -20.41172742439350074, -69.98991178896608290 ) ) ;
#36158=CARTESIAN_POINT ( 'NONE',  ( 13.53986639234880052, -22.60027724769790325, -68.84585897299571400 ) ) ;
#36159=CARTESIAN_POINT ( 'NONE',  ( 8.222937397696199469, -15.61618894467929941, -32.14999999999999858 ) ) ;
#36164=AXIS2_PLACEMENT_3D ( 'NONE', #35030, #11210, #43433 ) ;
#36166=CARTESIAN_POINT ( 'NONE',  ( 13.85074091091579973, -23.53892423692099811, -78.09698001689919522 ) ) ;
#36169=FACE_OUTER_BOUND ( 'NONE', #20025, .T. ) ;
#36173=CARTESIAN_POINT ( 'NONE',  ( 9.807825181025211947, -10.75444290033733452, -78.71600221907445416 ) ) ;
#36179=CARTESIAN_POINT ( 'NONE',  ( 22.46007903505417502, -20.47789928629981304, -72.00068286951631080 ) ) ;
#36181=CARTESIAN_POINT ( 'NONE',  ( 12.28685844389720039, -9.236010473171079482, -77.55994138999389520 ) ) ;
#36198=ORIENTED_EDGE ( 'NONE', *, *, #21264, .T. ) ;
#36203=CARTESIAN_POINT ( 'NONE',  ( 11.27217187505504725, -9.290089935112355590, -58.79930474092849124 ) ) ;
#36210=CARTESIAN_POINT ( 'NONE',  ( 20.08011741788975613, -22.53811379943914872, -65.84286859354855892 ) ) ;
#36211=CARTESIAN_POINT ( 'NONE',  ( 10.54937000320200013, -9.550273756326699726, -43.05547522733549926 ) ) ;
#36217=CARTESIAN_POINT ( 'NONE',  ( 14.73780803183720067, -8.297888458486630370, -33.67265358074869397 ) ) ;
#36220=CARTESIAN_POINT ( 'NONE',  ( 23.76270136862467908, -17.78029879744761388, -59.88032873326731931 ) ) ;
#36224=CARTESIAN_POINT ( 'NONE',  ( 8.030996740944530643, -17.14100808875369708, -42.44846103827049433 ) ) ;
#36225=ORIENTED_EDGE ( 'NONE', *, *, #38637, .T. ) ;
#36229=CARTESIAN_POINT ( 'NONE',  ( 16.00113812002476621, -23.55770649663861604, -40.01306273174144224 ) ) ;
#36249=CARTESIAN_POINT ( 'NONE',  ( 12.14992344158154935, -8.703599321502185404, -72.84100158868179165 ) ) ;
#36254=CARTESIAN_POINT ( 'NONE',  ( 22.90093740082441798, -15.61701879830229700, -34.45285756426908819 ) ) ;
#36255=CARTESIAN_POINT ( 'NONE',  ( 10.21207254689429966, -11.00732563776159978, -81.23899999999999011 ) ) ;
#36259=ORIENTED_EDGE ( 'NONE', *, *, #31513, .F. ) ;
#36262=ORIENTED_EDGE ( 'NONE', *, *, #4303, .F. ) ;
#36264=CARTESIAN_POINT ( 'NONE',  ( 18.38973105523400164, -21.99613282959019500, -81.23899999999999011 ) ) ;
#36265=CARTESIAN_POINT ( 'NONE',  ( 8.428869108528790122, -13.54539397395445022, -62.59100196226616220 ) ) ;
#36266=CARTESIAN_POINT ( 'NONE',  ( 20.11812032201747868, -8.703696620057041144, -73.45899818277568727 ) ) ;
#36276=AXIS2_PLACEMENT_3D ( 'NONE', #10827, #15530, #51179 ) ;
#36283=CARTESIAN_POINT ( 'NONE',  ( 10.10036780576549909, -10.59794361762400072, -62.50834448790610054 ) ) ;
#36284=ORIENTED_EDGE ( 'NONE', *, *, #2891, .T. ) ;
#36301=CARTESIAN_POINT ( 'NONE',  ( 23.58066320393950122, -15.38603876551069938, -41.05750806020520116 ) ) ;
#36302=CARTESIAN_POINT ( 'NONE',  ( 17.90515509213406631, -22.20707059168299935, -76.86949976336627799 ) ) ;
#36315=VERTEX_POINT ( 'NONE', #25569 ) ;
#36318=DIRECTION ( 'NONE',  ( 1.000000000000000000, 2.460964292799963328E-14, 0.000000000000000000 ) ) ;
#36319=CARTESIAN_POINT ( 'NONE',  ( 18.20465248542906878, -7.911098894993664032, -79.37566619958934666 ) ) ;
#36323=VERTEX_POINT ( 'NONE', #48677 ) ;
#36324=CARTESIAN_POINT ( 'NONE',  ( 9.807675336324628290, -20.47774281110765671, -56.29929133037190070 ) ) ;
#36325=CARTESIAN_POINT ( 'NONE',  ( 23.00624656684072988, -16.56722779529380674, -32.89035143740448319 ) ) ;
#36330=ORIENTED_EDGE ( 'NONE', *, *, #8613, .T. ) ;
#36333=CARTESIAN_POINT ( 'NONE',  ( 15.91507200766546148, -15.77520395844511292, -41.53556505950739819 ) ) ;
#36335=CARTESIAN_POINT ( 'NONE',  ( 23.41669115755540176, -12.69245071001490111, -53.89097489251149398 ) ) ;
#36345=CARTESIAN_POINT ( 'NONE',  ( 22.60505408289549933, -18.42104331184100019, -50.97736833369739884 ) ) ;
#36346=CARTESIAN_POINT ( 'NONE',  ( 8.223569788570660677, -15.61625877447020017, -68.79233150823709764 ) ) ;
#36355=CARTESIAN_POINT ( 'NONE',  ( 18.31496508388832822, -7.941593517220971066, -55.09610085757195463 ) ) ;
#36360=DIRECTION ( 'NONE',  ( 0.000000000000000000, 0.000000000000000000, 1.000000000000000000 ) ) ;
#36361=CARTESIAN_POINT ( 'NONE',  ( 12.14990264437689227, -22.52876680156642308, -74.17433492201509182 ) ) ;
#36364=ORIENTED_EDGE ( 'NONE', *, *, #35909, .T. ) ;
#36367=LINE ( 'NONE', #44242, #13671 ) ;
#36372=CARTESIAN_POINT ( 'NONE',  ( 16.22559063631150167, -8.563944026890579764, -67.95695684075589327 ) ) ;
#36375=FACE_OUTER_BOUND ( 'NONE', #20831, .T. ) ;
#36379=ORIENTED_EDGE ( 'NONE', *, *, #8675, .T. ) ;
#36385=DIRECTION ( 'NONE',  ( 0.000000000000000000, 0.000000000000000000, -1.000000000000000000 ) ) ;
#36389=CARTESIAN_POINT ( 'NONE',  ( 20.11806024363774625, -22.52871719054864386, -59.84102336720449955 ) ) ;
#36390=CARTESIAN_POINT ( 'NONE',  ( 24.04492193170107939, -15.63426495621359358, -43.79305225079668418 ) ) ;
#36392=CARTESIAN_POINT ( 'NONE',  ( 9.807770915243924748, -20.47786536020769077, -44.29935507129472683 ) ) ;
#36394=B_SPLINE_CURVE_WITH_KNOTS ( 'NONE', 3,
 ( #12921, #28875, #26235, #34353, #5572, #13942, #17618, #42241, #22038, #45653, #18377, #30169, #41981, #50100, #38574, #10272, #2393, #22300 ),
 .UNSPECIFIED., .F., .F.,
 ( 4, 2, 2, 2, 2, 2, 2, 2, 4 ),
 ( 0.5000012918607925627, 0.5625011303781934924, 0.6250009688955943110, 0.6875008074129951297, 0.7500006459303960593, 0.8125004844477969890, 0.8750003229651980297, 0.9375001614825990703, 1.000000000000000000 ),
 .UNSPECIFIED. ) ;
#36399=EDGE_CURVE ( 'NONE', #32624, #1526, #24793, .T. ) ;
#36400=CARTESIAN_POINT ( 'NONE',  ( 12.77254040467190066, -8.087329116576368548, -73.15866903151089673 ) ) ;
#36408=CARTESIAN_POINT ( 'NONE',  ( 22.46248482608730157, -19.54762395644669937, -64.40959883343299452 ) ) ;
#36409=DIRECTION ( 'NONE',  ( 0.000000000000000000, 0.000000000000000000, 1.000000000000000000 ) ) ;
#36417=CARTESIAN_POINT ( 'NONE',  ( 19.61369162610559869, -8.141295552874010966, -77.14635284413580507 ) ) ;
#36429=CARTESIAN_POINT ( 'NONE',  ( 9.221335198055678362, -19.60018521617414322, -72.62567728624490826 ) ) ;
#36431=CARTESIAN_POINT ( 'NONE',  ( 9.325642639948160451, -13.77508026015089904, -37.53688731232609399 ) ) ;
#36443=CARTESIAN_POINT ( 'NONE',  ( 20.29259189943645580, -21.02752101800459172, -70.74448910382146494 ) ) ;
#36448=CARTESIAN_POINT ( 'NONE',  ( 11.27214737950822077, -21.94226950413872146, -72.21594989029324552 ) ) ;
#36455=DIRECTION ( 'NONE',  ( 0.000000000000000000, 0.000000000000000000, -1.000000000000000000 ) ) ;
#36457=DIRECTION ( 'NONE',  ( -1.000000000000000000, 0.000000000000000000, 0.000000000000000000 ) ) ;
#36461=CARTESIAN_POINT ( 'NONE',  ( 24.04461175216078317, -15.61617380819018663, -65.50766589912049653 ) ) ;
#36462=EDGE_CURVE ( 'NONE', #41688, #36323, #16291, .T. ) ;
#36463=CARTESIAN_POINT ( 'NONE',  ( 8.406715080065760404, -18.49242873124940090, -40.67890729542689598 ) ) ;
#36469=VERTEX_POINT ( 'NONE', #2524 ) ;
#36470=CARTESIAN_POINT ( 'NONE',  ( 17.16956147491267615, -23.52717800495802791, -42.25066452978246190 ) ) ;
#36471=CARTESIAN_POINT ( 'NONE',  ( 13.40559671880919979, -8.258002636450779477, -79.39947069499679344 ) ) ;
#36479=CARTESIAN_POINT ( 'NONE',  ( 10.82531766377809923, -21.92501428935559815, -40.23033096848919854 ) ) ;
#36485=CARTESIAN_POINT ( 'NONE',  ( 9.807868667392284578, -20.47799079033555003, -64.58399863705557209 ) ) ;
#36498=CARTESIAN_POINT ( 'NONE',  ( 22.46011041234203987, -10.75452168438129164, -61.58399571921993498 ) ) ;
#36499=CARTESIAN_POINT ( 'NONE',  ( 8.222930619450961487, -15.61639179890759976, -64.50766849176299900 ) ) ;
#36502=DIRECTION ( 'NONE',  ( 1.000000000000000000, 0.000000000000000000, 0.000000000000000000 ) ) ;
#36507=CARTESIAN_POINT ( 'NONE',  ( 12.84391639521409978, -21.85461860611620111, -81.10729939731689342 ) ) ;
#36510=DIRECTION ( 'NONE',  ( 1.000000000000000000, 0.000000000000000000, 0.000000000000000000 ) ) ;
#36515=ORIENTED_EDGE ( 'NONE', *, *, #1221, .T. ) ;
#36519=ORIENTED_EDGE ( 'NONE', *, *, #31789, .T. ) ;
#36521=DIRECTION ( 'NONE',  ( 1.000000000000000000, 2.460964292799963328E-14, 0.000000000000000000 ) ) ;
#36522=CARTESIAN_POINT ( 'NONE',  ( 21.76556302292190281, -19.92121040802560117, -81.23899999999999011 ) ) ;
#36529=ADVANCED_FACE ( 'NONE', ( #18754 ), #22175, .T. ) ;
#36532=ADVANCED_FACE ( 'NONE', ( #14832 ), #17983, .T. ) ;
#36545=CARTESIAN_POINT ( 'NONE',  ( 23.54765475985599821, -13.04256444658469860, -59.18114938323410001 ) ) ;
#36549=CARTESIAN_POINT ( 'NONE',  ( 24.04513741079867017, -15.61618875311435417, -79.79232954107749265 ) ) ;
#36554=CARTESIAN_POINT ( 'NONE',  ( 8.222942234697445230, -16.65177182868387717, -36.75066472735249334 ) ) ;
#36560=CARTESIAN_POINT ( 'NONE',  ( 11.06214720078926739, -21.70954254531401872, -34.22858903880150905 ) ) ;
#36562=EDGE_LOOP ( 'NONE', ( #3376, #10433, #48177, #36117 ) ) ;
#36563=CARTESIAN_POINT ( 'NONE',  ( 20.39734384171130088, -9.506355900195050168, -46.76127109678569838 ) ) ;
#36571=CARTESIAN_POINT ( 'NONE',  ( 24.04493740182211425, -16.65173924940748051, -77.83399516818887776 ) ) ;
#36576=ORIENTED_EDGE ( 'NONE', *, *, #48613, .T. ) ;
#36592=CARTESIAN_POINT ( 'NONE',  ( 24.04492500195047455, -15.60001557533511019, -59.79167491129597067 ) ) ;
#36598=CARTESIAN_POINT ( 'NONE',  ( 8.222955699658124118, -16.65187040858989675, -54.46600195242484688 ) ) ;
#36599=CARTESIAN_POINT ( 'NONE',  ( 11.28616805192099903, -21.78756480114309824, -66.72444172481789337 ) ) ;
#36602=DIRECTION ( 'NONE',  ( 1.000000000000000000, 2.460964292799963328E-14, 0.000000000000000000 ) ) ;
#36607=ORIENTED_EDGE ( 'NONE', *, *, #13707, .F. ) ;
#36614=CARTESIAN_POINT ( 'NONE',  ( 22.81209844268250109, -13.20389820966570049, -32.14999999999999858 ) ) ;
#36624=CARTESIAN_POINT ( 'NONE',  ( 17.25281598583540088, -22.57971318743560118, -67.29646813280298545 ) ) ;
#36626=DIRECTION ( 'NONE',  ( 0.000000000000000000, 0.000000000000000000, -1.000000000000000000 ) ) ;
#36631=CARTESIAN_POINT ( 'NONE',  ( 9.083428079434199276, -15.43486864872139996, -61.46100449353919259 ) ) ;
#36634=CARTESIAN_POINT ( 'NONE',  ( 23.83903838438579115, -17.68686092435233803, -79.87566697560022533 ) ) ;
#36641=CARTESIAN_POINT ( 'NONE',  ( 16.13393739769620083, -15.61618894467929941, -32.14999999999999858 ) ) ;
#36659=CARTESIAN_POINT ( 'NONE',  ( 8.368826086083149818, -12.84386746725390083, -74.90148551491050455 ) ) ;
#36665=CARTESIAN_POINT ( 'NONE',  ( 17.90519802043555586, -22.20705845982418936, -36.86948528380446533 ) ) ;
#36666=CARTESIAN_POINT ( 'NONE',  ( 20.54387153675149946, -9.611259744901818891, -63.93428524705119287 ) ) ;
#36672=EDGE_CURVE ( 'NONE', #18872, #8034, #49081, .T. ) ;
#36682=CARTESIAN_POINT ( 'NONE',  ( 20.99564080419046164, -9.290043960182757132, -79.21600316462195224 ) ) ;
#36684=ORIENTED_EDGE ( 'NONE', *, *, #15359, .F. ) ;
#36686=VECTOR ( 'NONE', #11678, 1000.000000000000000 ) ;
#36687=ADVANCED_FACE ( 'NONE', ( #44155 ), #35260, .T. ) ;
#36691=CARTESIAN_POINT ( 'NONE',  ( 23.16503989757309867, -15.06287498962899996, -36.42782227743549583 ) ) ;
#36700=CARTESIAN_POINT ( 'NONE',  ( 23.12959127530770331, -18.17890647944599891, -61.17911655036449758 ) ) ;
#36717=CARTESIAN_POINT ( 'NONE',  ( 9.367097141674031846, -15.61601956221279863, -71.84717978381000592 ) ) ;
#36719=CARTESIAN_POINT ( 'NONE',  ( 9.922022971808480918, -12.84297312065496754, -49.58660389420793280 ) ) ;
#36724=CARTESIAN_POINT ( 'NONE',  ( 24.04493740857834538, -14.58064761262398790, -35.46599892844898250 ) ) ;
#36726=CARTESIAN_POINT ( 'NONE',  ( 19.35590054169199803, -23.20576558337710082, -44.16454026222609741 ) ) ;
#36727=CARTESIAN_POINT ( 'NONE',  ( 22.58446406675447449, -13.52685100215215641, -56.35316686890462989 ) ) ;
#36731=CARTESIAN_POINT ( 'NONE',  ( 20.66546011552009787, -21.52990145569759761, -36.52453509903889994 ) ) ;
#36736=CARTESIAN_POINT ( 'NONE',  ( 14.72050101380589915, -23.46848077975802127, -60.34919524473630048 ) ) ;
#36739=CARTESIAN_POINT ( 'NONE',  ( 10.11025315938129943, -9.986095792159350282, -52.74692207654089060 ) ) ;
#36756=CARTESIAN_POINT ( 'NONE',  ( 15.24822960659503046, -22.38319987333287031, -64.99448789959322426 ) ) ;
#36759=CARTESIAN_POINT ( 'NONE',  ( 17.19412305922981332, -22.35806894703990366, -66.90336922568695854 ) ) ;
#36764=CARTESIAN_POINT ( 'NONE',  ( 8.222963321015376081, -14.58045169080828707, -72.54933512887784275 ) ) ;
#36772=VECTOR ( 'NONE', #27352, 1000.000000000000000 ) ;
#36782=CARTESIAN_POINT ( 'NONE',  ( 22.58000039849400054, -18.80532364725490169, -81.23899999999999011 ) ) ;
#36791=CARTESIAN_POINT ( 'NONE',  ( 20.84741856749390365, -10.36969921949989981, -42.58016164095369760 ) ) ;
#36800=CARTESIAN_POINT ( 'NONE',  ( 9.221442925756241138, -19.60036937649121214, -68.62566444102958485 ) ) ;
#36808=CARTESIAN_POINT ( 'NONE',  ( 22.87033105319540027, -19.64207377926320319, -63.45897166066949069 ) ) ;
#36812=AXIS2_PLACEMENT_3D ( 'NONE', #40909, #28846, #44849 ) ;
#36818=( BOUNDED_CURVE ( )  B_SPLINE_CURVE ( 2, ( #39993, #20307, #51278 ),
 .UNSPECIFIED., .F., .T. ) 
 B_SPLINE_CURVE_WITH_KNOTS ( ( 3, 3 ),
 ( 2.168627590050209886, 3.232274745523169734 ),
 .UNSPECIFIED. ) 
 CURVE ( )  GEOMETRIC_REPRESENTATION_ITEM ( )  RATIONAL_B_SPLINE_CURVE ( ( 1.425426480542939967, 1.425426480542939967, 1.323085463760209857 ) ) 
 REPRESENTATION_ITEM ( '' )  );
#36823=CYLINDRICAL_SURFACE ( 'NONE', #28946, 7.910999999999997812 ) ;
#36827=CARTESIAN_POINT ( 'NONE',  ( 22.90012247355228325, -16.27786605360535077, -70.87830227662946925 ) ) ;
#36828=EDGE_CURVE ( 'NONE', #8412, #13106, #24710, .T. ) ;
#36830=CARTESIAN_POINT ( 'NONE',  ( 23.49301428767259736, -16.77837725375670175, -43.11720026785929605 ) ) ;
#36835=CARTESIAN_POINT ( 'NONE',  ( 12.89372882336123638, -8.399748356796177262, -81.15800232914327239 ) ) ;
#36837=CARTESIAN_POINT ( 'NONE',  ( 12.14976757460917867, -22.52869039637574033, -78.45899712908982337 ) ) ;
#36842=VERTEX_POINT ( 'NONE', #1169 ) ;
#36844=ORIENTED_EDGE ( 'NONE', *, *, #41852, .T. ) ;
#36847=CARTESIAN_POINT ( 'NONE',  ( 17.16951619896303782, -7.705193419797750742, -79.33399943592132786 ) ) ;
#36857=CARTESIAN_POINT ( 'NONE',  ( 17.16939711463305684, -23.52720157518136546, -55.96593682117922697 ) ) ;
#36864=CARTESIAN_POINT ( 'NONE',  ( 9.367491665984019278, -15.61623476897930018, -53.45282021618999124 ) ) ;
#36868=CARTESIAN_POINT ( 'NONE',  ( 21.93099174023785025, -19.12845236462728238, -46.62617237298687911 ) ) ;
#36870=CARTESIAN_POINT ( 'NONE',  ( 16.28635962228009859, -23.46243104246319788, -64.50631165503649811 ) ) ;
#36875=CYLINDRICAL_SURFACE ( 'NONE', #45461, 7.910999999999997812 ) ;
#36885=AXIS2_PLACEMENT_3D ( 'NONE', #22317, #35151, #43040 ) ;
#36886=CARTESIAN_POINT ( 'NONE',  ( 16.26610795940585774, -7.638794151532966481, -55.01276702998251977 ) ) ;
#36887=AXIS2_PLACEMENT_3D ( 'NONE', #26861, #10375, #34718 ) ;
#36888=CARTESIAN_POINT ( 'NONE',  ( 23.27131239030429910, -14.57976881098799815, -32.14999999999999858 ) ) ;
#36892=CARTESIAN_POINT ( 'NONE',  ( 24.04493738366187827, -16.65172975277582168, -73.54933447873786179 ) ) ;
#36897=CARTESIAN_POINT ( 'NONE',  ( 22.65185334536269934, -12.92187439852739850, -68.72240889194819147 ) ) ;
#36898=VERTEX_POINT ( 'NONE', #49908 ) ;
#36904=CARTESIAN_POINT ( 'NONE',  ( 10.29205353740080042, -19.56776478976249933, -65.26351318459290951 ) ) ;
#36909=ORIENTED_EDGE ( 'NONE', *, *, #32159, .T. ) ;
#36926=CARTESIAN_POINT ( 'NONE',  ( 10.22109382420207346, -12.20808149134441756, -67.61948648231498282 ) ) ;
#36933=CARTESIAN_POINT ( 'NONE',  ( 8.499441539007790425, -17.43311507835980123, -36.93812364489689770 ) ) ;
#36938=VERTEX_POINT ( 'NONE', #39847 ) ;
#36941=CARTESIAN_POINT ( 'NONE',  ( 9.367206039829609310, -15.61603166621950045, -73.45282021618999124 ) ) ;
#36962=CARTESIAN_POINT ( 'NONE',  ( 24.04380548879042223, -15.76082440701389054, -65.79815003220092251 ) ) ;
#36965=CARTESIAN_POINT ( 'NONE',  ( 9.294393911660149499, -12.66194776880280060, -81.36245008104749843 ) ) ;
#36971=ORIENTED_EDGE ( 'NONE', *, *, #37604, .F. ) ;
#36972=CARTESIAN_POINT ( 'NONE',  ( 17.06628174423480004, -8.224475449209380784, -78.60728138436078893 ) ) ;
#36991=CARTESIAN_POINT ( 'NONE',  ( 24.04475233726670780, -15.61618925176752271, -59.50766149565701113 ) ) ;
#36992=CARTESIAN_POINT ( 'NONE',  ( 16.13393739769620083, -15.61618894467929941, -23.15000000000000213 ) ) ;
#36998=CARTESIAN_POINT ( 'NONE',  ( 24.14537261347669883, -17.56545184108060198, -49.86830329880680068 ) ) ;
#36999=CARTESIAN_POINT ( 'NONE',  ( 17.27328981822006781, -8.887235580817069547, -56.00650926761637294 ) ) ;
#37002=CIRCLE ( 'NONE', #22763, 2.576499999999998902 ) ;
#37004=CARTESIAN_POINT ( 'NONE',  ( 17.51573946485870081, -8.295170104904951103, -37.79203799605679848 ) ) ;
#37006=CARTESIAN_POINT ( 'NONE',  ( 17.16941988147922160, -7.705179696712606940, -33.04933253539134341 ) ) ;
#37009=CARTESIAN_POINT ( 'NONE',  ( 23.93131328127537216, -16.97972217673644835, -59.84741592005993027 ) ) ;
#37010=B_SPLINE_CURVE_WITH_KNOTS ( 'NONE', 3,
 ( #40992, #48342, #48603, #36017, #11936, #16105, #36791, #28143, #20535, #28923 ),
 .UNSPECIFIED., .F., .F.,
 ( 4, 1, 1, 1, 1, 1, 1, 4 ),
 ( 0.000000000000000000, 0.04961520431741933690, 0.1288341353810688872, 0.2080530664447206579, 0.2872719975083702360, 0.3664909285720209242, 0.4457098596356703912, 0.4999963331327971772 ),
 .UNSPECIFIED. ) ;
#37012=CARTESIAN_POINT ( 'NONE',  ( 8.436496967347979492, -18.57120697004150145, -56.39099290546749899 ) ) ;
#37016=CARTESIAN_POINT ( 'NONE',  ( 9.637419681166790042, -20.21905395439925002, -40.31160479408269737 ) ) ;
#37019=CARTESIAN_POINT ( 'NONE',  ( 9.367509130462650546, -15.61619940421079988, -51.84717978381009118 ) ) ;
#37023=EDGE_CURVE ( 'NONE', #35823, #21743, #15998, .T. ) ;
#37034=CARTESIAN_POINT ( 'NONE',  ( 13.35882351263044221, -21.87618856300440839, -67.08522217579282199 ) ) ;
#37036=CARTESIAN_POINT ( 'NONE',  ( 11.27230809297926051, -9.289986881467834579, -77.08399725981655592 ) ) ;
#37037=CARTESIAN_POINT ( 'NONE',  ( 20.29259450369849560, -10.20485895348243410, -48.16115496514827754 ) ) ;
#37053=CARTESIAN_POINT ( 'NONE',  ( 20.11399144799549887, -21.27607163836539783, -81.23899999999999011 ) ) ;
#37063=VERTEX_POINT ( 'NONE', #19914 ) ;
#37065=B_SPLINE_CURVE_WITH_KNOTS ( 'NONE', 3,
 ( #16590, #28375, #8222, #8484, #7720, #24430, #20509, #40444, #4535, #32543, #28117, #47805, #48579, #27867, #28634, #23665, #39679, #3785, #35993, #19755, #35746, #40193, #11911, #43867, #39940, #109, #16081, #32040, #33861 ),
 .UNSPECIFIED., .F., .F.,
 ( 4, 2, 1, 1, 1, 1, 1, 2, 2, 2, 2, 2, 2, 2, 2, 2, 4 ),
 ( 0.5000038086628445511, 0.5002479474281459337, 0.5004920861934472054, 0.5009803637240499707, 0.5019569187852552794, 0.5039100289076660077, 0.5078162491524875755, 0.5156286896421305999, 0.5312535706214167597, 0.5625033325799890793, 0.6250028564971334966, 0.6875023804142779138, 0.7500019043314223310, 0.8125014282485667483, 0.8750009521657111655, 0.9375004760828555828, 1.000000000000000000 ),
 .UNSPECIFIED. ) ;
#37072=CARTESIAN_POINT ( 'NONE',  ( 8.428856657643047257, -17.68693864638044744, -68.70899797463333414 ) ) ;
#37076=CARTESIAN_POINT ( 'NONE',  ( 22.64876182410736050, -18.03120546031163585, -54.96075032149187933 ) ) ;
#37078=CARTESIAN_POINT ( 'NONE',  ( 19.22389005490540015, -22.82999104616420283, -75.65868704446690174 ) ) ;
#37079=ORIENTED_EDGE ( 'NONE', *, *, #45508, .T. ) ;
#37088=EDGE_CURVE ( 'NONE', #27935, #25861, #12075, .T. ) ;
#37093=CARTESIAN_POINT ( 'NONE',  ( 8.291851457509455514, -16.78737382061565953, -34.46050489558400187 ) ) ;
#37095=FACE_OUTER_BOUND ( 'NONE', #35183, .T. ) ;
#37097=CARTESIAN_POINT ( 'NONE',  ( 9.205714170480751690, -12.87640478306839853, -48.18721185593089729 ) ) ;
#37106=CARTESIAN_POINT ( 'NONE',  ( 18.71043739769620018, -15.61618894467929941, -31.39999999999999858 ) ) ;
#37130=CARTESIAN_POINT ( 'NONE',  ( 21.21558964501896938, -20.08614974262806285, -46.68245235485807854 ) ) ;
#37133=CARTESIAN_POINT ( 'NONE',  ( 20.81968612761309956, -21.91146546216959834, -68.30882034609030029 ) ) ;
#37144=CARTESIAN_POINT ( 'NONE',  ( 20.11812388789995154, -8.703698750585735056, -41.45899779116474804 ) ) ;
#37146=VERTEX_POINT ( 'NONE', #36941 ) ;
#37151=CARTESIAN_POINT ( 'NONE',  ( 8.223600577592289795, -15.61621812327629932, -68.50766849176299900 ) ) ;
#37152=CARTESIAN_POINT ( 'NONE',  ( 23.15196511571160087, -18.23446988725689977, -32.14999999999999858 ) ) ;
#37156=DIRECTION ( 'NONE',  ( 0.000000000000000000, 0.000000000000000000, 1.000000000000000000 ) ) ;
#37157=CARTESIAN_POINT ( 'NONE',  ( 23.83903610038404608, -17.68687214694392651, -51.87566247315886869 ) ) ;
#37162=CARTESIAN_POINT ( 'NONE',  ( 22.79673239389820338, -13.30324233633820086, -58.74082357793209752 ) ) ;
#37169=CARTESIAN_POINT ( 'NONE',  ( 22.71369373737119801, -18.15574898672049997, -62.57006952842979075 ) ) ;
#37174=ORIENTED_EDGE ( 'NONE', *, *, #6646, .T. ) ;
#37189=CARTESIAN_POINT ( 'NONE',  ( 9.221411471344291400, -19.60031560563376374, -44.34101869606306678 ) ) ;
#37191=CARTESIAN_POINT ( 'NONE',  ( 22.90093741817085515, -14.73039762558461341, -68.41115124640887757 ) ) ;
#37192=FACE_OUTER_BOUND ( 'NONE', #42159, .T. ) ;
#37196=CARTESIAN_POINT ( 'NONE',  ( 8.334470150558480839, -16.48513208769189831, -32.97717709171600120 ) ) ;
#37199=CARTESIAN_POINT ( 'NONE',  ( 22.90097009252848892, -15.61618913824531418, -68.84717732178738459 ) ) ;
#37204=CARTESIAN_POINT ( 'NONE',  ( 17.32262310423930174, -8.664240623128929286, -36.40108501799139873 ) ) ;
#37206=ORIENTED_EDGE ( 'NONE', *, *, #11171, .F. ) ;
#37213=CARTESIAN_POINT ( 'NONE',  ( 12.41372322625400137, -22.97436356901700094, -80.15667222455330432 ) ) ;
#37220=ADVANCED_FACE ( 'NONE', ( #8914 ), #38988, .F. ) ;
#37224=ORIENTED_EDGE ( 'NONE', *, *, #24149, .T. ) ;
#37230=CARTESIAN_POINT ( 'NONE',  ( 8.713847312995159911, -16.28566013226560116, -81.20401221892029753 ) ) ;
#37237=CARTESIAN_POINT ( 'NONE',  ( 12.98003058962980028, -8.866406267853768952, -72.42820476139830532 ) ) ;
#37241=DIRECTION ( 'NONE',  ( 0.000000000000000000, 0.000000000000000000, -1.000000000000000000 ) ) ;
#37249=AXIS2_PLACEMENT_3D ( 'NONE', #21898, #10651, #18502 ) ;
#37251=FACE_OUTER_BOUND ( 'NONE', #35314, .T. ) ;
#37252=VERTEX_POINT ( 'NONE', #48755 ) ;
#37254=CARTESIAN_POINT ( 'NONE',  ( 11.97526568333010033, -10.20486919016092564, -69.74448779737157622 ) ) ;
#37258=FACE_OUTER_BOUND ( 'NONE', #28453, .T. ) ;
#37262=CARTESIAN_POINT ( 'NONE',  ( 16.71759420731690327, -7.391709338982750843, -57.31488281878699098 ) ) ;
#37264=CARTESIAN_POINT ( 'NONE',  ( 9.560404261625569333, -13.76607691521293830, -55.53990993375253282 ) ) ;
#37268=CARTESIAN_POINT ( 'NONE',  ( 17.98718783828190126, -8.400084967489489074, -43.81267675689189645 ) ) ;
#37269=CARTESIAN_POINT ( 'NONE',  ( 11.43117294225049996, -10.64118341557829872, -32.14999999999999858 ) ) ;
#37271=CARTESIAN_POINT ( 'NONE',  ( 9.122145535666252414, -19.41028161033098343, -60.63421390308896264 ) ) ;
#37274=CARTESIAN_POINT ( 'NONE',  ( 24.06642615182659739, -13.36711294005660022, -49.41972697186898955 ) ) ;
#37283=ORIENTED_EDGE ( 'NONE', *, *, #45508, .F. ) ;
#37292=DIRECTION ( 'NONE',  ( 0.000000000000000000, 0.000000000000000000, 1.000000000000000000 ) ) ;
#37298=CARTESIAN_POINT ( 'NONE',  ( 22.72481188910181515, -13.84494795670818057, -48.36948871484188572 ) ) ;
#37306=ORIENTED_EDGE ( 'NONE', *, *, #46055, .T. ) ;
#37312=CARTESIAN_POINT ( 'NONE',  ( 20.27230028841029963, -21.17689101966990251, -81.23899999999999011 ) ) ;
#37318=ORIENTED_EDGE ( 'NONE', *, *, #34664, .T. ) ;
#37337=CARTESIAN_POINT ( 'NONE',  ( 22.59532618109970059, -20.07008647076710162, -69.47961042150460287 ) ) ;
#37344=B_SPLINE_CURVE_WITH_KNOTS ( 'NONE', 3,
 ( #4528, #20500, #51722, #16582, #345, #35739, #35985, #12672, #12154, #7447, #3520, #16331, #32285, #8216, #51471, #15570, #16074, #11640 ),
 .UNSPECIFIED., .F., .F.,
 ( 4, 2, 2, 2, 2, 2, 2, 2, 4 ),
 ( 0.5000009992646622381, 0.5625008743565794722, 0.6250007494484968174, 0.6875006245404140515, 0.7500004996323312856, 0.8125003747242485197, 0.8750002498161656428, 0.9375001249080827659, 1.000000000000000000 ),
 .UNSPECIFIED. ) ;
#37348=CARTESIAN_POINT ( 'NONE',  ( 9.366929721696807931, -16.50193097571266421, -79.41115341879661571 ) ) ;
#37350=CARTESIAN_POINT ( 'NONE',  ( 24.04426633253695655, -15.72747050290504056, -33.51214286250507257 ) ) ;
#37353=CARTESIAN_POINT ( 'NONE',  ( 18.30701343718470042, -22.74250881295229831, -39.47312943893279424 ) ) ;
#37358=CYLINDRICAL_SURFACE ( 'NONE', #42123, 7.910999999999997812 ) ;
#37364=ORIENTED_EDGE ( 'NONE', *, *, #32524, .F. ) ;
#37371=CARTESIAN_POINT ( 'NONE',  ( 24.04527307164895333, -15.61618901697373119, -57.79233174308600951 ) ) ;
#37377=CARTESIAN_POINT ( 'NONE',  ( 22.89142707005135691, -16.00359460448838789, -72.47105089344913154 ) ) ;
#37378=CARTESIAN_POINT ( 'NONE',  ( 10.68011837214288029, -11.14422995437498543, -46.06579460775301271 ) ) ;
#37380=CARTESIAN_POINT ( 'NONE',  ( 22.90108808520262329, -15.61618901356150069, -52.45282226904397049 ) ) ;
#37389=CARTESIAN_POINT ( 'NONE',  ( 8.927887674289250342, -18.72417784031090093, -66.88287958694499480 ) ) ;
#37399=VERTEX_POINT ( 'NONE', #39031 ) ;
#37406=CARTESIAN_POINT ( 'NONE',  ( 23.09136781754329704, -18.42403774965039887, -32.14999999999999858 ) ) ;
#37410=CARTESIAN_POINT ( 'NONE',  ( 23.04646567172652993, -19.60031090604470094, -51.95899602180234211 ) ) ;
#37412=ORIENTED_EDGE ( 'NONE', *, *, #44721, .T. ) ;
#37413=CARTESIAN_POINT ( 'NONE',  ( 22.75640274483500036, -18.04219634376060100, -60.95895364771359226 ) ) ;
#37416=AXIS2_PLACEMENT_3D ( 'NONE', #30518, #3017, #22907 ) ;
#37422=CARTESIAN_POINT ( 'NONE',  ( 23.06275954296619801, -16.93299659040459915, -76.51260139562678830 ) ) ;
#37425=DIRECTION ( 'NONE',  ( 0.000000000000000000, 0.000000000000000000, -1.000000000000000000 ) ) ;
#37438=CARTESIAN_POINT ( 'NONE',  ( 20.99561100367103350, -21.94235771815155900, -59.79935458015073380 ) ) ;
#37441=CARTESIAN_POINT ( 'NONE',  ( 11.27225585075783343, -21.94235148362552579, -44.21602647793709195 ) ) ;
#37443=VERTEX_POINT ( 'NONE', #50560 ) ;
#37450=CARTESIAN_POINT ( 'NONE',  ( 12.28771955365369983, -22.90926077143079809, -80.44681068936390034 ) ) ;
#37457=AXIS2_PLACEMENT_3D ( 'NONE', #40175, #40947, #4270 ) ;
#37458=CARTESIAN_POINT ( 'NONE',  ( 9.093524979847760648, -15.19767719791919980, -33.86607922395559456 ) ) ;
#37467=CARTESIAN_POINT ( 'NONE',  ( 9.831796340808351076, -10.29963566149569942, -78.73073146540821199 ) ) ;
#37471=DIRECTION ( 'NONE',  ( 0.000000000000000000, 0.000000000000000000, -1.000000000000000000 ) ) ;
#37480=CARTESIAN_POINT ( 'NONE',  ( 24.04037527269505503, -15.90671900147433782, -65.80402047898783735 ) ) ;
#37482=CARTESIAN_POINT ( 'NONE',  ( 9.602139829674678495, -12.95570267495170036, -33.57594075914519749 ) ) ;
#37485=CARTESIAN_POINT ( 'NONE',  ( 8.428876690002429228, -17.68701148082665497, -58.42433507561374029 ) ) ;
#37489=CARTESIAN_POINT ( 'NONE',  ( 12.39356905812690179, -22.05950633734969912, -69.73476110523529314 ) ) ;
#37497=CARTESIAN_POINT ( 'NONE',  ( 14.04007584740629788, -23.31488602239420516, -76.37656314211675124 ) ) ;
#37500=CARTESIAN_POINT ( 'NONE',  ( 19.36791954131713922, -22.86483927959923435, -45.87411009050862987 ) ) ;
#37507=CARTESIAN_POINT ( 'NONE',  ( 22.90090927591486292, -15.61618926791037687, -70.45281771081829447 ) ) ;
#37508=CARTESIAN_POINT ( 'NONE',  ( 8.428870326585922612, -17.68698834907383599, -70.42433541781397821 ) ) ;
#37515=CARTESIAN_POINT ( 'NONE',  ( 18.85737764037289921, -23.39857889253620016, -50.18517902306130196 ) ) ;
#37521=CARTESIAN_POINT ( 'NONE',  ( 22.85349008618740285, -12.39837828030880118, -48.09049903432739370 ) ) ;
#37527=CARTESIAN_POINT ( 'NONE',  ( 23.73155033226879951, -12.41322181943569980, -53.38067352504989316 ) ) ;
#37534=VERTEX_POINT ( 'NONE', #42181 ) ;
#37543=CARTESIAN_POINT ( 'NONE',  ( 8.222339619445261150, -15.61627490117209938, -70.79233150823699816 ) ) ;
#37549=CARTESIAN_POINT ( 'NONE',  ( 22.04685654012394735, -12.20821177133414892, -48.28615521496443108 ) ) ;
#37551=CARTESIAN_POINT ( 'NONE',  ( 9.494855085389646732, -17.51523721219662022, -73.75786096057412067 ) ) ;
#37554=CARTESIAN_POINT ( 'NONE',  ( 13.53484056975250027, -8.242504967360991586, -81.23899999999999011 ) ) ;
#37555=CARTESIAN_POINT ( 'NONE',  ( 22.90118952179220813, -15.61618876469732875, -46.84717865327674247 ) ) ;
#37564=CARTESIAN_POINT ( 'NONE',  ( 24.04343812156989912, -15.78374718670210264, -77.51440025672197009 ) ) ;
#37572=CARTESIAN_POINT ( 'NONE',  ( 24.04465409553882083, -15.68853894113726710, -33.79524008575338456 ) ) ;
#37575=CARTESIAN_POINT ( 'NONE',  ( 22.90065299155850198, -15.61618013372109637, -50.45281880338879432 ) ) ;
#37576=ORIENTED_EDGE ( 'NONE', *, *, #39346, .F. ) ;
#37584=CARTESIAN_POINT ( 'NONE',  ( 16.60947325484960047, -7.782887352646469914, -72.80680552617660339 ) ) ;
#37604=EDGE_CURVE ( 'NONE', #49951, #27673, #31499, .T. ) ;
#37605=CARTESIAN_POINT ( 'NONE',  ( 23.41830238215899840, -14.05262854882809975, -55.00003992740209924 ) ) ;
#37615=CARTESIAN_POINT ( 'NONE',  ( 9.367363532653184777, -14.62080165624493766, -53.89401576057853305 ) ) ;
#37630=CARTESIAN_POINT ( 'NONE',  ( 24.04493067738190959, -15.60426386090046869, -77.50719664004228093 ) ) ;
#37643=CARTESIAN_POINT ( 'NONE',  ( 18.13911242106300037, -8.028961472324999349, -59.59473792909199830 ) ) ;
#37644=DIRECTION ( 'NONE',  ( 1.000000000000000000, 0.000000000000000000, 0.000000000000000000 ) ) ;
#37656=B_SPLINE_CURVE_WITH_KNOTS ( 'NONE', 3,
 ( #27766, #11028, #7863, #51372, #23811, #39830, #31936, #26996, #15471, #11544, #39071, #3162, #19132, #31422, #51111, #15214, #23558, #31169, #47450, #27506, #39573, #3679, #35642, #4177, #20153, #36390, #248, #36146 ),
 .UNSPECIFIED., .F., .F.,
 ( 4, 2, 2, 2, 2, 2, 2, 2, 2, 2, 1, 1, 1, 1, 2, 4 ),
 ( 0.000000000000000000, 0.06250045316978908305, 0.1250009063395781661, 0.1875013595093672769, 0.2500018126791563322, 0.3125022658489454153, 0.3750027190187345538, 0.4375031721885235814, 0.4687533987734182062, 0.4843785120658654630, 0.4921910687120890637, 0.4960973470352010306, 0.4980504861967569585, 0.4990270557775348670, 0.4995153405679237379, 0.5000036253583125534 ),
 .UNSPECIFIED. ) ;
#37659=CARTESIAN_POINT ( 'NONE',  ( 23.02572387508500285, -13.73427156000250093, -32.14999999999999858 ) ) ;
#37667=CARTESIAN_POINT ( 'NONE',  ( 14.22831053668800116, -22.40670773495260093, -61.43426723409519496 ) ) ;
#37673=CARTESIAN_POINT ( 'NONE',  ( 22.72481288133749899, -17.38742503737659106, -42.53615302188016045 ) ) ;
#37677=CARTESIAN_POINT ( 'NONE',  ( 18.80263846160409713, -9.087744005176290329, -72.07634125606418252 ) ) ;
#37689=CARTESIAN_POINT ( 'NONE',  ( 23.79983412839517598, -13.61705418525005129, -39.42650676693061484 ) ) ;
#37702=ORIENTED_EDGE ( 'NONE', *, *, #14736, .F. ) ;
#37703=CARTESIAN_POINT ( 'NONE',  ( 8.222914093092873244, -14.70876443408920231, -32.82885229014726036 ) ) ;
#37706=CARTESIAN_POINT ( 'NONE',  ( 18.20470625429515366, -7.911114086817085500, -57.09100124538479548 ) ) ;
#37708=CARTESIAN_POINT ( 'NONE',  ( 19.66219730728080251, -22.62604840133040085, -38.36406440404209661 ) ) ;
#37720=CARTESIAN_POINT ( 'NONE',  ( 11.57174743202489964, -10.23757062443000088, -32.12326274055600095 ) ) ;
#37744=CARTESIAN_POINT ( 'NONE',  ( 9.874923758134890761, -18.86692839231439933, -45.30034255656079978 ) ) ;
#37752=CARTESIAN_POINT ( 'NONE',  ( 23.11151459842839984, -18.22772311948279977, -77.18134062521549765 ) ) ;
#37755=CARTESIAN_POINT ( 'NONE',  ( 23.69469079014621116, -13.18663225633502911, -49.69345251610035064 ) ) ;
#37758=( BOUNDED_CURVE ( )  B_SPLINE_CURVE ( 2, ( #4123, #32131, #40288 ),
 .UNSPECIFIED., .F., .T. ) 
 B_SPLINE_CURVE_WITH_KNOTS ( ( 3, 3 ),
 ( 1.104980434577240045, 2.168627590050199672 ),
 .UNSPECIFIED. ) 
 CURVE ( )  GEOMETRIC_REPRESENTATION_ITEM ( )  RATIONAL_B_SPLINE_CURVE ( ( 1.323085463760209857, 1.425426480542939967, 1.425426480542939967 ) ) 
 REPRESENTATION_ITEM ( '' )  );
#37761=CARTESIAN_POINT ( 'NONE',  ( 23.03994194550808672, -19.61239988445705862, -75.95950967876112259 ) ) ;
#37762=CARTESIAN_POINT ( 'NONE',  ( 18.22483727046438773, -9.153516611488269561, -62.05237194099072440 ) ) ;
#37765=CARTESIAN_POINT ( 'NONE',  ( 16.06492382637960858, -23.55873069923232777, -46.01057597322125048 ) ) ;
#37768=B_SPLINE_CURVE_WITH_KNOTS ( 'NONE', 3,
 ( #23227, #22974, #26918, #14873, #19058, #35031, #43689, #51036, #15395, #34776, #46605, #30836, #3603, #46866, #3343, #47624, #27691, #31607 ),
 .UNSPECIFIED., .F., .F.,
 ( 4, 2, 2, 2, 2, 2, 2, 2, 4 ),
 ( 0.5000000029181979055, 0.5625000025534231396, 0.6250000021886483736, 0.6875000018238737187, 0.7500000014590989528, 0.8125000010943241868, 0.8750000007295495319, 0.9375000003647747659, 1.000000000000000000 ),
 .UNSPECIFIED. ) ;
#37770=CARTESIAN_POINT ( 'NONE',  ( 9.367379825797401693, -15.61607429561870042, -45.84717978380999881 ) ) ;
#37774=FACE_OUTER_BOUND ( 'NONE', #14802, .T. ) ;
#37781=CARTESIAN_POINT ( 'NONE',  ( 8.189894513438611412, -13.40827076027780151, -52.87862267922429282 ) ) ;
#37782=CARTESIAN_POINT ( 'NONE',  ( 9.366455112259469473, -15.61627688590920116, -55.45282021618999835 ) ) ;
#37786=CARTESIAN_POINT ( 'NONE',  ( 10.27832463521709983, -20.22254248962530099, -43.02048744625579246 ) ) ;
#37788=CARTESIAN_POINT ( 'NONE',  ( 8.894205530028397533, -15.14404388050549954, -32.14999999999999858 ) ) ;
#37795=CARTESIAN_POINT ( 'NONE',  ( 11.89147504607354655, -8.873838868181545436, -60.82910890462889597 ) ) ;
#37797=CARTESIAN_POINT ( 'NONE',  ( 7.901851024471708840, -16.08038141849450042, -54.48973855994069737 ) ) ;
#37798=VERTEX_POINT ( 'NONE', #49480 ) ;
#37803=CARTESIAN_POINT ( 'NONE',  ( 8.223340741289188571, -15.61635616670070092, -42.79233150823699816 ) ) ;
#37828=CARTESIAN_POINT ( 'NONE',  ( 8.222918173831372357, -14.85904556795307485, -80.53814063808331980 ) ) ;
#37830=ORIENTED_EDGE ( 'NONE', *, *, #48986, .T. ) ;
#37836=CARTESIAN_POINT ( 'NONE',  ( 24.04493740255118439, -15.61827380739441118, -77.50775418025503427 ) ) ;
#37842=VERTEX_POINT ( 'NONE', #48696 ) ;
#37844=CARTESIAN_POINT ( 'NONE',  ( 12.36442939451902667, -22.59821236439503522, -34.44981817989418715 ) ) ;
#37846=B_SPLINE_CURVE_WITH_KNOTS ( 'NONE', 3,
 ( #4704, #49521, #20672, #13613, #21190, #29064, #45060, #1808, #9161, #25378 ),
 .UNSPECIFIED., .F., .F.,
 ( 4, 1, 1, 1, 1, 1, 1, 4 ),
 ( 0.4999989579104466841, 0.5363602085422365384, 0.6155791396058006848, 0.6947980706695208175, 0.7740170017330827434, 0.8532359327968050966, 0.9324548638603670225, 1.000000000000000000 ),
 .UNSPECIFIED. ) ;
#37858=CARTESIAN_POINT ( 'NONE',  ( 23.81821264185619924, -14.02287097416230033, -71.22242690490419648 ) ) ;
#37861=B_SPLINE_CURVE_WITH_KNOTS ( 'NONE', 3,
 ( #18731, #50967, #3275, #15330, #43373, #26851, #39440, #34710, #31033, #30774, #10888, #47059, #46797, #38400, #30260, #18217, #46281, #10367 ),
 .UNSPECIFIED., .F., .F.,
 ( 4, 2, 2, 2, 2, 2, 2, 2, 4 ),
 ( 0.000000000000000000, 0.06250000073800097977, 0.1250000014760019595, 0.1875000022140029254, 0.2500000029520039191, 0.3125000036900049127, 0.3750000044280058509, 0.4375000051660068445, 0.5000000059040078382 ),
 .UNSPECIFIED. ) ;
#37862=CARTESIAN_POINT ( 'NONE',  ( 2.277530937145189949, -15.61618894467929941, -32.14999999999999858 ) ) ;
#37870=CARTESIAN_POINT ( 'NONE',  ( 12.14972608106025120, -8.703710964786449011, -42.84096575448170086 ) ) ;
#37872=CARTESIAN_POINT ( 'NONE',  ( 12.14970654918197823, -8.703721948391146768, -59.12570771485219012 ) ) ;
#37880=CARTESIAN_POINT ( 'NONE',  ( 10.64020559113360065, -20.64864412837480145, -51.83128268485729961 ) ) ;
#37883=CARTESIAN_POINT ( 'NONE',  ( 11.97533377483439487, -21.02756021161885158, -69.16115284857546897 ) ) ;
#37889=CARTESIAN_POINT ( 'NONE',  ( 24.04518460902906085, -15.61618869790763675, -47.79232989768991757 ) ) ;
#37904=CARTESIAN_POINT ( 'NONE',  ( 24.01027070323695867, -16.38076406562427678, -49.53846147474892092 ) ) ;
#37908=CARTESIAN_POINT ( 'NONE',  ( 9.901417542572799491, -10.84728510343080110, -73.22039407203469352 ) ) ;
#37929=CARTESIAN_POINT ( 'NONE',  ( 9.221370973493520751, -19.60024637595736863, -46.62569193087001906 ) ) ;
#37934=CARTESIAN_POINT ( 'NONE',  ( 23.03988594485150188, -14.18425534339259997, -70.78210109960220109 ) ) ;
#37937=FACE_OUTER_BOUND ( 'NONE', #46068, .T. ) ;
#37938=CARTESIAN_POINT ( 'NONE',  ( 24.04493739769619864, -15.61618894467929941, -32.14999999999999858 ) ) ;
#37942=CARTESIAN_POINT ( 'NONE',  ( 23.18677759228159729, -15.61816030595169913, -74.45290918797279289 ) ) ;
#37943=DIRECTION ( 'NONE',  ( 1.000000000000000000, 0.000000000000000000, 0.000000000000000000 ) ) ;
#37951=CARTESIAN_POINT ( 'NONE',  ( 24.00787544518242100, -14.82575727831162382, -39.47583133721960991 ) ) ;
#37965=CARTESIAN_POINT ( 'NONE',  ( 8.222903922732800908, -15.61639209420869889, -32.79233150823699816 ) ) ;
#37966=CARTESIAN_POINT ( 'NONE',  ( 9.221497967028252418, -19.60046347223059726, -48.62566517465766935 ) ) ;
#37967=ORIENTED_EDGE ( 'NONE', *, *, #15071, .T. ) ;
#37968=CARTESIAN_POINT ( 'NONE',  ( 8.222930384839667539, -14.58069280931489153, -52.83399830599484659 ) ) ;
#37970=CARTESIAN_POINT ( 'NONE',  ( 17.30631058744340223, -7.454800704868429939, -79.33774565447329508 ) ) ;
#37988=CARTESIAN_POINT ( 'NONE',  ( 20.99566025495300536, -9.290059480944934833, -57.50066464107244713 ) ) ;
#38000=VERTEX_POINT ( 'NONE', #10865 ) ;
#38004=CARTESIAN_POINT ( 'NONE',  ( 9.620888334170560441, -12.91013081656500106, -49.57816483399619756 ) ) ;
#38011=CARTESIAN_POINT ( 'NONE',  ( 20.08119151113339740, -9.297496097080600208, -72.74508048565279239 ) ) ;
#38012=VECTOR ( 'NONE', #1190, 1000.000000000000000 ) ;
#38014=CARTESIAN_POINT ( 'NONE',  ( 23.15473124193005461, -11.90455973904859732, -49.63748291447825522 ) ) ;
#38018=CARTESIAN_POINT ( 'NONE',  ( 9.797968754430565141, -20.46465235352011192, -76.58461035990077903 ) ) ;
#38019=CARTESIAN_POINT ( 'NONE',  ( 21.26777047317277081, -11.15835231960324414, -62.22513457443928786 ) ) ;
#38021=CARTESIAN_POINT ( 'NONE',  ( 10.86351723737203123, -21.58463999176102277, -46.23780422378855093 ) ) ;
#38022=EDGE_LOOP ( 'NONE', ( #37306, #36519, #14046, #30673, #22213 ) ) ;
#38027=B_SPLINE_CURVE_WITH_KNOTS ( 'NONE', 3,
 ( #45960, #37836, #41499, #18169, #49894, #10054, #26016, #29437, #42027, #9545, #25497, #5613, #37564, #34136, #46229, #1672, #6383, #2440, #18423, #17660, #11350, #27315, #23621, #35707, #31738, #43576, #7676, #47009, #50663, #26798, #7163, #22856, #51183, #35442, #43828, #18683, #38877, #11608, #51691, #47767, #15278, #27827, #42810, #19716, #27569, #30982, #23360, #31234, #19195, #7926, #3224, #3487, #2965, #47260, #23876, #39640, #18939, #35180, #47512, #34656 ),
 .UNSPECIFIED., .F., .F.,
 ( 4, 2, 1, 1, 1, 1, 1, 2, 2, 2, 2, 2, 2, 2, 2, 1, 1, 1, 1, 1, 1, 2, 2, 2, 2, 2, 2, 1, 1, 1, 1, 1, 2, 2, 2, 2, 2, 4 ),
 ( 0.5000034598518116047, 0.5001255293196273932, 0.5002475987874431818, 0.5004917377230646558, 0.5009800155943028299, 0.5019565713367789561, 0.5039096828217313195, 0.5078159057916349362, 0.5156283517314436127, 0.5312532436110607437, 0.5625030273702946726, 0.5937528111295286015, 0.6093777030091455105, 0.6250025948887624194, 0.6251246643565719907, 0.6252467338243815620, 0.6254908727600008156, 0.6259791506312393228, 0.6269557063737165592, 0.6289088178586710320, 0.6328150408285799777, 0.6406274867683978691, 0.6562523786480337629, 0.6875021624073054394, 0.7187519461665772269, 0.7500017299258489034, 0.7502458688614681570, 0.7504900077970874106, 0.7509782856683260288, 0.7519548414108030432, 0.7539079528957572940, 0.7578141758656659066, 0.7656266218054831318, 0.7812515136851174713, 0.8125012974443863722, 0.8750008649629243962, 0.9375004324814621981, 1.000000000000000000 ),
 .UNSPECIFIED. ) ;
#38031=CARTESIAN_POINT ( 'NONE',  ( 24.04497561966918440, -15.61618908881887080, -69.50766602643473391 ) ) ;
#38033=ORIENTED_EDGE ( 'NONE', *, *, #11718, .F. ) ;
#38034=LINE ( 'NONE', #29882, #35004 ) ;
#38037=CARTESIAN_POINT ( 'NONE',  ( 11.23390675766243518, -21.85624464617543694, -66.21956934538100370 ) ) ;
#38038=CARTESIAN_POINT ( 'NONE',  ( 10.20798635145410138, -9.883316693052110580, -53.03706054135160031 ) ) ;
#38039=B_SPLINE_CURVE_WITH_KNOTS ( 'NONE', 3,
 ( #39310, #19888, #43252, #19121, #39060, #18860, #31159, #31668, #11536, #35364, #34845, #51101, #35879, #15201, #12615, #51618, #7340, #51363 ),
 .UNSPECIFIED., .F., .F.,
 ( 4, 2, 2, 2, 2, 2, 2, 2, 4 ),
 ( 0.000000000000000000, 0.06250000036477473819, 0.1250000007295494764, 0.1875000010943242146, 0.2500000014590989528, 0.3125000018238737187, 0.3750000021886484292, 0.4375000025534231396, 0.5000000029181979055 ),
 .UNSPECIFIED. ) ;
#38046=CARTESIAN_POINT ( 'NONE',  ( 22.48979959896199787, -19.50330992088589710, -48.40737475858179550 ) ) ;
#38048=CARTESIAN_POINT ( 'NONE',  ( 9.780793637630969428, -12.57087751220609917, -32.14999999999999858 ) ) ;
#38049=EDGE_CURVE ( 'NONE', #14401, #12539, #31012, .T. ) ;
#38054=CARTESIAN_POINT ( 'NONE',  ( 15.84222111805427424, -7.629322965617999053, -60.99577838100516658 ) ) ;
#38055=CARTESIAN_POINT ( 'NONE',  ( 22.07021184574940165, -9.894006984415741002, -65.26351318459300899 ) ) ;
#38084=CARTESIAN_POINT ( 'NONE',  ( 19.76827833599991990, -21.66053548658283034, -47.17485964264358955 ) ) ;
#38086=EDGE_CURVE ( 'NONE', #49444, #37399, #19731, .T. ) ;
#38088=CARTESIAN_POINT ( 'NONE',  ( 8.428888757039553425, -17.68705536023493607, -80.42433531602081587 ) ) ;
#38090=VERTEX_POINT ( 'NONE', #44113 ) ;
#38095=CARTESIAN_POINT ( 'NONE',  ( 20.99564406849854237, -9.290046565741832296, -63.21600299103990750 ) ) ;
#38097=EDGE_LOOP ( 'NONE', ( #34156, #46285 ) ) ;
#38099=B_SPLINE_CURVE_WITH_KNOTS ( 'NONE', 3,
 ( #2047, #17770, #33740, #30060, #45560, #38210, #25359, #46090, #26388, #49755, #41361, #2571, #1532, #13846, #5476, #50272, #6502, #29803 ),
 .UNSPECIFIED., .F., .F.,
 ( 4, 2, 2, 2, 2, 2, 2, 2, 4 ),
 ( 0.5000015730941113068, 0.5625013764573473241, 0.6250011798205833413, 0.6875009831838194696, 0.7500007865470554869, 0.8125005899102915041, 0.8750003932735277434, 0.9375001966367638717, 1.000000000000000000 ),
 .UNSPECIFIED. ) ;
#38104=CARTESIAN_POINT ( 'NONE',  ( 12.90691782988471559, -22.86298708769336585, -34.42568375498250788 ) ) ;
#38116=CARTESIAN_POINT ( 'NONE',  ( 13.52842820780809951, -23.01876079806860176, -67.89523180023219595 ) ) ;
#38126=CARTESIAN_POINT ( 'NONE',  ( 23.46945290812993079, -12.58981197008611375, -65.38307690060923960 ) ) ;
#38128=CARTESIAN_POINT ( 'NONE',  ( 9.543049929519856533, -17.38738464657387794, -79.36948662140328281 ) ) ;
#38130=CARTESIAN_POINT ( 'NONE',  ( 20.99557285898455206, -21.94238817380684026, -56.08401504527179782 ) ) ;
#38134=CARTESIAN_POINT ( 'NONE',  ( 15.13944710363159984, -8.232579841174930024, -54.52472634102049653 ) ) ;
#38137=CARTESIAN_POINT ( 'NONE',  ( 21.54529026121558744, -19.77481651483016023, -68.66115164695051476 ) ) ;
#38140=CARTESIAN_POINT ( 'NONE',  ( 16.52003647484010429, -23.51837224676972582, -61.99213453326030532 ) ) ;
#38142=CARTESIAN_POINT ( 'NONE',  ( 22.90067702240739322, -15.61618873416334807, -54.84718332859007006 ) ) ;
#38143=CIRCLE ( 'NONE', #21359, 2.576499999999998902 ) ;
#38144=CARTESIAN_POINT ( 'NONE',  ( 10.46343333517600094, -19.39436818664529838, -81.23899999999999011 ) ) ;
#38148=ADVANCED_FACE ( 'NONE', ( #2408 ), #46720, .T. ) ;
#38149=EDGE_LOOP ( 'NONE', ( #28440, #2772, #46804, #14824 ) ) ;
#38155=EDGE_LOOP ( 'NONE', ( #32323, #17207, #29873, #6223 ) ) ;
#38156=CARTESIAN_POINT ( 'NONE',  ( 22.81411286000173888, -16.71917825895734921, -72.50489804183278864 ) ) ;
#38157=CARTESIAN_POINT ( 'NONE',  ( 17.01975655319769487, -22.38318595458896709, -52.91115215000503014 ) ) ;
#38158=CARTESIAN_POINT ( 'NONE',  ( 17.01971462380884859, -8.849185945517076490, -53.99448858704194976 ) ) ;
#38160=CARTESIAN_POINT ( 'NONE',  ( 24.04493704540187693, -15.61897246368578429, -49.50777781568486091 ) ) ;
#38164=CARTESIAN_POINT ( 'NONE',  ( 21.17919601613330016, -9.605189604746890097, -69.73476110523539262 ) ) ;
#38169=EDGE_CURVE ( 'NONE', #51178, #44797, #48411, .T. ) ;
#38174=AXIS2_PLACEMENT_3D ( 'NONE', #1316, #17048, #4464 ) ;
#38176=CARTESIAN_POINT ( 'NONE',  ( 16.13393739769620083, -3.616188944679339823, -22.14999999999999858 ) ) ;
#38178=AXIS2_PLACEMENT_3D ( 'NONE', #50956, #11133, #3263 ) ;
#38186=CARTESIAN_POINT ( 'NONE',  ( 12.30690527417384494, -8.626895769526717217, -44.84843753875242811 ) ) ;
#38191=CARTESIAN_POINT ( 'NONE',  ( 23.11815408353849577, -14.63472246044799796, -76.80273986043728485 ) ) ;
#38199=CARTESIAN_POINT ( 'NONE',  ( 13.25502815134339940, -22.05470121444239595, -75.08666063648169597 ) ) ;
#38209=CARTESIAN_POINT ( 'NONE',  ( 24.04493527958818078, -15.61020189840042427, -39.50743058786228801 ) ) ;
#38210=CARTESIAN_POINT ( 'NONE',  ( 20.29259522008245042, -21.02751836791847495, -54.74448911140668628 ) ) ;
#38212=ORIENTED_EDGE ( 'NONE', *, *, #41621, .F. ) ;
#38217=CARTESIAN_POINT ( 'NONE',  ( 9.366383648607859769, -15.61614502978449970, -45.45282021618989177 ) ) ;
#38219=B_SPLINE_CURVE_WITH_KNOTS ( 'NONE', 3,
 ( #34126, #37828, #46741, #41492, #41750, #50136, #14234, #1663, #21560, #6374 ),
 .UNSPECIFIED., .F., .F.,
 ( 4, 2, 2, 2, 4 ),
 ( 0.000000000000000000, 0.1250000005901855116, 0.2500000011803710231, 0.3750000017705565347, 0.5000000023607420463 ),
 .UNSPECIFIED. ) ;
#38223=ORIENTED_EDGE ( 'NONE', *, *, #9627, .F. ) ;
#38229=CARTESIAN_POINT ( 'NONE',  ( 20.49355919092259981, -22.14155831442439748, -42.32501095722299311 ) ) ;
#38238=CARTESIAN_POINT ( 'NONE',  ( 14.27580295341549999, -22.41985674678640095, -45.43204315924410253 ) ) ;
#38243=DIRECTION ( 'NONE',  ( 1.000000000000000000, 2.460964292799963328E-14, 0.000000000000000000 ) ) ;
#38252=CARTESIAN_POINT ( 'NONE',  ( 10.83871905795021284, -21.53117133270660943, -32.52469633233020119 ) ) ;
#38253=PRODUCT_DEFINITION ( 'UNKNOWN', '', #12651, #48890 ) ;
#38257=ORIENTED_EDGE ( 'NONE', *, *, #43141, .F. ) ;
#38259=CARTESIAN_POINT ( 'NONE',  ( 9.366959348133711671, -14.73023002513620128, -41.49448685887290367 ) ) ;
#38262=CARTESIAN_POINT ( 'NONE',  ( 23.04447129454539933, -14.20655070842010126, -40.38876883061639234 ) ) ;
#38269=CARTESIAN_POINT ( 'NONE',  ( 9.489348988027188625, -19.79185572368299972, -38.10891372031139213 ) ) ;
#38272=CARTESIAN_POINT ( 'NONE',  ( 24.04491681007057480, -15.59668230724852300, -49.79154587196198634 ) ) ;
#38279=CARTESIAN_POINT ( 'NONE',  ( 22.90093587091927319, -15.61081685778595762, -62.45257565318340909 ) ) ;
#38280=CARTESIAN_POINT ( 'NONE',  ( 20.29261247985267502, -10.20487329796221054, -58.16115334902455203 ) ) ;
#38283=ORIENTED_EDGE ( 'NONE', *, *, #8638, .T. ) ;
#38285=CARTESIAN_POINT ( 'NONE',  ( 20.11809584606473678, -8.703681988134835734, -47.45899950725307548 ) ) ;
#38286=ORIENTED_EDGE ( 'NONE', *, *, #23589, .T. ) ;
#38292=CARTESIAN_POINT ( 'NONE',  ( 23.06214062797170072, -3.616188944679339823, -32.14999999999999858 ) ) ;
#38293=CARTESIAN_POINT ( 'NONE',  ( 22.89127052530449546, -15.22560942949823470, -72.43445116809684237 ) ) ;
#38296=CARTESIAN_POINT ( 'NONE',  ( 12.29178504908659875, -8.320944919562059283, -67.13803027067569928 ) ) ;
#38297=DIRECTION ( 'NONE',  ( 0.000000000000000000, 0.000000000000000000, -1.000000000000000000 ) ) ;
#38300=ORIENTED_EDGE ( 'NONE', *, *, #51108, .F. ) ;
#38302=CARTESIAN_POINT ( 'NONE',  ( 21.83716472214950244, -10.82245429508140155, -40.01016806583820085 ) ) ;
#38303=CARTESIAN_POINT ( 'NONE',  ( 8.886432599889248607, -17.14058911653749817, -32.14999999999999858 ) ) ;
#38304=CARTESIAN_POINT ( 'NONE',  ( 24.04493739769619864, -15.61618894467929941, -32.14999999999999858 ) ) ;
#38310=CARTESIAN_POINT ( 'NONE',  ( 20.89934259796100235, -8.887620450098559388, -63.20382097693880041 ) ) ;
#38313=B_SPLINE_CURVE_WITH_KNOTS ( 'NONE', 3,
 ( #42613, #22920, #38686, #6707, #18746, #23690, #23174, #43384, #11418, #47578, #15079, #3808, #51502, #7742, #30785, #39192, #42872, #15603 ),
 .UNSPECIFIED., .F., .F.,
 ( 4, 2, 2, 2, 2, 2, 2, 2, 4 ),
 ( 0.000000000000000000, 0.06249962094764476006, 0.1249992418952895201, 0.1874988628429342663, 0.2499984837905790402, 0.3124981047382238142, 0.3749977256858685326, 0.4374973466335133065, 0.4999969675811580805 ),
 .UNSPECIFIED. ) ;
#38320=CARTESIAN_POINT ( 'NONE',  ( 18.81513785123362936, -8.134968765430629745, -81.11711141586931717 ) ) ;
#38322=CARTESIAN_POINT ( 'NONE',  ( 12.75708233038401751, -8.434022097740552226, -65.15251670430993158 ) ) ;
#38340=EDGE_CURVE ( 'NONE', #40450, #5413, #45915, .T. ) ;
#38342=CARTESIAN_POINT ( 'NONE',  ( 10.38933687974308384, -19.70790301870552241, -47.65017322902551911 ) ) ;
#38343=ORIENTED_EDGE ( 'NONE', *, *, #23800, .F. ) ;
#38350=CARTESIAN_POINT ( 'NONE',  ( 14.36266436798912771, -22.20705554833075013, -45.03617451210310918 ) ) ;
#38357=CARTESIAN_POINT ( 'NONE',  ( 21.79569638026020328, -9.937173318903379737, -31.54232391275619563 ) ) ;
#38360=CARTESIAN_POINT ( 'NONE',  ( 22.87052914506156398, -16.27176351700221346, -50.48368888301278901 ) ) ;
#38362=CARTESIAN_POINT ( 'NONE',  ( 16.13734155123387026, -22.38318897308463917, -46.95266346626168286 ) ) ;
#38371=ADVANCED_FACE ( 'NONE', ( #49385 ), #13481, .T. ) ;
#38372=CARTESIAN_POINT ( 'NONE',  ( 24.34134549961779825, -14.82804368003519890, -35.47719510467199910 ) ) ;
#38383=CARTESIAN_POINT ( 'NONE',  ( 16.13393739769620083, -15.61618894467929941, -22.14999999999999858 ) ) ;
#38392=CARTESIAN_POINT ( 'NONE',  ( 19.61755955990300038, -9.030517303204650403, -50.72221764996669435 ) ) ;
#38394=ORIENTED_EDGE ( 'NONE', *, *, #32206, .F. ) ;
#38399=CARTESIAN_POINT ( 'NONE',  ( 24.04481203031673076, -15.61619115162449312, -61.50767625960597229 ) ) ;
#38400=CARTESIAN_POINT ( 'NONE',  ( 21.54530244994622379, -11.45757809935890137, -74.24448689220467656 ) ) ;
#38407=ORIENTED_EDGE ( 'NONE', *, *, #50096, .F. ) ;
#38417=CARTESIAN_POINT ( 'NONE',  ( 18.81810784640891399, -23.12961269479223603, -49.89815809426819015 ) ) ;
#38420=CARTESIAN_POINT ( 'NONE',  ( 10.52882599906690153, -21.10886349454530375, -78.76571924648798984 ) ) ;
#38424=CARTESIAN_POINT ( 'NONE',  ( 24.04493742325405137, -16.65172786793846882, -79.54933697072902987 ) ) ;
#38431=CARTESIAN_POINT ( 'NONE',  ( 8.537791930192160095, -13.64506687344660030, -52.36832131176279859 ) ) ;
#38434=ADVANCED_FACE ( 'NONE', ( #22345 ), #15014, .T. ) ;
#38440=CARTESIAN_POINT ( 'NONE',  ( 22.00297652178539920, -11.84456943261250039, -32.14999999999999858 ) ) ;
#38443=CARTESIAN_POINT ( 'NONE',  ( 24.04491913310489082, -15.59780088466810710, -45.50693619046535332 ) ) ;
#38447=CARTESIAN_POINT ( 'NONE',  ( 22.48516629158629954, -12.54952123915529860, -78.70399420596410778 ) ) ;
#38448=VERTEX_POINT ( 'NONE', #34657 ) ;
#38455=CARTESIAN_POINT ( 'NONE',  ( 9.166073574391180756, -14.52466137448119987, -73.50228201520940274 ) ) ;
#38456=CARTESIAN_POINT ( 'NONE',  ( 19.68346084944639784, -21.71073103174810015, -79.17930779234599470 ) ) ;
#38457=CARTESIAN_POINT ( 'NONE',  ( 15.09849273411411197, -7.705176520340744517, -67.25066374008305559 ) ) ;
#38462=ORIENTED_EDGE ( 'NONE', *, *, #12422, .T. ) ;
#38466=CARTESIAN_POINT ( 'NONE',  ( 24.04493137009028558, -15.60562024842286633, -39.50724629200023941 ) ) ;
#38475=DIRECTION ( 'NONE',  ( 1.000000000000000000, 0.000000000000000000, 0.000000000000000000 ) ) ;
#38485=CARTESIAN_POINT ( 'NONE',  ( 15.24822371850887670, -8.849178727619387175, -51.91115236531553734 ) ) ;
#38487=CARTESIAN_POINT ( 'NONE',  ( 9.835386274950829844, -10.93484284064630074, -41.21594592233229548 ) ) ;
#38492=CARTESIAN_POINT ( 'NONE',  ( 20.25033824699210072, -9.889252315854481168, -78.54555634383710583 ) ) ;
#38494=CARTESIAN_POINT ( 'NONE',  ( 9.421037744642760003, -13.45296509530860085, -41.94641019244480162 ) ) ;
#38495=CARTESIAN_POINT ( 'NONE',  ( 9.366937397696199596, -15.61618894467949836, -28.45282021618999835 ) ) ;
#38504=AXIS2_PLACEMENT_3D ( 'NONE', #23947, #39712, #8774 ) ;
#38514=CARTESIAN_POINT ( 'NONE',  ( 24.02557101327613154, -15.05142125834110089, -71.48493766499311164 ) ) ;
#38522=CARTESIAN_POINT ( 'NONE',  ( 22.88346836455789557, -14.35432754477256090, -40.78781185829218003 ) ) ;
#38525=CARTESIAN_POINT ( 'NONE',  ( 18.07474544453310017, -22.39673632833200045, -40.86408241699809452 ) ) ;
#38532=CARTESIAN_POINT ( 'NONE',  ( 18.42293784796460088, -23.12266782108029872, -39.69329234158379194 ) ) ;
#38540=CARTESIAN_POINT ( 'NONE',  ( 22.45032208304290577, -20.49099972680067339, -76.00127256676395859 ) ) ;
#38541=CARTESIAN_POINT ( 'NONE',  ( 22.75694797707483374, -14.18238632346227845, -62.38495220962165888 ) ) ;
#38542=DIRECTION ( 'NONE',  ( 0.000000000000000000, 0.000000000000000000, -1.000000000000000000 ) ) ;
#38547=CARTESIAN_POINT ( 'NONE',  ( 24.04493737206227877, -14.58064542962933352, -47.75066675682263906 ) ) ;
#38548=ORIENTED_EDGE ( 'NONE', *, *, #21330, .F. ) ;
#38561=CARTESIAN_POINT ( 'NONE',  ( 18.80293497738039932, -23.41741782066900157, -66.18740309791239440 ) ) ;
#38562=CARTESIAN_POINT ( 'NONE',  ( 9.221499647708412795, -19.60046634496452356, -48.34100205621588486 ) ) ;
#38566=CARTESIAN_POINT ( 'NONE',  ( 17.24066946489620022, -22.98380985896210049, -52.68519703601729987 ) ) ;
#38568=CARTESIAN_POINT ( 'NONE',  ( 9.036293696460461433, -17.93112585678219872, -32.14999999999999858 ) ) ;
#38574=CARTESIAN_POINT ( 'NONE',  ( 9.221490736555526979, -11.63192677752850024, -50.95899774428340834 ) ) ;
#38576=CARTESIAN_POINT ( 'NONE',  ( 19.78512659345921421, -8.570954873263845641, -61.15985033246573011 ) ) ;
#38577=CARTESIAN_POINT ( 'NONE',  ( 23.03293134511480034, -11.10103632018729947, -67.32320539224708966 ) ) ;
#38579=CARTESIAN_POINT ( 'NONE',  ( 20.11790897856640115, -22.39793288440460017, -32.14999999999999858 ) ) ;
#38588=CARTESIAN_POINT ( 'NONE',  ( 16.58613412942849408, -7.681895695860129436, -81.02569497777129470 ) ) ;
#38591=CARTESIAN_POINT ( 'NONE',  ( 24.04493737206098203, -15.04802456787528619, -65.76947574710013100 ) ) ;
#38596=LINE ( 'NONE', #30191, #46696 ) ;
#38611=ORIENTED_EDGE ( 'NONE', *, *, #24833, .F. ) ;
#38626=CARTESIAN_POINT ( 'NONE',  ( 8.497902144169069416, -12.50593227557700082, -32.91545205119220441 ) ) ;
#38629=CARTESIAN_POINT ( 'NONE',  ( 17.53270220351207698, -22.29603902678120519, -50.88730431063954995 ) ) ;
#38630=CARTESIAN_POINT ( 'NONE',  ( 10.22098660000356318, -19.02411275232799781, -47.28612486470034781 ) ) ;
#38636=AXIS2_PLACEMENT_3D ( 'NONE', #39069, #24063, #36144 ) ;
#38637=EDGE_CURVE ( 'NONE', #21295, #13019, #43106, .T. ) ;
#38640=EDGE_CURVE ( 'NONE', #16604, #32526, #26451, .T. ) ;
#38644=CARTESIAN_POINT ( 'NONE',  ( 11.24524132308850000, -22.25571999044219851, -34.20969220765409347 ) ) ;
#38661=CARTESIAN_POINT ( 'NONE',  ( 21.54527684569834989, -19.77483519589170058, -62.66115525799357044 ) ) ;
#38664=ADVANCED_FACE ( 'NONE', ( #24690 ), #355, .T. ) ;
#38667=CARTESIAN_POINT ( 'NONE',  ( 18.71541599555600044, -22.60494152200909923, -49.45471475294879582 ) ) ;
#38670=CARTESIAN_POINT ( 'NONE',  ( 12.72598263503342686, -21.52912116282474742, -69.11948608177338826 ) ) ;
#38679=ORIENTED_EDGE ( 'NONE', *, *, #16012, .T. ) ;
#38685=EDGE_LOOP ( 'NONE', ( #29302, #1417, #25412, #41692 ) ) ;
#38686=CARTESIAN_POINT ( 'NONE',  ( 9.507079698477085117, -14.03414070217627341, -79.52724392247833407 ) ) ;
#38697=EDGE_CURVE ( 'NONE', #23033, #37842, #37065, .T. ) ;
#38698=VECTOR ( 'NONE', #7273, 1000.000000000000000 ) ;
#38699=AXIS2_PLACEMENT_3D ( 'NONE', #20199, #48002, #28059 ) ;
#38704=CARTESIAN_POINT ( 'NONE',  ( 9.460335462710569132, -19.74532752270490121, -54.11113779516249878 ) ) ;
#38711=CARTESIAN_POINT ( 'NONE',  ( 21.39116947223989840, -11.14063841565600121, -32.14999999999999858 ) ) ;
#38715=CARTESIAN_POINT ( 'NONE',  ( 9.367498100245670756, -15.05912955991499658, -35.87337699974327165 ) ) ;
#38718=CARTESIAN_POINT ( 'NONE',  ( 9.185203505404999191, -16.82352339236760130, -73.79242048001970034 ) ) ;
#38725=DIRECTION ( 'NONE',  ( 1.000000000000000000, 2.460964292799963328E-14, 0.000000000000000000 ) ) ;
#38726=CARTESIAN_POINT ( 'NONE',  ( 13.89842162571510009, -9.131180857971619602, -81.84667608724390675 ) ) ;
#38728=CARTESIAN_POINT ( 'NONE',  ( 12.14988920053796306, -22.52875919624318257, -42.17433473518147480 ) ) ;
#38729=CARTESIAN_POINT ( 'NONE',  ( 21.54526587704876661, -19.77485033222403743, -40.66111538846325146 ) ) ;
#38732=VERTEX_POINT ( 'NONE', #45942 ) ;
#38737=CARTESIAN_POINT ( 'NONE',  ( 16.96763219941080081, -8.612796041803930436, -62.38489440685859222 ) ) ;
#38747=CARTESIAN_POINT ( 'NONE',  ( 22.89955372608299555, -15.46837744865813313, -46.44587548950233469 ) ) ;
#38752=CARTESIAN_POINT ( 'NONE',  ( 24.04493740047237083, -15.60197482040396721, -33.79175808096959344 ) ) ;
#38757=CARTESIAN_POINT ( 'NONE',  ( 22.45595482960829870, -10.96658216752249970, -45.81064392402229402 ) ) ;
#38761=CARTESIAN_POINT ( 'NONE',  ( 10.22105663364766848, -12.20814506941904831, -77.61948635994986034 ) ) ;
#38763=CARTESIAN_POINT ( 'NONE',  ( 16.91867857995320179, -8.607141901655479543, -46.38267033200749978 ) ) ;
#38764=CARTESIAN_POINT ( 'NONE',  ( 21.54526522592269444, -11.45752699557874088, -44.24446278245023478 ) ) ;
#38766=EDGE_CURVE ( 'NONE', #30137, #31815, #15802, .T. ) ;
#38773=AXIS2_PLACEMENT_3D ( 'NONE', #38953, #6979, #30540 ) ;
#38776=B_SPLINE_CURVE_WITH_KNOTS ( 'NONE', 3,
 ( #50263, #2562, #39236, #30829, #30317, #2824, #15130, #22450, #31087, #42917, #47115, #38728, #14349, #11204, #46341, #51028, #3334, #42396 ),
 .UNSPECIFIED., .F., .F.,
 ( 4, 2, 2, 2, 2, 2, 2, 2, 4 ),
 ( 0.4999993651278294982, 0.5624994444868508525, 0.6249995238458720959, 0.6874996032048934502, 0.7499996825639148046, 0.8124997619229360479, 0.8749998412819574023, 0.9374999206409786456, 1.000000000000000000 ),
 .UNSPECIFIED. ) ;
#38780=CARTESIAN_POINT ( 'NONE',  ( 24.04527307164895333, -15.61618901697373119, -57.79233174308600951 ) ) ;
#38781=CARTESIAN_POINT ( 'NONE',  ( 14.35738282767117902, -23.35377304929353315, -32.36411522678612585 ) ) ;
#38785=ORIENTED_EDGE ( 'NONE', *, *, #11718, .T. ) ;
#38787=CARTESIAN_POINT ( 'NONE',  ( 21.54530377845328815, -11.45757991958564048, -42.24448642716485125 ) ) ;
#38790=CARTESIAN_POINT ( 'NONE',  ( 21.81560882561450043, -11.43753264368949907, -46.25096972932429651 ) ) ;
#38793=CARTESIAN_POINT ( 'NONE',  ( 24.04493739769619864, -15.61618894467929941, -32.14999999999999858 ) ) ;
#38796=CARTESIAN_POINT ( 'NONE',  ( 21.66969093749800024, -20.60263879829989619, -81.30072504052380111 ) ) ;
#38798=DIRECTION ( 'NONE',  ( 1.000000000000000000, 0.000000000000000000, 0.000000000000000000 ) ) ;
#38805=ORIENTED_EDGE ( 'NONE', *, *, #40805, .T. ) ;
#38810=CARTESIAN_POINT ( 'NONE',  ( 15.09844379329638819, -7.705182437209532331, -47.25066575756055443 ) ) ;
#38821=CYLINDRICAL_SURFACE ( 'NONE', #16770, 7.910999999999997812 ) ;
#38823=CARTESIAN_POINT ( 'NONE',  ( 13.26310097102749985, -23.34542035971960061, -68.40553316769378966 ) ) ;
#38824=CARTESIAN_POINT ( 'NONE',  ( 14.06336589401369430, -23.32131682797999161, -48.09100240289522077 ) ) ;
#38829=CARTESIAN_POINT ( 'NONE',  ( 9.907410570274159056, -11.52509404568959894, -51.41769413899928765 ) ) ;
#38831=CARTESIAN_POINT ( 'NONE',  ( 9.011357356587289757, -17.82701623712219785, -32.14999999999999858 ) ) ;
#38833=CARTESIAN_POINT ( 'NONE',  ( 9.366908763506170743, -15.61636271700460021, -33.45282021618999835 ) ) ;
#38838=CARTESIAN_POINT ( 'NONE',  ( 21.33354701331730752, -9.619326380292379852, -61.23501538585083637 ) ) ;
#38839=CARTESIAN_POINT ( 'NONE',  ( 21.68697980347609899, -9.521400946021341127, -59.24287442375779733 ) ) ;
#38845=CARTESIAN_POINT ( 'NONE',  ( 18.38973105523400164, -21.99613282959019500, -81.23899999999999011 ) ) ;
#38851=DIRECTION ( 'NONE',  ( 1.000000000000000000, 2.460964292799963328E-14, 0.000000000000000000 ) ) ;
#38863=DIRECTION ( 'NONE',  ( 0.000000000000000000, 0.000000000000000000, -1.000000000000000000 ) ) ;
#38877=CARTESIAN_POINT ( 'NONE',  ( 18.16485855442270392, -23.27956588526017256, -77.92524956637772959 ) ) ;
#38880=DIRECTION ( 'NONE',  ( 1.062456999999999985E-16, -7.719205000000000365E-17, 1.000000000000000000 ) ) ;
#38889=CARTESIAN_POINT ( 'NONE',  ( 21.13657264101065181, -20.24127860378771615, -50.69013539568535975 ) ) ;
#38892=CARTESIAN_POINT ( 'NONE',  ( 11.97534086647365825, -10.20481231275635459, -63.74448752987081690 ) ) ;
#38899=CARTESIAN_POINT ( 'NONE',  ( 15.00846012470890045, -23.78417636420700276, -34.05125434552689967 ) ) ;
#38919=CARTESIAN_POINT ( 'NONE',  ( 8.891688449396310645, -17.36448082797300074, -67.99194462183578480 ) ) ;
#38921=ORIENTED_EDGE ( 'NONE', *, *, #43818, .F. ) ;
#38934=CARTESIAN_POINT ( 'NONE',  ( 22.84324496511920088, -11.76751259666689897, -81.23899999999999011 ) ) ;
#38949=EDGE_CURVE ( 'NONE', #17454, #16042, #8279, .T. ) ;
#38950=CARTESIAN_POINT ( 'NONE',  ( 21.75904242978619507, -11.76187703652407279, -40.26184854905846322 ) ) ;
#38953=CARTESIAN_POINT ( 'NONE',  ( 16.13393739769620083, -15.61618894467929941, -81.65000000000000568 ) ) ;
#38955=DIRECTION ( 'NONE',  ( 0.000000000000000000, 0.000000000000000000, 1.000000000000000000 ) ) ;
#38958=CARTESIAN_POINT ( 'NONE',  ( 16.55472973932799974, -7.779755955850329308, -56.80458145132549674 ) ) ;
#38965=CARTESIAN_POINT ( 'NONE',  ( 20.06281976506910070, -10.10654536788180025, -32.14999999999999858 ) ) ;
#38967=AXIS2_PLACEMENT_3D ( 'NONE', #33268, #278, #44559 ) ;
#38968=CARTESIAN_POINT ( 'NONE',  ( 8.738424198519890496, -18.52118839557869023, -32.38844566117526824 ) ) ;
#38974=CARTESIAN_POINT ( 'NONE',  ( 24.04493741069041235, -16.65172996398426264, -37.54933800668455035 ) ) ;
#38977=CARTESIAN_POINT ( 'NONE',  ( 22.38708172792839690, -18.87820445042670059, -73.00023116938359635 ) ) ;
#38985=CARTESIAN_POINT ( 'NONE',  ( 22.87259979537421728, -16.95485826009387864, -78.91015894931038588 ) ) ;
#38988=B_SPLINE_SURFACE_WITH_KNOTS ( 'NONE', 3, 3, ( 
 ( #24862, #21709, #9170, #40873, #4975, #37720, #1815, #20945, #17545, #1042, #17036, #32988, #25642, #49530, #13119, #33255, #37458, #29072, #21459, #41386, #45066, #25128, #41645, #25385, #41134, #33517, #9936, #5245, #21199, #17294, #33770, #9682, #37204, #29831, #49781, #41911, #1304, #49272, #5503, #13365, #29330, #45331, #9436, #13621, #29583, #14386, #6272, #7050, #23000, #3117, #42952, #47148, #19084, #22488, #2858, #50033, #30864, #30091, #42173, #10719, #35060, #18057, #18822, #34023, #26946, #14126, #2597, #38494, #18570, #39021, #46117, #18305, #10202, #51065, #46893, #26162, #22230, #14643, #34276, #50809, #7302, #15165, #2078, #26674, #34547, #42437, #30611, #23254, #50299, #38238, #22745, #2331, #30350, #34806, #11238, #38763, #50551, #14899, #27198, #46378, #10982, #10463, #26418, #46634, #42696, #31123, #6526, #6792, #43211, #51835, #47652, #20107, #3888, #20358, #16443, #32397, #47908, #4389, #40297, #39269, #19603, #35328, #3373, #51327, #36345, #19854, #40041, #8072, #44224, #11758, #455, #48158, #48418, #27457, #35844, #39530, #12262, #43967, #15678, #12519, #204, #12011, #36099, #8590, #32142, #24277, #8325, #24017, #16182, #15934, #51580, #28486, #35592, #4131, #27964, #3631, #31377, #28223, #44485, #19345, #15426, #31633, #47404, #11500, #43460, #7561, #23509, #31891, #27715, #43716, #7817, #23770, #39782, #37162, #32677, #997, #21661, #29282, #28762, #1259, #13574, #20900, #29538, #41342, #5459, #13075, #33210, #37413, #45542, #21412, #37667, #1515, #16996, #17500, #32944, #1771, #33469, #9637, #49487, #24555, #17246, #48971, #4928, #44764, #29028, #45025, #17752, #9124, #45284, #48704, #44503, #12808, #25593, #8867, #49228, #41598, #5706, #33722, #25077, #12538, #28505, #8605, #40568, #41092, #9393, #4664, #20637, #36624, #21155, #726, #5203, #25341, #13322, #16721, #24820, #40829, #36897, #13826, #26901, #46848, #34758, #30042, #42385, #34501, #50763, #6224, #46067, #7005, #19039, #37934, #14339, #26113, #14857, #14597, #22181, #50507, #2286, #30566, #18260, #46327, #10155, #29783, #34229, #38977, #2813, #42124, #45802, #21923, #38718, #18782, #49736, #46587, #3070, #9891, #33974, #6746, #10675, #41861, #30308, #18528, #30820, #42908, #22955, #6482, #10935, #25847, #5965, #38191, #2029, #18009, #49988, #14081, #10416, #26631, #42648, #50251, #26369, #22440, #22702, #38447, #2549, #31587, #35284, #8023, #39739, #11455, #36052, #47866, #7774, #15890, #4344, #27924, #20060, #39997, #3842, #11969, #47608 ),
 ( #43926, #35015, #32097, #23973, #44179, #48116, #43164, #23724, #3324, #40252, #51282, #31333, #4086, #39488, #47359, #39227, #162, #16137, #12215, #28177, #8278, #24227, #3586, #35803, #31078, #51019, #11194, #23207, #43674, #15119, #47105, #51787, #27156, #7258, #19301, #35548, #19558, #51538, #15379, #27413, #43416, #7517, #23465, #15635, #11708, #27671, #19815, #31845, #17186, #25536, #37353, #20312, #28959, #40764, #8801, #32874, #41540, #665, #411, #41024, #36301, #12470, #1194, #29478, #5140, #4865, #21094, #45484, #4595, #29217, #40506, #20570, #20832, #36830, #21349, #16398, #32354, #44440, #48907, #28694, #33143, #933, #9582, #45224, #1452, #25279, #48373, #9061, #24754, #12740, #16655, #16930, #13005, #28438, #44959, #49169, #36563, #8546, #32612, #41283, #48639, #25009, #33407, #13521, #17440, #37097, #49425, #13262, #24490, #9332, #5393, #44697, #10623, #38667, #42593, #14285, #22648, #10098, #22388, #26057, #50193, #38392, #42066, #25790, #21603, #34704, #2753, #6689, #37880, #30252, #42329, #18725, #14026, #1972, #14803, #26845, #45744, #22127, #33919, #50704, #2491, #29985, #6429, #6168, #18471, #38134, #2234, #17951, #37605, #18210, #46790, #26577, #49936, #1713, #29728, #46535, #30768, #5656, #34444, #10882, #17695, #41799, #14543, #50453, #49681, #34174, #26321, #46008, #10359, #46273, #5905, #13774, #30512, #33665, #9838, #21869, #19243, #39685, #32750, #20709, #4742, #31537, #23412, #19759, #31027, #35225, #3532, #36700, #15583, #11137, #31276, #801, #7724, #7201, #47555, #43872, #51231, #7970, #35750, #51732, #43366, #11651, #15827, #23920, #31792, #16802, #47810, #47309, #11916, #11397, #39943, #27870, #3010, #27616, #27359, #15323, #23156, #7458, #39433, #48777, #19503, #23668, #27107, #22902, #43110, #12881, #39173, #43622, #42855, #6951, #38919, #35493, #18982, #34963, #50960, #15059, #51483, #3790, #47052, #3268, #13904, #37489, #45882, #33286, #45615, #49304, #21490, #9714, #13399, #49042, #44842, #6045, #25930, #29861, #9204, #1590, #13651, #9969, #37237, #25156, #38011, #50063, #17066, #45363, #5275, #41944, #25674, #1335, #29612, #29357, #41676, #9467, #25414, #41162, #8947, #41416, #18085, #33801, #21225, #24889, #1068, #17828, #49811, #28838, #5783, #34054, #40901, #13149, #37752, #21744, #20972, #5535, #49565, #17324, #33547, #17578, #29099, #36972, #1849, #22002, #5011, #33018, #2107, #45097, #3408, #43245, #27229, #2889, #46667, #42987, #2361, #42468, #26709, #7334, #38796, #34316, #2630 ),
 ( #14674, #34840, #39054, #15194, #23032, #23282, #3148, #18602, #19115, #34579, #39304, #35095, #19375, #31154, #14159, #22776, #50584, #30643, #42728, #35358, #46409, #46147, #50839, #30127, #6303, #46924, #10236, #14931, #10750, #30896, #26195, #50329, #51095, #14416, #30385, #6823, #18855, #47181, #42205, #22262, #38269, #11009, #22522, #26978, #7082, #11269, #18338, #10496, #26453, #6556, #38532, #51358, #35626, #47436, #15457, #11530, #48190, #3922, #27997, #47942, #36129, #11790, #28254, #4163, #32174, #23541, #19883, #51613, #20139, #12044, #31662, #12295, #24051, #15967, #8106, #31408, #234, #44253, #8361, #40070, #16217, #31921, #27749, #24310, #43747, #27488, #43495, #3664, #39559, #51869, #7595, #19635, #15706, #47686, #7849, #23798, #39813, #44002, #35874, #14580, #51519, #46571, #42631, #39205, #50742, #6728, #50490, #51265, #15360, #47342, #35266, #39469, #11438, #14840, #47087, #42368, #23189, #22425, #34484, #3050, #27397, #10399, #11176, #26353, #19284, #6469, #46831, #30802, #10919, #31316, #38431, #10658, #2533, #43398, #3305, #18511, #30546, #6986, #26616, #43146, #22684, #38704, #7241, #35529, #23446, #7497, #34996, #26881, #3571, #2792, #18764, #22939, #19538, #19020, #34737, #42892, #15619, #27143, #38958, #51001, #46310, #15100, #31061, #8525, #24473, #32080, #394, #4577, #32592, #40485, #40748, #20550, #20041, #36545, #142, #4847, #651, #48622, #16634, #43656, #20295, #36034, #23956, #11950, #16119, #48098, #20814, #12197, #12450, #51769, #11691, #15873, #12722, #27905, #36283, #44679, #24733, #28677, #28158, #8782, #36808, #914, #31572, #44162, #28420, #47592, #27653, #7758, #40235, #23706, #8258, #48356, #24211, #4325, #44424, #16378, #31828, #39720, #3824, #19797, #35786, #43909, #32336, #47844, #8003, #39978, #4072, #26037, #38116, #5122, #33389, #45205, #17931, #33647, #41266, #17679, #21331, #49666, #37337, #13504, #49151, #48884, #1438, #6150, #21851, #9316, #12988, #41010, #5887, #37858, #16909, #1695, #22105, #32855, #1175, #25774, #13754, #9044, #49408, #37584, #13247, #21586, #41522, #17170, #24990, #41781, #25516, #28939, #29711, #17423, #29460, #29197, #44943, #45465, #21075, #1954, #25260, #37078, #33122, #33902, #49914, #5375, #45722, #9564, #5640, #9823, #14008, #29968, #45986, #10078, #42047, #34421, #6928, #26823, #2463, #46251, #27085, #10856, #23385, #14267, #30489, #50939, #43344, #31255, #15300, #42833, #34680, #31004, #42308, #46512, #14779, #47286, #22882, #22367, #42571, #11376, #18960 ),
 ( #43088, #3247, #11116, #27340, #7180, #6663, #23137, #22628, #7437, #39151, #19219, #35205, #30234, #38899, #38644, #10601, #50432, #2732, #18705, #2212, #50681, #34940, #38372, #34155, #18451, #51207, #14521, #2987, #18190, #50170, #10340, #30747, #26298, #47031, #6408, #26557, #46770, #15035, #44359, #20489, #24411, #48043, #4516, #43850, #4265, #7946, #32019, #20235, #23896, #7701, #3511, #16570, #36479, #40423, #19735, #12142, #24150, #585, #47786, #35728, #48553, #8721, #27591, #4017, #15805, #32525, #36224, #11894, #40170, #39921, #43599, #8464, #12661, #28614, #28354, #44615, #39410, #19978, #335, #35469, #16318, #15561, #23645, #28097, #19478, #51461, #32273, #31515, #12391, #47533, #35972, #91, #16062, #11630, #39661, #3767, #51711, #31766, #48295, #27848, #44105, #8204, #40943, #21530, #29904, #41718, #24669, #33327, #45139, #13189, #37274, #45921, #5054, #4783, #45402, #40684, #16843, #5574, #33840, #9507, #9250, #25454, #49855, #8985, #33590, #44880, #24930, #25199, #41205, #25711, #20752, #36739, #48815, #1374, #33060, #37527, #5314, #5825, #1891, #17869, #49344, #21788, #37797, #846, #21014, #32792, #12923, #28878, #13945, #21270, #41458, #1630, #29652, #49085, #37012, #49605, #1111, #17107, #17361, #29139, #13692, #29402, #13442, #17621, #45656, #9759, #42769, #31190, #2927, #46971, #14973, #30688, #38839, #22561, #22303, #30940, #2397, #46711, #39093, #22041, #41986, #10537, #11054, #18896, #10012, #7125, #34882, #19159, #23076, #18129, #50621, #30172, #15241, #10275, #6344, #50881, #14457, #38310, #27020, #25973, #3188, #43028, #35138, #51143, #34092, #14718, #46192, #6088, #26238, #18381, #38055, #30425, #34356, #14202, #2149, #50106, #42245, #50373, #46451, #26494, #42511, #10796, #6599, #38577, #2671, #18643, #34618, #26756, #6869, #22817, #27276, #20177, #11311, #47725, #31700, #11831, #274, #43285, #11569, #7374, #48235, #40109, #19421, #23323, #7888, #27529, #44041, #525, #12330, #47222, #3961, #15747, #35668, #23834, #16511, #43537, #39348, #16004, #3448, #35400, #28037, #4459, #31961, #27790, #47981, #20430, #31449, #4205, #15497, #47477, #43786, #39856, #28290, #51397, #7636, #23582, #19921, #3703, #8144, #35914, #44293, #24350, #40364, #31, #8401, #36417, #39599, #19671, #51652, #12083, #24089, #36166, #16257, #32212, #1313, #37467, #4987, #45595, #41394, #49539, #20686, #29080, #32727, #5511, #37213, #8924, #33525, #45339, #5253, #13376, #1825, #25392, #17557, #1566, #17303, #9445, #45073 ) ),
 .UNSPECIFIED., .F., .F., .F.,
 ( 4, 4 ),
 ( 4, 1, 1, 1, 1, 1, 1, 1, 1, 1, 1, 1, 1, 1, 1, 1, 1, 1, 1, 1, 1, 1, 1, 1, 1, 1, 1, 1, 1, 1, 1, 1, 1, 1, 1, 1, 1, 1, 1, 1, 1, 1, 1, 1, 1, 1, 1, 1, 1, 1, 1, 1, 1, 1, 1, 1, 1, 1, 1, 1, 1, 1, 1, 1, 1, 1, 1, 1, 1, 1, 1, 1, 1, 1, 1, 1, 1, 1, 1, 1, 1, 1, 1, 1, 1, 1, 1, 1, 1, 1, 1, 1, 1, 1, 1, 1, 1, 1, 1, 1, 1, 1, 1, 1, 1, 1, 1, 1, 1, 1, 1, 1, 1, 1, 1, 1, 1, 1, 1, 1, 1, 1, 1, 1, 1, 1, 1, 1, 1, 1, 1, 1, 1, 1, 1, 1, 1, 1, 1, 1, 1, 1, 1, 1, 1, 1, 1, 1, 1, 1, 1, 1, 1, 1, 1, 1, 1, 1, 1, 1, 1, 1, 1, 1, 1, 1, 1, 1, 1, 1, 1, 1, 1, 1, 1, 1, 1, 1, 1, 1, 1, 1, 1, 1, 1, 1, 1, 1, 1, 1, 1, 1, 1, 1, 1, 1, 1, 1, 1, 1, 1, 1, 1, 1, 1, 1, 1, 1, 1, 1, 1, 1, 1, 1, 1, 1, 1, 1, 1, 1, 1, 1, 1, 1, 1, 1, 1, 1, 1, 1, 1, 1, 1, 1, 1, 1, 1, 1, 1, 1, 1, 1, 1, 1, 1, 1, 1, 1, 1, 1, 1, 1, 1, 1, 1, 1, 1, 1, 1, 1, 1, 1, 1, 1, 1, 1, 1, 1, 1, 1, 1, 1, 1, 1, 1, 1, 1, 1, 1, 1, 1, 1, 1, 1, 1, 1, 1, 1, 1, 1, 1, 1, 1, 1, 1, 1, 1, 1, 1, 1, 1, 1, 1, 1, 1, 1, 1, 1, 1, 1, 1, 1, 1, 1, 4 ),
 ( 0.000000000000000000, 0.1320977415905860153 ),
 ( 8.301129254626310683, 8.798876478335710516, 9.296623702045119231, 9.794370925754529722, 10.29211814946389936, 10.78986537317329919, 11.28761259688270080, 11.78535982059210063, 12.28310704430160172, 12.78085426801099977, 13.27860149172039961, 13.77634871542980122, 14.27409593913919927, 14.77184316284859911, 15.26959038655800072, 15.76733761026740055, 16.26508483397680038, 16.76283205768620022, 17.26057928139560005, 17.75832650510499988, 18.25607372881439971, 18.75382095252380310, 19.25156817623319938, 19.74931539994259921, 20.24706262365200260, 20.74480984736149836, 21.24255707107090174, 21.74030429478030157, 22.23805151848970141, 22.73579874219910124, 23.23354596590850107, 23.73129318961789735, 24.22904041332729719, 24.72678763703670057, 25.22453486074610041, 25.72228208445550024, 26.22002930816490007, 26.71777653187429991, 27.21552375558369974, 27.71327097929309957, 28.21101820300250296, 28.70876542671189924, 29.20651265042139855, 29.70425987413079838, 30.20200709784019821, 30.69975432154959805, 31.19750154525900143, 31.69524876896840127, 32.19299599267780110, 32.69074321638719738, 33.18849044009660076, 33.68623766380599704, 34.18398488751540043, 34.68173211122479671, 35.17947933493420010, 35.67722655864360348, 36.17497378235299976, 36.67272100606240315, 37.17046822977179943, 37.66821545348130229, 38.16596267719069857, 38.66370990090010196, 39.16145712460949824, 39.65920434831890162, 40.15695157202829790, 40.65469879573769418, 41.15244601944709757, 41.65019324315649385, 42.14794046686590434, 42.64568769057530062, 43.14343491428470401, 43.64118213799410029, 44.13892936170350367, 44.63667658541289995, 45.13442380912230334, 45.63217103283169962, 46.12991825654119538, 46.62766548025059876, 47.12541270395999504, 47.62315992766939843, 48.12090715137879471, 48.61865437508820520, 49.11640159879760148, 49.61414882250700487, 50.11189604621640115, 50.60964326992579743, 51.10739049363520081, 51.60513771734459709, 52.10288494105400048, 52.60063216476339676, 53.09837938847280014, 53.59612661218219642, 54.09387383589159981, 54.59162105960110267, 55.08936828331050606, 55.58711550701990234, 56.08486273072930572, 56.58260995443870200, 57.08035717814809828, 57.57810440185750167, 58.07585162556689795, 58.57359884927630134, 59.07134607298569762, 59.56909329669510100, 60.06684052040449728, 60.56458774411389356, 61.06233496782330405, 61.56008219153270034, 62.05782941524210372, 62.55557663895150000, 63.05332386266090339, 63.55107108637029967, 64.04881831007979542, 64.54656553378920592, 65.04431275749860220, 65.54205998120799848, 66.03980720491739476, 66.53755442862680525, 67.03530165233620153, 67.53304887604559781, 68.03079609975499409, 68.52854332346439037, 69.02629054717380086, 69.52403777088319714, 70.02178499459259342, 70.51953221830200391, 71.01727944201140019, 71.51502666572079647, 72.01277388943020696, 72.51052111313960324, 73.00826833684909900, 73.50601556055850949, 74.00376278426789156, 74.50151000797730205, 74.99925723168669833, 75.49700445539609461, 75.99475167910550510, 76.49249890281490138, 76.99024612652429767, 77.48799335023369395, 77.98574057394310444, 78.48348779765250072, 78.98123502136189700, 79.47898224507130749, 79.97672946878068956, 80.47447669249010005, 80.97222391619961002, 81.46997113990889261, 81.96771836361840258, 82.46546558732779886, 82.96321281103719514, 83.46096003474660563, 83.95870725845600191, 84.45645448216539819, 84.95420170587479447, 85.45194892958420496, 85.94969615329360124, 86.44744337700299752, 86.94519060071240801, 87.44293782442179008, 87.94068504813120057, 88.43843227184059685, 88.93617949555000735, 89.43392671925940363, 89.93167394296891359, 90.42942116667829566, 90.92716839038770615, 91.42491561409710243, 91.92266283780649871, 92.42041006151590921, 92.91815728522529128, 93.41590450893470177, 93.91365173264409805, 94.41139895635349433, 94.90914618006290482, 95.40689340377230110, 95.90464062748169738, 96.40238785119109366, 96.90013507490050415, 97.39788229860990043, 97.89562952231929671, 98.39337674602870720, 98.89112396973820296, 99.38887119344759924, 99.88661841715700973, 100.3843656408659939, 100.8821128645760012, 101.3798600882849996, 101.8776073119949928, 102.3753545357040053, 102.8731017594130037, 103.3708489831229969, 103.8685962068319952, 104.3663434305420026, 104.8640906542510010, 105.3618378779599993, 105.8595851016700067, 106.3573323253789908, 106.8550795490889982, 107.3528267727979966, 107.8505739965069949, 108.3483212202170023, 108.8460684439259865, 109.3438156676359938, 109.8415628913450064, 110.3393101150540048, 110.8370573387639979, 111.3348045624730105, 111.8325517861829894, 112.3302990098920020, 112.8280462336020094, 113.3257934573109935, 113.8235406810200061, 114.3212879047299992, 114.8190351284389976, 115.3167823521490050, 115.8145295758580033, 116.3122767995670017, 116.8100240232769949, 117.3077712469860074, 117.8055184706960006, 118.3032656944049990, 118.8010129181139973, 119.2987601418239905, 119.7965073655330031, 120.2942545892429962, 120.7920018129519946, 121.2897490366610072, 121.7874962603710003, 122.2852434840799987, 122.7829907077900060, 123.2807379314990044, 123.7784851552080028, 124.2762323789180101, 124.7739796026270085, 125.2717268263370016, 125.7694740500460000, 126.2672212737549984, 126.7649684974650057, 127.2627157211740041, 127.7604629448839972, 128.2582101685930240, 128.7559573923030030, 129.2537046160119871, 129.7514518397209997, 130.2491990634310071, 130.7469462871399912, 131.2446935108499986, 131.7424407345590112, 132.2401879582679953, 132.7379351819779743, 133.2356824056870153, 133.7334296293969942, 134.2311768531059784, 134.7289240768150194, 135.2266713005249983, 135.7244185242340109, 136.2221657479440182, 136.7199129716530024, 137.2176601953619866, 137.7154074190719939, 138.2131546427810065, 138.7109018664909854, 139.2086490901999980, 139.7063963139089822, 140.2041435376189895, 140.7018907613280021, 141.1996379850380094, 141.6973852087470220, 142.1951324324560062, 142.6928796561659851, 143.1906268798749977, 143.6883741035850051, 144.1861213272939892, 144.6838685510039966, 145.1816157747130092, 145.6793629984219933, 146.1771102221320007, 146.6748574458410133, 147.1726046695509922, 147.6703518932600048, 148.1680991169690174, 148.6658463406789963, 149.1635935643879805, 149.6613407880980162, 150.1590880118070004, 150.6568352355159846, 151.1545824592260203, 151.6523296829350045, 152.1500769066449834, 152.6478241303539960, 153.1455713540630086, 153.6433185777729875, 154.1410658014820001, 154.6388130251920074, 155.1365602489009916, 155.6343074726100042, 156.1320546963200115, 156.6298019200289957, 157.1275491437390031, 157.6252963674480156, 158.1230435911569998, 158.6207908148670072, 159.1185380385759913, 159.6162852622859987, 160.1140324859950113, 160.6117797097039954, 161.1095269334140028, 161.6072741571230154, 162.1050213808329943, 162.6027686045419784, 163.1005158282520142, 163.5982630519609984, 164.0960102756699825, 164.5937574993799899 ),
 .UNSPECIFIED. ) ;
#38990=DIRECTION ( 'NONE',  ( 1.000000000000000000, 0.000000000000000000, 0.000000000000000000 ) ) ;
#38995=CARTESIAN_POINT ( 'NONE',  ( 20.21022320103229930, -9.860630481422070659, -62.54333226898589260 ) ) ;
#38999=ADVANCED_FACE ( 'NONE', ( #22709 ), #7265, .T. ) ;
#39000=CARTESIAN_POINT ( 'NONE',  ( 23.79191500766741996, -17.66738227821284113, -55.59098426646090729 ) ) ;
#39003=DIRECTION ( 'NONE',  ( -0.8660254037844384856, 0.5000000000000003331, 0.000000000000000000 ) ) ;
#39010=CARTESIAN_POINT ( 'NONE',  ( 20.11812491441067152, -22.52867852696467210, -48.12566617391976109 ) ) ;
#39013=CIRCLE ( 'NONE', #39855, 3.076499999999999346 ) ;
#39014=CARTESIAN_POINT ( 'NONE',  ( 8.779189791706480506, -18.35378556284099716, -40.89907019807789368 ) ) ;
#39021=CARTESIAN_POINT ( 'NONE',  ( 14.29653415316120046, -8.806893203457351049, -42.26328591669919632 ) ) ;
#39023=ORIENTED_EDGE ( 'NONE', *, *, #41450, .T. ) ;
#39024=DIRECTION ( 'NONE',  ( -1.000000000000000000, 0.000000000000000000, 0.000000000000000000 ) ) ;
#39029=CARTESIAN_POINT ( 'NONE',  ( 18.20467892795669229, -7.911106368036362468, -47.09100263401473541 ) ) ;
#39031=CARTESIAN_POINT ( 'NONE',  ( 13.64499661450167878, -17.42451027335708602, -22.14999999999999858 ) ) ;
#39035=CARTESIAN_POINT ( 'NONE',  ( 14.38779660597143462, -7.866279551837843442, -64.93722419047314531 ) ) ;
#39037=CARTESIAN_POINT ( 'NONE',  ( 11.82116268612174359, -8.893085577089458127, -70.82645228965780859 ) ) ;
#39045=CARTESIAN_POINT ( 'NONE',  ( 22.22400857603370028, -12.05900013647219993, -40.67890729542689598 ) ) ;
#39048=CARTESIAN_POINT ( 'NONE',  ( 9.809908155058138846, -12.49381599532109988, -55.59880359483129553 ) ) ;
#39054=CARTESIAN_POINT ( 'NONE',  ( 9.773944590104200358, -20.21402263050010006, -32.08827495947629416 ) ) ;
#39060=CARTESIAN_POINT ( 'NONE',  ( 9.807676903462912321, -20.47774473141403817, -40.58400665967682386 ) ) ;
#39064=EDGE_LOOP ( 'NONE', ( #14644, #10997, #21015, #40598 ) ) ;
#39069=CARTESIAN_POINT ( 'NONE',  ( 16.13393739769620083, -15.61618894467929941, -28.45282021618999835 ) ) ;
#39071=CARTESIAN_POINT ( 'NONE',  ( 17.48820068928834459, -23.48304697401851016, -44.23826555476666300 ) ) ;
#39080=CARTESIAN_POINT ( 'NONE',  ( 22.55256813713110020, -20.79150531053719675, -60.00832647494999605 ) ) ;
#39082=ORIENTED_EDGE ( 'NONE', *, *, #45689, .T. ) ;
#39083=ORIENTED_EDGE ( 'NONE', *, *, #42745, .F. ) ;
#39086=CARTESIAN_POINT ( 'NONE',  ( 18.90477078506000197, -8.700324852274359699, -55.85395427856209949 ) ) ;
#39090=CARTESIAN_POINT ( 'NONE',  ( 8.222937397696199469, -15.61618894467929941, -32.14999999999999858 ) ) ;
#39093=CARTESIAN_POINT ( 'NONE',  ( 11.58913342612299857, -22.49568584263250415, -60.19350159652129406 ) ) ;
#39094=CARTESIAN_POINT ( 'NONE',  ( 21.52056153400079808, -21.16699044271719998, -32.14999999999999858 ) ) ;
#39101=DIRECTION ( 'NONE',  ( 1.000000000000000000, 0.000000000000000000, 0.000000000000000000 ) ) ;
#39106=CARTESIAN_POINT ( 'NONE',  ( 20.69249140832376810, -9.085681294808187758, -65.48617898402430626 ) ) ;
#39109=CARTESIAN_POINT ( 'NONE',  ( 23.52846977382590055, -14.70647209751679974, -78.19369283850278407 ) ) ;
#39124=EDGE_CURVE ( 'NONE', #10051, #13019, #25163, .T. ) ;
#39125=CARTESIAN_POINT ( 'NONE',  ( 17.65201533994627070, -8.962439695671685413, -66.02401901343213808 ) ) ;
#39129=EDGE_CURVE ( 'NONE', #7977, #15209, #28876, .T. ) ;
#39135=CARTESIAN_POINT ( 'NONE',  ( 22.91193804342860574, -14.92565144664893850, -80.42032930067895791 ) ) ;
#39141=CARTESIAN_POINT ( 'NONE',  ( 16.65784958574153407, -23.52864899547403610, -50.27127475680247670 ) ) ;
#39146=CARTESIAN_POINT ( 'NONE',  ( 9.367501421782780113, -15.61622054991689978, -37.45282021618999835 ) ) ;
#39151=CARTESIAN_POINT ( 'NONE',  ( 24.05051738721850185, -13.31173972757300028, -33.41750289701789711 ) ) ;
#39152=VERTEX_POINT ( 'NONE', #25544 ) ;
#39173=CARTESIAN_POINT ( 'NONE',  ( 20.68452214731360428, -21.51524588413079897, -67.35819317332679645 ) ) ;
#39180=CARTESIAN_POINT ( 'NONE',  ( 9.077368987888030816, -13.86164298377170034, -81.23899999999999011 ) ) ;
#39184=ORIENTED_EDGE ( 'NONE', *, *, #3375, .T. ) ;
#39188=CARTESIAN_POINT ( 'NONE',  ( 21.96651055732200319, -10.35688966336140027, -81.23899999999999011 ) ) ;
#39190=STYLED_ITEM ( 'NONE', ( #35896 ), #44821 ) ;
#39192=CARTESIAN_POINT ( 'NONE',  ( 21.86911740259973413, -11.93844100352546000, -80.27148098536147813 ) ) ;
#39205=CARTESIAN_POINT ( 'NONE',  ( 9.741898527687681053, -20.16905477484420217, -48.09049903432729423 ) ) ;
#39216=DIRECTION ( 'NONE',  ( 1.000000000000000000, 2.460964292799963328E-14, 0.000000000000000000 ) ) ;
#39217=DIRECTION ( 'NONE',  ( 0.000000000000000000, 0.000000000000000000, -1.000000000000000000 ) ) ;
#39218=EDGE_CURVE ( 'NONE', #38090, #13535, #11456, .T. ) ;
#39225=CARTESIAN_POINT ( 'NONE',  ( 8.222339619445261150, -15.61627490117209938, -70.79233150823699816 ) ) ;
#39227=CARTESIAN_POINT ( 'NONE',  ( 9.388128293077700803, -18.77858577391589989, -33.92780426447939846 ) ) ;
#39234=CARTESIAN_POINT ( 'NONE',  ( 16.13393739769620083, -15.61618894467929941, -28.45282021618999835 ) ) ;
#39235=CARTESIAN_POINT ( 'NONE',  ( 24.04508668034977248, -15.61618904219531778, -35.79233368253564862 ) ) ;
#39236=CARTESIAN_POINT ( 'NONE',  ( 23.83903754356633797, -17.68686498457494238, -41.59100066116396732 ) ) ;
#39250=CARTESIAN_POINT ( 'NONE',  ( 21.14288210468432183, -10.65101126812107957, -32.59857632693771734 ) ) ;
#39256=VERTEX_POINT ( 'NONE', #9590 ) ;
#39263=CARTESIAN_POINT ( 'NONE',  ( 8.328589087560620996, -16.43061226767880001, -48.97940116656710074 ) ) ;
#39269=CARTESIAN_POINT ( 'NONE',  ( 12.69742525569020053, -9.457216345917659694, -50.18517902306119538 ) ) ;
#39275=ADVANCED_FACE ( 'NONE', ( #1460 ), #45752, .T. ) ;
#39278=CARTESIAN_POINT ( 'NONE',  ( 8.223454620794861114, -15.61605491354059971, -46.50766849176290663 ) ) ;
#39285=CARTESIAN_POINT ( 'NONE',  ( 17.01354725415873759, -23.50622319154220818, -32.25706115642341842 ) ) ;
#39287=ORIENTED_EDGE ( 'NONE', *, *, #23115, .T. ) ;
#39292=B_SPLINE_CURVE_WITH_KNOTS ( 'NONE', 3,
 ( #20514, #610, #49627, #32549, #49112, #41227, #25222, #29422, #5341, #12685, #28638, #32817, #37037, #1135, #37549, #37298, #33613, #9531 ),
 .UNSPECIFIED., .F., .F.,
 ( 4, 2, 2, 2, 2, 2, 2, 2, 4 ),
 ( 0.000000000000000000, 0.06250012490808277976, 0.1250002498161655595, 0.1875003747242483532, 0.2500004996323311190, 0.3125006245404138849, 0.3750007494484967063, 0.4375008743565794722, 0.5000009992646622381 ),
 .UNSPECIFIED. ) ;
#39297=CARTESIAN_POINT ( 'NONE',  ( 21.56449732505549832, -11.11601366231700005, -56.23255504334029098 ) ) ;
#39302=ORIENTED_EDGE ( 'NONE', *, *, #16144, .T. ) ;
#39304=CARTESIAN_POINT ( 'NONE',  ( 23.80184081761380099, -17.28652279287269877, -33.35577785649419980 ) ) ;
#39306=ORIENTED_EDGE ( 'NONE', *, *, #14140, .T. ) ;
#39310=CARTESIAN_POINT ( 'NONE',  ( 8.223148984577919762, -15.61599292915740023, -40.79233150823699816 ) ) ;
#39316=CYLINDRICAL_SURFACE ( 'NONE', #22694, 6.766999999999998572 ) ;
#39323=DIRECTION ( 'NONE',  ( 1.000000000000000000, 2.460964292799963328E-14, 0.000000000000000000 ) ) ;
#39325=CARTESIAN_POINT ( 'NONE',  ( 18.20459673516950261, -7.911083136343404654, -69.37566667060073655 ) ) ;
#39327=CARTESIAN_POINT ( 'NONE',  ( 8.790427394441779896, -19.36526628291030150, -60.64207792345899151 ) ) ;
#39337=CARTESIAN_POINT ( 'NONE',  ( 19.73032284921290369, -9.091412665812349303, -51.89300772538119588 ) ) ;
#39338=AXIS2_PLACEMENT_3D ( 'NONE', #46768, #27077, #6923 ) ;
#39341=CARTESIAN_POINT ( 'NONE',  ( 9.539384564179858472, -19.34381366239919942, -32.14999999999999858 ) ) ;
#39343=CONICAL_SURFACE ( 'NONE', #16736, 12.92820323027549989, 0.7481802937784480800 ) ;
#39346=EDGE_CURVE ( 'NONE', #1287, #1526, #20804, .T. ) ;
#39348=CARTESIAN_POINT ( 'NONE',  ( 7.967372319093019684, -14.48043565900760044, -72.55165484244589891 ) ) ;
#39349=EDGE_CURVE ( 'NONE', #10310, #1136, #36394, .T. ) ;
#39350=CARTESIAN_POINT ( 'NONE',  ( 20.82227175848069933, -21.85412434938530168, -32.14999999999999858 ) ) ;
#39360=DIRECTION ( 'NONE',  ( 0.000000000000000000, 0.000000000000000000, -1.000000000000000000 ) ) ;
#39362=CARTESIAN_POINT ( 'NONE',  ( 23.22922891231669951, -13.34384827310289978, -76.13400063084860392 ) ) ;
#39369=CARTESIAN_POINT ( 'NONE',  ( 17.80236287562073016, -23.36212981481903483, -61.94013304973208278 ) ) ;
#39379=VERTEX_POINT ( 'NONE', #25452 ) ;
#39381=CARTESIAN_POINT ( 'NONE',  ( 12.67868222463649808, -21.76466606210399846, -37.51015005288219584 ) ) ;
#39382=CARTESIAN_POINT ( 'NONE',  ( 14.36277553031169596, -22.20708433113889058, -59.03615343158287487 ) ) ;
#39386=VERTEX_POINT ( 'NONE', #9754 ) ;
#39392=CARTESIAN_POINT ( 'NONE',  ( 24.15879671053109945, -17.50942769270979937, -33.86607922395569403 ) ) ;
#39395=CARTESIAN_POINT ( 'NONE',  ( 24.03634747343981104, -15.99279584001448917, -49.80748426219081182 ) ) ;
#39399=CARTESIAN_POINT ( 'NONE',  ( 17.90521437699635854, -9.025324052677705211, -64.03615484355167098 ) ) ;
#39401=CARTESIAN_POINT ( 'NONE',  ( 23.03046715727910154, -11.87124236738749872, -73.85414552054359660 ) ) ;
#39410=CARTESIAN_POINT ( 'NONE',  ( 15.48260933934249906, -23.83558627473800229, -44.03283965954289414 ) ) ;
#39432=B_SPLINE_CURVE_WITH_KNOTS ( 'NONE', 3,
 ( #13467, #8746, #25481, #24694, #40712, #28902, #12946, #44904, #41485, #9010 ),
 .UNSPECIFIED., .F., .F.,
 ( 4, 1, 1, 1, 1, 1, 1, 4 ),
 ( 0.5000038607551413605, 0.5558869319517651952, 0.6351058630153233464, 0.7143247940790398154, 0.7935437251426000760, 0.8727626562061583382, 0.9519815872698746961, 1.000000000000000000 ),
 .UNSPECIFIED. ) ;
#39433=CARTESIAN_POINT ( 'NONE',  ( 8.703688250329728149, -15.07021097222849981, -66.09069027630890503 ) ) ;
#39436=ORIENTED_EDGE ( 'NONE', *, *, #1565, .T. ) ;
#39438=CARTESIAN_POINT ( 'NONE',  ( 11.61470965350185125, -20.68213784063762972, -35.18459255138716912 ) ) ;
#39440=CARTESIAN_POINT ( 'NONE',  ( 12.72603970786425975, -9.703224440543703366, -73.78615355345934290 ) ) ;
#39441=CARTESIAN_POINT ( 'NONE',  ( 8.975894543716849583, -15.11915247762119918, -81.23899999999999011 ) ) ;
#39447=CARTESIAN_POINT ( 'NONE',  ( 22.58862951581259892, -11.28899428718860065, -81.23899999999999011 ) ) ;
#39454=CARTESIAN_POINT ( 'NONE',  ( 23.83903502047883194, -13.54550035082508508, -53.42433795965683885 ) ) ;
#39464=CARTESIAN_POINT ( 'NONE',  ( 16.13393739769620083, -15.61618894467929941, -32.14999999999999858 ) ) ;
#39469=CARTESIAN_POINT ( 'NONE',  ( 23.78998258546389977, -17.34005676619050007, -49.35800193134529934 ) ) ;
#39470=ADVANCED_FACE ( 'NONE', ( #13440 ), #33585, .T. ) ;
#39481=CARTESIAN_POINT ( 'NONE',  ( 12.04533177224588236, -22.42911352436259875, -32.17980570764689929 ) ) ;
#39485=FACE_OUTER_BOUND ( 'NONE', #8643, .T. ) ;
#39488=CARTESIAN_POINT ( 'NONE',  ( 15.11696271606249908, -22.99673460733349728, -33.61092854022489718 ) ) ;
#39511=DIRECTION ( 'NONE',  ( 1.000000000000000000, 0.000000000000000000, 0.000000000000000000 ) ) ;
#39513=CARTESIAN_POINT ( 'NONE',  ( 15.64891603104893392, -8.847981134172776763, -45.93003584796989003 ) ) ;
#39523=CARTESIAN_POINT ( 'NONE',  ( 12.98069885294330028, -22.80255341299470118, -58.64411075632859394 ) ) ;
#39529=CARTESIAN_POINT ( 'NONE',  ( 10.22106801927327346, -19.02425228399541979, -39.28615407111802682 ) ) ;
#39530=CARTESIAN_POINT ( 'NONE',  ( 22.63286885114739988, -12.87639896407969964, -52.72018481709699955 ) ) ;
#39532=EDGE_LOOP ( 'NONE', ( #39946, #28697, #21561, #25557 ) ) ;
#39537=CARTESIAN_POINT ( 'NONE',  ( 8.223439258000311725, -15.61632852289070073, -42.50766849176289952 ) ) ;
#39554=CARTESIAN_POINT ( 'NONE',  ( 10.07334972078679947, -19.22338116399880192, -55.28192787057680135 ) ) ;
#39559=CARTESIAN_POINT ( 'NONE',  ( 17.93175953304550063, -23.25520614277689901, -45.71393110241879754 ) ) ;
#39571=CARTESIAN_POINT ( 'NONE',  ( 16.13393739769620083, -15.61618894467929941, -28.45282021618999835 ) ) ;
#39573=CARTESIAN_POINT ( 'NONE',  ( 24.03103897938508027, -16.12241053893984954, -43.81269848352728502 ) ) ;
#39574=CARTESIAN_POINT ( 'NONE',  ( 17.61008469349813765, -7.820132634352628287, -77.06721755149550290 ) ) ;
#39578=CARTESIAN_POINT ( 'NONE',  ( 9.221411231516558615, -19.60031519639062125, -36.34100132133150396 ) ) ;
#39580=FACE_OUTER_BOUND ( 'NONE', #36562, .T. ) ;
#39583=CARTESIAN_POINT ( 'NONE',  ( 15.23130163646179902, -7.420582271682119924, -71.25741468598400274 ) ) ;
#39590=CARTESIAN_POINT ( 'NONE',  ( 17.56685828210809674, -8.305003572650919708, -53.79426207090799750 ) ) ;
#39599=CARTESIAN_POINT ( 'NONE',  ( 22.76032741071229637, -10.70969568529780069, -77.30479070626310545 ) ) ;
#39604=CARTESIAN_POINT ( 'NONE',  ( 9.543027317544861887, -13.84507546134918243, -59.53614541435187846 ) ) ;
#39615=CARTESIAN_POINT ( 'NONE',  ( 13.94802033108170036, -22.73858042681539970, -78.82744428701170136 ) ) ;
#39620=B_SPLINE_CURVE_WITH_KNOTS ( 'NONE', 3,
 ( #17532, #48470, #45052, #36926, #24849, #25110, #41629, #16753, #12571, #5233, #5736, #28534, #33241, #45573, #21184, #1030, #37191, #25625 ),
 .UNSPECIFIED., .F., .F.,
 ( 4, 2, 2, 2, 2, 2, 2, 2, 4 ),
 ( 0.000000000000000000, 0.06249984979688257697, 0.1249996995937651539, 0.1874995493906477240, 0.2499993991875303079, 0.3124992489844128918, 0.3749990987812954479, 0.4374989485781780596, 0.4999987983750606158 ),
 .UNSPECIFIED. ) ;
#39622=CARTESIAN_POINT ( 'NONE',  ( 22.90093739902486547, -15.61819515586083007, -40.45291899317828666 ) ) ;
#39629=CARTESIAN_POINT ( 'NONE',  ( 16.13393739769620083, -15.61618894467929941, -28.45282021618999835 ) ) ;
#39633=CARTESIAN_POINT ( 'NONE',  ( 21.20968439552399332, -11.07233059872317504, -66.22059550987238197 ) ) ;
#39636=CARTESIAN_POINT ( 'NONE',  ( 9.807722577752867821, -10.75457455335917345, -55.00065746664166255 ) ) ;
#39640=CARTESIAN_POINT ( 'NONE',  ( 9.807731428018854558, -20.47781564507460317, -78.29930256865087301 ) ) ;
#39646=CARTESIAN_POINT ( 'NONE',  ( 9.516401703503628795, -10.69776019232130082, -40.99578301968139726 ) ) ;
#39648=CARTESIAN_POINT ( 'NONE',  ( 15.09840566293024544, -23.52719084560120422, -68.04933387242864740 ) ) ;
#39649=CARTESIAN_POINT ( 'NONE',  ( 11.57284508314511839, -22.11046742300001355, -50.48724504311571337 ) ) ;
#39651=CARTESIAN_POINT ( 'NONE',  ( 19.54194781300750705, -9.703288880315998455, -64.11948836174622102 ) ) ;
#39653=CARTESIAN_POINT ( 'NONE',  ( 23.84366418157409839, -17.08140582607870073, -76.07227559032499187 ) ) ;
#39661=CARTESIAN_POINT ( 'NONE',  ( 13.02783844833949978, -7.978462186946989831, -46.88472117783310011 ) ) ;
#39679=CARTESIAN_POINT ( 'NONE',  ( 20.99557435765482083, -9.289990908401488667, -75.50070639236554371 ) ) ;
#39685=CARTESIAN_POINT ( 'NONE',  ( 15.49352249817719951, -23.03889485929130032, -59.59473792909209777 ) ) ;
#39686=CARTESIAN_POINT ( 'NONE',  ( 24.04493741938377482, -14.58065008469615442, -41.46600060825795708 ) ) ;
#39693=CARTESIAN_POINT ( 'NONE',  ( 10.02166945824849975, -11.31308309140620061, -81.23899999999999011 ) ) ;
#39697=VERTEX_POINT ( 'NONE', #47220 ) ;
#39699=ORIENTED_EDGE ( 'NONE', *, *, #26962, .T. ) ;
#39701=CARTESIAN_POINT ( 'NONE',  ( 23.51633084124399886, -16.17647175568000151, -81.23899999999999011 ) ) ;
#39711=CARTESIAN_POINT ( 'NONE',  ( 8.617734227332851660, -18.16589664370942714, -50.40348811642825666 ) ) ;
#39712=DIRECTION ( 'NONE',  ( 0.000000000000000000, 0.000000000000000000, 1.000000000000000000 ) ) ;
#39714=CARTESIAN_POINT ( 'NONE',  ( 18.42426853117639141, -9.190374877662996767, -40.06164972454276807 ) ) ;
#39719=CARTESIAN_POINT ( 'NONE',  ( 22.90066830340121840, -15.61618925674170022, -38.84718272210749035 ) ) ;
#39720=CARTESIAN_POINT ( 'NONE',  ( 8.982413567481659200, -18.84766772212099895, -66.15241531683260234 ) ) ;
#39722=CARTESIAN_POINT ( 'NONE',  ( 16.13393739769620083, -15.61618894467929941, -28.45282021618999835 ) ) ;
#39729=CARTESIAN_POINT ( 'NONE',  ( 10.31685475978553512, -21.02859939406643619, -32.26922283058762275 ) ) ;
#39730=CARTESIAN_POINT ( 'NONE',  ( 24.04519454997480210, -15.61618869140488997, -79.50766696426083513 ) ) ;
#39735=CARTESIAN_POINT ( 'NONE',  ( 24.04503344477293680, -15.61618896013167479, -37.50766614148061251 ) ) ;
#39736=CARTESIAN_POINT ( 'NONE',  ( 24.04493737644245144, -14.58063772939740410, -71.75066733987638656 ) ) ;
#39738=VERTEX_POINT ( 'NONE', #40360 ) ;
#39739=CARTESIAN_POINT ( 'NONE',  ( 12.95169883137720035, -21.91030696805099964, -79.49618351660049598 ) ) ;
#39745=CARTESIAN_POINT ( 'NONE',  ( 8.222937397696199469, -15.61618894467929941, -32.14999999999999858 ) ) ;
#39750=CARTESIAN_POINT ( 'NONE',  ( 20.11811607905615062, -8.703694080318976845, -67.17433328788270330 ) ) ;
#39756=DIRECTION ( 'NONE',  ( 0.000000000000000000, 0.000000000000000000, -1.000000000000000000 ) ) ;
#39759=ORIENTED_EDGE ( 'NONE', *, *, #1805, .T. ) ;
#39763=CARTESIAN_POINT ( 'NONE',  ( 16.13393739769620083, -15.61618894467929941, -32.14999999999999858 ) ) ;
#39765=CARTESIAN_POINT ( 'NONE',  ( 22.70470264617900824, -13.96621614738498884, -46.37453375972514635 ) ) ;
#39770=ORIENTED_EDGE ( 'NONE', *, *, #50209, .F. ) ;
#39773=CARTESIAN_POINT ( 'NONE',  ( 17.74255979488508572, -9.022132406956300699, -34.02905390904911087 ) ) ;
#39774=CARTESIAN_POINT ( 'NONE',  ( 24.04468182044177738, -15.61618932230105017, -75.79232603942232060 ) ) ;
#39775=CARTESIAN_POINT ( 'NONE',  ( 23.98148330126149830, -15.56354976708660054, -58.01035930781969796 ) ) ;
#39782=CARTESIAN_POINT ( 'NONE',  ( 20.88396115700760092, -10.40276075773470055, -58.58238571580489662 ) ) ;
#39789=DIRECTION ( 'NONE',  ( 1.000000000000000000, 0.000000000000000000, 0.000000000000000000 ) ) ;
#39790=CARTESIAN_POINT ( 'NONE',  ( 22.46011834663439188, -10.75453258091564024, -47.29933625624753546 ) ) ;
#39795=CARTESIAN_POINT ( 'NONE',  ( 20.11811815720405860, -22.52868256293315241, -58.12566465286644757 ) ) ;
#39797=FACE_OUTER_BOUND ( 'NONE', #21239, .T. ) ;
#39799=LINE ( 'NONE', #47165, #5513 ) ;
#39802=ORIENTED_EDGE ( 'NONE', *, *, #41265, .F. ) ;
#39807=CARTESIAN_POINT ( 'NONE',  ( 20.97293342565509988, -10.48523619318929967, -60.19350159652129406 ) ) ;
#39813=CARTESIAN_POINT ( 'NONE',  ( 20.62477853380519832, -9.180422162592339674, -46.98143399943669607 ) ) ;
#39818=DIRECTION ( 'NONE',  ( 0.000000000000000000, 0.000000000000000000, 1.000000000000000000 ) ) ;
#39819=B_SPLINE_CURVE_WITH_KNOTS ( 'NONE', 3,
 ( #8813, #44970, #9343, #48126, #12225, #24237, #28706, #24764, #9072, #41034, #28188, #8289, #676, #40774, #40264, #4354, #32365, #20323 ),
 .UNSPECIFIED., .F., .F.,
 ( 4, 2, 2, 2, 2, 2, 2, 2, 4 ),
 ( 0.4999985363739877231, 0.5624987193272391606, 0.6249989022804905980, 0.6874990852337419245, 0.7499992681869933620, 0.8124994511402450215, 0.8749996340934966810, 0.9374998170467483405, 1.000000000000000000 ),
 .UNSPECIFIED. ) ;
#39823=ORIENTED_EDGE ( 'NONE', *, *, #38766, .T. ) ;
#39830=CARTESIAN_POINT ( 'NONE',  ( 10.79762425054842012, -21.53695137437687990, -44.52557491237572407 ) ) ;
#39831=CARTESIAN_POINT ( 'NONE',  ( 21.04251040983138310, -9.375720499378973116, -77.21978301587714100 ) ) ;
#39835=CARTESIAN_POINT ( 'NONE',  ( 23.83903384211122400, -17.68688342934473212, -61.87566199814707346 ) ) ;
#39836=DIRECTION ( 'NONE',  ( 0.000000000000000000, 0.000000000000000000, -1.000000000000000000 ) ) ;
#39838=CARTESIAN_POINT ( 'NONE',  ( 26.52624224310950396, -9.616188944679349149, -22.14999999999999858 ) ) ;
#39839=CARTESIAN_POINT ( 'NONE',  ( 21.82943438648850076, -21.57807070353640100, -72.04960399662019199 ) ) ;
#39845=CARTESIAN_POINT ( 'NONE',  ( 8.686118456258421716, -15.42465090483799983, -61.24084159088819490 ) ) ;
#39847=CARTESIAN_POINT ( 'NONE',  ( 22.90121638405171467, -15.61618906730874734, -72.84718036870921765 ) ) ;
#39853=CARTESIAN_POINT ( 'NONE',  ( 16.13393739769620083, -15.61618894467929941, -32.14999999999999858 ) ) ;
#39855=AXIS2_PLACEMENT_3D ( 'NONE', #34497, #22434, #31072 ) ;
#39856=CARTESIAN_POINT ( 'NONE',  ( 14.09735820809919993, -7.626503975077850050, -74.92822277435439560 ) ) ;
#39861=EDGE_CURVE ( 'NONE', #42806, #16604, #38143, .T. ) ;
#39868=ADVANCED_FACE ( 'NONE', ( #4457 ), #13124, .T. ) ;
#39872=CARTESIAN_POINT ( 'NONE',  ( 21.90095873945579896, -20.33298432383600129, -76.45087635510310520 ) ) ;
#39880=VERTEX_POINT ( 'NONE', #44038 ) ;
#39881=CARTESIAN_POINT ( 'NONE',  ( 7.349327706869664745, -6.831579253852827271, -22.14999999999998792 ) ) ;
#39883=CARTESIAN_POINT ( 'NONE',  ( 17.41965231446239670, -8.681529881159590900, -68.40553316769369019 ) ) ;
#39891=CARTESIAN_POINT ( 'NONE',  ( 9.367100842286962603, -16.03594358554465416, -41.82744396597921366 ) ) ;
#39893=CARTESIAN_POINT ( 'NONE',  ( 22.84872475465979846, -14.59283129166942494, -66.40475728675967559 ) ) ;
#39894=ORIENTED_EDGE ( 'NONE', *, *, #17547, .F. ) ;
#39895=ORIENTED_EDGE ( 'NONE', *, *, #2144, .T. ) ;
#39896=CARTESIAN_POINT ( 'NONE',  ( 20.11803733297233165, -8.703646999513249938, -55.45899019443132971 ) ) ;
#39903=CARTESIAN_POINT ( 'NONE',  ( 13.28146700901381827, -21.80339731933624847, -81.09015078194161674 ) ) ;
#39906=CARTESIAN_POINT ( 'NONE',  ( 24.04493055343453278, -15.62694002210068156, -65.50809896301348090 ) ) ;
#39907=CARTESIAN_POINT ( 'NONE',  ( 8.330844340317721475, -12.95264641754989832, -42.89703736520829125 ) ) ;
#39908=CARTESIAN_POINT ( 'NONE',  ( 9.221425662475672524, -19.60033986558276808, -68.34100135745960358 ) ) ;
#39912=CARTESIAN_POINT ( 'NONE',  ( 11.61399867763840099, -21.53875998735910002, -34.94015647776650013 ) ) ;
#39913=ADVANCED_FACE ( 'NONE', ( #46123 ), #22236, .T. ) ;
#39916=B_SPLINE_CURVE_WITH_KNOTS ( 'NONE', 3,
 ( #25787, #49677, #29981, #13768, #30247, #42588, #10092, #42062, #22122, #42326, #6684, #2230, #6426, #2486, #22644, #38661, #2749, #11394, #35994, #47806, #7721, #51730, #111, #3786, #15824, #19756, #11912, #47552, #47305 ),
 .UNSPECIFIED., .F., .F.,
 ( 4, 2, 1, 1, 1, 1, 1, 2, 2, 2, 2, 2, 2, 2, 2, 2, 4 ),
 ( 0.5000074908953238140, 0.5002516278626603086, 0.5004957648299966921, 0.5009840387646694593, 0.5019605866340145495, 0.5039136823727047299, 0.5078198738500852016, 0.5156322568048457011, 0.5312570227143668111, 0.5625065545334089201, 0.6250056181714933601, 0.6875046818095776890, 0.7500037454476620180, 0.8125028090857464580, 0.8750018727238310090, 0.9375009363619155600, 1.000000000000000000 ),
 .UNSPECIFIED. ) ;
#39921=CARTESIAN_POINT ( 'NONE',  ( 13.98591064026810038, -7.655742866829910120, -42.92377462465219651 ) ) ;
#39926=CARTESIAN_POINT ( 'NONE',  ( 20.29253959100516624, -21.02756285422321625, -56.74444169921939363 ) ) ;
#39928=ORIENTED_EDGE ( 'NONE', *, *, #33363, .T. ) ;
#39930=DIRECTION ( 'NONE',  ( 0.000000000000000000, 0.000000000000000000, -1.000000000000000000 ) ) ;
#39940=CARTESIAN_POINT ( 'NONE',  ( 9.807682588839810478, -10.75462586085395245, -75.00070004298494553 ) ) ;
#39943=CARTESIAN_POINT ( 'NONE',  ( 21.49792027126889948, -10.44565879097549832, -64.82318737929099939 ) ) ;
#39944=CARTESIAN_POINT ( 'NONE',  ( 9.807870126734302474, -10.75438522751455395, -72.71600167733724618 ) ) ;
#39946=ORIENTED_EDGE ( 'NONE', *, *, #38340, .T. ) ;
#39948=CARTESIAN_POINT ( 'NONE',  ( 22.80495416686178345, -16.79151856191942471, -34.50832474881546830 ) ) ;
#39949=B_SPLINE_CURVE_WITH_KNOTS ( 'NONE', 3,
 ( #39998, #15891, #8547, #48374, #51788, #36054, #31847, #36302, #3843, #47609, #15636, #14668, #7775, #8280, #4087, #27925, #34573, #27672 ),
 .UNSPECIFIED., .F., .F.,
 ( 4, 2, 2, 2, 2, 2, 2, 2, 4 ),
 ( 0.5000000032568245878, 0.5625000028497215698, 0.6250000024426184408, 0.6875000020355153119, 0.7500000016284122939, 0.8125000012213092759, 0.8750000008142061469, 0.9375000004071030180, 1.000000000000000000 ),
 .UNSPECIFIED. ) ;
#39950=CARTESIAN_POINT ( 'NONE',  ( 9.206240469540899696, -13.25622428000860076, -81.23899999999999011 ) ) ;
#39957=CARTESIAN_POINT ( 'NONE',  ( 22.63910790963710085, -11.37884432564429815, -81.23899999999999011 ) ) ;
#39959=ORIENTED_EDGE ( 'NONE', *, *, #43202, .T. ) ;
#39964=ORIENTED_EDGE ( 'NONE', *, *, #30668, .F. ) ;
#39978=CARTESIAN_POINT ( 'NONE',  ( 23.31239132799949587, -18.78739492248890031, -67.41991821385059325 ) ) ;
#39981=CARTESIAN_POINT ( 'NONE',  ( 21.80209328419340054, -11.41921765328320149, -76.64430199831019763 ) ) ;
#39986=EDGE_CURVE ( 'NONE', #48851, #36898, #16357, .T. ) ;
#39989=EDGE_CURVE ( 'NONE', #49314, #49834, #26425, .T. ) ;
#39993=CARTESIAN_POINT ( 'NONE',  ( 16.13393739769620083, -27.61618894467930474, -22.14999999999999858 ) ) ;
#39995=CARTESIAN_POINT ( 'NONE',  ( 9.367870520905830389, -16.42710664673399990, -71.80902927999524366 ) ) ;
#39997=CARTESIAN_POINT ( 'NONE',  ( 22.99224927569089871, -17.26127340059479920, -80.92212427574548883 ) ) ;
#39998=CARTESIAN_POINT ( 'NONE',  ( 22.90071877914020249, -15.61618922162072565, -76.45281474520940890 ) ) ;
#40008=CYLINDRICAL_SURFACE ( 'NONE', #25267, 6.766999999999998572 ) ;
#40015=CARTESIAN_POINT ( 'NONE',  ( 22.46011021147963405, -10.75452141403957107, -79.58400001792948331 ) ) ;
#40019=ORIENTED_EDGE ( 'NONE', *, *, #48613, .F. ) ;
#40023=CARTESIAN_POINT ( 'NONE',  ( 12.72603455780808801, -9.703227352568038810, -35.78615263577922434 ) ) ;
#40029=CARTESIAN_POINT ( 'NONE',  ( 16.15327313186332248, -8.825424306557579257, -33.95380833013259547 ) ) ;
#40031=CARTESIAN_POINT ( 'NONE',  ( 9.097165979443349926, -12.14191267488699921, -55.15847778952939962 ) ) ;
#40041=CARTESIAN_POINT ( 'NONE',  ( 17.30144337755399775, -22.57172551358950230, -51.29424405795189301 ) ) ;
#40049=CARTESIAN_POINT ( 'NONE',  ( 16.13393739769620083, -15.61618894467929941, -32.14999999999999858 ) ) ;
#40050=CARTESIAN_POINT ( 'NONE',  ( 20.29253893682858845, -10.20481459075288555, -76.16113288888496413 ) ) ;
#40065=CARTESIAN_POINT ( 'NONE',  ( 22.95140634437030158, -13.80934754108039897, -50.37035414463250049 ) ) ;
#40070=CARTESIAN_POINT ( 'NONE',  ( 8.286224014182360875, -15.60423765184120093, -44.28799034327369100 ) ) ;
#40071=VERTEX_POINT ( 'NONE', #8079 ) ;
#40075=B_SPLINE_CURVE_WITH_KNOTS ( 'NONE', 3,
 ( #19957, #12120, #7925, #23875, #35949, #36203, #16295, #70, #40662, #16043, #31998, #48019, #5551, #45898, #20994, #45633, #5030, #36991 ),
 .UNSPECIFIED., .F., .F.,
 ( 4, 2, 2, 2, 2, 2, 2, 2, 4 ),
 ( 0.000000000000000000, 0.06250000038613703901, 0.1250000007722740780, 0.1875000011584111170, 0.2500000015445481560, 0.3125000019306851118, 0.3750000023168220120, 0.4375000027029589678, 0.5000000030890958680 ),
 .UNSPECIFIED. ) ;
#40078=FACE_OUTER_BOUND ( 'NONE', #32000, .T. ) ;
#40082=CARTESIAN_POINT ( 'NONE',  ( 20.99557930478071910, -9.289994860631022533, -75.21597186361574927 ) ) ;
#40084=DIRECTION ( 'NONE',  ( 0.000000000000000000, 0.000000000000000000, -1.000000000000000000 ) ) ;
#40087=CARTESIAN_POINT ( 'NONE',  ( 8.575657855873597413, -13.18837314039375563, -76.60667932582364870 ) ) ;
#40089=CARTESIAN_POINT ( 'NONE',  ( 13.49824643614018349, -8.118921815336832992, -48.89997689786164869 ) ) ;
#40094=CARTESIAN_POINT ( 'NONE',  ( 13.71920826666440085, -7.732547446001079905, -69.19772247832989365 ) ) ;
#40100=CARTESIAN_POINT ( 'NONE',  ( 23.57163437498810055, -16.04903704635959727, -64.25116097130579362 ) ) ;
#40102=CARTESIAN_POINT ( 'NONE',  ( 12.71325777259860068, -22.74941205225429997, -32.14999999999999858 ) ) ;
#40109=CARTESIAN_POINT ( 'NONE',  ( 11.99450341294459932, -22.74695377005799912, -70.17508691053730274 ) ) ;
#40111=EDGE_CURVE ( 'NONE', #15986, #11267, #44483, .T. ) ;
#40116=EDGE_CURVE ( 'NONE', #50303, #33352, #24401, .T. ) ;
#40118=CARTESIAN_POINT ( 'NONE',  ( 8.223516320988901285, -15.61608250808600040, -78.50766849176299900 ) ) ;
#40122=CARTESIAN_POINT ( 'NONE',  ( 22.33324507534229042, -20.60314842766364052, -66.00806682646168611 ) ) ;
#40124=CARTESIAN_POINT ( 'NONE',  ( 9.474876936629032187, -18.95738746930799934, -77.08462780361209354 ) ) ;
#40138=CARTESIAN_POINT ( 'NONE',  ( 9.508341806066903601, -17.57833688292872054, -41.75489552743931654 ) ) ;
#40142=CARTESIAN_POINT ( 'NONE',  ( 23.83903348036886527, -13.54549273453152125, -55.70899880447446861 ) ) ;
#40147=CARTESIAN_POINT ( 'NONE',  ( 16.23376603976204535, -8.830308542783665615, -49.95748267700136580 ) ) ;
#40150=ORIENTED_EDGE ( 'NONE', *, *, #27725, .F. ) ;
#40154=CARTESIAN_POINT ( 'NONE',  ( 22.22981637867615845, -20.73180715974339705, -65.73000105463430032 ) ) ;
#40156=CARTESIAN_POINT ( 'NONE',  ( 13.15967284984390062, -7.926164857894950622, -47.17485964264369613 ) ) ;
#40160=CARTESIAN_POINT ( 'NONE',  ( 24.00939179868683482, -16.38255829204414482, -49.82319880720410055 ) ) ;
#40164=CARTESIAN_POINT ( 'NONE',  ( 10.74321899375740053, -10.47353895711630045, -37.47516227180229720 ) ) ;
#40167=CARTESIAN_POINT ( 'NONE',  ( 13.70487115333438588, -23.21378410962326555, -60.39054555587951967 ) ) ;
#40170=CARTESIAN_POINT ( 'NONE',  ( 10.44585770868170016, -9.647230060552569597, -42.76533676252499561 ) ) ;
#40175=CARTESIAN_POINT ( 'NONE',  ( 16.13393739769620083, -15.61618894467929941, -22.64999999999999858 ) ) ;
#40188=CLOSED_SHELL ( 'NONE', ( #31450, #17982, #27656, #10898, #10644, #29575, #5808, #20311, #47280, #26979, #36532, #10410, #40223, #38434, #1955, #34162, #9405, #32966, #50064, #12761, #6080, #41175, #18842, #31105, #21141, #27084, #41457, #9474, #15001, #14018, #39913, #3296, #30285, #40638, #15972, #15929, #2232, #42807, #18209, #38999, #28551, #19966, #33790, #49253, #30022, #18051, #2253, #31956, #6161, #21854, #23640, #26112, #40592, #33484, #46739, #30549, #49716, #20446, #615, #42787, #13031, #7684, #1183, #13378, #51118, #50802, #36529, #5812, #8017, #18554, #28267, #22578, #42712, #32144, #18745, #32558, #25657, #7576, #31545, #18546, #11065, #26124, #36006, #37220, #3069, #1878, #8088, #44004, #35468, #9291, #29798, #12614, #33357, #43733, #3549, #29054, #32450, #31249, #13771, #17859, #39275, #21634, #3006, #5078, #45008, #38148, #7506, #25357, #36687, #23611, #21504, #38664, #18117, #31326, #17964, #33392, #42481, #17812, #10602, #42846, #39868, #38371, #23315, #531, #46652, #39470, #50940, #50594, #35723, #13853, #26975, #13094, #48983, #24606 ) ) ;
#40190=CARTESIAN_POINT ( 'NONE',  ( 9.366809454094768839, -15.61635577034980038, -65.45282021618999124 ) ) ;
#40191=CARTESIAN_POINT ( 'NONE',  ( 9.366937397696199596, -15.61618894467949836, -28.45282021618999835 ) ) ;
#40193=CARTESIAN_POINT ( 'NONE',  ( 14.06314481641416769, -7.911118301919978890, -75.20904927136304252 ) ) ;
#40195=CARTESIAN_POINT ( 'NONE',  ( 12.89352330978772798, -8.399289503860947192, -32.14999999999999858 ) ) ;
#40196=CARTESIAN_POINT ( 'NONE',  ( 9.543049689180366002, -17.38738376894362503, -61.36949275306091067 ) ) ;
#40197=( BOUNDED_CURVE ( )  B_SPLINE_CURVE ( 2, ( #43427, #40263, #35557 ),
 .UNSPECIFIED., .F., .T. ) 
 B_SPLINE_CURVE_WITH_KNOTS ( ( 3, 3 ),
 ( 2.168627590050199672, 3.232274745523169734 ),
 .UNSPECIFIED. ) 
 CURVE ( )  GEOMETRIC_REPRESENTATION_ITEM ( )  RATIONAL_B_SPLINE_CURVE ( ( 1.425426480542939967, 1.425426480542939967, 1.323085463760209857 ) ) 
 REPRESENTATION_ITEM ( '' )  );
#40198=CARTESIAN_POINT ( 'NONE',  ( 15.00545154534380110, -8.943947291303700808, -81.89948870795299740 ) ) ;
#40200=ORIENTED_EDGE ( 'NONE', *, *, #21909, .F. ) ;
#40204=CARTESIAN_POINT ( 'NONE',  ( 9.898088180596179342, -11.52557894097520119, -81.23899999999999011 ) ) ;
#40210=CARTESIAN_POINT ( 'NONE',  ( 22.80170779281839799, -18.40375469871939984, -81.23899999999999011 ) ) ;
#40213=CARTESIAN_POINT ( 'NONE',  ( 12.59310188071810011, -21.71578262099550116, -69.51459820258429545 ) ) ;
#40216=DIRECTION ( 'NONE',  ( 0.000000000000000000, 0.000000000000000000, -1.000000000000000000 ) ) ;
#40223=ADVANCED_FACE ( 'NONE', ( #29014 ), #48958, .T. ) ;
#40235=CARTESIAN_POINT ( 'NONE',  ( 14.63845944065399962, -7.912274753621379553, -64.72647455768748159 ) ) ;
#40238=CARTESIAN_POINT ( 'NONE',  ( 9.989812541601329698, -12.15320050589289913, -76.01055054980109560 ) ) ;
#40249=CARTESIAN_POINT ( 'NONE',  ( 22.46011455092658693, -20.47785052632239200, -54.00066733230272575 ) ) ;
#40252=CARTESIAN_POINT ( 'NONE',  ( 23.28731277692780210, -13.53390210943540062, -32.97717709171589462 ) ) ;
#40254=ORIENTED_EDGE ( 'NONE', *, *, #36462, .F. ) ;
#40257=CARTESIAN_POINT ( 'NONE',  ( 23.63393739769620083, -15.61618894467930119, -81.65000000000000568 ) ) ;
#40263=CARTESIAN_POINT ( 'NONE',  ( 4.133937397696232807, -18.83157925385280862, -22.14999999999998792 ) ) ;
#40264=CARTESIAN_POINT ( 'NONE',  ( 9.221418464489284261, -19.60032756090027561, -52.34100133722100168 ) ) ;
#40269=B_SPLINE_CURVE_WITH_KNOTS ( 'NONE', 3,
 ( #7028, #46874, #10960, #11736, #7282, #43186, #23232, #22465, #26924, #35306, #27436, #22979, #39000, #47381, #43439, #7542, #27943, #7796, #183, #36857, #48931, #28720, #20593, #16163, #36324, #20337, #20855, #24514, #32901 ),
 .UNSPECIFIED., .F., .F.,
 ( 4, 2, 1, 1, 1, 1, 1, 2, 2, 2, 2, 2, 2, 2, 2, 2, 4 ),
 ( 0.5000036478644217519, 0.5002477867082379959, 0.5004919255520542398, 0.5009802032396866167, 0.5019567586149512595, 0.5039098693654808780, 0.5078160908665402262, 0.5156285338686588116, 0.5312534198728956492, 0.5625031918813692133, 0.6250027358983164527, 0.6875022799152636921, 0.7500018239322110425, 0.8125013679491581708, 0.8750009119661055212, 0.9375004559830526496, 1.000000000000000000 ),
 .UNSPECIFIED. ) ;
#40272=CARTESIAN_POINT ( 'NONE',  ( 20.11808686960868897, -8.703676620365614625, -79.45899972692541269 ) ) ;
#40279=CARTESIAN_POINT ( 'NONE',  ( 9.366488261363459245, -15.61629045172390029, -39.45282021618999835 ) ) ;
#40287=CARTESIAN_POINT ( 'NONE',  ( 16.70374668832650045, -8.852716093271043363, -33.97954381835977244 ) ) ;
#40288=CARTESIAN_POINT ( 'NONE',  ( 5.741632552282960766, -9.616188944679340267, -22.14999999999999858 ) ) ;
#40290=CARTESIAN_POINT ( 'NONE',  ( 23.92893553353459879, -16.52434733056690064, -54.04941275463870198 ) ) ;
#40296=CARTESIAN_POINT ( 'NONE',  ( 22.52282493614631420, -13.38585152154421820, -28.45282021618999835 ) ) ;
#40297=CARTESIAN_POINT ( 'NONE',  ( 10.17382535701520041, -11.84529732107350064, -50.02674116093399448 ) ) ;
#40300=ORIENTED_EDGE ( 'NONE', *, *, #4300, .F. ) ;
#40305=CARTESIAN_POINT ( 'NONE',  ( 9.367749763036480104, -16.28101815411259068, -77.81590886694031894 ) ) ;
#40306=DIRECTION ( 'NONE',  ( 1.000000000000000000, 0.000000000000000000, 0.000000000000000000 ) ) ;
#40310=CARTESIAN_POINT ( 'NONE',  ( 16.13393739769620083, -15.61618894467929941, -31.39999999999999858 ) ) ;
#40322=CARTESIAN_POINT ( 'NONE',  ( 23.17208530007939871, -15.16118037244739902, -68.43227042713769492 ) ) ;
#40336=CARTESIAN_POINT ( 'NONE',  ( 8.222930619450961487, -15.61639179890759976, -64.50766849176299900 ) ) ;
#40341=ORIENTED_EDGE ( 'NONE', *, *, #19095, .T. ) ;
#40350=CARTESIAN_POINT ( 'NONE',  ( 15.22672021889999883, -23.81128974005859789, -76.32742627405569635 ) ) ;
#40351=CARTESIAN_POINT ( 'NONE',  ( 9.366584228470589579, -15.61631960056659985, -37.84717978380999881 ) ) ;
#40352=DIRECTION ( 'NONE',  ( 0.000000000000000000, 0.000000000000000000, -1.000000000000000000 ) ) ;
#40354=ORIENTED_EDGE ( 'NONE', *, *, #40709, .F. ) ;
#40355=CARTESIAN_POINT ( 'NONE',  ( 8.852402460927230265, -14.03950166758260032, -63.30053379854238926 ) ) ;
#40360=CARTESIAN_POINT ( 'NONE',  ( 22.90099491887654182, -15.61618908163285546, -52.84717737022585027 ) ) ;
#40364=CARTESIAN_POINT ( 'NONE',  ( 8.951113142255618271, -11.56776253131459953, -76.67103925775408868 ) ) ;
#40377=CARTESIAN_POINT ( 'NONE',  ( 10.88488332746739928, -20.32681417541479973, -37.22001158807169929 ) ) ;
#40390=CARTESIAN_POINT ( 'NONE',  ( 10.22105613155544113, -19.02423196159752905, -71.28615407210328669 ) ) ;
#40400=CYLINDRICAL_SURFACE ( 'NONE', #18521, 7.910999999999997812 ) ;
#40403=LINE ( 'NONE', #44594, #2639 ) ;
#40404=FACE_OUTER_BOUND ( 'NONE', #22883, .T. ) ;
#40411=CARTESIAN_POINT ( 'NONE',  ( 23.57040948703929928, -12.05506511639750045, -47.65017322902539831 ) ) ;
#40417=CARTESIAN_POINT ( 'NONE',  ( 9.758604362744099703, -19.47129238020390218, -39.05954089307470412 ) ) ;
#40423=CARTESIAN_POINT ( 'NONE',  ( 8.457331809849481630, -18.62491747308059686, -40.38876883061629997 ) ) ;
#40424=ORIENTED_EDGE ( 'NONE', *, *, #25718, .F. ) ;
#40429=CARTESIAN_POINT ( 'NONE',  ( 22.90078880164185549, -15.66462774376105926, -56.45510315590827588 ) ) ;
#40441=CARTESIAN_POINT ( 'NONE',  ( 11.97539491867874162, -21.02760647153319695, -65.16115419653750962 ) ) ;
#40444=CARTESIAN_POINT ( 'NONE',  ( 24.04215757223157723, -15.38968104315445196, -75.78321347473215042 ) ) ;
#40448=CARTESIAN_POINT ( 'NONE',  ( 21.54527544888350121, -19.77483684844828815, -60.66116240694285722 ) ) ;
#40450=VERTEX_POINT ( 'NONE', #27025 ) ;
#40463=CARTESIAN_POINT ( 'NONE',  ( 22.65849246206020240, -18.66984389996769877, -81.23899999999999011 ) ) ;
#40474=AXIS2_PLACEMENT_3D ( 'NONE', #6485, #22443, #42651 ) ;
#40485=CARTESIAN_POINT ( 'NONE',  ( 10.75986719944589964, -9.897262674175308916, -58.54739793472509746 ) ) ;
#40495=B_SPLINE_CURVE_WITH_KNOTS ( 'NONE', 3,
 ( #6087, #50371, #22560, #50620, #2669, #14201, #10274, #37795, #41715, #10794, #38054, #26754, #33839, #22302, #38576, #49604, #38838, #42768, #18642, #49852, #2147, #17620, #13944, #13691, #33588, #29650, #14716, #50103, #18380, #46710, #30171, #18127, #14456, #2395, #5824, #25972 ),
 .UNSPECIFIED., .F., .F.,
 ( 4, 2, 2, 2, 2, 2, 2, 2, 2, 2, 2, 2, 2, 1, 1, 1, 1, 1, 1, 2, 4 ),
 ( 0.000000000000000000, 0.06250075854269371289, 0.1250015170853874258, 0.1875022756280811387, 0.2500030341707748516, 0.3125037927134685645, 0.3437541719848153932, 0.3750045512561622774, 0.4062549305275091616, 0.4375053097988559903, 0.4687556890702028745, 0.4843808787058762610, 0.4921934735237130099, 0.4960997709326313565, 0.4980529196370905298, 0.4990294939893200610, 0.4995177811654347710, 0.4997619247534921261, 0.4998839965475208036, 0.4999450324445350868, 0.5000060683415493701 ),
 .UNSPECIFIED. ) ;
#40500=CARTESIAN_POINT ( 'NONE',  ( 24.02064451092653741, -16.24823765856366009, -33.53311993805902347 ) ) ;
#40501=DIRECTION ( 'NONE',  ( 0.000000000000000000, 0.000000000000000000, 1.000000000000000000 ) ) ;
#40502=CARTESIAN_POINT ( 'NONE',  ( 17.16953199081255477, -23.52718221652492403, -54.25066654575565650 ) ) ;
#40503=ORIENTED_EDGE ( 'NONE', *, *, #38637, .F. ) ;
#40506=CARTESIAN_POINT ( 'NONE',  ( 17.86279105191340122, -8.369275161513289873, -42.64188668147749439 ) ) ;
#40507=EDGE_CURVE ( 'NONE', #49314, #41906, #23197, .T. ) ;
#40512=CARTESIAN_POINT ( 'NONE',  ( 8.332397351126385132, -14.10177087609484303, -80.85327594137434915 ) ) ;
#40515=CARTESIAN_POINT ( 'NONE',  ( 17.16945347175581560, -23.52719342952614312, -78.25066314212283203 ) ) ;
#40522=ORIENTED_EDGE ( 'NONE', *, *, #11312, .F. ) ;
#40525=CARTESIAN_POINT ( 'NONE',  ( 24.04513741079867017, -15.61618875311435417, -79.79232954107749265 ) ) ;
#40528=VERTEX_POINT ( 'NONE', #3192 ) ;
#40529=EDGE_LOOP ( 'NONE', ( #51626, #18191 ) ) ;
#40532=CARTESIAN_POINT ( 'NONE',  ( 19.47520249253551583, -9.405029089961901789, -66.50427882218234288 ) ) ;
#40535=CARTESIAN_POINT ( 'NONE',  ( 8.222476383702659319, -15.61632876086509825, -54.50766849176299900 ) ) ;
#40537=DIRECTION ( 'NONE',  ( 0.000000000000000000, 0.000000000000000000, -1.000000000000000000 ) ) ;
#40541=CARTESIAN_POINT ( 'NONE',  ( 22.32406200693392506, -12.82697318663033137, -34.31802238708871045 ) ) ;
#40543=CARTESIAN_POINT ( 'NONE',  ( 9.633650982238179949, -20.01312243389589796, -64.82318737929099939 ) ) ;
#40550=CARTESIAN_POINT ( 'NONE',  ( 9.366455112259469473, -15.61627688590920116, -55.45282021618999835 ) ) ;
#40557=CARTESIAN_POINT ( 'NONE',  ( 9.221415312945399734, -11.63205571590753529, -36.67433565377826454 ) ) ;
#40559=CARTESIAN_POINT ( 'NONE',  ( 23.76555765687864863, -13.48533909360518201, -55.42104307077845959 ) ) ;
#40560=CARTESIAN_POINT ( 'NONE',  ( 23.14726890598120335, -14.09743467301990094, -32.14999999999999858 ) ) ;
#40563=DIRECTION ( 'NONE',  ( 1.000000000000000000, 0.000000000000000000, 0.000000000000000000 ) ) ;
#40564=CARTESIAN_POINT ( 'NONE',  ( 15.09841886250152321, -23.52719244016399713, -52.33399699069794053 ) ) ;
#40565=CARTESIAN_POINT ( 'NONE',  ( 24.04464518807997919, -15.61618401921712618, -71.50767245506341396 ) ) ;
#40567=ORIENTED_EDGE ( 'NONE', *, *, #51867, .F. ) ;
#40568=CARTESIAN_POINT ( 'NONE',  ( 19.47520249252229618, -9.405029089986481239, -66.50427882216689568 ) ) ;
#40571=LINE ( 'NONE', #33473, #11014 ) ;
#40575=CARTESIAN_POINT ( 'NONE',  ( 9.250578338074079809, -17.15304507097850006, -69.38289759990119876 ) ) ;
#40579=CARTESIAN_POINT ( 'NONE',  ( 20.99565895510886193, -21.94231944923553712, -80.08399982392677430 ) ) ;
#40588=CARTESIAN_POINT ( 'NONE',  ( 22.46008168199778865, -10.75448223654004742, -75.29930970037709415 ) ) ;
#40592=ADVANCED_FACE ( 'NONE', ( #16781 ), #9671, .T. ) ;
#40598=ORIENTED_EDGE ( 'NONE', *, *, #46340, .T. ) ;
#40602=CARTESIAN_POINT ( 'NONE',  ( 20.61809888542150304, -22.53536633855610205, -74.10929620427440057 ) ) ;
#40609=CARTESIAN_POINT ( 'NONE',  ( 15.24815623221091521, -22.38319100513449200, -36.99448562645851979 ) ) ;
#40610=CARTESIAN_POINT ( 'NONE',  ( 8.714178796388031500, -14.94248566914980003, -67.26148035172319339 ) ) ;
#40618=CARTESIAN_POINT ( 'NONE',  ( 23.06214062797170072, -27.61618894467930119, -24.15000000000000213 ) ) ;
#40628=ORIENTED_EDGE ( 'NONE', *, *, #9938, .F. ) ;
#40635=CARTESIAN_POINT ( 'NONE',  ( 21.22754492721490038, -10.73789807064090063, -34.20969220765409347 ) ) ;
#40638=ADVANCED_FACE ( 'NONE', ( #32463 ), #48492, .T. ) ;
#40644=CARTESIAN_POINT ( 'NONE',  ( 8.222937397696199469, -15.61618894467929941, -32.14999999999999858 ) ) ;
#40647=CARTESIAN_POINT ( 'NONE',  ( 9.588669338623654781, -13.31599288703087858, -67.95535226952054586 ) ) ;
#40648=LINE ( 'NONE', #45102, #4767 ) ;
#40654=LINE ( 'NONE', #25168, #31820 ) ;
#40658=CARTESIAN_POINT ( 'NONE',  ( 9.221369605823916515, -11.63213385460635685, -54.95899190682911239 ) ) ;
#40662=CARTESIAN_POINT ( 'NONE',  ( 15.09830787208028902, -7.705198857361269305, -58.96596456551435494 ) ) ;
#40668=CARTESIAN_POINT ( 'NONE',  ( 18.40285012985609825, -23.54302659091490213, -40.20359370904520091 ) ) ;
#40670=CYLINDRICAL_SURFACE ( 'NONE', #15437, 6.766999999999998572 ) ;
#40675=CARTESIAN_POINT ( 'NONE',  ( 22.38096263179139811, -11.55646364244059932, -36.04922151265719776 ) ) ;
#40676=CARTESIAN_POINT ( 'NONE',  ( 15.09831361134191496, -7.705198193276967089, -32.96599948321726714 ) ) ;
#40684=CARTESIAN_POINT ( 'NONE',  ( 11.19896969917839868, -22.22140010887079953, -50.21191628250519301 ) ) ;
#40685=ORIENTED_EDGE ( 'NONE', *, *, #15091, .F. ) ;
#40689=DIRECTION ( 'NONE',  ( 1.000000000000000000, 2.460964292799963328E-14, 0.000000000000000000 ) ) ;
#40690=CARTESIAN_POINT ( 'NONE',  ( 16.51210842463290263, -8.573494442649787217, -56.36425564602672011 ) ) ;
#40709=EDGE_CURVE ( 'NONE', #4493, #43673, #45478, .T. ) ;
#40712=CARTESIAN_POINT ( 'NONE',  ( 17.70165363224570143, -22.49258516525739893, -61.27582937196799406 ) ) ;
#40724=ORIENTED_EDGE ( 'NONE', *, *, #15718, .T. ) ;
#40727=CARTESIAN_POINT ( 'NONE',  ( 20.81226749614940275, -20.80205290968870102, -81.23899999999999011 ) ) ;
#40740=DIRECTION ( 'NONE',  ( 0.000000000000000000, 0.000000000000000000, -1.000000000000000000 ) ) ;
#40742=EDGE_CURVE ( 'NONE', #630, #10139, #27732, .T. ) ;
#40743=CARTESIAN_POINT ( 'NONE',  ( 8.222946539407685052, -16.65180334102045023, -68.75066474143523010 ) ) ;
#40748=CARTESIAN_POINT ( 'NONE',  ( 14.14244093349880060, -8.025359608152760060, -58.70583579685229836 ) ) ;
#40749=VERTEX_POINT ( 'NONE', #22758 ) ;
#40759=CARTESIAN_POINT ( 'NONE',  ( 24.04493739840414435, -15.61820873891454120, -33.50774649806280081 ) ) ;
#40764=CARTESIAN_POINT ( 'NONE',  ( 9.197401484353060042, -18.33485844670460096, -39.94844302531450353 ) ) ;
#40766=VERTEX_POINT ( 'NONE', #20895 ) ;
#40773=CARTESIAN_POINT ( 'NONE',  ( 9.366365007129969555, -15.61616877484880028, -59.84717978381009118 ) ) ;
#40774=CARTESIAN_POINT ( 'NONE',  ( 9.807778990346434966, -20.47787572195374750, -52.29933454858549169 ) ) ;
#40778=ORIENTED_EDGE ( 'NONE', *, *, #30330, .F. ) ;
#40789=CARTESIAN_POINT ( 'NONE',  ( 22.03527629826074374, -11.75396699927941491, -66.66271668430944430 ) ) ;
#40791=CARTESIAN_POINT ( 'NONE',  ( 22.46008339447744717, -10.75448427898152914, -59.58402698800288277 ) ) ;
#40796=CARTESIAN_POINT ( 'NONE',  ( 16.73169708462201299, -22.35857779895397712, -46.92468125870891527 ) ) ;
#40798=CARTESIAN_POINT ( 'NONE',  ( 10.56734057524939985, -21.14789278779199933, -62.76349517163679081 ) ) ;
#40805=EDGE_CURVE ( 'NONE', #11854, #44438, #47985, .T. ) ;
#40810=EDGE_CURVE ( 'NONE', #19003, #10310, #11046, .T. ) ;
#40816=CARTESIAN_POINT ( 'NONE',  ( 20.11806848324613028, -8.703665624651682364, -37.17433713982433119 ) ) ;
#40820=CARTESIAN_POINT ( 'NONE',  ( 23.41199157575060141, -16.89843572899400215, -32.14999999999999858 ) ) ;
#40822=CARTESIAN_POINT ( 'NONE',  ( 16.13393739769620083, -15.61618894467929941, -22.14999999999999858 ) ) ;
#40829=CARTESIAN_POINT ( 'NONE',  ( 20.57457857590170036, -10.13683997779680013, -68.56397102982089109 ) ) ;
#40836=CARTESIAN_POINT ( 'NONE',  ( 23.17486471576589935, -16.02594643184229994, -64.47132387395669184 ) ) ;
#40846=CARTESIAN_POINT ( 'NONE',  ( 20.11812592182209158, -22.52867792443588257, -63.84100292245498309 ) ) ;
#40858=ORIENTED_EDGE ( 'NONE', *, *, #40742, .F. ) ;
#40860=MECHANICAL_DESIGN_GEOMETRIC_PRESENTATION_REPRESENTATION('',(#39190),#25796);
#40862=CARTESIAN_POINT ( 'NONE',  ( 16.12625695005860038, -7.768470256960290143, -35.51218288575169879 ) ) ;
#40867=EDGE_LOOP ( 'NONE', ( #7214, #37079, #47066, #8755 ) ) ;
#40869=EDGE_CURVE ( 'NONE', #47211, #4764, #17906, .T. ) ;
#40873=CARTESIAN_POINT ( 'NONE',  ( 9.138897765566639464, -16.51739104625019650, -31.80638701630149967 ) ) ;
#40893=CARTESIAN_POINT ( 'NONE',  ( 12.76051422255349976, -9.422436061403089980, -35.79407082892649328 ) ) ;
#40901=CARTESIAN_POINT ( 'NONE',  ( 22.12150465969970270, -11.18271033062140063, -76.86446490096111006 ) ) ;
#40909=CARTESIAN_POINT ( 'NONE',  ( 23.18393739769649642, -15.61618894467929941, -20.74999999999999289 ) ) ;
#40912=CARTESIAN_POINT ( 'NONE',  ( 8.223124147305879816, -15.61599092713959891, -72.50766849176299900 ) ) ;
#40915=EDGE_CURVE ( 'NONE', #1577, #31691, #20389, .T. ) ;
#40920=CARTESIAN_POINT ( 'NONE',  ( 8.223124147305879816, -15.61599092713959891, -72.50766849176299900 ) ) ;
#40921=CARTESIAN_POINT ( 'NONE',  ( 22.90093740148115486, -14.73038825474736413, -70.41115655435802978 ) ) ;
#40924=VERTEX_POINT ( 'NONE', #7253 ) ;
#40926=CARTESIAN_POINT ( 'NONE',  ( 24.01558619446240073, -16.31994774379832336, -65.53600668441687560 ) ) ;
#40927=CARTESIAN_POINT ( 'NONE',  ( 7.933294100319239206, -16.47185801921769865, -48.75923826391599647 ) ) ;
#40928=LINE ( 'NONE', #13934, #12942 ) ;
#40931=EDGE_CURVE ( 'NONE', #16669, #33243, #31582, .T. ) ;
#40933=CARTESIAN_POINT ( 'NONE',  ( 8.886083854397551107, -17.34109845536059780, -37.15828654754790250 ) ) ;
#40937=CARTESIAN_POINT ( 'NONE',  ( 10.90613698351470084, -11.11335884447900035, -32.14999999999999858 ) ) ;
#40941=CARTESIAN_POINT ( 'NONE',  ( 8.222928832386770637, -16.58847042571065344, -60.75319795691873992 ) ) ;
#40943=CARTESIAN_POINT ( 'NONE',  ( 12.51690838597220079, -23.02563034314670176, -48.15222407485109812 ) ) ;
#40947=DIRECTION ( 'NONE',  ( 0.000000000000000000, 0.000000000000000000, -1.000000000000000000 ) ) ;
#40956=CARTESIAN_POINT ( 'NONE',  ( 9.366943396716600034, -16.50203108585677825, -53.41115344186808755 ) ) ;
#40960=CARTESIAN_POINT ( 'NONE',  ( 22.87803198333132570, -16.19128746702614308, -66.47989374956529218 ) ) ;
#40963=CARTESIAN_POINT ( 'NONE',  ( 11.27237125087875036, -9.289939099700770697, -72.79933495156693368 ) ) ;
#40965=CARTESIAN_POINT ( 'NONE',  ( 24.04493737658144425, -16.65173835530648105, -75.54933311882003011 ) ) ;
#40977=VERTEX_POINT ( 'NONE', #22951 ) ;
#40984=CARTESIAN_POINT ( 'NONE',  ( 23.35742708719739724, -16.95913214825089810, -81.23899999999999011 ) ) ;
#40988=VERTEX_POINT ( 'NONE', #51015 ) ;
#40992=CARTESIAN_POINT ( 'NONE',  ( 9.367366684597708826, -15.61630833865650025, -41.84717978380999170 ) ) ;
#40993=CARTESIAN_POINT ( 'NONE',  ( 23.24415347406168308, -19.18663440281774157, -33.94030009962079930 ) ) ;
#41001=CARTESIAN_POINT ( 'NONE',  ( 23.06214062797170072, -3.616188944679349593, -24.15000000000000213 ) ) ;
#41010=CARTESIAN_POINT ( 'NONE',  ( 18.97802158468009992, -8.301960802179829457, -70.90555118064968099 ) ) ;
#41016=CARTESIAN_POINT ( 'NONE',  ( 23.04645056301411543, -11.63203867424703120, -43.34097441868176048 ) ) ;
#41020=CARTESIAN_POINT ( 'NONE',  ( 16.33480707122532394, -23.55604788584398079, -33.99953662611090976 ) ) ;
#41024=CARTESIAN_POINT ( 'NONE',  ( 22.56719568149739885, -11.85854577478619909, -40.89907019807789368 ) ) ;
#41034=CARTESIAN_POINT ( 'NONE',  ( 15.09839649219260593, -23.52718973776712375, -52.04933381677249571 ) ) ;
#41038=EDGE_CURVE ( 'NONE', #37399, #49444, #39013, .T. ) ;
#41043=CARTESIAN_POINT ( 'NONE',  ( 14.06328890421924882, -7.911080998336773362, -79.20899914491724303 ) ) ;
#41047=AXIS2_PLACEMENT_3D ( 'NONE', #2370, #38542, #6313 ) ;
#41056=CARTESIAN_POINT ( 'NONE',  ( 17.90524532213879993, -9.025332794473378328, -36.03615195047114383 ) ) ;
#41064=CARTESIAN_POINT ( 'NONE',  ( 14.82090148184650147, -23.35328686801410214, -66.56600386269050773 ) ) ;
#41065=EDGE_CURVE ( 'NONE', #49152, #27637, #14196, .T. ) ;
#41080=CARTESIAN_POINT ( 'NONE',  ( 24.00223188529327345, -14.76797646811701803, -55.47349681351633421 ) ) ;
#41082=CARTESIAN_POINT ( 'NONE',  ( 22.73493107740300090, -13.03252716129409983, -32.14999999999999858 ) ) ;
#41092=CARTESIAN_POINT ( 'NONE',  ( 22.03527629823739886, -11.75396699929470046, -66.66271668429399710 ) ) ;
#41096=DIRECTION ( 'NONE',  ( 1.000000000000000000, 2.460964292799963328E-14, 0.000000000000000000 ) ) ;
#41099=CARTESIAN_POINT ( 'NONE',  ( 22.83553112445549971, -13.41818980498730163, -60.35193945864850207 ) ) ;
#41102=CARTESIAN_POINT ( 'NONE',  ( 8.428884788794746896, -17.68704093276265965, -80.70899836890637857 ) ) ;
#41105=ORIENTED_EDGE ( 'NONE', *, *, #48464, .F. ) ;
#41114=CARTESIAN_POINT ( 'NONE',  ( 9.807761426623416767, -20.47785318488935857, -60.29935320495772544 ) ) ;
#41125=LINE ( 'NONE', #29819, #35346 ) ;
#41127=CARTESIAN_POINT ( 'NONE',  ( 18.52227178108019601, -8.140722163069080253, -33.61092854022489718 ) ) ;
#41134=CARTESIAN_POINT ( 'NONE',  ( 20.51938203757270074, -21.13981406646960082, -35.13358212097359257 ) ) ;
#41141=FACE_OUTER_BOUND ( 'NONE', #28975, .T. ) ;
#41144=DIRECTION ( 'NONE',  ( 0.000000000000000000, 0.000000000000000000, -1.000000000000000000 ) ) ;
#41154=CARTESIAN_POINT ( 'NONE',  ( 22.43485972733980205, -19.59174867206459680, -80.41182290828409407 ) ) ;
#41162=CARTESIAN_POINT ( 'NONE',  ( 21.18999090978099886, -10.14416763429719914, -74.80477269330700096 ) ) ;
#41174=DIRECTION ( 'NONE',  ( 0.000000000000000000, 0.000000000000000000, -1.000000000000000000 ) ) ;
#41175=ADVANCED_FACE ( 'NONE', ( #43668 ), #36823, .T. ) ;
#41176=ORIENTED_EDGE ( 'NONE', *, *, #21264, .F. ) ;
#41179=ORIENTED_EDGE ( 'NONE', *, *, #44975, .T. ) ;
#41187=ORIENTED_EDGE ( 'NONE', *, *, #50209, .T. ) ;
#41191=CARTESIAN_POINT ( 'NONE',  ( 10.67428282541060192, -21.79477227803790029, -56.52269350815079463 ) ) ;
#41197=CARTESIAN_POINT ( 'NONE',  ( 9.992168748469609341, -19.83345958628190076, -49.04112620709079806 ) ) ;
#41200=CARTESIAN_POINT ( 'NONE',  ( 18.20456740063047008, -7.911074884095184778, -33.09099907805137519 ) ) ;
#41205=CARTESIAN_POINT ( 'NONE',  ( 10.05407090363459943, -21.18556450423380255, -52.27160849015929500 ) ) ;
#41209=CYLINDRICAL_SURFACE ( 'NONE', #29070, 6.766999999999998572 ) ;
#41225=CONICAL_SURFACE ( 'NONE', #6073, 12.92820323027549989, 0.7481802937784480800 ) ;
#41227=CARTESIAN_POINT ( 'NONE',  ( 11.97534830454654298, -10.20480668565649118, -47.74448746576103986 ) ) ;
#41229=CARTESIAN_POINT ( 'NONE',  ( 16.13393739769620083, -15.61618894467929941, -28.45282021618999835 ) ) ;
#41233=CARTESIAN_POINT ( 'NONE',  ( 14.64227698520870113, -7.857630305424530448, -81.23899999999999011 ) ) ;
#41235=EDGE_LOOP ( 'NONE', ( #30729, #29536, #31092, #40778 ) ) ;
#41243=CARTESIAN_POINT ( 'NONE',  ( 20.58428850091829787, -20.97262704213749984, -81.23899999999999011 ) ) ;
#41248=CARTESIAN_POINT ( 'NONE',  ( 22.83067611733696722, -17.21599180179194022, -68.92243437301439712 ) ) ;
#41252=DIRECTION ( 'NONE',  ( 0.000000000000000000, 0.000000000000000000, -1.000000000000000000 ) ) ;
#41260=DIRECTION ( 'NONE',  ( 0.000000000000000000, 0.000000000000000000, -1.000000000000000000 ) ) ;
#41261=VECTOR ( 'NONE', #7650, 1000.000000000000114 ) ;
#41265=EDGE_CURVE ( 'NONE', #29694, #15474, #31064, .T. ) ;
#41266=CARTESIAN_POINT ( 'NONE',  ( 17.56455728119119897, -7.899967399639820087, -68.84585897299560031 ) ) ;
#41270=CARTESIAN_POINT ( 'NONE',  ( 22.90085274204890808, -15.61618877333890332, -76.84718755697707593 ) ) ;
#41274=CARTESIAN_POINT ( 'NONE',  ( 14.06317034403552313, -7.911111693438598103, -42.92429533349460513 ) ) ;
#41283=CARTESIAN_POINT ( 'NONE',  ( 22.55572082845609927, -19.39340907418709747, -47.23658468316739345 ) ) ;
#41285=VERTEX_POINT ( 'NONE', #29211 ) ;
#41307=CARTESIAN_POINT ( 'NONE',  ( 20.29253929434950976, -21.02756302329809657, -72.74444564148153347 ) ) ;
#41309=CARTESIAN_POINT ( 'NONE',  ( 9.366647546311250849, -15.61604444486649967, -65.84717978381009118 ) ) ;
#41314=CARTESIAN_POINT ( 'NONE',  ( 20.93810839686982561, -20.38192891622346892, -46.70153489369711508 ) ) ;
#41316=CARTESIAN_POINT ( 'NONE',  ( 8.474797562328269862, -17.32625460829050112, -68.94257179459920337 ) ) ;
#41321=DIRECTION ( 'NONE',  ( 0.000000000000000000, 0.000000000000000000, -1.000000000000000000 ) ) ;
#41324=CARTESIAN_POINT ( 'NONE',  ( 21.90486186017893644, -19.18926943320902012, -33.02368868574395577 ) ) ;
#41326=VERTEX_POINT ( 'NONE', #49931 ) ;
#41334=CARTESIAN_POINT ( 'NONE',  ( 23.38712508359760278, -17.09264023749170391, -32.14999999999999858 ) ) ;
#41337=DIRECTION ( 'NONE',  ( 0.000000000000000000, 0.000000000000000000, 1.000000000000000000 ) ) ;
#41338=CARTESIAN_POINT ( 'NONE',  ( 9.366468209001951095, -15.46638865352482561, -49.85422095549364485 ) ) ;
#41341=ORIENTED_EDGE ( 'NONE', *, *, #40116, .F. ) ;
#41342=CARTESIAN_POINT ( 'NONE',  ( 15.64736352786460039, -8.580152770550549590, -60.32520219920449733 ) ) ;
#41349=CARTESIAN_POINT ( 'NONE',  ( 21.29521595269359935, -10.80955161965160194, -66.21414035735629966 ) ) ;
#41350=CARTESIAN_POINT ( 'NONE',  ( 16.86121012496890259, -15.61618894467929941, -82.15000000000000568 ) ) ;
#41361=CARTESIAN_POINT ( 'NONE',  ( 14.36273960662768090, -22.20707503043608000, -55.03615486043509009 ) ) ;
#41370=B_SPLINE_CURVE_WITH_KNOTS ( 'NONE', 3,
 ( #4023, #97, #4523, #47793, #12149, #40429, #15810, #31771, #32025, #48050, #28103, #8210, #44364, #27854, #43855, #16326, #39926, #48300, #45664, #44886, #5059, #45407, #21795, #21535, #29144, #9255, #29658, #29910, #17626 ),
 .UNSPECIFIED., .F., .F.,
 ( 4, 2, 1, 1, 1, 1, 1, 2, 2, 2, 2, 2, 2, 2, 2, 2, 4 ),
 ( 0.5000037344877438228, 0.5002478732892634561, 0.5004920120907830894, 0.5009802896938223560, 0.5019568448999010002, 0.5039099553120580666, 0.5078161761363726434, 0.5156286177850016861, 0.5312535010822597714, 0.5625032676767758311, 0.6250028008658078393, 0.6875023340548398476, 0.7500018672438718559, 0.8125014004329038642, 0.8750009336219359835, 0.9375004668109679917, 1.000000000000000000 ),
 .UNSPECIFIED. ) ;
#41372=VERTEX_POINT ( 'NONE', #42450 ) ;
#41375=ORIENTED_EDGE ( 'NONE', *, *, #21004, .T. ) ;
#41378=CARTESIAN_POINT ( 'NONE',  ( 23.77197502537190132, -17.41816804884900094, -34.08624212660669883 ) ) ;
#41386=CARTESIAN_POINT ( 'NONE',  ( 16.00572161013059969, -8.564513971789889268, -34.34139281033739621 ) ) ;
#41388=VECTOR ( 'NONE', #38297, 1000.000000000000000 ) ;
#41394=CARTESIAN_POINT ( 'NONE',  ( 20.94623932155910140, -8.921080969116559345, -79.20604505178991417 ) ) ;
#41395=DIRECTION ( 'NONE',  ( 0.000000000000000000, 0.000000000000000000, -1.000000000000000000 ) ) ;
#41401=CARTESIAN_POINT ( 'NONE',  ( 11.27224164520935901, -9.290037151915401026, -68.79933606627460563 ) ) ;
#41410=CARTESIAN_POINT ( 'NONE',  ( 11.03079100840449911, -10.74787757151459822, -37.69532517445329489 ) ) ;
#41415=VERTEX_POINT ( 'NONE', #35606 ) ;
#41416=CARTESIAN_POINT ( 'NONE',  ( 23.47605554803709893, -16.88109819232330011, -75.12164841756148803 ) ) ;
#41420=CARTESIAN_POINT ( 'NONE',  ( 22.76597515051138032, -11.21741694172178150, -49.60607765262594882 ) ) ;
#41425=CARTESIAN_POINT ( 'NONE',  ( 8.222342146248220018, -15.61610160653870061, -76.79233150823698395 ) ) ;
#41427=CARTESIAN_POINT ( 'NONE',  ( 24.04476371472169305, -15.67281184061405597, -71.50995035837887315 ) ) ;
#41439=DIRECTION ( 'NONE',  ( 0.000000000000000000, 0.000000000000000000, -1.000000000000000000 ) ) ;
#41441=CARTESIAN_POINT ( 'NONE',  ( 23.79191596521776830, -13.56499935927118194, -43.70900647343250256 ) ) ;
#41443=CARTESIAN_POINT ( 'NONE',  ( 21.87095150668039878, -21.53813027917859912, -56.04737992176900008 ) ) ;
#41448=CARTESIAN_POINT ( 'NONE',  ( 8.841563762076869892, -14.09041682418759933, -47.29830972369120445 ) ) ;
#41450=EDGE_CURVE ( 'NONE', #30137, #16752, #15439, .T. ) ;
#41457=ADVANCED_FACE ( 'NONE', ( #3644 ), #51594, .T. ) ;
#41458=CARTESIAN_POINT ( 'NONE',  ( 21.97196478570849720, -21.43857307197580297, -55.75724145695859590 ) ) ;
#41485=CARTESIAN_POINT ( 'NONE',  ( 9.367777563323313572, -16.29676251027069966, -61.81516750865657883 ) ) ;
#41486=ORIENTED_EDGE ( 'NONE', *, *, #35690, .F. ) ;
#41492=CARTESIAN_POINT ( 'NONE',  ( 8.761419361326980848, -12.64912489806860840, -80.62955707704453800 ) ) ;
#41493=ORIENTED_EDGE ( 'NONE', *, *, #6824, .T. ) ;
#41494=ORIENTED_EDGE ( 'NONE', *, *, #5784, .T. ) ;
#41499=CARTESIAN_POINT ( 'NONE',  ( 24.04493739766370553, -15.61621743414952945, -77.50767718564499376 ) ) ;
#41500=CARTESIAN_POINT ( 'NONE',  ( 22.46011667808101109, -10.75453029109795011, -63.29933646154306359 ) ) ;
#41510=CARTESIAN_POINT ( 'NONE',  ( 24.04493117584121364, -15.62644129081893674, -33.79274222580392717 ) ) ;
#41515=CARTESIAN_POINT ( 'NONE',  ( 16.13393739769620083, -15.61618894467929941, -32.14999999999999858 ) ) ;
#41519=CARTESIAN_POINT ( 'NONE',  ( 19.72595728692159867, -21.68578137661910077, -63.17708371749489515 ) ) ;
#41522=CARTESIAN_POINT ( 'NONE',  ( 23.98053627935140142, -15.48339521895720061, -73.28211911255830557 ) ) ;
#41523=VERTEX_POINT ( 'NONE', #51847 ) ;
#41524=AXIS2_PLACEMENT_3D ( 'NONE', #409, #48370, #16396 ) ;
#41530=CIRCLE ( 'NONE', #49117, 4.296700167715679086 ) ;
#41531=CARTESIAN_POINT ( 'NONE',  ( 23.85151994168742462, -13.77020273865184841, -65.43299463483448619 ) ) ;
#41540=CARTESIAN_POINT ( 'NONE',  ( 12.88601828706359953, -8.911137431892139915, -40.42375661169619860 ) ) ;
#41546=CARTESIAN_POINT ( 'NONE',  ( 9.221357130620331688, -19.60022191152414095, -62.34097168116907994 ) ) ;
#41549=LINE ( 'NONE', #37106, #41863 ) ;
#41561=EDGE_LOOP ( 'NONE', ( #6132, #23300, #40685, #38343, #32573, #29881, #10378, #45171, #36684, #19778, #545, #5610, #23691, #3967, #11539, #22541, #6167, #19428, #44130, #5599, #5093, #10204, #370, #51105, #18886, #12570, #2766, #36016, #1278, #19891, #22387, #40200, #19942, #46200, #5365, #2826, #8193, #7364, #42681, #6121, #22138, #3398, #8567, #41675, #26652, #49553, #2574, #46193, #42803, #39770, #1678, #10046, #3119, #22033, #48791, #44079, #9137, #10483, #25702, #36364, #48920, #50010, #9919, #9910, #837, #9760, #50582, #50316, #37967, #48689, #2629, #18276, #23571, #36379, #19710, #46609, #15009, #36330, #9954, #18426, #12226, #8901, #49829, #18856, #35356, #16612, #31600, #5799, #2012, #26805, #24619, #43176, #17362, #20988, #45572, #30613, #1067, #4494, #26922, #34517, #45024, #43120, #15537 ) ) ;
#41563=CARTESIAN_POINT ( 'NONE',  ( 24.03110856329654155, -15.13910014759192535, -77.48847149410299551 ) ) ;
#41569=CARTESIAN_POINT ( 'NONE',  ( 24.04484584168765338, -15.65733071861149028, -49.50932076728930298 ) ) ;
#41572=VECTOR ( 'NONE', #39756, 1000.000000000000000 ) ;
#41573=CARTESIAN_POINT ( 'NONE',  ( 21.51830670342329910, -9.906958280997308464, -59.75317579121929867 ) ) ;
#41580=EDGE_CURVE ( 'NONE', #47534, #25231, #22295, .T. ) ;
#41592=CARTESIAN_POINT ( 'NONE',  ( 23.38129519385890021, -17.13736245159219607, -32.14999999999999858 ) ) ;
#41594=CARTESIAN_POINT ( 'NONE',  ( 20.12545638205761733, -8.759847604476449945, -45.17547658566174817 ) ) ;
#41596=CARTESIAN_POINT ( 'NONE',  ( 14.06319310886902407, -23.32127208991568779, -46.37571296203240934 ) ) ;
#41598=CARTESIAN_POINT ( 'NONE',  ( 15.07367541409689871, -22.58887879154509903, -65.39521378727610568 ) ) ;
#41603=CARTESIAN_POINT ( 'NONE',  ( 18.21836968370325138, -14.10176024214774593, -22.64999999999999858 ) ) ;
#41604=CARTESIAN_POINT ( 'NONE',  ( 9.543099337633478285, -17.38756428688266809, -43.36948683488909495 ) ) ;
#41607=CARTESIAN_POINT ( 'NONE',  ( 10.04829391747680134, -19.18094729950349731, -71.28415194542810696 ) ) ;
#41621=EDGE_CURVE ( 'NONE', #29694, #15276, #48431, .T. ) ;
#41629=CARTESIAN_POINT ( 'NONE',  ( 12.72604264528349027, -9.703222777469695970, -67.78615274844003125 ) ) ;
#41630=CARTESIAN_POINT ( 'NONE',  ( 8.222845792583640900, -15.61638830267690103, -48.79233150823699816 ) ) ;
#41632=CARTESIAN_POINT ( 'NONE',  ( 24.04493739826821042, -14.58063923811300988, -53.75066785666746938 ) ) ;
#41633=DIRECTION ( 'NONE',  ( 0.8660254037844387076, -0.4999999999999998890, 0.000000000000000000 ) ) ;
#41634=CARTESIAN_POINT ( 'NONE',  ( 15.88724090743389894, -23.46003292791059991, -38.52250226616929751 ) ) ;
#41641=CARTESIAN_POINT ( 'NONE',  ( 12.71325777259860068, -22.74941205225429997, -32.14999999999999858 ) ) ;
#41645=CARTESIAN_POINT ( 'NONE',  ( 23.15448228781169959, -14.94201639938200010, -34.81670639671909839 ) ) ;
#41648=VERTEX_POINT ( 'NONE', #27978 ) ;
#41653=CARTESIAN_POINT ( 'NONE',  ( 20.11812230705482918, -8.703697806114258029, -57.45899798619976195 ) ) ;
#41669=CARTESIAN_POINT ( 'NONE',  ( 13.34527985300699982, -22.09430192571580065, -43.08221248677949688 ) ) ;
#41675=ORIENTED_EDGE ( 'NONE', *, *, #33330, .F. ) ;
#41676=CARTESIAN_POINT ( 'NONE',  ( 11.07009171580209994, -10.15137776328389840, -74.32945910692518510 ) ) ;
#41679=CARTESIAN_POINT ( 'NONE',  ( 8.222845792583640900, -15.61638830267690103, -48.79233150823699816 ) ) ;
#41684=CARTESIAN_POINT ( 'NONE',  ( 8.222944117552916765, -14.58059227398267410, -44.83399173169763685 ) ) ;
#41688=VERTEX_POINT ( 'NONE', #4143 ) ;
#41691=CARTESIAN_POINT ( 'NONE',  ( 8.223528471986069732, -15.61608932669300032, -46.79233150823699816 ) ) ;
#41692=ORIENTED_EDGE ( 'NONE', *, *, #1467, .T. ) ;
#41697=ORIENTED_EDGE ( 'NONE', *, *, #43426, .T. ) ;
#41699=CARTESIAN_POINT ( 'NONE',  ( 22.84576648276765454, -14.72542540978770198, -72.41083198718504832 ) ) ;
#41701=CARTESIAN_POINT ( 'NONE',  ( 9.243092856068470198, -11.08860884499529931, -50.97736833369750542 ) ) ;
#41702=DIRECTION ( 'NONE',  ( 0.5000000000000003331, -0.8660254037844383745, 0.000000000000000000 ) ) ;
#41708=CARTESIAN_POINT ( 'NONE',  ( 8.997941842051611516, -17.75727774128869996, -47.13987186156389697 ) ) ;
#41709=CARTESIAN_POINT ( 'NONE',  ( 9.063471803478160282, -18.03476473673429936, -32.14999999999999858 ) ) ;
#41715=CARTESIAN_POINT ( 'NONE',  ( 12.76582758031636544, -8.383476218416783254, -60.86875003376393778 ) ) ;
#41718=CARTESIAN_POINT ( 'NONE',  ( 8.466531389232500260, -12.58409300121869911, -48.62753766123279320 ) ) ;
#41736=CARTESIAN_POINT ( 'NONE',  ( 10.63552672802458687, -20.03320595643863911, -57.63175854304461865 ) ) ;
#41740=CARTESIAN_POINT ( 'NONE',  ( 18.89370190350303602, -21.85803478350294426, -66.82003588566664121 ) ) ;
#41744=CARTESIAN_POINT ( 'NONE',  ( 18.20460759450573107, -23.32129168142665776, -75.92435657186162246 ) ) ;
#41746=CARTESIAN_POINT ( 'NONE',  ( 13.36620148929459972, -22.10326818851440223, -73.47554475576528432 ) ) ;
#41750=CARTESIAN_POINT ( 'NONE',  ( 9.080919143135764315, -11.95389120226177226, -80.66002922336500092 ) ) ;
#41751=ORIENTED_EDGE ( 'NONE', *, *, #29740, .T. ) ;
#41765=VECTOR ( 'NONE', #43002, 1000.000000000000000 ) ;
#41769=CARTESIAN_POINT ( 'NONE',  ( 23.06214062797170072, -27.61618894467930119, -24.14999999999999858 ) ) ;
#41781=CARTESIAN_POINT ( 'NONE',  ( 16.87426238886190077, -23.42891363524900328, -73.75743269893999354 ) ) ;
#41782=ORIENTED_EDGE ( 'NONE', *, *, #35062, .F. ) ;
#41783=CARTESIAN_POINT ( 'NONE',  ( 22.66096180266447746, -13.24646063577329969, -48.73573848298972422 ) ) ;
#41791=CARTESIAN_POINT ( 'NONE',  ( 23.94246574329788046, -14.28158910010441396, -65.45377657909587299 ) ) ;
#41799=CARTESIAN_POINT ( 'NONE',  ( 23.58208950757730094, -15.43807525510060152, -57.05973213505619412 ) ) ;
#41804=CARTESIAN_POINT ( 'NONE',  ( 22.90000843106822259, -14.87822356394483059, -74.81246489664891897 ) ) ;
#41805=CARTESIAN_POINT ( 'NONE',  ( 14.06315599067715283, -23.32126188359937657, -62.09098641193147472 ) ) ;
#41807=CARTESIAN_POINT ( 'NONE',  ( 15.09848396724155961, -7.705177579893296880, -35.25066358517401710 ) ) ;
#41808=DIRECTION ( 'NONE',  ( 0.000000000000000000, 0.000000000000000000, -1.000000000000000000 ) ) ;
#41811=ORIENTED_EDGE ( 'NONE', *, *, #49644, .T. ) ;
#41827=CIRCLE ( 'NONE', #15942, 6.999999999999999112 ) ;
#41829=CARTESIAN_POINT ( 'NONE',  ( 24.04491473693991921, -15.63666989667861174, -49.50848968882522172 ) ) ;
#41833=CARTESIAN_POINT ( 'NONE',  ( 19.09934987693050346, -22.88207336569690042, -76.38915131457939367 ) ) ;
#41834=B_SPLINE_CURVE_WITH_KNOTS ( 'NONE', 3,
 ( #50800, #14888, #30853, #27705, #4631, #12506, #15924, #19592, #28475, #31880, #44474, #40029, #40287, #39773, #16172, #8837, #8581, #3876, #20097, #24009, #40541, #51820, #19844, #35582, #11999, #24523 ),
 .UNSPECIFIED., .F., .F.,
 ( 4, 2, 2, 2, 2, 2, 2, 2, 2, 2, 2, 2, 4 ),
 ( 0.000000000000000000, 0.03124985050885574836, 0.06249970101771149672, 0.09374955152656724855, 0.1249994020354229934, 0.1562492525442786551, 0.1874991030531343028, 0.2187489535619900061, 0.2499988040708456538, 0.3124985050885567550, 0.3749982061062678285, 0.4374979071239790129, 0.4999976081416900864 ),
 .UNSPECIFIED. ) ;
#41838=B_SPLINE_CURVE_WITH_KNOTS ( 'NONE', 3,
 ( #19945, #48005, #40647, #23860, #4745, #39883, #48258, #54, #547, #20712 ),
 .UNSPECIFIED., .F., .F.,
 ( 4, 1, 1, 1, 1, 1, 1, 4 ),
 ( 0.000000000000000000, 0.04151989875101936428, 0.1207388298145684186, 0.1999577608781174798, 0.2791766919418271486, 0.3583956230053761960, 0.4376145540690835611, 0.4999959824775806472 ),
 .UNSPECIFIED. ) ;
#41846=ORIENTED_EDGE ( 'NONE', *, *, #39861, .F. ) ;
#41852=EDGE_CURVE ( 'NONE', #3678, #1577, #10870, .T. ) ;
#41861=CARTESIAN_POINT ( 'NONE',  ( 18.91091419587250044, -22.09931774463699838, -75.21836123916489214 ) ) ;
#41863=VECTOR ( 'NONE', #41808, 1000.000000000000000 ) ;
#41870=CARTESIAN_POINT ( 'NONE',  ( 22.69578901594789855, -18.20166028220740273, -78.57229360328089740 ) ) ;
#41874=CARTESIAN_POINT ( 'NONE',  ( 22.68450450196613843, -17.37076082248510289, -40.53613820532829237 ) ) ;
#41887=EDGE_CURVE ( 'NONE', #4707, #50665, #41530, .T. ) ;
#41898=CARTESIAN_POINT ( 'NONE',  ( 9.807870791654629272, -20.47799351597511475, -48.58399859126286202 ) ) ;
#41902=CARTESIAN_POINT ( 'NONE',  ( 7.922186500973898760, -16.35708704190409790, -80.76368641361838741 ) ) ;
#41906=VERTEX_POINT ( 'NONE', #17241 ) ;
#41908=CARTESIAN_POINT ( 'NONE',  ( 13.56856140308030056, -9.046454919155269891, -78.22868061958250507 ) ) ;
#41911=CARTESIAN_POINT ( 'NONE',  ( 23.15708489307130336, -16.26268599235770296, -36.87639860437320038 ) ) ;
#41922=CARTESIAN_POINT ( 'NONE',  ( 12.20479792536879948, -10.10644435241950134, -32.14999999999999858 ) ) ;
#41934=CARTESIAN_POINT ( 'NONE',  ( 24.04493739796119556, -16.65172873511394869, -73.83399818621970212 ) ) ;
#41937=CARTESIAN_POINT ( 'NONE',  ( 23.17755585561640075, -15.97674090469540076, -48.46909979910559230 ) ) ;
#41938=FACE_OUTER_BOUND ( 'NONE', #21447, .T. ) ;
#41944=CARTESIAN_POINT ( 'NONE',  ( 16.83676928204470258, -23.03324507772050111, -73.53726979628909532 ) ) ;
#41947=CYLINDRICAL_SURFACE ( 'NONE', #11149, 7.910999999999997812 ) ;
#41953=CARTESIAN_POINT ( 'NONE',  ( 22.84259504164056409, -14.71167573906013004, -62.41017214630380039 ) ) ;
#41956=CARTESIAN_POINT ( 'NONE',  ( 19.54197421750533081, -9.703304665228225545, -58.11948669415193081 ) ) ;
#41971=CARTESIAN_POINT ( 'NONE',  ( 13.85732796729022986, -23.21488026636175306, -66.10023604892785443 ) ) ;
#41972=CARTESIAN_POINT ( 'NONE',  ( 9.336894014525560337, -20.28340667082309778, -48.60080040178890215 ) ) ;
#41973=CARTESIAN_POINT ( 'NONE',  ( 21.64576443335199585, -11.59628691946671886, -56.25250486724262799 ) ) ;
#41977=CARTESIAN_POINT ( 'NONE',  ( 22.63087827937219743, -11.96975877461539994, -42.06986027349229573 ) ) ;
#41979=CARTESIAN_POINT ( 'NONE',  ( 9.682426609870530498, -12.74603349750159964, -32.14999999999999858 ) ) ;
#41981=CARTESIAN_POINT ( 'NONE',  ( 11.27236231982013770, -9.289945855619381021, -51.08399742131821597 ) ) ;
#41986=CARTESIAN_POINT ( 'NONE',  ( 7.889072482538179720, -15.54602314267300045, -60.51037732077569586 ) ) ;
#41987=ORIENTED_EDGE ( 'NONE', *, *, #37088, .F. ) ;
#41991=CARTESIAN_POINT ( 'NONE',  ( 9.131712051400846519, -19.42118211742113587, -40.34903064087519198 ) ) ;
#41997=EDGE_LOOP ( 'NONE', ( #13173, #32324, #42370, #33436 ) ) ;
#42000=CARTESIAN_POINT ( 'NONE',  ( 22.60295963412389852, -10.99248356359692380, -65.59471942785054921 ) ) ;
#42009=CARTESIAN_POINT ( 'NONE',  ( 22.90093739934872374, -15.62378126355319985, -66.45317726807988379 ) ) ;
#42027=CARTESIAN_POINT ( 'NONE',  ( 24.04493438893774737, -15.62471349072081139, -77.50801464174854516 ) ) ;
#42030=AXIS2_PLACEMENT_3D ( 'NONE', #21104, #32622, #12750 ) ;
#42035=CARTESIAN_POINT ( 'NONE',  ( 21.72396248402345975, -21.29268565403493696, -34.04455158046467744 ) ) ;
#42037=CARTESIAN_POINT ( 'NONE',  ( 18.57770503654736061, -22.23212114670332795, -49.23455185029879289 ) ) ;
#42047=CARTESIAN_POINT ( 'NONE',  ( 17.82483774787520048, -23.27958272219449753, -77.71837925212109610 ) ) ;
#42049=DIRECTION ( 'NONE',  ( 0.000000000000000000, 0.000000000000000000, -1.000000000000000000 ) ) ;
#42054=CARTESIAN_POINT ( 'NONE',  ( 9.366504787982940172, -15.61629640169840094, -69.84717978381009118 ) ) ;
#42056=CARTESIAN_POINT ( 'NONE',  ( 24.04493737838489409, -16.65173502485940205, -35.83399554789317421 ) ) ;
#42057=CARTESIAN_POINT ( 'NONE',  ( 24.04477596867337041, -15.61618922203197357, -43.50766101656756746 ) ) ;
#42059=CARTESIAN_POINT ( 'NONE',  ( 11.97526630703813488, -21.02750917104722461, -79.16115263443646199 ) ) ;
#42062=CARTESIAN_POINT ( 'NONE',  ( 22.89855973853233451, -15.80993545744688333, -62.46194232920734635 ) ) ;
#42066=CARTESIAN_POINT ( 'NONE',  ( 22.33916946346290189, -11.49286633441439953, -50.88065551209390236 ) ) ;
#42071=CARTESIAN_POINT ( 'NONE',  ( 9.909523820307871489, -18.91395403005434517, -75.69203052425869771 ) ) ;
#42072=CARTESIAN_POINT ( 'NONE',  ( 16.92763237404272658, -23.48995300663941066, -61.97569791650314386 ) ) ;
#42074=CARTESIAN_POINT ( 'NONE',  ( 18.64395816326117483, -9.025107475687542902, -54.46300130049679922 ) ) ;
#42075=CARTESIAN_POINT ( 'NONE',  ( 10.70613124693099927, -19.68844507227139928, -81.23899999999999011 ) ) ;
#42078=VERTEX_POINT ( 'NONE', #28891 ) ;
#42096=CARTESIAN_POINT ( 'NONE',  ( 12.93056411727340205, -22.78034606313060095, -74.64633483117989954 ) ) ;
#42113=CARTESIAN_POINT ( 'NONE',  ( 20.29013637266969994, -10.24695330870310173, -32.14999999999999858 ) ) ;
#42117=B_SPLINE_CURVE_WITH_KNOTS ( 'NONE', 3,
 ( #23816, #51378, #12312, #35378, #36150, #8379, #27510, #3684, #8125, #35646, #24329, #24070, #28273, #4183, #27250, #39835, #51631, #43512 ),
 .UNSPECIFIED., .F., .F.,
 ( 4, 2, 2, 2, 2, 2, 2, 2, 4 ),
 ( 0.000000000000000000, 0.06250019386976815583, 0.1250003877395363117, 0.1875005816093044675, 0.2500007754790726233, 0.3125009693488408624, 0.3750011632186091570, 0.4375013570883773961, 0.5000015509581456907 ),
 .UNSPECIFIED. ) ;
#42118=CARTESIAN_POINT ( 'NONE',  ( 17.97808210774817184, -7.902931223253473192, -45.08245229423729938 ) ) ;
#42123=AXIS2_PLACEMENT_3D ( 'NONE', #33412, #18476, #17956 ) ;
#42124=CARTESIAN_POINT ( 'NONE',  ( 16.79927617522759675, -22.63757652019199895, -73.31710689363809763 ) ) ;
#42134=CARTESIAN_POINT ( 'NONE',  ( 10.53030345648840083, -19.89892701156700028, -75.24509849860899635 ) ) ;
#42144=CARTESIAN_POINT ( 'NONE',  ( 10.93711667326426706, -9.623292665671325352, -38.78027754126386384 ) ) ;
#42150=FACE_OUTER_BOUND ( 'NONE', #25157, .T. ) ;
#42159=EDGE_LOOP ( 'NONE', ( #4517, #23112, #23283, #28074 ) ) ;
#42163=CARTESIAN_POINT ( 'NONE',  ( 11.74154980093570089, -22.11954798377650278, -44.70157888913149691 ) ) ;
#42167=ORIENTED_EDGE ( 'NONE', *, *, #38049, .F. ) ;
#42169=DIRECTION ( 'NONE',  ( 0.000000000000000000, 0.000000000000000000, -1.000000000000000000 ) ) ;
#42172=VECTOR ( 'NONE', #28222, 1000.000000000000000 ) ;
#42173=CARTESIAN_POINT ( 'NONE',  ( 19.78667132190540201, -9.582939898486838359, -40.52046943329969508 ) ) ;
#42181=CARTESIAN_POINT ( 'NONE',  ( 23.13393739769569990, -15.61618894467929941, -23.74958330439410048 ) ) ;
#42188=CARTESIAN_POINT ( 'NONE',  ( 12.79606686025591600, -8.364588515209828046, -70.87015286643487855 ) ) ;
#42196=DIRECTION ( 'NONE',  ( 0.000000000000000000, 0.000000000000000000, -1.000000000000000000 ) ) ;
#42199=CARTESIAN_POINT ( 'NONE',  ( 18.32725043397720199, -8.913060076642750573, -50.05347842037799211 ) ) ;
#42200=DIRECTION ( 'NONE',  ( 0.000000000000000000, 0.000000000000000000, -1.000000000000000000 ) ) ;
#42205=CARTESIAN_POINT ( 'NONE',  ( 16.02219763869389979, -23.46311588517269797, -37.79203799605679848 ) ) ;
#42208=CARTESIAN_POINT ( 'NONE',  ( 24.00580240620973882, -14.79998447179700705, -49.75944949806702766 ) ) ;
#42213=CARTESIAN_POINT ( 'NONE',  ( 22.88621463017819124, -15.16096302198837087, -62.43140197241153544 ) ) ;
#42218=CARTESIAN_POINT ( 'NONE',  ( 20.99563923973620305, -9.290042711380010587, -47.50066625719156121 ) ) ;
#42226=CARTESIAN_POINT ( 'NONE',  ( 22.81271906878893674, -14.50446391198467211, -72.40033769317329870 ) ) ;
#42228=CARTESIAN_POINT ( 'NONE',  ( 13.76993472929000006, -23.51518960550360049, -62.38489440685859222 ) ) ;
#42236=CARTESIAN_POINT ( 'NONE',  ( 16.60938827565720288, -8.181093769243290126, -41.75298454923780156 ) ) ;
#42237=CARTESIAN_POINT ( 'NONE',  ( 8.841948616896502244, -16.75224457701870406, -32.14999999999999858 ) ) ;
#42241=CARTESIAN_POINT ( 'NONE',  ( 18.20469862234147129, -7.911111929476298599, -51.37566333439941246 ) ) ;
#42245=CARTESIAN_POINT ( 'NONE',  ( 11.15293902025540085, -22.18675786014680185, -66.21414035735639914 ) ) ;
#42255=CARTESIAN_POINT ( 'NONE',  ( 20.82450310336395205, -9.200888125289733210, -81.20852785396732543 ) ) ;
#42274=B_SPLINE_CURVE_WITH_KNOTS ( 'NONE', 3,
 ( #28822, #4995, #1318, #33270, #45345, #41401, #5519, #21474, #1572, #49545, #9950, #10481, #10735, #6540, #21986, #26435, #2615, #26689 ),
 .UNSPECIFIED., .F., .F.,
 ( 4, 2, 2, 2, 2, 2, 2, 2, 4 ),
 ( 0.000000000000000000, 0.06250019453820399029, 0.1250003890764079806, 0.1875005836146119709, 0.2500007781528159612, 0.3125009726910198404, 0.3750011672292237197, 0.4375013617674275990, 0.5000015563056314782 ),
 .UNSPECIFIED. ) ;
#42281=AXIS2_PLACEMENT_3D ( 'NONE', #8011, #15109, #39216 ) ;
#42286=CARTESIAN_POINT ( 'NONE',  ( 15.24811531979822377, -22.38318606151044676, -44.99450808075278729 ) ) ;
#42300=CARTESIAN_POINT ( 'NONE',  ( 16.19411604853889486, -22.38296026765021907, -46.94999358384413313 ) ) ;
#42308=CARTESIAN_POINT ( 'NONE',  ( 11.18413446363969932, -9.526349358606669426, -80.57026077041129497 ) ) ;
#42313=CARTESIAN_POINT ( 'NONE',  ( 9.740363391916037727, -12.79400397788338140, -47.97990518416660422 ) ) ;
#42323=CARTESIAN_POINT ( 'NONE',  ( 22.72480952368614382, -17.38744173618666267, -78.53615067353597112 ) ) ;
#42326=CARTESIAN_POINT ( 'NONE',  ( 22.87920569102662682, -16.16927548186827579, -62.47886883811316494 ) ) ;
#42329=CARTESIAN_POINT ( 'NONE',  ( 8.922492023814040607, -13.74489261382869998, -52.14815840911180089 ) ) ;
#42333=CARTESIAN_POINT ( 'NONE',  ( 9.543078926210201374, -17.38749007367445998, -69.36948668258585826 ) ) ;
#42335=FACE_OUTER_BOUND ( 'NONE', #24461, .T. ) ;
#42336=CARTESIAN_POINT ( 'NONE',  ( 21.26062805952274459, -21.67729426163444018, -61.78425362803765353 ) ) ;
#42338=VECTOR ( 'NONE', #47410, 1000.000000000000000 ) ;
#42348=CARTESIAN_POINT ( 'NONE',  ( 22.89855956817655880, -15.80994150920190755, -72.46193828865773412 ) ) ;
#42350=AXIS2_PLACEMENT_3D ( 'NONE', #51778, #12207, #15881 ) ;
#42351=DIRECTION ( 'NONE',  ( 1.000000000000000000, 0.000000000000000000, 0.000000000000000000 ) ) ;
#42353=DIRECTION ( 'NONE',  ( 0.000000000000000000, 0.000000000000000000, 1.000000000000000000 ) ) ;
#42357=CARTESIAN_POINT ( 'NONE',  ( 21.17583492150360058, -21.63000777762489690, -78.29040566010620239 ) ) ;
#42368=CARTESIAN_POINT ( 'NONE',  ( 11.43684957307149830, -21.90300961580910055, -49.99175337985419532 ) ) ;
#42370=ORIENTED_EDGE ( 'NONE', *, *, #16385, .T. ) ;
#42379=B_SPLINE_CURVE_WITH_KNOTS ( 'NONE', 3,
 ( #10630, #42075, #27114, #38144, #18218, #30775, #26329, #34184, #26069, #26852, #42863, #43118, #10889, #21880, #33929, #2499, #22655, #49945, #50712, #14036, #50201, #26584, #14294, #29996, #46282, #6957, #10368, #18479, #50460, #46799, #14550, #30519, #42602, #6697, #2761, #19251, #47818, #47564, #51491, #39441, #43630, #12421, #24183, #7209, #15837, #27624, #11662, #19769, #28386, #3541, #39180, #27876, #23163, #51240, #39950, #16347, #43879, #7733, #7976, #32304, #31800, #48326, #35233, #11925, #40204, #23676, #23927, #39693, #51741, #4045, #3798, #27367, #3277, #36255, #4292, #20264, #35758, #15331, #20009, #8231, #15592, #31284, #47317, #11407, #366, #36001, #118, #43374, #7468, #23420, #16091, #32050, #19511, #35501, #48072, #31546, #12170, #28129, #44134, #45435, #5346, #16601, #32557, #48848, #37554, #616, #33618, #8493, #28644, #1401, #41233, #1661 ),
 .UNSPECIFIED., .F., .F.,
 ( 4, 3, 3, 3, 3, 3, 3, 3, 3, 3, 3, 3, 3, 3, 3, 3, 3, 3, 3, 3, 3, 3, 3, 3, 3, 3, 3, 3, 3, 3, 3, 3, 3, 3, 3, 3, 3, 4 ),
 ( -1.533736992487469974, -1.476288708613060052, -1.420671483735689966, -1.384064782255480131, -1.360357242476590178, -1.351866781456839917, -1.295064174654980027, -1.237933406125270031, -1.182875639009639990, -1.170176701831340038, -1.162728788953599990, -1.127817871894019941, -1.070863248456429995, -1.013122296642539943, -0.9549592239029349727, -0.9075319219357990130, -0.8918603538934489761, -0.8833676238340290032, -0.8240633799986251118, -0.7652500160343930213, -0.7062545498940289157, -0.6468558762931539974, -0.6146511409503889745, -0.6051424443490369676, -0.5954651498571321699, -0.5353212793362460697, -0.4746770670517450608, -0.4139651071065320043, -0.3892179935510320377, -0.3405657443571530330, -0.3192803853348309406, -0.3088845131001689559, -0.2992958165493331268, -0.2386552343498948847, -0.1768311013664789488, -0.1147878690630650400, -0.05320817752461537431, 0.000000000000000000 ),
 .UNSPECIFIED. ) ;
#42382=CARTESIAN_POINT ( 'NONE',  ( 10.94780721248439548, -10.83637588594239531, -36.08420929373698982 ) ) ;
#42385=CARTESIAN_POINT ( 'NONE',  ( 10.11051084926620014, -19.28509774568809831, -69.67303606471168109 ) ) ;
#42388=AXIS2_PLACEMENT_3D ( 'NONE', #2827, #34771, #46344 ) ;
#42390=DIRECTION ( 'NONE',  ( 0.000000000000000000, 0.000000000000000000, -1.000000000000000000 ) ) ;
#42394=CARTESIAN_POINT ( 'NONE',  ( 23.06349459023610038, -14.30325489761369973, -72.39321698031869801 ) ) ;
#42395=CARTESIAN_POINT ( 'NONE',  ( 8.222937397696199469, -15.61618894467929941, -32.14999999999999858 ) ) ;
#42396=CARTESIAN_POINT ( 'NONE',  ( 8.223439258000311725, -15.61632852289070073, -42.50766849176289952 ) ) ;
#42398=ORIENTED_EDGE ( 'NONE', *, *, #49044, .T. ) ;
#42402=B_SPLINE_CURVE_WITH_KNOTS ( 'NONE', 3,
 ( #1172, #1691, #24471, #13245, #41519, #17168, #32851, #33120, #5636, #32588, #5373 ),
 .UNSPECIFIED., .F., .F.,
 ( 4, 1, 1, 1, 1, 1, 1, 1, 4 ),
 ( 0.4999978458836923934, 0.5065141047152040832, 0.5857330357787533526, 0.6649519668423027330, 0.7441708979060125406, 0.8233898289695594785, 0.9026087600332693972, 0.9818276910968208870, 1.000000000000000000 ),
 .UNSPECIFIED. ) ;
#42404=CARTESIAN_POINT ( 'NONE',  ( 24.04523214473702097, -15.61618869705131729, -47.50766735973101618 ) ) ;
#42405=CARTESIAN_POINT ( 'NONE',  ( 24.03855097274092500, -15.27262742755435632, -39.49384892683895032 ) ) ;
#42423=CARTESIAN_POINT ( 'NONE',  ( 10.33399650447251261, -10.17551119628275025, -33.03228949958723604 ) ) ;
#42426=CARTESIAN_POINT ( 'NONE',  ( 9.366715917462860475, -15.61603296970410071, -51.45282021618999835 ) ) ;
#42428=CARTESIAN_POINT ( 'NONE',  ( 22.27743955675109788, -20.49923397962109917, -44.22626530275000079 ) ) ;
#42430=AXIS2_PLACEMENT_3D ( 'NONE', #45585, #9679, #29827 ) ;
#42437=CARTESIAN_POINT ( 'NONE',  ( 23.10375731890249895, -14.53722210533389969, -44.79829171073519944 ) ) ;
#42443=CARTESIAN_POINT ( 'NONE',  ( 9.366937397696199596, -15.61618894467949836, -28.45282021618999835 ) ) ;
#42450=CARTESIAN_POINT ( 'NONE',  ( 22.90118952179220813, -15.61618876469732875, -46.84717865327674247 ) ) ;
#42452=CARTESIAN_POINT ( 'NONE',  ( 23.96699468023455282, -14.48491286449858428, -71.46203103834751857 ) ) ;
#42457=B_SPLINE_CURVE_WITH_KNOTS ( 'NONE', 3,
 ( #35040, #51049, #15146, #11220, #27183, #43190, #40023, #36081, #49195, #12242, #41056, #48935, #438, #4113, #13036, #16427, #28989, #24517 ),
 .UNSPECIFIED., .F., .F.,
 ( 4, 2, 2, 2, 2, 2, 2, 2, 4 ),
 ( 0.000000000000000000, 0.06249982867297892986, 0.1249996573459578597, 0.1874994860189367896, 0.2499993146919157194, 0.3124991433648947603, 0.3749989720378738012, 0.4374988007108528421, 0.4999986293838318829 ),
 .UNSPECIFIED. ) ;
#42459=CARTESIAN_POINT ( 'NONE',  ( 20.99565881307366766, -21.94231955833456382, -74.08399818326770969 ) ) ;
#42462=CARTESIAN_POINT ( 'NONE',  ( 9.151501097378190508, -14.62213562185059956, -41.49783386550709707 ) ) ;
#42468=CARTESIAN_POINT ( 'NONE',  ( 21.53393071017169902, -10.48321867350180092, -80.82541145414198525 ) ) ;
#42475=CARTESIAN_POINT ( 'NONE',  ( 8.428852126995982630, -13.54545571365708767, -44.87565280027760650 ) ) ;
#42476=CARTESIAN_POINT ( 'NONE',  ( 15.31576361048525747, -23.52281516480273282, -46.04045315081875600 ) ) ;
#42479=EDGE_LOOP ( 'NONE', ( #39895, #38286, #5088, #34230 ) ) ;
#42481=ADVANCED_FACE ( 'NONE', ( #50576 ), #47680, .T. ) ;
#42492=CARTESIAN_POINT ( 'NONE',  ( 9.366908763506170743, -15.61636271700460021, -33.45282021618999835 ) ) ;
#42494=CARTESIAN_POINT ( 'NONE',  ( 8.428822445502495597, -13.54556363260618923, -68.87566510286049493 ) ) ;
#42496=CARTESIAN_POINT ( 'NONE',  ( 16.29407891153249821, -23.85979705954510166, -64.28614875238559989 ) ) ;
#42497=CARTESIAN_POINT ( 'NONE',  ( 24.04493742051697680, -16.65172778451557534, -47.54933648736709983 ) ) ;
#42501=CARTESIAN_POINT ( 'NONE',  ( 12.32795013852219945, -22.02096488050650080, -54.90332710579869513 ) ) ;
#42502=CARTESIAN_POINT ( 'NONE',  ( 9.303925792589840427, -18.78836378116810124, -32.14999999999999858 ) ) ;
#42503=CARTESIAN_POINT ( 'NONE',  ( 9.386603864545342901, -14.93147129003910933, -61.48498468630781844 ) ) ;
#42511=CARTESIAN_POINT ( 'NONE',  ( 12.16686956752729998, -8.388112192194309813, -66.84789180586530222 ) ) ;
#42513=CARTESIAN_POINT ( 'NONE',  ( 19.90939373821190017, -22.53927847089380165, -32.14999999999999858 ) ) ;
#42518=DIRECTION ( 'NONE',  ( 1.000000000000000000, 0.000000000000000000, 0.000000000000000000 ) ) ;
#42520=CARTESIAN_POINT ( 'NONE',  ( 18.08327279923313569, -7.911801705270725016, -81.08663926983665249 ) ) ;
#42534=CARTESIAN_POINT ( 'NONE',  ( 24.04496217889941789, -15.61618911842929869, -37.79232902657031445 ) ) ;
#42536=CARTESIAN_POINT ( 'NONE',  ( 14.06322549156652535, -23.32128047233873858, -76.09102434139356319 ) ) ;
#42549=CARTESIAN_POINT ( 'NONE',  ( 21.54527739906354711, -19.77483417149147016, -44.66116455897760318 ) ) ;
#42557=ORIENTED_EDGE ( 'NONE', *, *, #7102, .F. ) ;
#42562=CARTESIAN_POINT ( 'NONE',  ( 9.456108772904830317, -16.86908816385087206, -51.39384808471273658 ) ) ;
#42563=CARTESIAN_POINT ( 'NONE',  ( 21.10768686100733049, -20.20497612657083408, -46.69000373621759081 ) ) ;
#42571=CARTESIAN_POINT ( 'NONE',  ( 21.96499996289010070, -20.86864479655330129, -81.52088794317478460 ) ) ;
#42588=CARTESIAN_POINT ( 'NONE',  ( 22.90078882061835586, -15.66462506390463361, -62.45510662821025250 ) ) ;
#42593=CARTESIAN_POINT ( 'NONE',  ( 15.06541911040859993, -22.98944894335520317, -49.61315261507599672 ) ) ;
#42595=ORIENTED_EDGE ( 'NONE', *, *, #43755, .F. ) ;
#42596=CARTESIAN_POINT ( 'NONE',  ( 9.367478339302499180, -15.61624867646989756, -69.45282021618999124 ) ) ;
#42602=CARTESIAN_POINT ( 'NONE',  ( 9.093616821199461242, -16.36736670071820043, -81.23899999999999011 ) ) ;
#42604=VERTEX_POINT ( 'NONE', #2820 ) ;
#42613=CARTESIAN_POINT ( 'NONE',  ( 9.367479537931210132, -15.61613030728229923, -79.45282021618999124 ) ) ;
#42615=CARTESIAN_POINT ( 'NONE',  ( 8.223551834036749497, -15.61610457483330094, -62.79233150823698395 ) ) ;
#42631=CARTESIAN_POINT ( 'NONE',  ( 12.69125976124770006, -22.66847360106410036, -47.93206117220019991 ) ) ;
#42639=CARTESIAN_POINT ( 'NONE',  ( 24.04501723819814529, -15.61618889329698412, -35.50767088183642528 ) ) ;
#42643=CARTESIAN_POINT ( 'NONE',  ( 24.04018637339055786, -15.32013480239626801, -45.49576358883199134 ) ) ;
#42645=CARTESIAN_POINT ( 'NONE',  ( 13.85919928309939309, -8.940252629490174741, -36.24264715586421914 ) ) ;
#42648=CARTESIAN_POINT ( 'NONE',  ( 9.225955441871899865, -14.19409736079129836, -77.91180489532798958 ) ) ;
#42651=DIRECTION ( 'NONE',  ( 1.000000000000000000, 2.460964292799963328E-14, 0.000000000000000000 ) ) ;
#42655=CARTESIAN_POINT ( 'NONE',  ( 19.97295785153600178, -9.699730489520039356, -74.13603346371829161 ) ) ;
#42658=CARTESIAN_POINT ( 'NONE',  ( 16.13393739769620083, -15.61618894467929941, -22.14999999999999858 ) ) ;
#42659=ORIENTED_EDGE ( 'NONE', *, *, #21004, .F. ) ;
#42673=EDGE_CURVE ( 'NONE', #37146, #16669, #37861, .T. ) ;
#42681=ORIENTED_EDGE ( 'NONE', *, *, #40915, .F. ) ;
#42683=CARTESIAN_POINT ( 'NONE',  ( 23.83903863463931927, -17.68685968673479536, -47.87566667355078920 ) ) ;
#42687=CARTESIAN_POINT ( 'NONE',  ( 9.965952473861209526, -20.46827195828559809, -42.80032454360480187 ) ) ;
#42692=B_SPLINE_CURVE_WITH_KNOTS ( 'NONE', 3,
 ( #47802, #27864, #19751, #19993, #36498, #16587, #602, #4801, #32540, #35990, #16078, #44121, #28372, #48312, #48835, #12677, #9002, #20768 ),
 .UNSPECIFIED., .F., .F.,
 ( 4, 2, 2, 2, 2, 2, 2, 2, 4 ),
 ( 0.5000015509581456907, 0.5625013570883774516, 0.6250011632186092125, 0.6875009693488410845, 0.7500007754790728454, 0.8125005816093046063, 0.8750003877395364782, 0.9375001938697682391, 1.000000000000000000 ),
 .UNSPECIFIED. ) ;
#42696=CARTESIAN_POINT ( 'NONE',  ( 9.132806620530429242, -16.46867179815689752, -47.80861109115259211 ) ) ;
#42697=CARTESIAN_POINT ( 'NONE',  ( 21.74289213372750140, -11.34042165171269900, -44.63985384860789907 ) ) ;
#42702=CARTESIAN_POINT ( 'NONE',  ( 11.27234840095610480, -9.289956386053781046, -50.79933430464781452 ) ) ;
#42711=CARTESIAN_POINT ( 'NONE',  ( 15.09848549043149468, -23.52720049154072868, -58.33399804516979970 ) ) ;
#42712=ADVANCED_FACE ( 'NONE', ( #18478 ), #7207, .T. ) ;
#42713=CARTESIAN_POINT ( 'NONE',  ( 24.04490467417627642, -15.59160216054836212, -71.50668363288305329 ) ) ;
#42717=ORIENTED_EDGE ( 'NONE', *, *, #2891, .F. ) ;
#42722=CARTESIAN_POINT ( 'NONE',  ( 11.35694743959450115, -10.42745830638049931, -43.71596393528839286 ) ) ;
#42726=LINE ( 'NONE', #34051, #25605 ) ;
#42728=CARTESIAN_POINT ( 'NONE',  ( 12.26232734644089994, -8.789961311109230735, -34.62328075351209122 ) ) ;
#42730=AXIS2_PLACEMENT_3D ( 'NONE', #30025, #10397, #9377 ) ;
#42737=CARTESIAN_POINT ( 'NONE',  ( 22.90093739726882660, -15.61526481454825088, -62.45278487061211337 ) ) ;
#42738=CARTESIAN_POINT ( 'NONE',  ( 22.06336741109733524, -20.87868580843650079, -45.73877504285819384 ) ) ;
#42743=CARTESIAN_POINT ( 'NONE',  ( 9.807821837080062721, -10.75444719097494328, -47.00066525792952632 ) ) ;
#42745=EDGE_CURVE ( 'NONE', #14302, #38090, #40648, .T. ) ;
#42756=CARTESIAN_POINT ( 'NONE',  ( 17.30174806873700177, -23.77823147657889891, -68.24709530556638981 ) ) ;
#42757=CARTESIAN_POINT ( 'NONE',  ( 8.222964014181659564, -16.65193127518642768, -48.46600188287622757 ) ) ;
#42762=CARTESIAN_POINT ( 'NONE',  ( 23.04786251081229764, -12.84052085656660047, -54.11113779516239930 ) ) ;
#42763=CARTESIAN_POINT ( 'NONE',  ( 10.29616392687819904, -11.80022295320810066, -32.14999999999999858 ) ) ;
#42768=CARTESIAN_POINT ( 'NONE',  ( 22.23466283676619426, -10.53884220764341251, -61.28681395474006877 ) ) ;
#42769=CARTESIAN_POINT ( 'NONE',  ( 9.705988999922061211, -20.77992791024760066, -58.29224725099440008 ) ) ;
#42770=CARTESIAN_POINT ( 'NONE',  ( 21.38252174147899964, -21.31749193139690135, -32.14999999999999858 ) ) ;
#42773=CARTESIAN_POINT ( 'NONE',  ( 11.97521368704360967, -10.20490852744658739, -59.74446477439609993 ) ) ;
#42787=ADVANCED_FACE ( 'NONE', ( #11659 ), #19766, .F. ) ;
#42791=LINE ( 'NONE', #46210, #43486 ) ;
#42796=CARTESIAN_POINT ( 'NONE',  ( 12.14978265628979237, -22.52869892617844272, -76.17435607522669727 ) ) ;
#42801=CARTESIAN_POINT ( 'NONE',  ( 9.799758126153289339, -13.15607537077775646, -65.57083617002002995 ) ) ;
#42803=ORIENTED_EDGE ( 'NONE', *, *, #22106, .F. ) ;
#42806=VERTEX_POINT ( 'NONE', #51490 ) ;
#42807=ADVANCED_FACE ( 'NONE', ( #21231 ), #15590, .T. ) ;
#42810=CARTESIAN_POINT ( 'NONE',  ( 16.11774638449731967, -23.52717341023336672, -78.00832281184233352 ) ) ;
#42811=CARTESIAN_POINT ( 'NONE',  ( 16.13393739769620083, -15.61618894467929941, -32.14999999999999858 ) ) ;
#42818=CARTESIAN_POINT ( 'NONE',  ( 23.76387005758689952, -12.49099332496719938, -37.66858791500939674 ) ) ;
#42821=CARTESIAN_POINT ( 'NONE',  ( 22.82186787310235943, -16.68413300609983452, -50.50321592674860938 ) ) ;
#42831=CARTESIAN_POINT ( 'NONE',  ( 16.13393739769620083, -15.61618894467929941, -81.23899999999999011 ) ) ;
#42833=CARTESIAN_POINT ( 'NONE',  ( 9.678901947420619933, -20.07928830891850325, -80.09494718402959279 ) ) ;
#42841=VECTOR ( 'NONE', #50233, 1000.000000000000000 ) ;
#42846=ADVANCED_FACE ( 'NONE', ( #47563 ), #8951, .T. ) ;
#42855=CARTESIAN_POINT ( 'NONE',  ( 13.66038192480450064, -22.64386406956009878, -67.67506889758119826 ) ) ;
#42858=CARTESIAN_POINT ( 'NONE',  ( 22.90111010729205177, -15.61618905465553553, -68.45282213299155671 ) ) ;
#42863=CARTESIAN_POINT ( 'NONE',  ( 9.905352207939319698, -18.56992711498079984, -81.23899999999999011 ) ) ;
#42869=CARTESIAN_POINT ( 'NONE',  ( 23.37832472556300090, -13.25337072732409816, -81.23899999999999011 ) ) ;
#42872=CARTESIAN_POINT ( 'NONE',  ( 22.26208788750698275, -12.63896016920059218, -80.30869283850560691 ) ) ;
#42874=CARTESIAN_POINT ( 'NONE',  ( 11.27230637084539033, -9.289988185851985492, -63.08399882191634589 ) ) ;
#42890=CARTESIAN_POINT ( 'NONE',  ( 21.72984300404249680, -19.90902013391950121, -43.05547522733549926 ) ) ;
#42892=CARTESIAN_POINT ( 'NONE',  ( 8.353661292524970250, -14.58951864196060022, -56.32926786494370219 ) ) ;
#42899=CARTESIAN_POINT ( 'NONE',  ( 20.17759926101160062, -10.17506160504910007, -32.14999999999999858 ) ) ;
#42903=CARTESIAN_POINT ( 'NONE',  ( 24.04464085855207856, -15.54218241719844329, -45.50469856519234924 ) ) ;
#42905=CARTESIAN_POINT ( 'NONE',  ( 24.04493740884162634, -16.65171840150751237, -45.83401224397450591 ) ) ;
#42908=CARTESIAN_POINT ( 'NONE',  ( 9.081943790392930538, -15.50689421925920009, -75.85211268767389470 ) ) ;
#42917=CARTESIAN_POINT ( 'NONE',  ( 15.09846545302023557, -23.52719806942911518, -42.04933457646342276 ) ) ;
#42918=CARTESIAN_POINT ( 'NONE',  ( 24.04507396969289346, -15.61618901627517531, -67.50767071486835391 ) ) ;
#42920=FACE_OUTER_BOUND ( 'NONE', #4088, .T. ) ;
#42933=CARTESIAN_POINT ( 'NONE',  ( 22.90086341797264780, -15.61618933298137790, -46.45282805145726002 ) ) ;
#42938=CARTESIAN_POINT ( 'NONE',  ( 9.351597708753779159, -11.46406213175773914, -32.96709167677747132 ) ) ;
#42941=CARTESIAN_POINT ( 'NONE',  ( 19.54197222412561530, -9.703303471313775574, -52.11948516037260504 ) ) ;
#42943=CARTESIAN_POINT ( 'NONE',  ( 23.86338609116459963, -16.97352843302460101, -44.06782744062260093 ) ) ;
#42952=CARTESIAN_POINT ( 'NONE',  ( 18.19108902640479997, -22.36234980482430146, -39.25296653628179655 ) ) ;
#42953=CYLINDRICAL_SURFACE ( 'NONE', #33498, 6.766999999999998572 ) ;
#42957=B_SPLINE_CURVE_WITH_KNOTS ( 'NONE', 3,
 ( #3172, #42497, #22803, #18115, #50868, #50089, #10262, #30671, #19143, #34082, #38824, #14185, #11037, #30157, #38562, #6329, #42757, #30923 ),
 .UNSPECIFIED., .F., .F.,
 ( 4, 2, 2, 2, 2, 2, 2, 2, 4 ),
 ( 0.5000006933586850222, 0.5625006066888493805, 0.6250005200190137389, 0.6875004333491780972, 0.7500003466793425666, 0.8125002600095068139, 0.8750001733396712833, 0.9375000866698356417, 1.000000000000000000 ),
 .UNSPECIFIED. ) ;
#42962=CONICAL_SURFACE ( 'NONE', #38773, 7.500000000000000000, 0.7853981633974476129 ) ;
#42968=DIRECTION ( 'NONE',  ( 0.000000000000000000, 0.000000000000000000, -1.000000000000000000 ) ) ;
#42971=CARTESIAN_POINT ( 'NONE',  ( 9.925381647341668057, -20.56393483659768151, -32.57822336751156200 ) ) ;
#42978=CARTESIAN_POINT ( 'NONE',  ( 15.09848983909765785, -23.52720101742690773, -74.33399818031571726 ) ) ;
#42981=CARTESIAN_POINT ( 'NONE',  ( 16.72752280990699703, -22.64400617729399912, -58.92599869950339553 ) ) ;
#42987=CARTESIAN_POINT ( 'NONE',  ( 14.76533666768029995, -8.292680193320569160, -80.50853572988759765 ) ) ;
#43001=EDGE_LOOP ( 'NONE', ( #10154, #1553, #205, #31743 ) ) ;
#43002=DIRECTION ( 'NONE',  ( 0.000000000000000000, 0.000000000000000000, 1.000000000000000000 ) ) ;
#43007=CIRCLE ( 'NONE', #36276, 7.910999999999997812 ) ;
#43011=CARTESIAN_POINT ( 'NONE',  ( 20.99560049988850352, -9.290011782261316853, -69.50066706253579696 ) ) ;
#43012=CARTESIAN_POINT ( 'NONE',  ( 18.24066274319899961, -7.644713022709090033, -59.37457502644110008 ) ) ;
#43016=ORIENTED_EDGE ( 'NONE', *, *, #882, .T. ) ;
#43019=CARTESIAN_POINT ( 'NONE',  ( 8.955746707395579875, -13.62112698603560190, -53.31894848452630242 ) ) ;
#43028=CARTESIAN_POINT ( 'NONE',  ( 20.33320876516510012, -22.71188064396640272, -63.83757242544770349 ) ) ;
#43029=CARTESIAN_POINT ( 'NONE',  ( 20.71981744919569834, -21.94173720618249845, -32.14999999999999858 ) ) ;
#43040=DIRECTION ( 'NONE',  ( 1.000000000000000000, 2.460964292799963328E-14, 0.000000000000000000 ) ) ;
#43042=CARTESIAN_POINT ( 'NONE',  ( 10.52283474022480014, -10.71494210199229968, -79.46119573552070392 ) ) ;
#43049=B_SPLINE_CURVE_WITH_KNOTS ( 'NONE', 3,
 ( #15845, #43126, #35509, #7983, #11931, #22915, #16099, #39188, #23684, #23935, #35764, #35242, #27633, #51747, #43888, #31806, #43380, #39447, #15075, #3026, #39957, #4051, #20016, #38934, #50976, #7477, #27122, #18999, #51498, #15340, #3548, #23426, #46806, #7218, #42869, #10895, #6964, #36009, #27376, #47571, #124, #11669, #15599, #31551, #26859, #47068, #19518, #47826, #11154, #23171, #3284, #31293, #47323, #11414, #43636, #7739, #39701, #3805, #19777, #21310, #48079, #40984, #13227, #9290, #28652, #24966, #626, #12963, #16885, #40210, #8500, #32831, #40463, #29176, #44920, #4558, #36782, #12698, #5356, #45178, #48598, #44654, #5096, #12177, #24189, #36522, #20527, #16609, #32567, #28915, #25236, #8238, #8761, #9022, #48333, #28136, #33097, #21050, #24709, #40727, #4822, #20790, #890, #41243, #48857, #37312, #37053, #1149, #17146, #49128, #28395, #1412, #32058, #44142, #4299, #20271, #24449, #36264 ),
 .UNSPECIFIED., .F., .F.,
 ( 4, 3, 3, 3, 3, 3, 3, 3, 3, 3, 3, 3, 3, 3, 3, 3, 3, 3, 3, 3, 3, 3, 3, 3, 3, 3, 3, 3, 3, 3, 3, 3, 3, 3, 3, 3, 3, 3, 3, 4 ),
 ( -1.528706106645210117, -1.467014400978620126, -1.462406257103989971, -1.400361489177680108, -1.359972591548769927, -1.338075497077110043, -1.325535052222839960, -1.316390772004420118, -1.255261729574910001, -1.194475196635949921, -1.135862752391179953, -1.120187264403469829, -1.112461740117050013, -1.077250308146409985, -1.017356745748480007, -0.9572232276135819173, -0.8973750758446790154, -0.8492288645832469784, -0.8273183250403219891, -0.8205642567938971066, -0.7619152418095799240, -0.7047902307989519777, -0.6459350209392840103, -0.5874014364452070369, -0.5571792354581740492, -0.5439731168496340086, -0.5366754591832860743, -0.4791547776990519036, -0.4217814619618329708, -0.3651803038717780225, -0.3456238285489399154, -0.3024208499803220374, -0.2835195468565521182, -0.2726001362142098650, -0.2628186310418560989, -0.2067675312773959995, -0.1505665958059829723, -0.09476636028567830827, -0.04010237144085015970, 0.000000000000000000 ),
 .UNSPECIFIED. ) ;
#43058=ORIENTED_EDGE ( 'NONE', *, *, #20421, .F. ) ;
#43070=CARTESIAN_POINT ( 'NONE',  ( 8.222956458069184293, -14.58050192852516957, -34.54933503248848581 ) ) ;
#43071=ORIENTED_EDGE ( 'NONE', *, *, #11184, .T. ) ;
#43072=CARTESIAN_POINT ( 'NONE',  ( 24.08898506460380062, -13.44825525616480100, -33.70764136182839366 ) ) ;
#43076=CARTESIAN_POINT ( 'NONE',  ( 23.63709980183327275, -18.22008787322180723, -49.89870660227276744 ) ) ;
#43088=CARTESIAN_POINT ( 'NONE',  ( 12.71325777259860068, -22.74941205225429997, -32.14999999999999858 ) ) ;
#43089=ORIENTED_EDGE ( 'NONE', *, *, #39124, .F. ) ;
#43098=CARTESIAN_POINT ( 'NONE',  ( 14.06331755925441129, -23.32130431222730138, -38.37566614555674249 ) ) ;
#43106=LINE ( 'NONE', #26314, #8891 ) ;
#43110=CARTESIAN_POINT ( 'NONE',  ( 23.55933089801509794, -15.00772719258320009, -67.04131744907229518 ) ) ;
#43118=CARTESIAN_POINT ( 'NONE',  ( 9.866497443904730602, -18.50142238704479780, -81.23899999999999011 ) ) ;
#43120=ORIENTED_EDGE ( 'NONE', *, *, #47820, .T. ) ;
#43125=CARTESIAN_POINT ( 'NONE',  ( 28.13393739769620083, -15.61618894467929941, -22.14999999999999858 ) ) ;
#43126=CARTESIAN_POINT ( 'NONE',  ( 21.53501286420519989, -9.851163535991840803, -81.23899999999999011 ) ) ;
#43130=CARTESIAN_POINT ( 'NONE',  ( 9.221408080047158506, -11.63206808030142092, -52.67433566774367648 ) ) ;
#43132=CARTESIAN_POINT ( 'NONE',  ( 17.16952344459745561, -7.705194454623752520, -63.33399937649863887 ) ) ;
#43135=AXIS2_PLACEMENT_3D ( 'NONE', #47462, #7625, #43271 ) ;
#43137=EDGE_CURVE ( 'NONE', #19523, #19102, #21502, .T. ) ;
#43138=CARTESIAN_POINT ( 'NONE',  ( 8.222924257981070184, -16.27420347773300691, -50.48118173969053402 ) ) ;
#43141=EDGE_CURVE ( 'NONE', #10825, #50973, #50007, .T. ) ;
#43142=CARTESIAN_POINT ( 'NONE',  ( 20.64627773545588596, -10.50382045408532505, -40.18285380126813067 ) ) ;
#43145=CARTESIAN_POINT ( 'NONE',  ( 16.13393739769620083, -15.61618894467929941, -24.90346750000000142 ) ) ;
#43146=CARTESIAN_POINT ( 'NONE',  ( 15.96737325713249867, -23.46214360745049632, -53.79426207090799750 ) ) ;
#43164=CARTESIAN_POINT ( 'NONE',  ( 14.61213889419929934, -8.323009066753440877, -32.50186350533419954 ) ) ;
#43174=CARTESIAN_POINT ( 'NONE',  ( 23.04647655710144605, -11.63208733966609820, -67.62566283886621932 ) ) ;
#43175=CARTESIAN_POINT ( 'NONE',  ( 9.205734167420699166, -27.61618894467930119, -24.15000000000000213 ) ) ;
#43176=ORIENTED_EDGE ( 'NONE', *, *, #8811, .T. ) ;
#43182=CARTESIAN_POINT ( 'NONE',  ( 9.367407790820902136, -15.61608574124520032, -61.84717978381009829 ) ) ;
#43184=EDGE_LOOP ( 'NONE', ( #1451, #36225, #3270, #32826 ) ) ;
#43186=CARTESIAN_POINT ( 'NONE',  ( 24.04476371124131617, -15.67281232776119460, -55.50994974416185102 ) ) ;
#43190=CARTESIAN_POINT ( 'NONE',  ( 11.97538441063065306, -10.20477936771429839, -35.74448608333058530 ) ) ;
#43197=CARTESIAN_POINT ( 'NONE',  ( 9.366647546311250849, -15.61604444486649967, -65.84717978381009118 ) ) ;
#43198=CARTESIAN_POINT ( 'NONE',  ( 22.90017504350882760, -16.53861086495556165, -50.89058099898073806 ) ) ;
#43200=CARTESIAN_POINT ( 'NONE',  ( 15.09846568087331775, -23.52719809933467587, -54.04933655904326173 ) ) ;
#43202=EDGE_CURVE ( 'NONE', #5111, #23033, #21939, .T. ) ;
#43203=CARTESIAN_POINT ( 'NONE',  ( 23.90878591523479813, -14.54919404267139882, -45.96908178614960150 ) ) ;
#43211=CARTESIAN_POINT ( 'NONE',  ( 18.21162691092170149, -8.876325039444729725, -48.44236253966159467 ) ) ;
#43212=CARTESIAN_POINT ( 'NONE',  ( 17.01967013855468380, -8.849179591706896275, -43.99445488068004551 ) ) ;
#43219=CARTESIAN_POINT ( 'NONE',  ( 9.807838715921571193, -10.75442553347946451, -46.71600211399567826 ) ) ;
#43225=CARTESIAN_POINT ( 'NONE',  ( 16.13393739769620083, -15.61618894467929941, -28.45282021618999835 ) ) ;
#43227=CARTESIAN_POINT ( 'NONE',  ( 13.09030777569590676, -22.94849230994849520, -32.41764226196748666 ) ) ;
#43238=CARTESIAN_POINT ( 'NONE',  ( 21.35923182362840222, -20.35315599744080117, -50.68722986888699467 ) ) ;
#43245=CARTESIAN_POINT ( 'NONE',  ( 10.00581152974459798, -19.85325857441549857, -79.87478428137869457 ) ) ;
#43252=CARTESIAN_POINT ( 'NONE',  ( 8.428791536887311864, -17.68670186955939272, -40.70900208874113702 ) ) ;
#43259=FACE_OUTER_BOUND ( 'NONE', #33511, .T. ) ;
#43266=CARTESIAN_POINT ( 'NONE',  ( 11.27985751389227609, -20.39062183032262254, -33.20531548096091967 ) ) ;
#43268=EDGE_CURVE ( 'NONE', #30849, #32691, #37768, .T. ) ;
#43269=CARTESIAN_POINT ( 'NONE',  ( 14.70217909044999871, -7.496288193711560410, -65.23677592514890478 ) ) ;
#43271=DIRECTION ( 'NONE',  ( 1.000000000000000000, 2.460964292799963328E-14, 0.000000000000000000 ) ) ;
#43276=CARTESIAN_POINT ( 'NONE',  ( 9.313614695934589349, -18.61450381289790101, -51.10081841474490005 ) ) ;
#43285=CARTESIAN_POINT ( 'NONE',  ( 24.33302514535889927, -16.48663757332040092, -69.54133546202839966 ) ) ;
#43291=CARTESIAN_POINT ( 'NONE',  ( 24.04516176800591865, -15.61618872104648226, -63.79232972929064971 ) ) ;
#43300=CARTESIAN_POINT ( 'NONE',  ( 22.19445665721740113, -19.94940946873740018, -70.43023759426799302 ) ) ;
#43306=CARTESIAN_POINT ( 'NONE',  ( 23.98964259220293371, -16.68387156175795383, -61.55060845666147884 ) ) ;
#43307=CARTESIAN_POINT ( 'NONE',  ( 20.99560800870527899, -9.290017777483981831, -37.50066705834722569 ) ) ;
#43313=CARTESIAN_POINT ( 'NONE',  ( 20.15227385440210028, -21.41235416792470048, -41.15422088180869054 ) ) ;
#43317=CARTESIAN_POINT ( 'NONE',  ( 10.16236763787109432, -19.36890979467511187, -37.66858791500941805 ) ) ;
#43319=ORIENTED_EDGE ( 'NONE', *, *, #31076, .T. ) ;
#43331=CARTESIAN_POINT ( 'NONE',  ( 13.22332444824007780, -22.99680140878987444, -50.41190558083048501 ) ) ;
#43334=CARTESIAN_POINT ( 'NONE',  ( 20.29259151353744883, -10.20485656652930118, -64.16115512084347472 ) ) ;
#43336=CARTESIAN_POINT ( 'NONE',  ( 23.60639345834430358, -18.01392704823980040, -72.11132903714400300 ) ) ;
#43344=CARTESIAN_POINT ( 'NONE',  ( 20.08350565795849718, -22.39760913111329899, -79.61963359764799009 ) ) ;
#43353=CARTESIAN_POINT ( 'NONE',  ( 20.99564373225254599, -21.94233159712619852, -38.08400039168056850 ) ) ;
#43358=LINE ( 'NONE', #23149, #36772 ) ;
#43366=CARTESIAN_POINT ( 'NONE',  ( 22.52917233249549867, -19.43818638934929766, -63.23880875801850010 ) ) ;
#43367=CARTESIAN_POINT ( 'NONE',  ( 17.16957802224845864, -7.705202244497520780, -41.04933447065145202 ) ) ;
#43371=CARTESIAN_POINT ( 'NONE',  ( 22.89996330215964804, -15.74029339777422543, -34.45865469882935628 ) ) ;
#43373=CARTESIAN_POINT ( 'NONE',  ( 10.72266900401992196, -11.45745232604984842, -73.66115355198333248 ) ) ;
#43374=CARTESIAN_POINT ( 'NONE',  ( 11.78849808412049960, -9.293787752828999160, -81.23899999999999011 ) ) ;
#43380=CARTESIAN_POINT ( 'NONE',  ( 22.56774556973750023, -11.25265918193379910, -81.23899999999999011 ) ) ;
#43381=CARTESIAN_POINT ( 'NONE',  ( 18.20469914615897977, -7.911112079811677411, -73.37566484845835646 ) ) ;
#43383=VERTEX_POINT ( 'NONE', #27430 ) ;
#43384=CARTESIAN_POINT ( 'NONE',  ( 13.46657045245495432, -9.346956680139966167, -79.82493874763157748 ) ) ;
#43393=CARTESIAN_POINT ( 'NONE',  ( 19.96336983191040559, -9.970646423659596636, -40.14281403636497458 ) ) ;
#43397=CARTESIAN_POINT ( 'NONE',  ( 9.366395830200795913, -16.73520444579738253, -43.79452874782144534 ) ) ;
#43398=CARTESIAN_POINT ( 'NONE',  ( 17.51060849981909939, -7.890159896082458602, -52.84363489814449366 ) ) ;
#43399=VERTEX_POINT ( 'NONE', #19575 ) ;
#43400=CYLINDRICAL_SURFACE ( 'NONE', #15456, 7.910999999999997812 ) ;
#43407=VECTOR ( 'NONE', #26988, 1000.000000000000000 ) ;
#43410=CARTESIAN_POINT ( 'NONE',  ( 24.04486360762935604, -15.57925695708305014, -45.50619014287734387 ) ) ;
#43412=CYLINDRICAL_SURFACE ( 'NONE', #34245, 7.910999999999997812 ) ;
#43413=CARTESIAN_POINT ( 'NONE',  ( 15.09847269682518878, -23.52719894729639449, -38.04933652063846239 ) ) ;
#43416=CARTESIAN_POINT ( 'NONE',  ( 9.825858312949119266, -19.58038275917900251, -37.88875081766039443 ) ) ;
#43426=EDGE_CURVE ( 'NONE', #17470, #10051, #34026, .T. ) ;
#43427=CARTESIAN_POINT ( 'NONE',  ( 5.741632552282950108, -21.61618894467929763, -22.14999999999999858 ) ) ;
#43433=DIRECTION ( 'NONE',  ( 1.000000000000000000, 2.460964292799963328E-14, 0.000000000000000000 ) ) ;
#43439=CARTESIAN_POINT ( 'NONE',  ( 23.04644915753889833, -19.60034241002689726, -55.67430029654918400 ) ) ;
#43442=CARTESIAN_POINT ( 'NONE',  ( 18.71923009779332503, -9.337457873371985073, -46.07711848848515501 ) ) ;
#43449=CARTESIAN_POINT ( 'NONE',  ( 10.93327293485905471, -20.38018394046732595, -51.61111978222447050 ) ) ;
#43450=CARTESIAN_POINT ( 'NONE',  ( 21.54530235781215453, -11.45757796651336768, -52.24448483740684424 ) ) ;
#43452=CARTESIAN_POINT ( 'NONE',  ( 16.68946024236489833, -7.788153305987209229, -57.53504572143799578 ) ) ;
#43460=CARTESIAN_POINT ( 'NONE',  ( 16.84831893358350285, -22.63275635300900035, -57.31488281878699098 ) ) ;
#43465=CARTESIAN_POINT ( 'NONE',  ( 23.83903791948154094, -13.54551468052735963, -51.42433247511532102 ) ) ;
#43467=B_SPLINE_CURVE_WITH_KNOTS ( 'NONE', 3,
 ( #10530, #26489, #42503, #30680, #46705, #2664, #10789, #6311, #34062, #50591, #33556, #26202, #26460, #46674, #6565, #13659, #37762, #50336, #49821, #10760, #38019, #6833, #26719, #1598, #38541, #41953, #2368, #42213, #1858, #6052, #17836, #2114, #22269, #17586, #38279, #42737, #18346 ),
 .UNSPECIFIED., .F., .F.,
 ( 4, 2, 2, 2, 2, 2, 2, 2, 2, 2, 2, 2, 2, 2, 1, 1, 1, 1, 1, 2, 4 ),
 ( 0.000000000000000000, 0.06250093636191540736, 0.1250018727238308147, 0.1875028090857462082, 0.2500037454476616294, 0.2812542136286192984, 0.3125046818095770229, 0.3437551499905348584, 0.3750056181714926384, 0.4062560863524504740, 0.4375065545334082540, 0.4687570227143661450, 0.4843822568048449240, 0.4921948738500844245, 0.4961011823727041747, 0.4980543366340139944, 0.4990309137646689042, 0.4995192023299963036, 0.4997633466126600310, 0.4998854187539919502, 0.5000074908953238140 ),
 .UNSPECIFIED. ) ;
#43469=CARTESIAN_POINT ( 'NONE',  ( 17.90512170467987474, -9.025297858467601131, -76.03613063694051277 ) ) ;
#43474=CARTESIAN_POINT ( 'NONE',  ( 24.04493509668306572, -15.60920340738896606, -71.50739165550209009 ) ) ;
#43486=VECTOR ( 'NONE', #1650, 1000.000000000000000 ) ;
#43487=CARTESIAN_POINT ( 'NONE',  ( 18.02732184005409977, -22.41013139733979997, -56.86630649184920117 ) ) ;
#43495=CARTESIAN_POINT ( 'NONE',  ( 23.52146105081359906, -18.26406402817810104, -45.39705537816429626 ) ) ;
#43508=LINE ( 'NONE', #47957, #41765 ) ;
#43510=CARTESIAN_POINT ( 'NONE',  ( 24.04635993889370127, -15.33348728407727712, -49.49630671588138142 ) ) ;
#43512=CARTESIAN_POINT ( 'NONE',  ( 24.04487853986463008, -15.61618860033810030, -61.79233400586811342 ) ) ;
#43514=CARTESIAN_POINT ( 'NONE',  ( 10.35043018118175695, -19.20900750040789262, -33.27603111959778914 ) ) ;
#43516=CARTESIAN_POINT ( 'NONE',  ( 23.80510751029979843, -18.63874897884280202, -77.91180489532798958 ) ) ;
#43517=DIRECTION ( 'NONE',  ( 0.000000000000000000, 0.000000000000000000, -1.000000000000000000 ) ) ;
#43525=CARTESIAN_POINT ( 'NONE',  ( 19.43693194943929825, -22.29428154633589898, -54.58645138154409437 ) ) ;
#43528=CARTESIAN_POINT ( 'NONE',  ( 24.04493739769619864, -15.61618894467929941, -32.14999999999999858 ) ) ;
#43529=CARTESIAN_POINT ( 'NONE',  ( 9.818495732055460223, -19.87888382093819928, -32.14999999999999858 ) ) ;
#43537=CARTESIAN_POINT ( 'NONE',  ( 8.416037913024730699, -18.51735220335379850, -72.39321698031869801 ) ) ;
#43538=CARTESIAN_POINT ( 'NONE',  ( 21.78353651810359892, -20.85666229875000255, -32.14999999999999858 ) ) ;
#43549=CARTESIAN_POINT ( 'NONE',  ( 8.728929033786567260, -12.74017886842098335, -64.91034747281507578 ) ) ;
#43550=CARTESIAN_POINT ( 'NONE',  ( 24.04468322966528859, -15.61618861995729013, -71.79233702014498419 ) ) ;
#43552=CARTESIAN_POINT ( 'NONE',  ( 8.687638548776371650, -15.37261707081270146, -77.24306566573929445 ) ) ;
#43562=CARTESIAN_POINT ( 'NONE',  ( 17.01976930770689833, -22.38318413455865397, -70.91115524790816949 ) ) ;
#43572=CARTESIAN_POINT ( 'NONE',  ( 11.27219963446819229, -9.290068936367397612, -55.08398911216916360 ) ) ;
#43576=CARTESIAN_POINT ( 'NONE',  ( 21.71415593298656788, -21.22378504329634552, -77.75844095104929465 ) ) ;
#43581=B_SPLINE_CURVE_WITH_KNOTS ( 'NONE', 3,
 ( #36835, #8284, #24494, #16403, #48645, #24759, #13010, #40512, #4870, #28700 ),
 .UNSPECIFIED., .F., .F.,
 ( 4, 2, 2, 2, 4 ),
 ( 0.1813467805151689483, 0.3860100853863767112, 0.5906733902575844741, 0.7953366951287922371, 1.000000000000000000 ),
 .UNSPECIFIED. ) ;
#43582=CARTESIAN_POINT ( 'NONE',  ( 23.04746735250069989, -11.12332531222269871, -35.60889570735529475 ) ) ;
#43584=CARTESIAN_POINT ( 'NONE',  ( 24.04470982567631410, -15.68103954860247740, -49.79493908758399101 ) ) ;
#43589=CARTESIAN_POINT ( 'NONE',  ( 8.380768790010019842, -14.40164206111660050, -73.06195620990739314 ) ) ;
#43599=CARTESIAN_POINT ( 'NONE',  ( 18.04724510464590281, -7.596090795186240641, -43.08221248677949688 ) ) ;
#43609=CARTESIAN_POINT ( 'NONE',  ( 23.83903723949826414, -17.68686655609902658, -37.87566771034045132 ) ) ;
#43622=CARTESIAN_POINT ( 'NONE',  ( 17.31586692445079834, -22.97212103600040223, -67.51663103545399736 ) ) ;
#43623=CARTESIAN_POINT ( 'NONE',  ( 11.27237412149550977, -9.289936927475686446, -40.79933478808754188 ) ) ;
#43627=CARTESIAN_POINT ( 'NONE',  ( 10.52996152801476093, -19.45088358834182074, -35.26171248262056679 ) ) ;
#43630=CARTESIAN_POINT ( 'NONE',  ( 8.974641593888140534, -14.92660264788080049, -81.23899999999999011 ) ) ;
#43636=CARTESIAN_POINT ( 'NONE',  ( 23.52286796769300281, -16.13183659920250079, -81.23899999999999011 ) ) ;
#43655=CARTESIAN_POINT ( 'NONE',  ( 12.28756344725089988, -21.52786946782889999, -43.53078881371720144 ) ) ;
#43656=CARTESIAN_POINT ( 'NONE',  ( 9.206818668722608123, -19.30424728178379823, -60.13177655599749727 ) ) ;
#43662=VECTOR ( 'NONE', #24739, 999.9999999999998863 ) ;
#43668=FACE_OUTER_BOUND ( 'NONE', #12791, .T. ) ;
#43670=CARTESIAN_POINT ( 'NONE',  ( 12.14989696424939147, -22.52876359041865229, -38.17433614912694395 ) ) ;
#43673=VERTEX_POINT ( 'NONE', #37371 ) ;
#43674=CARTESIAN_POINT ( 'NONE',  ( 8.916825887739390666, -17.46551200763889966, -35.98749647213350045 ) ) ;
#43676=EDGE_LOOP ( 'NONE', ( #47200, #39184, #8772, #36259 ) ) ;
#43687=ORIENTED_EDGE ( 'NONE', *, *, #30622, .F. ) ;
#43688=DIRECTION ( 'NONE',  ( 0.000000000000000000, 0.000000000000000000, -1.000000000000000000 ) ) ;
#43689=CARTESIAN_POINT ( 'NONE',  ( 20.11803275322282758, -8.703644260883391937, -39.45899364610082216 ) ) ;
#43690=DIRECTION ( 'NONE',  ( 0.000000000000000000, 0.000000000000000000, 1.000000000000000000 ) ) ;
#43696=CARTESIAN_POINT ( 'NONE',  ( 22.90093225693778223, -15.60714275223250525, -46.45240273082318794 ) ) ;
#43705=CARTESIAN_POINT ( 'NONE',  ( 22.90106509282977854, -15.61618896609811458, -36.45282238757207693 ) ) ;
#43706=CARTESIAN_POINT ( 'NONE',  ( 9.932201140091338587, -20.42505731288110127, -58.80254861845589431 ) ) ;
#43715=CARTESIAN_POINT ( 'NONE',  ( 9.543089160664727899, -17.38752728827747163, -39.36948714365400548 ) ) ;
#43716=CARTESIAN_POINT ( 'NONE',  ( 11.30419729876839874, -10.47652263729510125, -58.10707212942319444 ) ) ;
#43717=FACE_OUTER_BOUND ( 'NONE', #47263, .T. ) ;
#43722=CARTESIAN_POINT ( 'NONE',  ( 23.83903529911903618, -13.54550174322651657, -37.42433788284738938 ) ) ;
#43730=CARTESIAN_POINT ( 'NONE',  ( 12.14991080221749087, -22.52877141676245998, -58.45899808055179392 ) ) ;
#43732=CARTESIAN_POINT ( 'NONE',  ( 8.222339619445261150, -15.61627490117209938, -70.79233150823699816 ) ) ;
#43733=ADVANCED_FACE ( 'NONE', ( #20494 ), #41209, .T. ) ;
#43735=ORIENTED_EDGE ( 'NONE', *, *, #30270, .F. ) ;
#43742=CARTESIAN_POINT ( 'NONE',  ( 14.46176406050670060, -8.764445004118037730, -59.87662587226679278 ) ) ;
#43747=CARTESIAN_POINT ( 'NONE',  ( 22.37504268966269905, -10.85852639698109989, -45.08017965390980208 ) ) ;
#43755=EDGE_CURVE ( 'NONE', #34702, #8909, #30867, .T. ) ;
#43762=CARTESIAN_POINT ( 'NONE',  ( 18.79008633813485574, -8.139399684649680111, -77.11640214972752005 ) ) ;
#43763=CARTESIAN_POINT ( 'NONE',  ( 20.98332165578556285, -9.344388009994190725, -49.21715238545373694 ) ) ;
#43765=SURFACE_STYLE_USAGE ( .BOTH. , #15218 ) ;
#43767=CARTESIAN_POINT ( 'NONE',  ( 8.428888865400255170, -13.54532213638748317, -56.59100174228039748 ) ) ;
#43769=CARTESIAN_POINT ( 'NONE',  ( 17.77623415669070184, -7.536239600077499823, -69.35616034045709455 ) ) ;
#43773=EDGE_CURVE ( 'NONE', #19102, #30849, #32278, .T. ) ;
#43775=CARTESIAN_POINT ( 'NONE',  ( 22.89605187407040177, -18.74356829703729943, -68.37054538661389813 ) ) ;
#43778=DIRECTION ( 'NONE',  ( 0.000000000000000000, 0.000000000000000000, -1.000000000000000000 ) ) ;
#43779=CARTESIAN_POINT ( 'NONE',  ( 11.60083912566800102, -21.98623894961669833, -32.14999999999999858 ) ) ;
#43786=CARTESIAN_POINT ( 'NONE',  ( 10.52982223945920026, -9.568328661720299166, -74.76978491222729417 ) ) ;
#43787=CARTESIAN_POINT ( 'NONE',  ( 22.23384466866859910, -12.16604687330790213, -32.14999999999999858 ) ) ;
#43794=B_SPLINE_CURVE_WITH_KNOTS ( 'NONE', 3,
 ( #21260, #1623, #33582, #32518, #49080, #12648, #28347, #28609, #40676, #37006, #41200, #9244, #24405, #16835, #29394, #32783, #8715, #9501 ),
 .UNSPECIFIED., .F., .F.,
 ( 4, 2, 2, 2, 2, 2, 2, 2, 4 ),
 ( 0.000000000000000000, 0.06249999303177191518, 0.1249999860635438304, 0.1874999790953157386, 0.2499999721270876607, 0.3124999651588598049, 0.3749999581906319213, 0.4374999512224040932, 0.4999999442541762096 ),
 .UNSPECIFIED. ) ;
#43800=CARTESIAN_POINT ( 'NONE',  ( 16.27309551684129829, -23.60625643615314573, -66.28644551406529217 ) ) ;
#43802=CARTESIAN_POINT ( 'NONE',  ( 11.16483992176100060, -10.06508418258009918, -75.50024918233970084 ) ) ;
#43810=VECTOR ( 'NONE', #51792, 1000.000000000000000 ) ;
#43818=EDGE_CURVE ( 'NONE', #32526, #11866, #15687, .T. ) ;
#43827=DIRECTION ( 'NONE',  ( 1.000000000000000000, 0.000000000000000000, 0.000000000000000000 ) ) ;
#43828=CARTESIAN_POINT ( 'NONE',  ( 19.66452008112446492, -22.72169927725052574, -77.86093795788831073 ) ) ;
#43833=CARTESIAN_POINT ( 'NONE',  ( 21.51895211384039897, -21.85993273849760143, -46.06579460775299140 ) ) ;
#43835=CARTESIAN_POINT ( 'NONE',  ( 12.14982466399041705, -22.52872268964002700, -68.17433422315620817 ) ) ;
#43836=CARTESIAN_POINT ( 'NONE',  ( 14.95255119587064208, -23.45945773958777636, -50.33991548539275129 ) ) ;
#43837=( NAMED_UNIT ( * ) SI_UNIT ( $, .STERADIAN. ) SOLID_ANGLE_UNIT ( ) );
#43842=CARTESIAN_POINT ( 'NONE',  ( 16.38271474186759846, -23.06229203135920258, -32.72202640798520434 ) ) ;
#43843=CARTESIAN_POINT ( 'NONE',  ( 10.72260735920611907, -19.77484646530637846, -37.24448631176660740 ) ) ;
#43850=CARTESIAN_POINT ( 'NONE',  ( 11.21911071231070167, -8.995977515910739797, -38.80439020934399252 ) ) ;
#43854=CARTESIAN_POINT ( 'NONE',  ( 24.04790590996992705, -15.78420839348370208, -39.51442343626069231 ) ) ;
#43855=CARTESIAN_POINT ( 'NONE',  ( 22.04683847007901321, -19.02420019749379065, -56.61945810151985370 ) ) ;
#43864=CARTESIAN_POINT ( 'NONE',  ( 20.29261341095602944, -21.02750385110190834, -64.74448845417677489 ) ) ;
#43867=CARTESIAN_POINT ( 'NONE',  ( 11.27215316695904335, -9.290104087649041276, -75.08404200567380826 ) ) ;
#43871=AXIS2_PLACEMENT_3D ( 'NONE', #48548, #21524, #25193 ) ;
#43872=CARTESIAN_POINT ( 'NONE',  ( 13.37557373594179921, -8.695341868789380868, -62.44661944738240322 ) ) ;
#43878=CARTESIAN_POINT ( 'NONE',  ( 22.74436002974624671, -17.09899314720811248, -34.52302736558711160 ) ) ;
#43879=CARTESIAN_POINT ( 'NONE',  ( 9.311115770169109851, -12.88060009992239863, -81.23899999999999011 ) ) ;
#43886=ORIENTED_EDGE ( 'NONE', *, *, #34037, .T. ) ;
#43888=CARTESIAN_POINT ( 'NONE',  ( 22.50961056586849907, -11.15336966704510147, -81.23899999999999011 ) ) ;
#43891=CARTESIAN_POINT ( 'NONE',  ( 11.27236315750194784, -9.289945223521018036, -73.08399817834765599 ) ) ;
#43894=ORIENTED_EDGE ( 'NONE', *, *, #157, .F. ) ;
#43903=CARTESIAN_POINT ( 'NONE',  ( 22.83044329432877362, -14.62138923286050840, -40.40589576860565302 ) ) ;
#43909=CARTESIAN_POINT ( 'NONE',  ( 16.10092966880469945, -7.768535876849650634, -66.78616676534149121 ) ) ;
#43921=CARTESIAN_POINT ( 'NONE',  ( 16.13393739769620083, -15.61618894467929941, -32.14999999999999858 ) ) ;
#43924=CARTESIAN_POINT ( 'NONE',  ( 22.90093739769620029, -15.61618894467913243, -28.45282021618999835 ) ) ;
#43926=CARTESIAN_POINT ( 'NONE',  ( 13.04303129394959981, -22.06172762676530041, -31.70967419469809201 ) ) ;
#43927=CARTESIAN_POINT ( 'NONE',  ( 22.90101955563642733, -15.61618902498797290, -36.84717743668400658 ) ) ;
#43934=CARTESIAN_POINT ( 'NONE',  ( 22.46012340461659917, -10.75453950994439722, -35.58399600476455760 ) ) ;
#43949=AXIS2_PLACEMENT_3D ( 'NONE', #43145, #19537, #19283 ) ;
#43952=CARTESIAN_POINT ( 'NONE',  ( 15.16221966815624889, -8.902689794812856050, -45.90713210071369588 ) ) ;
#43957=LINE ( 'NONE', #36333, #19310 ) ;
#43959=CARTESIAN_POINT ( 'NONE',  ( 11.20381621344150069, -9.510400486163490541, -49.29627689082150255 ) ) ;
#43966=CARTESIAN_POINT ( 'NONE',  ( 9.366488261363459245, -15.61629045172390029, -39.45282021618999835 ) ) ;
#43967=CARTESIAN_POINT ( 'NONE',  ( 21.96868942811769898, -19.57828787301799878, -53.03706054135149373 ) ) ;
#43976=DIRECTION ( 'NONE',  ( 0.000000000000000000, 0.000000000000000000, -1.000000000000000000 ) ) ;
#43978=CARTESIAN_POINT ( 'NONE',  ( 17.01966338078927876, -8.849178626785063173, -75.99446377898397031 ) ) ;
#43982=CARTESIAN_POINT ( 'NONE',  ( 8.222958677519082826, -16.65189219951969690, -74.46600179554452836 ) ) ;
#43995=CARTESIAN_POINT ( 'NONE',  ( 13.21370044366810070, -9.196315516880730456, -57.81693366461269079 ) ) ;
#44002=CARTESIAN_POINT ( 'NONE',  ( 23.15260118800880207, -12.10547580035419912, -47.13987186156389697 ) ) ;
#44004=ADVANCED_FACE ( 'NONE', ( #36169 ), #4463, .T. ) ;
#44011=AXIS2_PLACEMENT_3D ( 'NONE', #39853, #3959, #24604 ) ;
#44023=CARTESIAN_POINT ( 'NONE',  ( 23.04646110145052873, -19.60031946873696995, -35.67433263960586487 ) ) ;
#44027=CARTESIAN_POINT ( 'NONE',  ( 23.98482941094870213, -18.13535838165310210, -71.89116613449300530 ) ) ;
#44032=CARTESIAN_POINT ( 'NONE',  ( 20.96026664345949797, -21.29185981398060079, -62.50834448790610054 ) ) ;
#44034=CARTESIAN_POINT ( 'NONE',  ( 11.44367971890009983, -21.85319165794779650, -32.14999999999999858 ) ) ;
#44038=CARTESIAN_POINT ( 'NONE',  ( 22.90079931266048874, -15.61618915558698184, -42.84717230777439312 ) ) ;
#44041=CARTESIAN_POINT ( 'NONE',  ( 15.09046434425009942, -7.437320765297320335, -70.96727622117339251 ) ) ;
#44054=CARTESIAN_POINT ( 'NONE',  ( 9.705356321231780825, -19.38182821955269830, -71.06398904277699557 ) ) ;
#44059=ORIENTED_EDGE ( 'NONE', *, *, #35261, .F. ) ;
#44073=EDGE_CURVE ( 'NONE', #20360, #16042, #33782, .T. ) ;
#44079=ORIENTED_EDGE ( 'NONE', *, *, #4651, .T. ) ;
#44081=B_SPLINE_CURVE_WITH_KNOTS ( 'NONE', 3,
 ( #4291, #36254, #365, #31542, #19508, #32302, #19248, #43371, #3795, #51488, #51237, #16346, #39948, #43878, #7975, #28384, #7463, #31797, #44133, #15328, #31281, #28127, #51737, #23417, #35498, #39438, #15588, #43627, #7730, #23673, #19764, #35755, #15832 ),
 .UNSPECIFIED., .F., .F.,
 ( 4, 2, 1, 1, 1, 1, 1, 2, 2, 2, 2, 2, 2, 2, 2, 2, 2, 2, 4 ),
 ( 0.4999976081416900864, 0.5002417499345896967, 0.5004858917274892516, 0.5009741753132884723, 0.5019507424848870247, 0.5039038768280834635, 0.5078101455144765630, 0.5156226828872626511, 0.5312477576328348272, 0.5624979071239791795, 0.6249982061062677730, 0.6874985050885564775, 0.7499988040708451820, 0.8124991030531336644, 0.8749994020354223689, 0.9062495515265667212, 0.9374997010177110734, 0.9687498505088556477, 1.000000000000000000 ),
 .UNSPECIFIED. ) ;
#44087=CARTESIAN_POINT ( 'NONE',  ( 23.52669840957137026, -18.53768046102651468, -65.62753320149030856 ) ) ;
#44088=CARTESIAN_POINT ( 'NONE',  ( 20.71434839502420289, -22.47202989612290125, -42.10484805457200252 ) ) ;
#44091=CARTESIAN_POINT ( 'NONE',  ( 14.37168384308351676, -23.35179302556277037, -50.36354003200006701 ) ) ;
#44096=CARTESIAN_POINT ( 'NONE',  ( 19.68464592544490088, -9.066443701053138682, -35.89078365052999686 ) ) ;
#44100=CARTESIAN_POINT ( 'NONE',  ( 11.85758210885778574, -22.34943485980089761, -60.47261281821599255 ) ) ;
#44105=CARTESIAN_POINT ( 'NONE',  ( 20.38268442930850100, -22.68236679202650308, -47.83534835059659684 ) ) ;
#44112=EDGE_LOOP ( 'NONE', ( #41486, #51801, #38921, #31540, #14858, #32876 ) ) ;
#44113=CARTESIAN_POINT ( 'NONE',  ( 9.366543050370410128, -15.61630854221780140, -53.84717978381009829 ) ) ;
#44114=B_SPLINE_CURVE_WITH_KNOTS ( 'NONE', 3,
 ( #34883, #15748, #42513, #22563, #47478, #19162, #38579, #30691, #27531, #2673, #43029, #39350, #14975, #27277, #47223, #46713, #10798, #26757, #7375, #23325, #3449, #35401, #42770, #39094, #50883, #43538, #30941, #3189, #7638, #46972, #11055, #35139, #51144, #4920, #988, #13313, #13567, #7889, #16986, #45275, #27792, #49479, #9385, #8858, #9115, #37406, #37152, #44752, #24810, #25330, #29271, #28754, #29530, #32935, #48961, #41592, #13064, #41334, #40820, #12797, #47726, #21147, #29019, #5447, #45534, #23835, #1761, #20891, #21404, #9630, #1507, #36888, #17491, #33457, #25585, #5701, #45015, #25065, #719, #40560, #21654, #37659, #31702, #4653, #36614, #41082, #5194, #20626, #1250, #17238, #33200, #49219, #11832, #43787, #16709, #32667, #48695, #50755, #50241, #18520, #46839, #34494, #38440, #2539, #26892, #21915, #26359, #38711, #14848, #10925, #6737, #22172, #30811, #18000, #49728, #42113, #42899, #38965 ),
 .UNSPECIFIED., .F., .F.,
 ( 4, 3, 3, 3, 3, 3, 3, 3, 3, 3, 3, 3, 3, 3, 3, 3, 3, 3, 3, 3, 3, 3, 3, 3, 3, 3, 3, 3, 3, 3, 3, 3, 3, 3, 3, 3, 3, 3, 3, 4 ),
 ( -1.528706106645139950, -1.467014403968580183, -1.462406257103959994, -1.400361489047440067, -1.359972591434809974, -1.338075497632319921, -1.325535015073280087, -1.316390772988770053, -1.255261730263310005, -1.194475198410479999, -1.135862753278430004, -1.120187266468789966, -1.112461743370449785, -1.077250308146380009, -1.017356746704059844, -0.9572232250175689572, -0.8973750609027659753, -0.8492288533768060921, -0.8273183019162870799, -0.8205642526347601828, -0.7619152277339599211, -0.7047902307989259985, -0.6459350262605879633, -0.5874014674332818098, -0.5571792625727400861, -0.5439733099578959452, -0.5366754859262510280, -0.4791548101318530151, -0.4217815166465830323, -0.3651804039304868965, -0.3456238285489439122, -0.3024208499803260342, -0.2835195468565561150, -0.2726001364230170587, -0.2628186309613229632, -0.2067675508394690720, -0.1505665974598759949, -0.09476632463357703706, -0.04010227761605178465, 0.000000000000000000 ),
 .UNSPECIFIED. ) ;
#44121=CARTESIAN_POINT ( 'NONE',  ( 12.14984836808695512, -8.703641790031165115, -61.12566380759824369 ) ) ;
#44128=CARTESIAN_POINT ( 'NONE',  ( 8.428860946447588987, -13.54542364617790007, -76.87566458011686166 ) ) ;
#44130=ORIENTED_EDGE ( 'NONE', *, *, #15718, .F. ) ;
#44133=CARTESIAN_POINT ( 'NONE',  ( 19.64202710409484354, -21.45867595000445149, -34.78082310848400738 ) ) ;
#44134=CARTESIAN_POINT ( 'NONE',  ( 12.45061392682710100, -8.818281481913160746, -81.23899999999999011 ) ) ;
#44142=CARTESIAN_POINT ( 'NONE',  ( 18.94624808374599922, -21.82521411516110277, -81.23899999999999011 ) ) ;
#44150=ORIENTED_EDGE ( 'NONE', *, *, #18084, .T. ) ;
#44152=CARTESIAN_POINT ( 'NONE',  ( 5.741632552282950108, -21.61618894467929763, -22.14999999999999858 ) ) ;
#44155=FACE_OUTER_BOUND ( 'NONE', #16910, .T. ) ;
#44162=CARTESIAN_POINT ( 'NONE',  ( 12.64206891719070036, -22.64424718988719931, -63.93428524705129234 ) ) ;
#44171=CARTESIAN_POINT ( 'NONE',  ( 8.223571189834400386, -15.61612039429540033, -78.79233150823698395 ) ) ;
#44175=DIRECTION ( 'NONE',  ( 1.000000000000000000, 0.000000000000000000, 0.000000000000000000 ) ) ;
#44179=CARTESIAN_POINT ( 'NONE',  ( 9.186759353120089955, -12.92497237842379931, -32.18498778107969116 ) ) ;
#44190=DIRECTION ( 'NONE',  ( 0.000000000000000000, 0.000000000000000000, 1.000000000000000000 ) ) ;
#44195=ORIENTED_EDGE ( 'NONE', *, *, #27017, .T. ) ;
#44197=LINE ( 'NONE', #27173, #38698 ) ;
#44202=ORIENTED_EDGE ( 'NONE', *, *, #15071, .F. ) ;
#44207=CARTESIAN_POINT ( 'NONE',  ( 24.04487537504365591, -15.58383510252001791, -59.79102400322322808 ) ) ;
#44208=DIRECTION ( 'NONE',  ( 1.000000000000000000, 0.000000000000000000, 0.000000000000000000 ) ) ;
#44209=VERTEX_POINT ( 'NONE', #1315 ) ;
#44213=CARTESIAN_POINT ( 'NONE',  ( 8.222678474964419948, -15.61600660124389961, -50.79233150823699816 ) ) ;
#44215=CARTESIAN_POINT ( 'NONE',  ( 20.86355735167390080, -21.87857209189399654, -52.30659627123909416 ) ) ;
#44219=CYLINDRICAL_SURFACE ( 'NONE', #17629, 6.766999999999998572 ) ;
#44224=CARTESIAN_POINT ( 'NONE',  ( 10.93327293488309948, -20.38018394044530268, -51.61111978220640140 ) ) ;
#44232=CARTESIAN_POINT ( 'NONE',  ( 22.90093739478795598, -14.73038937777455892, -38.41115654869280860 ) ) ;
#44236=CARTESIAN_POINT ( 'NONE',  ( 23.04647429551237536, -19.60029476399586557, -73.67433456739328790 ) ) ;
#44242=CARTESIAN_POINT ( 'NONE',  ( 24.04493739769619864, -15.61618894467929941, -32.14999999999999858 ) ) ;
#44243=CARTESIAN_POINT ( 'NONE',  ( 11.97538973034304455, -21.02760254491551350, -75.16115355296736311 ) ) ;
#44247=CARTESIAN_POINT ( 'NONE',  ( 21.32600670501789963, -20.38954992040629932, -66.68945394373800184 ) ) ;
#44251=CARTESIAN_POINT ( 'NONE',  ( 11.27236363464668401, -21.94243302856639843, -80.50066552057984381 ) ) ;
#44253=CARTESIAN_POINT ( 'NONE',  ( 11.85406245721990004, -22.19413837265960154, -43.97111461901920393 ) ) ;
#44264=ORIENTED_EDGE ( 'NONE', *, *, #26411, .F. ) ;
#44273=CARTESIAN_POINT ( 'NONE',  ( 21.39066400359539699, -9.703911137440838885, -81.23899999999999011 ) ) ;
#44277=CARTESIAN_POINT ( 'NONE',  ( 11.87246112257180108, -22.67469728656620021, -70.46522537534779929 ) ) ;
#44278=CARTESIAN_POINT ( 'NONE',  ( 18.59784447790332251, -9.007730646818817632, -38.46077722564568546 ) ) ;
#44282=CARTESIAN_POINT ( 'NONE',  ( 10.48872632231780067, -10.75426692560380104, -63.45897166066949069 ) ) ;
#44293=CARTESIAN_POINT ( 'NONE',  ( 8.829104702642069924, -19.44007963430999908, -76.35416353349960161 ) ) ;
#44296=DIRECTION ( 'NONE',  ( 1.000000000000000000, 2.460964292799963328E-14, 0.000000000000000000 ) ) ;
#44306=CARTESIAN_POINT ( 'NONE',  ( 11.27215347255375555, -21.94227403160163448, -72.50068352509246949 ) ) ;
#44308=CARTESIAN_POINT ( 'NONE',  ( 17.23033643585230124, -22.58328789946420301, -36.90313586381709854 ) ) ;
#44324=CARTESIAN_POINT ( 'NONE',  ( 9.807676993354524697, -20.47774494272987056, -72.29929351537433035 ) ) ;
#44338=CARTESIAN_POINT ( 'NONE',  ( 22.90067702240739322, -15.61618873416334807, -54.84718332859007006 ) ) ;
#44342=CARTESIAN_POINT ( 'NONE',  ( 19.63779757108790136, -8.152564895917599586, -45.43204315924410253 ) ) ;
#44346=( LENGTH_UNIT ( ) NAMED_UNIT ( * ) SI_UNIT ( .MILLI., .METRE. ) );
#44349=CARTESIAN_POINT ( 'NONE',  ( 12.57041540415229974, -9.073406294472009748, -35.57390792627550269 ) ) ;
#44355=EDGE_CURVE ( 'NONE', #8604, #26370, #38313, .T. ) ;
#44359=CARTESIAN_POINT ( 'NONE',  ( 16.01653867706220069, -23.86051658551030030, -38.01220089870790275 ) ) ;
#44364=CARTESIAN_POINT ( 'NONE',  ( 22.68450356906678422, -17.37076425861442175, -56.53614005759181538 ) ) ;
#44398=ORIENTED_EDGE ( 'NONE', *, *, #6446, .F. ) ;
#44424=CARTESIAN_POINT ( 'NONE',  ( 18.80162467749480015, -22.99658139768499865, -65.67710173045091437 ) ) ;
#44426=DIRECTION ( 'NONE',  ( 1.000000000000000000, 2.460964292799963328E-14, 0.000000000000000000 ) ) ;
#44436=CARTESIAN_POINT ( 'NONE',  ( 22.64011532494543388, -18.06274401070583835, -70.96223323988861864 ) ) ;
#44438=VERTEX_POINT ( 'NONE', #15851 ) ;
#44440=CARTESIAN_POINT ( 'NONE',  ( 12.07081295223539996, -21.86100392024429695, -43.75095171636819913 ) ) ;
#44449=AXIS2_PLACEMENT_3D ( 'NONE', #20728, #817, #49059 ) ;
#44461=EDGE_CURVE ( 'NONE', #40749, #32305, #17064, .T. ) ;
#44474=CARTESIAN_POINT ( 'NONE',  ( 15.02108337061823740, -8.917202890402387894, -33.90037646791326864 ) ) ;
#44476=CARTESIAN_POINT ( 'NONE',  ( 9.868248963658528439, -10.89094862918750017, -57.21816999718339503 ) ) ;
#44483=B_SPLINE_CURVE_WITH_KNOTS ( 'NONE', 3,
 ( #47657, #47915, #20112, #40557, #209, #36106, #51841, #716, #16706, #48692, #32663, #40816, #12794, #16190, #48426, #43722, #24540, #23776 ),
 .UNSPECIFIED., .F., .F.,
 ( 4, 2, 2, 2, 2, 2, 2, 2, 4 ),
 ( 0.000000000000000000, 0.06250018575575970459, 0.1250003715115194092, 0.1875005572672791276, 0.2500007430230388183, 0.3125009287787984258, 0.3750011145345580332, 0.4375013002903175852, 0.5000014860460771926 ),
 .UNSPECIFIED. ) ;
#44485=CARTESIAN_POINT ( 'NONE',  ( 16.51210842463260065, -8.573494442655439585, -56.36425564602360083 ) ) ;
#44494=DIRECTION ( 'NONE',  ( 1.000000000000000000, 0.000000000000000000, 0.000000000000000000 ) ) ;
#44495=CARTESIAN_POINT ( 'NONE',  ( 23.33463543114514849, -12.22107770882397482, -55.36731066630095910 ) ) ;
#44500=CARTESIAN_POINT ( 'NONE',  ( 24.04493739635935512, -15.61397715763259164, -71.50758368266318143 ) ) ;
#44503=CARTESIAN_POINT ( 'NONE',  ( 21.21177448402870169, -10.72148469425540007, -64.60302447664000169 ) ) ;
#44510=CARTESIAN_POINT ( 'NONE',  ( 9.240841536127231137, -14.12361126166039860, -63.52069670119340827 ) ) ;
#44513=CARTESIAN_POINT ( 'NONE',  ( 8.222732946675209931, -15.61637358666110131, -80.79233150823698395 ) ) ;
#44523=AXIS2_PLACEMENT_3D ( 'NONE', #25020, #44190, #5151 ) ;
#44524=ORIENTED_EDGE ( 'NONE', *, *, #22383, .T. ) ;
#44527=EDGE_CURVE ( 'NONE', #12539, #37063, #5828, .T. ) ;
#44528=CARTESIAN_POINT ( 'NONE',  ( 17.16947398661607593, -23.52719049786522376, -59.96602729019871703 ) ) ;
#44532=CARTESIAN_POINT ( 'NONE',  ( 8.222262383277058717, -15.61618471288229948, -44.50766849176299900 ) ) ;
#44534=ORIENTED_EDGE ( 'NONE', *, *, #5712, .F. ) ;
#44538=CARTESIAN_POINT ( 'NONE',  ( 18.29186039705039946, -23.57395800295140020, -72.20804185874750658 ) ) ;
#44544=CARTESIAN_POINT ( 'NONE',  ( 14.84020896475909979, -8.279094114505989310, -65.67710173045101385 ) ) ;
#44559=DIRECTION ( 'NONE',  ( 1.000000000000000000, 0.000000000000000000, 0.000000000000000000 ) ) ;
#44568=CARTESIAN_POINT ( 'NONE',  ( 16.22658542707289797, -23.06590471877949966, -80.72869863253859535 ) ) ;
#44575=CARTESIAN_POINT ( 'NONE',  ( 22.90093475162459313, -15.62310159663111619, -40.45314972491761552 ) ) ;
#44588=ORIENTED_EDGE ( 'NONE', *, *, #3544, .F. ) ;
#44593=FACE_OUTER_BOUND ( 'NONE', #42479, .T. ) ;
#44594=CARTESIAN_POINT ( 'NONE',  ( 29.99034385824719706, -15.61618894467929941, -32.14999999999999858 ) ) ;
#44598=CARTESIAN_POINT ( 'NONE',  ( 16.13393739769629676, -15.61618894467929941, -20.75000000000000000 ) ) ;
#44601=CARTESIAN_POINT ( 'NONE',  ( 7.890219331288808924, -15.46181116932459965, -44.79829171073519944 ) ) ;
#44602=DIRECTION ( 'NONE',  ( 0.000000000000000000, -5.782411586589432581E-16, 1.000000000000000000 ) ) ;
#44605=CARTESIAN_POINT ( 'NONE',  ( 23.04647467197195354, -19.60029406037446620, -41.95899769523001765 ) ) ;
#44606=CARTESIAN_POINT ( 'NONE',  ( 11.41311105421049987, -9.852467598734330423, -33.51421571862140070 ) ) ;
#44612=CARTESIAN_POINT ( 'NONE',  ( 24.04492352372650998, -15.63331151564256416, -59.79301433380418018 ) ) ;
#44615=CARTESIAN_POINT ( 'NONE',  ( 19.48597052431479781, -23.14922250540550053, -43.87440179741569324 ) ) ;
#44636=CARTESIAN_POINT ( 'NONE',  ( 11.68549127948460153, -10.14317847777680015, -80.12993496510929958 ) ) ;
#44638=CARTESIAN_POINT ( 'NONE',  ( 24.04526354826459666, -15.61618910718878794, -73.50766907743336276 ) ) ;
#44653=DIRECTION ( 'NONE',  ( 0.000000000000000000, 0.000000000000000000, -1.000000000000000000 ) ) ;
#44654=CARTESIAN_POINT ( 'NONE',  ( 22.23872575654229777, -19.32696879987259919, -81.23899999999999011 ) ) ;
#44679=CARTESIAN_POINT ( 'NONE',  ( 13.22842670730820025, -8.326143964624399985, -62.66678235003330144 ) ) ;
#44680=ORIENTED_EDGE ( 'NONE', *, *, #18450, .T. ) ;
#44692=CARTESIAN_POINT ( 'NONE',  ( 23.67181263347827525, -18.06420660938224998, -33.60759600576869843 ) ) ;
#44694=CARTESIAN_POINT ( 'NONE',  ( 9.807823418024582907, -20.47793272903095030, -54.58399883035956890 ) ) ;
#44697=CARTESIAN_POINT ( 'NONE',  ( 23.40224892329179696, -17.25275299940979679, -49.13783902869439402 ) ) ;
#44700=CARTESIAN_POINT ( 'NONE',  ( 16.00572161013059969, -8.564513971789514457, -34.34139281033760227 ) ) ;
#44702=DIRECTION ( 'NONE',  ( 0.7071067811865470176, -8.659560562354926695E-17, 0.7071067811865480168 ) ) ;
#44721=EDGE_CURVE ( 'NONE', #31721, #7977, #38034, .T. ) ;
#44724=CARTESIAN_POINT ( 'NONE',  ( 12.74054237723616900, -9.433355499570044600, -66.18740309792794108 ) ) ;
#44727=CARTESIAN_POINT ( 'NONE',  ( 23.64088819150179077, -13.06712943445810104, -59.68817848589910824 ) ) ;
#44735=CARTESIAN_POINT ( 'NONE',  ( 23.91605131074399893, -14.60354357934630087, -61.97130586100059446 ) ) ;
#44744=CARTESIAN_POINT ( 'NONE',  ( 9.221496542177588296, -11.63191685418159693, -40.95899807896893918 ) ) ;
#44749=CARTESIAN_POINT ( 'NONE',  ( 22.90095859539430379, -15.61618916398383661, -38.45281773784812174 ) ) ;
#44751=CYLINDRICAL_SURFACE ( 'NONE', #26475, 7.910999999999997812 ) ;
#44752=CARTESIAN_POINT ( 'NONE',  ( 23.20507000855700142, -18.04245328055489850, -32.14999999999999858 ) ) ;
#44756=EDGE_CURVE ( 'NONE', #31721, #15986, #1464, .T. ) ;
#44759=CARTESIAN_POINT ( 'NONE',  ( 18.20464644555056921, -23.32128070152664634, -52.20899666773274106 ) ) ;
#44764=CARTESIAN_POINT ( 'NONE',  ( 12.99575412164399779, -21.93238755621440106, -63.49395944174919748 ) ) ;
#44771=CARTESIAN_POINT ( 'NONE',  ( 12.88757487121280043, -21.87747388015940331, -65.10507532246559492 ) ) ;
#44783=CARTESIAN_POINT ( 'NONE',  ( 12.14992628989387313, -22.52878017980526693, -64.17433570710899460 ) ) ;
#44786=EDGE_CURVE ( 'NONE', #40766, #22439, #42117, .T. ) ;
#44797=VERTEX_POINT ( 'NONE', #44273 ) ;
#44800=CARTESIAN_POINT ( 'NONE',  ( 21.98482826927030231, -20.84627725470230075, -34.24467998873379315 ) ) ;
#44807=CARTESIAN_POINT ( 'NONE',  ( 8.862687950201170395, -17.23964983963449882, -69.16273469725010159 ) ) ;
#44809=DIRECTION ( 'NONE',  ( 0.000000000000000000, 0.000000000000000000, -1.000000000000000000 ) ) ;
#44821=MANIFOLD_SOLID_BREP ( 'Stock-MAS-691-1', #40188 ) ;
#44828=B_SPLINE_CURVE_WITH_KNOTS ( 'NONE', 3,
 ( #40118, #11838, #27798, #27283, #36173, #16265, #281, #26306, #34430, #5259, #28297, #16517, #36682, #20692, #4727, #32732, #21211, #13384 ),
 .UNSPECIFIED., .F., .F.,
 ( 4, 2, 2, 2, 2, 2, 2, 2, 4 ),
 ( 0.000000000000000000, 0.06250011819343853636, 0.1250002363868770727, 0.1875003545803156091, 0.2500004727737541455, 0.3125005909671927928, 0.3750007091606314402, 0.4375008273540700876, 0.5000009455475087350 ),
 .UNSPECIFIED. ) ;
#44831=CARTESIAN_POINT ( 'NONE',  ( 8.223247527389670353, -15.61637340300369914, -74.79233150823711185 ) ) ;
#44834=CARTESIAN_POINT ( 'NONE',  ( 21.92791489578599951, -19.63767914711110052, -38.64595234721679162 ) ) ;
#44841=FACE_OUTER_BOUND ( 'NONE', #17753, .T. ) ;
#44842=CARTESIAN_POINT ( 'NONE',  ( 23.26606227162260154, -17.77013627947239982, -71.16070186438059864 ) ) ;
#44846=CARTESIAN_POINT ( 'NONE',  ( 16.13393739769620083, -15.61618894467929941, -31.39999999999999858 ) ) ;
#44849=DIRECTION ( 'NONE',  ( -1.000000000000000000, 0.000000000000000000, 0.000000000000000000 ) ) ;
#44851=CARTESIAN_POINT ( 'NONE',  ( 24.03381973957637285, -16.06908004449718419, -71.52589682854927844 ) ) ;
#44860=CARTESIAN_POINT ( 'NONE',  ( 12.72591284326311190, -9.703296205089767312, -69.78615459468322513 ) ) ;
#44861=CARTESIAN_POINT ( 'NONE',  ( 21.80687142448134352, -11.85343762274402124, -50.26656186468857612 ) ) ;
#44867=CARTESIAN_POINT ( 'NONE',  ( 20.99564994467235479, -9.290051249912700371, -35.21599968409613268 ) ) ;
#44868=CARTESIAN_POINT ( 'NONE',  ( 24.25483720920119879, -17.04226969534990133, -43.84766453797169561 ) ) ;
#44869=CARTESIAN_POINT ( 'NONE',  ( 22.90070561427262064, -15.61618657793558818, -56.45282510079097449 ) ) ;
#44873=CARTESIAN_POINT ( 'NONE',  ( 8.729467296546598476, -16.44112522791030173, -33.19733999436699889 ) ) ;
#44874=CARTESIAN_POINT ( 'NONE',  ( 11.19819258504769977, -10.83938507832420051, -32.14999999999999858 ) ) ;
#44880=CARTESIAN_POINT ( 'NONE',  ( 21.21552280508710098, -22.10927838317979877, -51.79629490377759993 ) ) ;
#44885=CARTESIAN_POINT ( 'NONE',  ( 23.83903856107666641, -17.68686005063226574, -63.87566687503874618 ) ) ;
#44886=CARTESIAN_POINT ( 'NONE',  ( 17.01966273183835199, -22.38319939417082338, -56.91109783820547108 ) ) ;
#44902=EDGE_CURVE ( 'NONE', #31815, #21944, #39620, .T. ) ;
#44904=CARTESIAN_POINT ( 'NONE',  ( 9.638313984568736004, -18.10068106752252604, -61.73034261279407531 ) ) ;
#44908=FACE_OUTER_BOUND ( 'NONE', #20198, .T. ) ;
#44914=EDGE_LOOP ( 'NONE', ( #14038, #39759, #593, #10417 ) ) ;
#44920=CARTESIAN_POINT ( 'NONE',  ( 22.61477114348110007, -18.74635927958349768, -81.23899999999999011 ) ) ;
#44921=CARTESIAN_POINT ( 'NONE',  ( 8.222953192759320018, -14.58052584272395436, -62.54933522701458770 ) ) ;
#44931=CARTESIAN_POINT ( 'NONE',  ( 22.90066504558609850, -15.61618132107965984, -48.84717678326153845 ) ) ;
#44936=DIRECTION ( 'NONE',  ( 1.000000000000000000, 0.000000000000000000, 0.000000000000000000 ) ) ;
#44943=CARTESIAN_POINT ( 'NONE',  ( 18.06150950593789872, -8.008875755996218260, -74.86649773383069828 ) ) ;
#44954=CARTESIAN_POINT ( 'NONE',  ( 14.06314123691665507, -23.32125865919739738, -56.37568259043300856 ) ) ;
#44955=CARTESIAN_POINT ( 'NONE',  ( 9.243065035284324438, -19.52181753121742247, -34.34351632011016164 ) ) ;
#44959=CARTESIAN_POINT ( 'NONE',  ( 13.32728455275639945, -8.714783714848721274, -46.44439537253129657 ) ) ;
#44967=CARTESIAN_POINT ( 'NONE',  ( 23.04645612045855785, -19.60032880246072651, -77.95899556036906120 ) ) ;
#44970=CARTESIAN_POINT ( 'NONE',  ( 24.04493738312996243, -16.65173602022645838, -51.54933235314647533 ) ) ;
#44975=EDGE_CURVE ( 'NONE', #47941, #41326, #6476, .T. ) ;
#44982=ORIENTED_EDGE ( 'NONE', *, *, #8555, .T. ) ;
#44990=CARTESIAN_POINT ( 'NONE',  ( 10.22100544393300581, -12.20823257830125463, -53.61948740722137074 ) ) ;
#44991=B_SPLINE_CURVE_WITH_KNOTS ( 'NONE', 3,
 ( #13096, #744, #8626, #16742, #5221, #28261, #40846, #8369, #24317, #24574, #28784, #44783, #20656, #8887, #25098, #29047, #24059, #40336 ),
 .UNSPECIFIED., .F., .F.,
 ( 4, 2, 2, 2, 2, 2, 2, 2, 4 ),
 ( 0.5000008230189937342, 0.5625007201416195590, 0.6250006172642452729, 0.6875005143868710977, 0.7500004115094969226, 0.8125003086321226364, 0.8750002057547484613, 0.9375001028773741751, 1.000000000000000000 ),
 .UNSPECIFIED. ) ;
#44992=ORIENTED_EDGE ( 'NONE', *, *, #30270, .T. ) ;
#44995=CARTESIAN_POINT ( 'NONE',  ( 22.10690976917388539, -18.81397998849861253, -46.60927541014969222 ) ) ;
#44997=CARTESIAN_POINT ( 'NONE',  ( 23.73362326446910231, -13.65876147017249842, -65.93225241418160465 ) ) ;
#45008=ADVANCED_FACE ( 'NONE', ( #18811 ), #10707, .T. ) ;
#45010=CARTESIAN_POINT ( 'NONE',  ( 16.13393739769620083, -15.61618894467929941, -32.14999999999999858 ) ) ;
#45015=CARTESIAN_POINT ( 'NONE',  ( 23.20978547387309732, -14.32984258838409986, -32.14999999999999858 ) ) ;
#45024=ORIENTED_EDGE ( 'NONE', *, *, #7623, .T. ) ;
#45025=CARTESIAN_POINT ( 'NONE',  ( 9.127021151536109045, -16.41973352573810274, -63.81083516600379113 ) ) ;
#45032=CARTESIAN_POINT ( 'NONE',  ( 14.90922390191370006, -8.670497074903209977, -65.89726463310188365 ) ) ;
#45035=DIRECTION ( 'NONE',  ( 1.000000000000000000, 2.460964292799963328E-14, 0.000000000000000000 ) ) ;
#45052=CARTESIAN_POINT ( 'NONE',  ( 9.543104041351597289, -13.84479649607203733, -67.53615334925251545 ) ) ;
#45059=CARTESIAN_POINT ( 'NONE',  ( 24.36162650863650114, -16.15271744766720019, -79.81305924085479830 ) ) ;
#45060=CARTESIAN_POINT ( 'NONE',  ( 11.87323508190820931, -21.23659595403887934, -65.55365164941011358 ) ) ;
#45061=CARTESIAN_POINT ( 'NONE',  ( 9.205734167420709824, -3.616188944679339823, -32.14999999999999858 ) ) ;
#45066=CARTESIAN_POINT ( 'NONE',  ( 19.38808262899609858, -9.358945304426239176, -34.49983067246459001 ) ) ;
#45073=CARTESIAN_POINT ( 'NONE',  ( 18.77108585709959954, -23.07469878264739904, -81.89948870795299740 ) ) ;
#45079=CARTESIAN_POINT ( 'NONE',  ( 24.04493739769619864, -15.61618894467929941, -32.14999999999999858 ) ) ;
#45080=B_SPLINE_CURVE_WITH_KNOTS ( 'NONE', 3,
 ( #37019, #24936, #10018, #21275, #25980, #33065, #5580, #1898, #48822, #22048 ),
 .UNSPECIFIED., .F., .F.,
 ( 4, 1, 1, 1, 1, 1, 1, 4 ),
 ( 0.000000000000000000, 0.04040786132540063330, 0.1196267923890341062, 0.1988457234526539996, 0.2780646545162693273, 0.3572835855798892069, 0.4365025166435069215, 0.4999960598860723193 ),
 .UNSPECIFIED. ) ;
#45086=CARTESIAN_POINT ( 'NONE',  ( 9.807863465693298366, -20.47798411401742058, -74.58399817736376747 ) ) ;
#45090=CARTESIAN_POINT ( 'NONE',  ( 12.97538624507340010, -21.92223780171290315, -33.10062717276339583 ) ) ;
#45097=CARTESIAN_POINT ( 'NONE',  ( 16.35471799615400101, -23.06319825774929910, -79.55790855712409382 ) ) ;
#45101=CARTESIAN_POINT ( 'NONE',  ( 20.89221387562904297, -9.278317313805978017, -49.49732490764383641 ) ) ;
#45102=CARTESIAN_POINT ( 'NONE',  ( 9.366937397696199596, -15.61618894467949836, -28.45282021618999835 ) ) ;
#45108=CARTESIAN_POINT ( 'NONE',  ( 23.04644961876633502, -19.60034157972581070, -71.67430252639809396 ) ) ;
#45120=EDGE_LOOP ( 'NONE', ( #20140, #48992, #16531, #38257 ) ) ;
#45122=CARTESIAN_POINT ( 'NONE',  ( 23.98146874757331659, -14.58313711796746404, -43.75066625850210045 ) ) ;
#45124=CARTESIAN_POINT ( 'NONE',  ( 20.11402673884080272, -8.395274259375058890, -51.45268192007909391 ) ) ;
#45130=CARTESIAN_POINT ( 'NONE',  ( 12.19807860417640022, -9.290391812094439317, -45.55549324029149716 ) ) ;
#45133=CARTESIAN_POINT ( 'NONE',  ( 11.88110451476120133, -10.30869569151619913, -32.14999999999999858 ) ) ;
#45139=CARTESIAN_POINT ( 'NONE',  ( 18.56287218994199861, -7.736912551253769088, -49.10285124761459485 ) ) ;
#45147=ORIENTED_EDGE ( 'NONE', *, *, #40931, .F. ) ;
#45159=CARTESIAN_POINT ( 'NONE',  ( 9.366403394718119557, -15.61612932825470068, -61.45282021618999124 ) ) ;
#45160=DIRECTION ( 'NONE',  ( 1.000000000000000000, 2.460964292799963328E-14, 0.000000000000000000 ) ) ;
#45161=ORIENTED_EDGE ( 'NONE', *, *, #16012, .F. ) ;
#45162=CARTESIAN_POINT ( 'NONE',  ( 22.90121638405171467, -15.61618906730874734, -72.84718036870921765 ) ) ;
#45166=CIRCLE ( 'NONE', #34251, 6.999999999999999112 ) ;
#45171=ORIENTED_EDGE ( 'NONE', *, *, #3600, .F. ) ;
#45175=ORIENTED_EDGE ( 'NONE', *, *, #51108, .T. ) ;
#45178=CARTESIAN_POINT ( 'NONE',  ( 22.45577387985110107, -19.01145220004960024, -81.23899999999999011 ) ) ;
#45179=CARTESIAN_POINT ( 'NONE',  ( 23.04647095553203684, -11.63207687756748676, -63.34100319679465940 ) ) ;
#45192=B_SPLINE_CURVE_WITH_KNOTS ( 'NONE', 3,
 ( #7797, #32379, #20338, #35572, #39250, #15401, #36325, #51558, #436 ),
 .UNSPECIFIED., .F., .F.,
 ( 4, 1, 1, 1, 1, 1, 4 ),
 ( 0.000000000000000000, 0.07759967679297839760, 0.1709532882598540637, 0.2643068997267294384, 0.3576605111936237424, 0.4510141226604987841, 0.4999989276629364099 ),
 .UNSPECIFIED. ) ;
#45202=CARTESIAN_POINT ( 'NONE',  ( 14.67229395948385218, -22.51591050674139893, -55.41362847326020358 ) ) ;
#45205=CARTESIAN_POINT ( 'NONE',  ( 8.551749739990640364, -13.59204010960809939, -68.37054538661399761 ) ) ;
#45207=B_SPLINE_SURFACE_WITH_KNOTS ( 'NONE', 3, 3, ( 
 ( #27067, #38357, #23123, #19464, #3231, #18948, #19204, #11614, #22610, #27322, #38626, #18690, #34927, #7422, #23370, #43072, #39392, #31494, #35449, #46497, #34665, #50926, #50670, #10587, #3495, #51447, #18431, #43582, #27579, #15542, #14766, #15023, #7683, #46760, #30734, #2450, #50420, #10845, #30991, #26806, #42818, #6914, #47016, #11104, #8450, #32775, #27835, #32257, #4002, #3752, #8190, #12909, #28599, #16049, #19721, #47772, #40668, #32005, #24658, #36463, #28866, #39646, #7934, #32509, #23629, #23882, #28338, #20222, #44088, #4504, #24396, #31751, #48026, #39907, #36211, #48281, #35712, #77, #20474, #44868, #832, #36726, #12376, #4251, #11878, #44601, #51696, #15790, #12126, #44342, #35960, #28083, #16302, #43833, #8707, #20738, #4770, #24133, #16828, #571, #40156, #319, #48802, #40411, #16557, #48538, #12642, #17607, #9739, #41972, #40927, #33574, #17855, #25960, #13932, #21001, #29888, #36998, #45906, #37515, #45389, #9494, #18113, #25440, #41701, #29126, #5042, #45124, #9993, #5302, #49589, #22028, #6069, #1096, #30156, #1359, #37781, #38038, #49838, #49328, #5809, #2135, #34081, #50088, #5559, #1614, #9236, #17093, #14183, #13429, #8972, #25186, #21774, #24916, #29385, #33046, #41443, #49071, #13178, #41191, #21518, #1874, #21252, #33826, #37262, #17350, #13679, #33315, #29636, #45642, #25698, #19141, #3171, #46954, #50355, #14957, #7109, #43012, #10522, #26220, #47206, #39080, #2913, #14442, #30411, #39327, #23060, #51382, #11293, #46174, #18882, #14699, #34605, #6851, #15479, #26478, #42228, #30922, #34864, #10261, #11036, #27255, #27004, #30669, #35119, #3431, #46433, #51127, #42496, #6584, #46693, #15223, #31176, #50866, #43269, #19403, #7358, #22289, #22545, #22801, #38561, #18360, #23305, #2656, #6328, #35382, #38296, #18626, #2385, #34343, #50607, #10780, #26736, #42756, #38823, #27775, #8383, #31944, #16496, #40094, #43769, #23820, #31687, #4444, #36154, #7875, #32447, #44277, #4187, #12316, #506, #20411, #39583, #47967, #256, #24334, #44027, #39839, #44538, #16242, #24075, #20165, #19657, #48474, #36400, #3947, #15, #19906, #12575, #28539, #40602, #8639, #3688, #32196, #51636, #36659, #47709, #35900, #48217, #28277, #24590, #4702, #20671, #28022, #40350, #15731, #35650, #762, #15993, #31430, #11814, #47460, #11554, #27514, #43516, #7622, #23566, #12070, #8130, #17786, #25116, #13112, #25889, #37970, #4967, #33246, #45059, #28800, #49771, #33507, #37450, #1549, #41902, #20934, #25377, #49006, #48737 ),
 ( #29572, #6002, #32712, #1035, #25630, #16758, #17028, #21450, #13358, #37196, #49520, #17537, #24855, #41127, #32980, #29316, #41378, #44800, #9160, #13612, #21961, #45837, #29820, #5493, #49263, #40862, #21700, #12842, #8904, #5238, #45578, #29063, #21189, #9427, #36933, #1807, #13864, #33760, #1294, #9927, #9672, #17286, #45323, #37708, #41634, #5743, #23245, #19077, #10712, #2852, #35051, #34014, #26667, #10972, #51058, #7041, #14116, #22993, #30083, #39014, #30604, #38487, #2587, #11229, #18563, #34797, #22221, #50024, #38229, #3109, #50291, #42687, #15155, #31116, #46108, #2070, #46367, #30857, #47141, #42943, #42428, #50803, #18047, #42163, #34539, #30344, #10194, #27192, #18816, #22737, #38757, #43203, #6262, #6783, #34267, #26152, #50543, #7294, #2323, #10455, #18297, #14379, #26407, #6518, #22480, #14890, #14635, #46623, #46885, #26939, #39263, #23498, #43959, #35837, #7809, #20100, #24011, #47397, #47644, #3622, #51826, #12001, #51319, #15670, #36089, #28476, #16436, #445, #27956, #19846, #11493, #44215, #3364, #19338, #11750, #8064, #19594, #35585, #31882, #27449, #24269, #36335, #40290, #27707, #4381, #16174, #31625, #15926, #8315, #40031, #51570, #8584, #20349, #47901, #4125, #32388, #35320, #197, #48151, #48409, #12510, #15416, #44476, #31368, #43452, #32132, #23760, #39775, #7555, #3879, #12253, #39523, #43706, #28214, #45517, #20872, #13294, #37643, #41573, #701, #45776, #16969, #1491, #1743, #13550, #13046, #5429, #29512, #5686, #9614, #21131, #17222, #44735, #32649, #17726, #28998, #33696, #40798, #29254, #25567, #4633, #29757, #49711, #21635, #4901, #9097, #13801, #32915, #36870, #24526, #40543, #969, #17475, #25048, #20605, #33181, #48944, #44997, #24791, #49458, #45260, #41064, #36599, #37389, #49202, #21385, #16694, #48675, #12778, #5176, #9365, #33442, #37133, #1231, #28734, #25314, #41316, #8839, #49966, #27585, #35459, #38164, #30282, #18236, #15549, #31506, #19726, #23637, #17981, #51199, #30016, #15795, #10130, #6199, #2521, #7428, #43336, #31760, #50224, #11622, #14313, #14056, #43589, #37908, #46301, #23377, #5939, #39401, #2001, #46041, #10388, #26088, #42096, #3503, #47525, #51454, #19472, #11367, #22154, #31247, #7693, #39653, #2262, #41833, #3759, #35718, #18501, #34202, #26344, #51704, #9866, #25821, #21897, #33948, #34473, #42357, #6458, #22417, #38420, #15293, #47277, #27330, #36471, #47778, #32515, #28872, #16563, #32264, #48546, #5048, #32010, #4777, #16055, #48036, #48288, #12647, #28607 ),
 ( #32781, #8196, #1101, #24924, #11884, #28090, #43842, #27842, #7941, #44873, #28343, #44606, #36217, #48809, #326, #35966, #8977, #23888, #12383, #8714, #39912, #24664, #4008, #83, #44349, #12135, #44096, #40675, #839, #20744, #36731, #16833, #24139, #12916, #40933, #21007, #40164, #19969, #37004, #17100, #4510, #4257, #20229, #16311, #8456, #24403, #40417, #20480, #577, #1620, #21523, #45649, #38302, #13436, #13184, #1882, #21780, #33052, #17861, #14191, #33832, #17612, #49845, #42236, #17356, #41977, #1364, #33320, #33581, #13938, #29893, #37786, #45912, #26226, #30163, #9242, #37268, #9747, #29392, #5307, #18120, #45395, #2390, #10266, #49078, #9500, #29132, #45130, #25191, #46181, #13684, #9999, #6334, #25447, #25967, #49596, #34086, #41708, #41448, #5567, #49333, #6076, #22035, #37521, #50093, #38046, #5816, #2140, #22294, #41197, #21259, #29643, #25704, #47213, #30929, #30676, #31438, #3178, #11042, #27011, #6590, #35390, #43276, #46700, #38829, #26745, #23311, #39337, #27520, #47466, #26484, #7115, #38566, #23572, #18632, #14705, #43019, #15231, #51134, #39590, #2920, #42762, #3439, #19411, #43525, #11561, #42501, #23066, #2662, #18367, #34610, #10786, #39086, #31182, #11302, #34349, #6857, #51389, #22809, #22552, #15487, #46438, #18889, #27262, #14448, #7366, #10528, #50613, #34871, #50874, #14963, #7628, #50360, #30416, #46961, #19150, #35127, #24340, #16501, #514, #19913, #35656, #4709, #48480, #12322, #23827, #39845, #48745, #32453, #8911, #20678, #3695, #28283, #24080, #44032, #16247, #24861, #35904, #51643, #40355, #44282, #19664, #4451, #36666, #20417, #40100, #36408, #12849, #3951, #12582, #22, #15997, #4193, #28546, #44544, #8391, #8646, #28806, #769, #31692, #7880, #32202, #31948, #27781, #40610, #47972, #15738, #32718, #47715, #12074, #11819, #43775, #28028, #16765, #36158, #24597, #44807, #8134, #20170, #262, #48222, #51668, #3464, #35415, #43300, #16021, #47740, #19435, #44054, #3972, #15762, #23849, #12096, #31976, #51161, #7654, #11848, #19937, #3718, #51416, #4217, #27805, #35683, #31715, #31207, #8159, #47996, #15511, #31465, #11585, #47489, #28051, #24103, #288, #20191, #15254, #43802, #11327, #48249, #7391, #39362, #7902, #39872, #35927, #12343, #27546, #40124, #43552, #47236, #36181, #19174, #23597, #44, #39109, #16273, #35153, #27291, #39615, #23339, #19690, #32226, #43042, #7138, #23090, #3202, #32474, #49034, #41154, #25149, #44568, #8417, #29350, #37230, #36965, #48504, #12606, #21483 ),
 ( #8669, #24365, #13142, #17058, #28308, #29091, #9458, #45090, #12873, #9197, #37482, #28569, #1327, #24624, #40635, #28829, #5267, #17315, #33011, #33279, #1582, #25407, #4474, #4734, #40893, #20701, #539, #13392, #36691, #33540, #5528, #44308, #792, #40377, #20443, #36431, #41410, #8939, #49294, #17571, #16793, #45356, #44834, #49558, #1062, #32742, #48769, #24882, #16525, #5004, #20964, #14667, #26446, #38262, #46402, #34572, #38525, #21737, #30120, #34310, #42462, #26188, #25922, #26700, #50323, #6297, #22255, #1842, #30637, #2624, #41669, #34833, #6037, #6549, #42722, #18596, #2102, #10490, #50577, #46661, #10744, #10230, #2355, #33794, #37744, #6817, #18078, #22771, #29854, #18330, #38790, #45608, #18850, #2882, #13645, #45875, #50056, #29605, #21994, #9961, #9707, #25667, #17820, #46139, #41937, #5774, #49803, #30377, #14409, #22515, #13896, #38004, #34046, #14151, #42199, #35352, #40065, #3915, #43238, #46918, #23026, #15962, #7329, #51862, #11784, #4158, #14926, #35088, #7843, #50834, #51090, #3657, #47431, #19370, #31657, #35619, #7076, #23276, #15188, #11524, #23536, #11004, #27224, #47681, #20133, #27992, #12038, #39554, #31403, #39048, #19878, #30890, #26972, #39297, #19628, #31149, #47174, #43487, #3142, #35869, #47937, #31915, #3403, #43995, #27744, #51352, #27484, #8101, #51607, #11262, #42981, #24044, #7590, #15701, #19110, #15450, #43742, #23791, #39807, #41099, #48184, #5210, #12288, #21163, #12815, #20645, #36631, #45291, #733, #17004, #4417, #16211, #20383, #37169, #32422, #24828, #49235, #1266, #17255, #44510, #33218, #13083, #12547, #28770, #13330, #40836, #48445, #5466, #29290, #44771, #36904, #9400, #32168, #8875, #45032, #25349, #41349, #28249, #36124, #44247, #228, #4935, #16730, #32684, #8354, #48711, #32951, #36372, #24305, #479, #40322, #28513, #20908, #16467, #8614, #24562, #40575, #4672, #29036, #1004, #25086, #48978, #9132, #26377, #2559, #6491, #18016, #14088, #41607, #29546, #14605, #25855, #30573, #37677, #10162, #42394, #1522, #26637, #46595, #22448, #1778, #5973, #38455, #29790, #17759, #10684, #42655, #9644, #37942, #49743, #33477, #18533, #38199, #42134, #6233, #21420, #25600, #30049, #33730, #17507, #21930, #37422, #34509, #13833, #49494, #45549, #50515, #45811, #13581, #34236, #5713, #21669, #9898, #30316, #41870, #2036, #26122, #33982, #49997, #2295, #22189, #46077, #18268, #50260, #14347, #46338, #10425, #11918, #4541, #48583, #36507, #609, #28123, #24175, #14863, #38726, #40198 ) ),
 .UNSPECIFIED., .F., .F., .F.,
 ( 4, 4 ),
 ( 4, 1, 1, 1, 1, 1, 1, 1, 1, 1, 1, 1, 1, 1, 1, 1, 1, 1, 1, 1, 1, 1, 1, 1, 1, 1, 1, 1, 1, 1, 1, 1, 1, 1, 1, 1, 1, 1, 1, 1, 1, 1, 1, 1, 1, 1, 1, 1, 1, 1, 1, 1, 1, 1, 1, 1, 1, 1, 1, 1, 1, 1, 1, 1, 1, 1, 1, 1, 1, 1, 1, 1, 1, 1, 1, 1, 1, 1, 1, 1, 1, 1, 1, 1, 1, 1, 1, 1, 1, 1, 1, 1, 1, 1, 1, 1, 1, 1, 1, 1, 1, 1, 1, 1, 1, 1, 1, 1, 1, 1, 1, 1, 1, 1, 1, 1, 1, 1, 1, 1, 1, 1, 1, 1, 1, 1, 1, 1, 1, 1, 1, 1, 1, 1, 1, 1, 1, 1, 1, 1, 1, 1, 1, 1, 1, 1, 1, 1, 1, 1, 1, 1, 1, 1, 1, 1, 1, 1, 1, 1, 1, 1, 1, 1, 1, 1, 1, 1, 1, 1, 1, 1, 1, 1, 1, 1, 1, 1, 1, 1, 1, 1, 1, 1, 1, 1, 1, 1, 1, 1, 1, 1, 1, 1, 1, 1, 1, 1, 1, 1, 1, 1, 1, 1, 1, 1, 1, 1, 1, 1, 1, 1, 1, 1, 1, 1, 1, 1, 1, 1, 1, 1, 1, 1, 1, 1, 1, 1, 1, 1, 1, 1, 1, 1, 1, 1, 1, 1, 1, 1, 1, 1, 1, 1, 1, 1, 1, 1, 1, 1, 1, 1, 1, 1, 1, 1, 1, 1, 1, 1, 1, 1, 1, 1, 1, 1, 1, 1, 1, 1, 1, 1, 1, 1, 1, 1, 1, 1, 1, 1, 1, 1, 1, 1, 1, 1, 1, 1, 1, 1, 1, 1, 1, 1, 1, 1, 1, 1, 1, 1, 1, 1, 1, 1, 1, 1, 1, 1, 1, 1, 1, 1, 1, 1, 4 ),
 ( 0.000000000000000000, 0.1320977415905860153 ),
 ( 11.61503284781839973, 12.11278007152779956, 12.61052729523719940, 13.10827451894659923, 13.60602174265599906, 14.10376896636540067, 14.60151619007480051, 15.09926341378420034, 15.59701063749360017, 16.09475786120300000, 16.59250508491239984, 17.09025230862179967, 17.58799953233119950, 18.08574675604059934, 18.58349397974999917, 19.08124120345940256, 19.57898842716880239, 20.07673565087829815, 20.57448287458770153, 21.07223009829710136, 21.56997732200650120, 22.06772454571590103, 22.56547176942530086, 23.06321899313470070, 23.56096621684410053, 24.05871344055349681, 24.55646066426290020, 25.05420788797230003, 25.55195511168169986, 26.04970233539109969, 26.54744955910049953, 27.04519678280990291, 27.54294400651929919, 28.04069123022870258, 28.53843845393820189, 29.03618567764759817, 29.53393290135700155, 30.03168012506639784, 30.52942734877579767, 31.02717457248520105, 31.52492179619460089, 32.02266901990400072, 32.52041624361339700, 33.01816346732280039, 33.51591069103219667, 34.01365791474160005, 34.51140513845099633, 35.00915236216039972, 35.50689958586980310, 36.00464680957920649, 36.50239403328870225, 37.00014125699809853, 37.49788848070750191, 37.99563570441689819, 38.49338292812630158, 38.99113015183569786, 39.48887737554510124, 39.98662459925449753, 40.48437182296390091, 40.98211904667329719, 41.47986627038269347, 41.97761349409210396, 42.47536071780150024, 42.97310794151090363, 43.47085516522029991, 43.96860238892970330, 44.46634961263909958, 44.96409683634850296, 45.46184406005799872, 45.95959128376739500, 46.45733850747679838, 46.95508573118619466, 47.45283295489559805, 47.95058017860500144, 48.44832740231439772, 48.94607462602380110, 49.44382184973320449, 49.94156907344260077, 50.43931629715199705, 50.93706352086140043, 51.43481074457079671, 51.93255796828020010, 52.43030519198959638, 52.92805241569899977, 53.42579963940849552, 53.92354686311789891, 54.42129408682730229, 54.91904131053670568, 55.41678853424610196, 55.91453575795550535, 56.41228298166490163, 56.91003020537429791, 57.40777742908370129, 57.90552465279309757, 58.40327187650250096, 58.90101910021189724, 59.39876632392130062, 59.89651354763069691, 60.39426077134009319, 60.89200799504950368, 61.38975521875889996, 61.88750244246830334, 62.38524966617779910, 62.88299688988720249, 63.38074411359659877, 63.87849133730600215, 64.37623856101539843, 64.87398578472480892, 65.37173300843420520, 65.86948023214360148, 66.36722745585299776, 66.86497467956239404, 67.36272190327179032, 67.86046912698120082, 68.35821635069059710, 68.85596357440000759, 69.35371079810938966, 69.85145802181880015, 70.34920524552829590, 70.84695246923770640, 71.34469969294710268, 71.84244691665649896, 72.34019414036590945, 72.83794136407529152, 73.33568858778470201, 73.83343581149409829, 74.33118303520349457, 74.82893025891290506, 75.32667748262228713, 75.82442470633169762, 76.32217193004109390, 76.81991915375050439, 77.31766637745990067, 77.81541360116929695, 78.31316082487880692, 78.81090804858810372, 79.30865527229759948, 79.80640249600699576, 80.30414971971639204, 80.80189694342580253, 81.29964416713519881, 81.79739139084459509, 82.29513861455400558, 82.79288583826338765, 83.29063306197279815, 83.78838028568220864, 84.28612750939160492, 84.78387473310100120, 85.28162195681041169, 85.77936918051979376, 86.27711640422919004, 86.77486362793860053, 87.27261085164809629, 87.77035807535740730, 88.26810529906688885, 88.76585252277629934, 89.26359974648569562, 89.76134697019510611, 90.25909419390450239, 90.75684141761389867, 91.25458864132330916, 91.75233586503269123, 92.25008308874210172, 92.74783031245149800, 93.24557753616089428, 93.74332475987030477, 94.24107198357970105, 94.73881920728909733, 95.23656643099860730, 95.73431365470798937, 96.23206087841739986, 96.72980810212679614, 97.22755532583620663, 97.72530254954560291, 98.22304977325499920, 98.72079699696439548, 99.21854422067379176, 99.71629144438320225, 100.2140386680929964, 100.7117858918019948, 101.2095331155110074, 101.7072803392210005, 102.2050275629299989, 102.7027747866400063, 103.2005220103490046, 103.6982692340580030, 104.1960164577680104, 104.6937636814769945, 105.1915109051870019, 105.6892581288960002, 106.1870053526049986, 106.6847525763150060, 107.1824998000240043, 107.6802470237339975, 108.1779942474429959, 108.6757414711520084, 109.1734886948620016, 109.6712359185710000, 110.1689831422810073, 110.6667303659899915, 111.1644775896999988, 111.6622248134089972, 112.1599720371179956, 112.6577192608280029, 113.1554664845370013, 113.6532137082469944, 114.1509609319560070, 114.6487081556649912, 115.1464553793749985, 115.6442026030839969, 116.1419498267940043, 116.6396970505030026, 117.1374442742120010, 117.6351914979219941, 118.1329387216309925, 118.6306859453409999, 119.1284331690499982, 119.6261803927589966, 120.1239276164690040, 120.6216748401779881, 121.1194220638879955, 121.6171692875970081, 122.1149165113060064, 122.6126637350159996, 123.1104109587250122, 123.6081581824349911, 124.1059054061440037, 124.6036526298530021, 125.1013998535629952, 125.5991470772720078, 126.0968943009820009, 126.5946415246909993, 127.0923887484010066, 127.5901359721100050, 128.0878831958189892, 128.5856304195290249, 129.0833776432380091, 129.5811248669479880, 130.0788720906570006, 130.5766193143660132, 131.0743665380759921, 131.5721137617849763, 132.0698609854950121, 132.5676082092039962, 133.0653554329129804, 133.5631026566230162, 134.0608498803320003, 134.5585971040419793, 135.0563443277510203, 135.5540915514600044, 136.0518387751699834, 136.5495859988790244, 137.0473332225890033, 137.5450804462979875, 138.0428276700070001, 138.5405748937170074, 139.0383221174259916, 139.5360693411359989, 140.0338165648450115, 140.5315637885539957, 141.0293110122640030, 141.5270582359729872, 142.0248054596829945, 142.5225526833920071, 143.0202999071019860, 143.5180471308109986, 144.0157943545200112, 144.5135415782299901, 145.0112888019389743, 145.5090360256490101, 146.0067832493579942, 146.5045304730670068, 147.0022776967770142, 147.5000249204859983, 147.9977721441960057, 148.4955193679050183, 148.9932665916140024, 149.4910138153239814, 149.9887610390330224, 150.4865082627430013, 150.9842554864519855, 151.4820027101609980, 151.9797499338710054, 152.4774971575799896, 152.9752443812900253, 153.4729916049990095, 153.9707388287079937, 154.4684860524180010, 154.9662332761270136, 155.4639804998369925, 155.9617277235460051, 156.4594749472550177, 156.9572221709649966, 157.4549693946739808, 157.9527166183839881, 158.4504638420930007, 158.9482110658019849, 159.4459582895120207, 159.9437055132210048, 160.4414527369310122, 160.9391999606399963, 161.4369471843500037, 161.9346944080590163, 162.4324416317680004, 162.9301888554780078, 163.4279360791869919, 163.9256833028969993, 164.4234305266059835, 164.9211777503149960, 165.4189249740250034, 165.9166721977339876, 166.4144194214440233, 166.9121666451530075, 167.4099138688619917, 167.9076610925719990 ),
 .UNSPECIFIED. ) ;
#45208=VERTEX_POINT ( 'NONE', #43197 ) ;
#45209=DIRECTION ( 'NONE',  ( 0.000000000000000000, 0.000000000000000000, -1.000000000000000000 ) ) ;
#45216=CARTESIAN_POINT ( 'NONE',  ( 17.90516167065736042, -22.20706873477158894, -78.86948505268290432 ) ) ;
#45218=CARTESIAN_POINT ( 'NONE',  ( 12.14969623865099457, -22.52865004270027782, -56.45901417435899106 ) ) ;
#45219=CARTESIAN_POINT ( 'NONE',  ( 19.33599456300022723, -22.89773004841487847, -33.87591038700520585 ) ) ;
#45224=CARTESIAN_POINT ( 'NONE',  ( 19.18353301396849986, -8.818640789972748806, -44.70157888913149691 ) ) ;
#45240=VECTOR ( 'NONE', #26600, 1000.000000000000000 ) ;
#45246=AXIS2_PLACEMENT_3D ( 'NONE', #25033, #38880, #1217 ) ;
#45249=CARTESIAN_POINT ( 'NONE',  ( 22.87920509261272883, -16.16928286307435769, -72.47886173722646674 ) ) ;
#45250=CARTESIAN_POINT ( 'NONE',  ( 19.34932770686961589, -27.61618894467928698, -22.14999999999998792 ) ) ;
#45258=CARTESIAN_POINT ( 'NONE',  ( 10.72254675965764115, -19.77476841094461690, -47.24445590664701911 ) ) ;
#45260=CARTESIAN_POINT ( 'NONE',  ( 18.67428148936129872, -23.04137577650549673, -66.40756600056339209 ) ) ;
#45275=CARTESIAN_POINT ( 'NONE',  ( 22.63728796599880155, -19.53131553281569666, -32.14999999999999858 ) ) ;
#45278=DIRECTION ( 'NONE',  ( 1.000000000000000000, 0.000000000000000000, 0.000000000000000000 ) ) ;
#45284=CARTESIAN_POINT ( 'NONE',  ( 14.78993376734899989, -8.692590644946379896, -64.28614875238550042 ) ) ;
#45288=CARTESIAN_POINT ( 'NONE',  ( 22.90121965235462653, -15.61618904849089340, -42.45282069170939110 ) ) ;
#45291=CARTESIAN_POINT ( 'NONE',  ( 10.02550514365970002, -12.09062316108200008, -61.61944235566640060 ) ) ;
#45294=CARTESIAN_POINT ( 'NONE',  ( 24.04513741079867017, -15.61618875311435417, -79.79232954107749265 ) ) ;
#45300=CARTESIAN_POINT ( 'NONE',  ( 8.824272223518924818, -12.52937285024285430, -38.63483393334039562 ) ) ;
#45312=CARTESIAN_POINT ( 'NONE',  ( 8.222936843878629887, -16.65173236265913204, -44.46600688272611279 ) ) ;
#45318=ORIENTED_EDGE ( 'NONE', *, *, #18444, .F. ) ;
#45319=CARTESIAN_POINT ( 'NONE',  ( 12.14992535548874919, -8.703598238564360656, -56.84100149383260003 ) ) ;
#45323=CARTESIAN_POINT ( 'NONE',  ( 22.58091822151520134, -20.09091640553009839, -38.20562654191479623 ) ) ;
#45329=CARTESIAN_POINT ( 'NONE',  ( 22.90082190116586602, -14.57027037197810060, -46.79796611410813512 ) ) ;
#45331=CARTESIAN_POINT ( 'NONE',  ( 9.095229150429339882, -16.06244602788209974, -37.82702577713659764 ) ) ;
#45339=CARTESIAN_POINT ( 'NONE',  ( 8.509650980192089875, -12.47724301513739853, -80.63198581093510597 ) ) ;
#45340=CARTESIAN_POINT ( 'NONE',  ( 9.366937397696199596, -15.61618894467949836, -28.45282021618999835 ) ) ;
#45345=CARTESIAN_POINT ( 'NONE',  ( 9.807758692938932654, -10.75452821090589239, -68.71600247355699764 ) ) ;
#45356=CARTESIAN_POINT ( 'NONE',  ( 23.14492557087420010, -16.38339395781729735, -38.48751448508959783 ) ) ;
#45363=CARTESIAN_POINT ( 'NONE',  ( 22.73945831596759959, -19.06202523455430153, -73.22039407203459405 ) ) ;
#45366=DIRECTION ( 'NONE',  ( 0.000000000000000000, 0.000000000000000000, -1.000000000000000000 ) ) ;
#45374=ORIENTED_EDGE ( 'NONE', *, *, #35536, .F. ) ;
#45376=CARTESIAN_POINT ( 'NONE',  ( 16.13393739769620083, -15.61618894467929941, -32.14999999999999858 ) ) ;
#45380=CARTESIAN_POINT ( 'NONE',  ( 19.36900924991789807, -21.88331502330690270, -53.19549840347880121 ) ) ;
#45387=CARTESIAN_POINT ( 'NONE',  ( 10.76140486198004353, -21.45664709977270235, -66.24430264515250144 ) ) ;
#45389=CARTESIAN_POINT ( 'NONE',  ( 14.81123514133290087, -23.75456585884019844, -50.34361688518850286 ) ) ;
#45395=CARTESIAN_POINT ( 'NONE',  ( 19.04528445129210112, -22.47408600855129990, -44.60486606752809990 ) ) ;
#45402=CARTESIAN_POINT ( 'NONE',  ( 14.95141725257159848, -23.77611338154449783, -50.05347842037799211 ) ) ;
#45407=CARTESIAN_POINT ( 'NONE',  ( 14.36259785100323505, -22.20703835893396061, -57.03609844898498693 ) ) ;
#45408=CARTESIAN_POINT ( 'NONE',  ( 22.90108808520262329, -15.61618901356150069, -52.45282226904397049 ) ) ;
#45419=DIRECTION ( 'NONE',  ( 0.000000000000000000, 0.000000000000000000, 1.000000000000000000 ) ) ;
#45435=CARTESIAN_POINT ( 'NONE',  ( 12.62325813502959981, -8.714595329762380160, -81.23899999999999011 ) ) ;
#45443=CARTESIAN_POINT ( 'NONE',  ( 9.543053535305935142, -17.38739775376582841, -45.36949389193291182 ) ) ;
#45447=ORIENTED_EDGE ( 'NONE', *, *, #44756, .T. ) ;
#45452=LINE ( 'NONE', #29185, #45553 ) ;
#45461=AXIS2_PLACEMENT_3D ( 'NONE', #5436, #14062, #9870 ) ;
#45462=AXIS2_PLACEMENT_3D ( 'NONE', #48042, #28096, #19734 ) ;
#45465=CARTESIAN_POINT ( 'NONE',  ( 21.45970996866769909, -9.852258453645399428, -75.02493559595789918 ) ) ;
#45478=B_SPLINE_CURVE_WITH_KNOTS ( 'NONE', 3,
 ( #15178, #51595, #7580, #34561, #31646, #23524, #43730, #47667, #42711, #23265, #2872, #39795, #34820, #30878, #15691, #3130, #10993, #38780 ),
 .UNSPECIFIED., .F., .F.,
 ( 4, 2, 2, 2, 2, 2, 2, 2, 4 ),
 ( 0.000000000000000000, 0.06250001769099303162, 0.1250000353819860632, 0.1875000530729790948, 0.2500000707639721265, 0.3125000884549652413, 0.3750001061459584117, 0.4375001238369515266, 0.5000001415279446970 ),
 .UNSPECIFIED. ) ;
#45484=CARTESIAN_POINT ( 'NONE',  ( 9.042753068858660370, -13.33106331294909985, -42.16657309509579932 ) ) ;
#45487=CARTESIAN_POINT ( 'NONE',  ( 9.366560669795820360, -15.61606439180730099, -33.84717978380999881 ) ) ;
#45497=VERTEX_POINT ( 'NONE', #2779 ) ;
#45503=CONICAL_SURFACE ( 'NONE', #22878, 0.2705324999999987323, 1.029744258676660307 ) ;
#45508=EDGE_CURVE ( 'NONE', #37534, #31864, #35882, .T. ) ;
#45509=EDGE_LOOP ( 'NONE', ( #22713, #533, #35114, #23467 ) ) ;
#45510=CARTESIAN_POINT ( 'NONE',  ( 24.04493738792232804, -15.61196413652903736, -77.50751794856931554 ) ) ;
#45517=CARTESIAN_POINT ( 'NONE',  ( 8.724870845853098800, -13.02920606457709951, -59.11942434271038849 ) ) ;
#45534=CARTESIAN_POINT ( 'NONE',  ( 23.43719904012089827, -15.74375136141919995, -32.14999999999999858 ) ) ;
#45537=CARTESIAN_POINT ( 'NONE',  ( 20.11808254608159174, -22.52870385452940383, -52.12566311908927474 ) ) ;
#45538=EDGE_CURVE ( 'NONE', #31815, #3546, #17722, .T. ) ;
#45541=ORIENTED_EDGE ( 'NONE', *, *, #46320, .F. ) ;
#45542=CARTESIAN_POINT ( 'NONE',  ( 20.79454452025889921, -20.90970388501609989, -61.11739150984060132 ) ) ;
#45545=CARTESIAN_POINT ( 'NONE',  ( 22.90122612410699077, -15.61618894223031440, -74.45282020639018583 ) ) ;
#45546=CARTESIAN_POINT ( 'NONE',  ( 17.90524304069786510, -22.20704573693384987, -42.86948654708372430 ) ) ;
#45549=CARTESIAN_POINT ( 'NONE',  ( 12.10516040838770024, -21.40510202634260040, -77.14635284413569138 ) ) ;
#45553=VECTOR ( 'NONE', #17155, 1000.000000000000000 ) ;
#45558=CARTESIAN_POINT ( 'NONE',  ( 23.98529412776635183, -14.62549353487179182, -39.46773035656453743 ) ) ;
#45560=CARTESIAN_POINT ( 'NONE',  ( 21.54529383757935435, -19.77481161222722861, -54.66115604025567620 ) ) ;
#45562=ORIENTED_EDGE ( 'NONE', *, *, #34132, .F. ) ;
#45572=ORIENTED_EDGE ( 'NONE', *, *, #8046, .T. ) ;
#45573=CARTESIAN_POINT ( 'NONE',  ( 21.54530314169335625, -11.45757904198565491, -68.24448498028382915 ) ) ;
#45576=CARTESIAN_POINT ( 'NONE',  ( 17.16946032303731329, -7.705185438491676919, -53.33399987908899220 ) ) ;
#45577=CARTESIAN_POINT ( 'NONE',  ( 8.223251455316621161, -15.61600507739779786, -72.79233150823699816 ) ) ;
#45578=CARTESIAN_POINT ( 'NONE',  ( 20.90719767621910208, -21.84537299277410227, -36.30437219638799462 ) ) ;
#45581=VECTOR ( 'NONE', #40352, 1000.000000000000000 ) ;
#45585=CARTESIAN_POINT ( 'NONE',  ( 16.13393739769620083, -15.61618894467929941, -32.14999999999999858 ) ) ;
#45595=CARTESIAN_POINT ( 'NONE',  ( 17.16575499510360103, -7.435842179093509863, -79.04760718966269906 ) ) ;
#45599=EDGE_CURVE ( 'NONE', #26915, #48851, #49563, .T. ) ;
#45606=CARTESIAN_POINT ( 'NONE',  ( 24.00165179737271259, -16.46122918689899350, -65.82638113334461138 ) ) ;
#45608=CARTESIAN_POINT ( 'NONE',  ( 23.12128521099250023, -14.65726807586429992, -46.40940759145149741 ) ) ;
#45615=CARTESIAN_POINT ( 'NONE',  ( 9.420195413154878850, -12.38627208764589938, -70.21007469161709480 ) ) ;
#45618=CARTESIAN_POINT ( 'NONE',  ( 8.363305339577767228, -13.92330431280884007, -48.86050672628254432 ) ) ;
#45622=CARTESIAN_POINT ( 'NONE',  ( 24.03373631122487808, -16.07077874150862584, -75.81061925190356021 ) ) ;
#45623=CARTESIAN_POINT ( 'NONE',  ( 12.14983763036492448, -8.703647864385146704, -45.12563104342815734 ) ) ;
#45633=CARTESIAN_POINT ( 'NONE',  ( 23.83903273756216024, -13.54548894720846519, -59.42431809898250350 ) ) ;
#45634=CARTESIAN_POINT ( 'NONE',  ( 17.16954247147122814, -23.52718072034940278, -69.96600351109410099 ) ) ;
#45640=CARTESIAN_POINT ( 'NONE',  ( 24.03381980306747678, -15.16329903094799292, -43.77409963459896858 ) ) ;
#45642=CARTESIAN_POINT ( 'NONE',  ( 20.66633427577639992, -22.50386624515620326, -58.10707212942319444 ) ) ;
#45643=CARTESIAN_POINT ( 'NONE',  ( 22.90071998467804804, -15.61618839864605057, -72.45282571548244732 ) ) ;
#45649=CARTESIAN_POINT ( 'NONE',  ( 18.85638145099070329, -8.681133632583570403, -39.85173020371099284 ) ) ;
#45651=CARTESIAN_POINT ( 'NONE',  ( 9.062362672667880759, -14.30322387553499830, -32.14999999999999858 ) ) ;
#45653=CARTESIAN_POINT ( 'NONE',  ( 15.09848876230330639, -7.705177000359721085, -51.25066365736460483 ) ) ;
#45656=CARTESIAN_POINT ( 'NONE',  ( 16.96908921244479984, -23.81894714880170127, -57.97537152673989880 ) ) ;
#45664=CARTESIAN_POINT ( 'NONE',  ( 17.90512143763164588, -22.20708015056001372, -56.86943258823897196 ) ) ;
#45680=CARTESIAN_POINT ( 'NONE',  ( 22.49007974669167709, -18.02578827406430406, -66.56823315451654821 ) ) ;
#45684=CARTESIAN_POINT ( 'NONE',  ( 22.90093739769620029, -15.61618894467913243, -28.45282021618999835 ) ) ;
#45689=EDGE_CURVE ( 'NONE', #11008, #367, #19270, .T. ) ;
#45691=CIRCLE ( 'NONE', #23070, 12.00000000000000000 ) ;
#45695=CARTESIAN_POINT ( 'NONE',  ( 9.205734167420720482, -3.616188944679329609, -24.15000000000000213 ) ) ;
#45700=CARTESIAN_POINT ( 'NONE',  ( 12.72592204613637179, -21.52908688870203235, -45.11950636888933985 ) ) ;
#45705=EDGE_LOOP ( 'NONE', ( #39699, #2508, #949, #24954 ) ) ;
#45722=CARTESIAN_POINT ( 'NONE',  ( 9.297346275370859559, -11.76290852284069999, -76.45087635510310520 ) ) ;
#45730=FACE_OUTER_BOUND ( 'NONE', #45705, .T. ) ;
#45737=AXIS2_PLACEMENT_3D ( 'NONE', #29439, #9546, #5614 ) ;
#45738=CARTESIAN_POINT ( 'NONE',  ( 20.11801211374420006, -22.52874597533168100, -56.12568250423961302 ) ) ;
#45742=B_SPLINE_CURVE_WITH_KNOTS ( 'NONE', 3,
 ( #33334, #5832, #1116, #1637, #25717, #13699, #13195, #17112, #45928, #49349 ),
 .UNSPECIFIED., .F., .F.,
 ( 4, 1, 1, 1, 1, 1, 1, 4 ),
 ( 0.000000000000000000, 0.07136600257796542335, 0.1505849336415300554, 0.2298038647052530192, 0.3090227957688131410, 0.3882417268325360493, 0.4674606578961007508, 0.5000020751347326042 ),
 .UNSPECIFIED. ) ;
#45744=CARTESIAN_POINT ( 'NONE',  ( 23.54789985460810087, -16.35093721847229986, -53.09878558187529052 ) ) ;
#45749=CARTESIAN_POINT ( 'NONE',  ( 11.34022645397350004, -10.44290231406579927, -74.10929620427420161 ) ) ;
#45750=CARTESIAN_POINT ( 'NONE',  ( 12.14971913517640090, -22.52866241416458948, -62.17430703707206874 ) ) ;
#45752=CYLINDRICAL_SURFACE ( 'NONE', #27323, 6.766999999999998572 ) ;
#45758=CIRCLE ( 'NONE', #34853, 2.576499999999998902 ) ;
#45767=CARTESIAN_POINT ( 'NONE',  ( 24.04341712964290423, -15.44869698543556780, -77.50093736165744929 ) ) ;
#45776=CARTESIAN_POINT ( 'NONE',  ( 23.85371357567289863, -17.02750157961389732, -60.07005151547379995 ) ) ;
#45782=LINE ( 'NONE', #25825, #32030 ) ;
#45798=CARTESIAN_POINT ( 'NONE',  ( 12.69742525567431635, -9.457216345889188247, -50.18517902307924317 ) ) ;
#45802=CARTESIAN_POINT ( 'NONE',  ( 13.36620148929459972, -22.10326818851440223, -73.47554475576528432 ) ) ;
#45807=LINE ( 'NONE', #37938, #11841 ) ;
#45808=CARTESIAN_POINT ( 'NONE',  ( 11.97538130472928408, -21.02759617003068726, -43.16115338163687198 ) ) ;
#45811=CARTESIAN_POINT ( 'NONE',  ( 9.084867081448990689, -15.38561059954679955, -77.46322856839019266 ) ) ;
#45837=CARTESIAN_POINT ( 'NONE',  ( 8.972021738993211315, -18.82457042039120054, -34.87843143724279571 ) ) ;
#45841=B_SPLINE_CURVE_WITH_KNOTS ( 'NONE', 3,
 ( #3367, #23501, #35324, #47904, #12005, #14893, #34801, #51323, #15674, #27960 ),
 .UNSPECIFIED., .F., .F.,
 ( 4, 1, 1, 1, 1, 1, 1, 4 ),
 ( 0.000000000000000000, 0.06104662216038692080, 0.1402655532241073311, 0.2194844842876716440, 0.2987034153513898338, 0.3779223464149541467, 0.4571412774786768329, 0.4999989579104466841 ),
 .UNSPECIFIED. ) ;
#45846=CYLINDRICAL_SURFACE ( 'NONE', #26497, 7.910999999999997812 ) ;
#45852=CARTESIAN_POINT ( 'NONE',  ( 9.366359996283680545, -15.61618532483699973, -43.84717978381009118 ) ) ;
#45854=VECTOR ( 'NONE', #38863, 1000.000000000000000 ) ;
#45875=CARTESIAN_POINT ( 'NONE',  ( 14.15904947058580099, -22.38688878826850015, -47.04315903996049286 ) ) ;
#45882=CARTESIAN_POINT ( 'NONE',  ( 9.771079295578939394, -19.49184774166629808, -69.89319896736259352 ) ) ;
#45891=CARTESIAN_POINT ( 'NONE',  ( 17.01981038939924318, -8.849199620768295915, -57.99448672953406003 ) ) ;
#45895=CARTESIAN_POINT ( 'NONE',  ( 22.52085816870240009, -13.23982764291192815, -32.33926356356143827 ) ) ;
#45898=CARTESIAN_POINT ( 'NONE',  ( 22.46008303819101215, -10.75448409851621001, -59.29930691482108074 ) ) ;
#45903=DIRECTION ( 'NONE',  ( 0.000000000000000000, 0.000000000000000000, 1.000000000000000000 ) ) ;
#45904=CARTESIAN_POINT ( 'NONE',  ( 22.90078658882962159, -15.56738391629757778, -72.45053053649107255 ) ) ;
#45905=CARTESIAN_POINT ( 'NONE',  ( 11.27216508573649278, -9.290094983139432827, -43.08403395730018559 ) ) ;
#45906=CARTESIAN_POINT ( 'NONE',  ( 22.24259769081709948, -21.15396733309309596, -50.02674116093399448 ) ) ;
#45910=EDGE_LOOP ( 'NONE', ( #46849, #1207, #16552, #51789 ) ) ;
#45912=CARTESIAN_POINT ( 'NONE',  ( 8.789551320866550554, -16.86786260806620064, -43.17892530838289389 ) ) ;
#45914=CARTESIAN_POINT ( 'NONE',  ( 10.07444332260010000, -12.10786745998580116, -32.14999999999999858 ) ) ;
#45915=B_SPLINE_CURVE_WITH_KNOTS ( 'NONE', 3,
 ( #20272, #44921, #36265, #628, #374, #16355, #32568, #891, #23686, #49645, #22084, #2190, #38095, #41500, #45179, #33882, #9292, #29947 ),
 .UNSPECIFIED., .F., .F.,
 ( 4, 2, 2, 2, 2, 2, 2, 2, 4 ),
 ( 0.000000000000000000, 0.06250010287737421677, 0.1250002057547484335, 0.1875003086321226364, 0.2500004115094968671, 0.3125005143868710977, 0.3750006172642452729, 0.4375007201416195035, 0.5000008230189937342 ),
 .UNSPECIFIED. ) ;
#45921=CARTESIAN_POINT ( 'NONE',  ( 24.17771624763599903, -17.42736053297119980, -49.57816483399629703 ) ) ;
#45928=CARTESIAN_POINT ( 'NONE',  ( 22.90065710272254762, -15.15489767342495320, -70.82548965592042123 ) ) ;
#45929=EDGE_CURVE ( 'NONE', #21614, #34841, #15097, .T. ) ;
#45934=CARTESIAN_POINT ( 'NONE',  ( 23.98389812145492428, -14.41982823175175810, -65.74426863541066268 ) ) ;
#45938=CARTESIAN_POINT ( 'NONE',  ( 16.84831893358406418, -22.63275635301463140, -57.31488281879011737 ) ) ;
#45942=CARTESIAN_POINT ( 'NONE',  ( 9.367002091613079173, -15.61601527432330094, -39.84717978380999881 ) ) ;
#45960=CARTESIAN_POINT ( 'NONE',  ( 24.04483843941790866, -15.61617050235280679, -77.50767555791956909 ) ) ;
#45967=ORIENTED_EDGE ( 'NONE', *, *, #26317, .F. ) ;
#45970=CARTESIAN_POINT ( 'NONE',  ( 8.317661897737014698, -17.01424986305827858, -34.73604595880143364 ) ) ;
#45972=CARTESIAN_POINT ( 'NONE',  ( 22.72320028845815898, -17.73845357403389045, -48.94698896582607972 ) ) ;
#45981=B_SPLINE_CURVE_WITH_KNOTS ( 'NONE', 3,
 ( #18568, #1813, #22743, #38761, #2856, #2076, #18055, #18820, #34803, #13871, #46114, #34020, #25638, #13618, #46373, #50296, #10461, #29579 ),
 .UNSPECIFIED., .F., .F.,
 ( 4, 2, 2, 2, 2, 2, 2, 2, 4 ),
 ( 0.000000000000000000, 0.06249980390995341084, 0.1249996078199068217, 0.1874994117298602325, 0.2499992156398136434, 0.3124990195497670542, 0.3749988234597204650, 0.4374986273696738759, 0.4999984312796272867 ),
 .UNSPECIFIED. ) ;
#45986=CARTESIAN_POINT ( 'NONE',  ( 23.48373881468570090, -18.36703741633409948, -77.40150352786659482 ) ) ;
#45996=DIRECTION ( 'NONE',  ( 0.000000000000000000, 0.000000000000000000, -1.000000000000000000 ) ) ;
#45998=CARTESIAN_POINT ( 'NONE',  ( 20.99558456173523524, -9.289999057355428747, -43.21596523485415275 ) ) ;
#46008=CARTESIAN_POINT ( 'NONE',  ( 8.802719410737489980, -16.94281517916839874, -58.01035930781959138 ) ) ;
#46010=ORIENTED_EDGE ( 'NONE', *, *, #1633, .T. ) ;
#46014=CARTESIAN_POINT ( 'NONE',  ( 19.75585232009591863, -22.67399444841611000, -61.85680124542592750 ) ) ;
#46029=CARTESIAN_POINT ( 'NONE',  ( 23.99007353491660055, -14.66733099292005704, -77.46942086223019430 ) ) ;
#46031=FACE_OUTER_BOUND ( 'NONE', #51032, .T. ) ;
#46035=CARTESIAN_POINT ( 'NONE',  ( 24.04493184060211419, -15.62634507059355116, -49.50807437602926342 ) ) ;
#46039=AXIS2_PLACEMENT_3D ( 'NONE', #29678, #1659, #9535 ) ;
#46041=CARTESIAN_POINT ( 'NONE',  ( 23.02837255652150006, -19.36499027741710321, -74.17102124479808367 ) ) ;
#46050=CARTESIAN_POINT ( 'NONE',  ( 18.62387150434391003, -22.21488518936683221, -33.23232777544671279 ) ) ;
#46055=EDGE_CURVE ( 'NONE', #14553, #47534, #24400, .T. ) ;
#46061=CARTESIAN_POINT ( 'NONE',  ( 16.32680532830336517, -7.629206002645773310, -45.01510652521700706 ) ) ;
#46067=CARTESIAN_POINT ( 'NONE',  ( 15.24135970174500088, -8.620056853935039953, -70.30678751322059838 ) ) ;
#46068=EDGE_LOOP ( 'NONE', ( #5796, #22013, #26967, #27260 ) ) ;
#46069=AXIS2_PLACEMENT_3D ( 'NONE', #15066, #34970, #22396 ) ;
#46072=CARTESIAN_POINT ( 'NONE',  ( 9.807872590848809580, -10.75438206521125295, -40.71600156056624797 ) ) ;
#46077=CARTESIAN_POINT ( 'NONE',  ( 10.82216332218549937, -10.97640288017059973, -79.68135863817170161 ) ) ;
#46081=CARTESIAN_POINT ( 'NONE',  ( 12.72585196119663387, -21.52904731480777301, -41.11943263090543610 ) ) ;
#46089=CARTESIAN_POINT ( 'NONE',  ( 18.66382343656906073, -8.049420821458873831, -39.11066728049964070 ) ) ;
#46090=CARTESIAN_POINT ( 'NONE',  ( 17.90522083139575571, -22.20705201471875512, -54.86948871813314099 ) ) ;
#46100=EDGE_CURVE ( 'NONE', #42078, #22439, #49656, .T. ) ;
#46103=CARTESIAN_POINT ( 'NONE',  ( 11.27237203167939050, -21.94243938119325321, -48.50066542447320472 ) ) ;
#46108=CARTESIAN_POINT ( 'NONE',  ( 10.81856248199949988, -9.842668606344618709, -43.27563812998649695 ) ) ;
#46114=CARTESIAN_POINT ( 'NONE',  ( 17.90521547582839545, -9.025324361372922155, -78.03615171934956152 ) ) ;
#46117=CARTESIAN_POINT ( 'NONE',  ( 17.77056402554710246, -8.755867344676808273, -42.42172377882659617 ) ) ;
#46118=CARTESIAN_POINT ( 'NONE',  ( 9.367199122489369145, -14.48686353315465780, -43.90031557396017092 ) ) ;
#46123=FACE_OUTER_BOUND ( 'NONE', #7836, .T. ) ;
#46139=CARTESIAN_POINT ( 'NONE',  ( 22.49503038576149905, -12.57003486226449951, -48.31066193697829902 ) ) ;
#46146=EDGE_LOOP ( 'NONE', ( #13702, #34706, #16267, #46010 ) ) ;
#46147=CARTESIAN_POINT ( 'NONE',  ( 22.63968590808610415, -11.22734120214469833, -35.09859433989379340 ) ) ;
#46150=CARTESIAN_POINT ( 'NONE',  ( 24.04493739830126131, -15.61513439321896080, -49.79228809144822776 ) ) ;
#46155=CARTESIAN_POINT ( 'NONE',  ( 24.04213744851809409, -15.84352304058485394, -75.80147181961574177 ) ) ;
#46172=CARTESIAN_POINT ( 'NONE',  ( 14.41409827330783244, -23.35832077669386919, -66.07723603011802993 ) ) ;
#46174=CARTESIAN_POINT ( 'NONE',  ( 15.70667492358600015, -7.382103273874560223, -61.27582937196799406 ) ) ;
#46175=CARTESIAN_POINT ( 'NONE',  ( 16.13393739769620083, -15.61618894467929941, -32.14999999999999858 ) ) ;
#46177=EDGE_CURVE ( 'NONE', #16605, #34659, #11952, .T. ) ;
#46181=CARTESIAN_POINT ( 'NONE',  ( 19.30000495840850050, -8.872101904452820875, -45.87236896454599844 ) ) ;
#46182=CARTESIAN_POINT ( 'NONE',  ( 9.694235770851330258, -12.72427817909970038, -32.14999999999999858 ) ) ;
#46191=B_SPLINE_CURVE_WITH_KNOTS ( 'NONE', 3,
 ( #12468, #28692, #12737, #16652, #44694, #21092, #25007, #4084, #32095, #40502, #8276, #160, #13003, #40249, #33141, #5136, #27922, #24225 ),
 .UNSPECIFIED., .F., .F.,
 ( 4, 2, 2, 2, 2, 2, 2, 2, 4 ),
 ( 0.000000000000000000, 0.06249980336323174290, 0.1249996067264634858, 0.1874994100896952287, 0.2499992134529269716, 0.3124990168161584925, 0.3749988201793900133, 0.4374986235426215342, 0.4999984269058530550 ),
 .UNSPECIFIED. ) ;
#46192=CARTESIAN_POINT ( 'NONE',  ( 8.487904048203290586, -12.53059423256670080, -64.62976173608389274 ) ) ;
#46193=ORIENTED_EDGE ( 'NONE', *, *, #44756, .F. ) ;
#46200=ORIENTED_EDGE ( 'NONE', *, *, #45599, .F. ) ;
#46203=CARTESIAN_POINT ( 'NONE',  ( 23.66141598489997477, -13.08829882855880911, -65.68915168220915746 ) ) ;
#46210=CARTESIAN_POINT ( 'NONE',  ( 24.04493739769619864, -15.61618894467929941, -32.14999999999999858 ) ) ;
#46229=CARTESIAN_POINT ( 'NONE',  ( 24.02198689557684474, -16.27232187956634490, -77.53406589020798378 ) ) ;
#46236=ORIENTED_EDGE ( 'NONE', *, *, #10538, .F. ) ;
#46243=CARTESIAN_POINT ( 'NONE',  ( 16.30959015889229136, -22.38100858503597479, -46.94456242962048975 ) ) ;
#46251=CARTESIAN_POINT ( 'NONE',  ( 10.13557796846099812, -10.55590907640169895, -78.51056856275729956 ) ) ;
#46252=ORIENTED_EDGE ( 'NONE', *, *, #19706, .F. ) ;
#46263=CARTESIAN_POINT ( 'NONE',  ( 17.16942097546588641, -7.705179818260964097, -43.04929360077927925 ) ) ;
#46266=CARTESIAN_POINT ( 'NONE',  ( 9.221338892866903336, -11.63218626646301068, -58.95902533789330136 ) ) ;
#46271=ORIENTED_EDGE ( 'NONE', *, *, #32267, .T. ) ;
#46273=CARTESIAN_POINT ( 'NONE',  ( 11.03203224910719982, -10.18689265573519975, -58.32723503207409976 ) ) ;
#46276=ORIENTED_EDGE ( 'NONE', *, *, #4303, .T. ) ;
#46280=CARTESIAN_POINT ( 'NONE',  ( 16.62037960046279750, -23.51288716533397860, -61.98809266990242861 ) ) ;
#46281=CARTESIAN_POINT ( 'NONE',  ( 22.90093739746964374, -14.73039726793156490, -74.41115356083933818 ) ) ;
#46282=CARTESIAN_POINT ( 'NONE',  ( 9.187091958171290429, -16.78994149695390092, -81.23899999999999011 ) ) ;
#46285=ORIENTED_EDGE ( 'NONE', *, *, #21525, .T. ) ;
#46289=ORIENTED_EDGE ( 'NONE', *, *, #11383, .F. ) ;
#46295=CARTESIAN_POINT ( 'NONE',  ( 21.54527723138343731, -11.45754348139197987, -54.24448937358901901 ) ) ;
#46296=ORIENTED_EDGE ( 'NONE', *, *, #28364, .F. ) ;
#46297=CARTESIAN_POINT ( 'NONE',  ( 9.366937397696199596, -15.61618894467949836, -28.45282021618999835 ) ) ;
#46301=CARTESIAN_POINT ( 'NONE',  ( 12.93456956912729972, -8.450242176170609909, -73.37883193416179495 ) ) ;
#46310=CARTESIAN_POINT ( 'NONE',  ( 22.93787291984029864, -11.70553559853770054, -57.12145717557999802 ) ) ;
#46320=EDGE_CURVE ( 'NONE', #39256, #11348, #13183, .T. ) ;
#46322=CARTESIAN_POINT ( 'NONE',  ( 20.99559369598925329, -21.94237153941632457, -46.08404182597173104 ) ) ;
#46327=CARTESIAN_POINT ( 'NONE',  ( 16.56130706594500168, -8.576308665788749508, -72.36647972087459380 ) ) ;
#46332=CIRCLE ( 'NONE', #45462, 6.766999999999998572 ) ;
#46335=CARTESIAN_POINT ( 'NONE',  ( 24.04523903120960782, -15.61618918343368101, -41.50766953063602926 ) ) ;
#46338=CARTESIAN_POINT ( 'NONE',  ( 22.53697538243309850, -12.65922166745750133, -80.31511008668059048 ) ) ;
#46340=EDGE_CURVE ( 'NONE', #8663, #31804, #19465, .T. ) ;
#46341=CARTESIAN_POINT ( 'NONE',  ( 9.221472552717655091, -19.60042002319641341, -42.34100161347219426 ) ) ;
#46342=CARTESIAN_POINT ( 'NONE',  ( 22.55531716423215016, -17.79663242155549696, -40.55696725089184440 ) ) ;
#46344=DIRECTION ( 'NONE',  ( 1.000000000000000000, 0.000000000000000000, 0.000000000000000000 ) ) ;
#46348=CARTESIAN_POINT ( 'NONE',  ( 24.04334890807969316, -15.44487692207048823, -39.50078007227123322 ) ) ;
#46356=CARTESIAN_POINT ( 'NONE',  ( 9.813805456378791092, -13.11177490670652013, -45.57283591714075044 ) ) ;
#46362=CARTESIAN_POINT ( 'NONE',  ( 14.83305478682455281, -7.784683102609005978, -33.23989205926810087 ) ) ;
#46364=ORIENTED_EDGE ( 'NONE', *, *, #29327, .F. ) ;
#46367=CARTESIAN_POINT ( 'NONE',  ( 18.08605090678410221, -8.015136357095210329, -43.59251385424099823 ) ) ;
#46373=CARTESIAN_POINT ( 'NONE',  ( 22.04685577009000852, -12.20821031989865979, -78.28615093498937938 ) ) ;
#46378=CARTESIAN_POINT ( 'NONE',  ( 22.21314585784340068, -19.19191036455050181, -47.01642178051650234 ) ) ;
#46399=CARTESIAN_POINT ( 'NONE',  ( 22.90093740771515840, -14.73039777584664201, -42.41115299789638726 ) ) ;
#46402=CARTESIAN_POINT ( 'NONE',  ( 22.87897769365210010, -17.67701162083490019, -40.54720669274369982 ) ) ;
#46409=CARTESIAN_POINT ( 'NONE',  ( 19.75483718735349825, -8.653730120499389500, -34.94015647776650013 ) ) ;
#46416=CARTESIAN_POINT ( 'NONE',  ( 9.221435075809175430, -11.63202193102039494, -44.95897662767622904 ) ) ;
#46417=CARTESIAN_POINT ( 'NONE',  ( 11.97539275157860850, -10.20477305846235794, -57.74448680029835401 ) ) ;
#46422=CARTESIAN_POINT ( 'NONE',  ( 22.94861535714161249, -15.61996792560115388, -32.45282170169829783 ) ) ;
#46432=CARTESIAN_POINT ( 'NONE',  ( 9.807738766467371860, -10.75455377863122131, -69.00066549479555533 ) ) ;
#46433=CARTESIAN_POINT ( 'NONE',  ( 23.13768727496389843, -19.96707479845759892, -63.96927302813099203 ) ) ;
#46434=DIRECTION ( 'NONE',  ( 1.000000000000000000, 0.000000000000000000, 0.000000000000000000 ) ) ;
#46438=CARTESIAN_POINT ( 'NONE',  ( 8.765544488224740860, -14.51460838167160006, -57.27989503770729840 ) ) ;
#46441=CARTESIAN_POINT ( 'NONE',  ( 10.66075870651240010, -11.36616899821419935, -32.14999999999999858 ) ) ;
#46444=DIRECTION ( 'NONE',  ( 0.000000000000000000, 0.000000000000000000, -1.000000000000000000 ) ) ;
#46445=CIRCLE ( 'NONE', #6250, 6.999999999999999112 ) ;
#46450=DIRECTION ( 'NONE',  ( 1.000000000000000000, 2.460964292799963328E-14, 0.000000000000000000 ) ) ;
#46451=CARTESIAN_POINT ( 'NONE',  ( 7.910943552303420390, -15.01195974345870177, -66.53101608161080094 ) ) ;
#46460=CARTESIAN_POINT ( 'NONE',  ( 13.58441918655680247, -8.089074747756592743, -80.90380639364062176 ) ) ;
#46474=CARTESIAN_POINT ( 'NONE',  ( 8.223596773276058869, -15.61622589296290009, -36.79233150823699816 ) ) ;
#46476=CARTESIAN_POINT ( 'NONE',  ( 9.221395147010715831, -19.60028769851233932, -76.34101524102744918 ) ) ;
#46484=CARTESIAN_POINT ( 'NONE',  ( 22.90101955563642733, -15.61618902498797290, -36.84717743668400658 ) ) ;
#46489=CARTESIAN_POINT ( 'NONE',  ( 19.54191425816137340, -21.52910907363614967, -44.78617089442926158 ) ) ;
#46490=DIRECTION ( 'NONE',  ( 1.000000000000000000, 0.000000000000000000, 0.000000000000000000 ) ) ;
#46497=CARTESIAN_POINT ( 'NONE',  ( 14.86813092202610065, -23.76360903163029903, -34.34139281033739621 ) ) ;
#46498=LINE ( 'NONE', #10589, #1223 ) ;
#46501=CARTESIAN_POINT ( 'NONE',  ( 22.90093739753756807, -15.61847319962781455, -46.45292522842559890 ) ) ;
#46512=CARTESIAN_POINT ( 'NONE',  ( 14.69232761031780043, -7.902001992735149472, -80.72869863253859535 ) ) ;
#46519=DIRECTION ( 'NONE',  ( 1.000000000000000000, 2.460964292799963328E-14, 0.000000000000000000 ) ) ;
#46535=CARTESIAN_POINT ( 'NONE',  ( 8.747686520039062330, -14.64151345475930022, -56.10910496229269739 ) ) ;
#46540=CARTESIAN_POINT ( 'NONE',  ( 22.90076005816202809, -15.61619656631699193, -74.84717351858182610 ) ) ;
#46556=EDGE_LOOP ( 'NONE', ( #25816, #41375, #47088, #38785 ) ) ;
#46571=CARTESIAN_POINT ( 'NONE',  ( 16.47608743815100141, -23.45644924220759719, -47.77362331007279295 ) ) ;
#46581=CARTESIAN_POINT ( 'NONE',  ( 21.37438191210599925, -20.33663280004660123, -81.08056213787280342 ) ) ;
#46587=CARTESIAN_POINT ( 'NONE',  ( 14.39186542499959920, -8.781882511953600812, -74.26773406640160147 ) ) ;
#46595=CARTESIAN_POINT ( 'NONE',  ( 17.97980580075899937, -22.42319478683919698, -72.86853056670030071 ) ) ;
#46596=DIRECTION ( 'NONE',  ( 0.000000000000000000, 0.000000000000000000, 1.000000000000000000 ) ) ;
#46597=CARTESIAN_POINT ( 'NONE',  ( 20.11812210231799014, -8.703697681116109308, -67.45899657274037509 ) ) ;
#46605=CARTESIAN_POINT ( 'NONE',  ( 14.06318216190721948, -7.911108636151629625, -39.20899184368937540 ) ) ;
#46609=ORIENTED_EDGE ( 'NONE', *, *, #39218, .T. ) ;
#46618=CARTESIAN_POINT ( 'NONE',  ( 23.91381703268126913, -14.11266047478952324, -33.73155400743178234 ) ) ;
#46619=CARTESIAN_POINT ( 'NONE',  ( 9.367509130462650546, -15.61619940421079988, -51.84717978381009118 ) ) ;
#46620=ORIENTED_EDGE ( 'NONE', *, *, #33745, .F. ) ;
#46623=CARTESIAN_POINT ( 'NONE',  ( 16.34117822573379897, -23.46117452980159968, -48.50408758018539146 ) ) ;
#46634=CARTESIAN_POINT ( 'NONE',  ( 10.38933687974309983, -19.70790301870550110, -47.65017322902549779 ) ) ;
#46641=CARTESIAN_POINT ( 'NONE',  ( 14.06335861420489586, -7.911062947393018518, -57.20899805696373619 ) ) ;
#46651=CARTESIAN_POINT ( 'NONE',  ( 12.48250449044332910, -22.66554293210867499, -32.44440577955815996 ) ) ;
#46652=ADVANCED_FACE ( 'NONE', ( #31824 ), #23442, .T. ) ;
#46658=CARTESIAN_POINT ( 'NONE',  ( 22.90119541241246637, -15.61618911972255930, -40.84718082130915207 ) ) ;
#46661=CARTESIAN_POINT ( 'NONE',  ( 23.08048385509150080, -16.83604590837389736, -44.50815324592459632 ) ) ;
#46665=DIRECTION ( 'NONE',  ( 0.000000000000000000, 0.000000000000000000, -1.000000000000000000 ) ) ;
#46667=CARTESIAN_POINT ( 'NONE',  ( 11.43481287156209980, -9.834763918191741894, -80.35009786776028307 ) ) ;
#46673=CARTESIAN_POINT ( 'NONE',  ( 9.561418032738805195, -17.80800118497800710, -67.74410178669948834 ) ) ;
#46674=CARTESIAN_POINT ( 'NONE',  ( 16.04183317652673679, -8.830212154920634049, -61.94856816967541135 ) ) ;
#46676=CARTESIAN_POINT ( 'NONE',  ( 22.37272211114861520, -20.50159377728038734, -45.71923386948059687 ) ) ;
#46690=CARTESIAN_POINT ( 'NONE',  ( 9.366956702331082241, -16.36803544923866838, -33.41746239687156361 ) ) ;
#46693=CARTESIAN_POINT ( 'NONE',  ( 9.304449704656880371, -20.23580125596250312, -64.60302447664000169 ) ) ;
#46696=VECTOR ( 'NONE', #10811, 999.9999999999998863 ) ;
#46700=CARTESIAN_POINT ( 'NONE',  ( 8.709652693353499231, -14.99434456381809966, -51.25925627687220043 ) ) ;
#46702=CARTESIAN_POINT ( 'NONE',  ( 10.41617478728270108, -11.65339576855390114, -32.14999999999999858 ) ) ;
#46705=CARTESIAN_POINT ( 'NONE',  ( 9.668218123015291710, -13.53253765274168785, -61.55199406560768693 ) ) ;
#46706=LINE ( 'NONE', #31443, #25045 ) ;
#46710=CARTESIAN_POINT ( 'NONE',  ( 24.04485473594626299, -15.57709046178206691, -61.50610320075744397 ) ) ;
#46711=CARTESIAN_POINT ( 'NONE',  ( 15.42519564855719949, -23.83083475822490271, -60.03506373439409316 ) ) ;
#46713=CARTESIAN_POINT ( 'NONE',  ( 21.08334951516359723, -21.61472930959210004, -32.14999999999999858 ) ) ;
#46720=CYLINDRICAL_SURFACE ( 'NONE', #24748, 6.766999999999998572 ) ;
#46724=CYLINDRICAL_SURFACE ( 'NONE', #48607, 6.766999999999998572 ) ;
#46735=CARTESIAN_POINT ( 'NONE',  ( 8.222931813264825252, -16.65169553128620450, -76.46600585124562599 ) ) ;
#46739=ADVANCED_FACE ( 'NONE', ( #3297 ), #4946, .F. ) ;
#46741=CARTESIAN_POINT ( 'NONE',  ( 8.332394648117634972, -14.10178411776632679, -80.56861278440374008 ) ) ;
#46742=ORIENTED_EDGE ( 'NONE', *, *, #46958, .F. ) ;
#46756=CYLINDRICAL_SURFACE ( 'NONE', #46952, 7.910999999999997812 ) ;
#46760=CARTESIAN_POINT ( 'NONE',  ( 9.997500756706150682, -21.12317227560119903, -36.55952288011869911 ) ) ;
#46761=DIRECTION ( 'NONE',  ( 0.000000000000000000, 0.000000000000000000, 1.000000000000000000 ) ) ;
#46762=CARTESIAN_POINT ( 'NONE',  ( 8.223013028489239318, -15.61598591435789984, -40.50766849176299189 ) ) ;
#46763=CARTESIAN_POINT ( 'NONE',  ( 9.543081973236891002, -13.84487673733323732, -63.53615373438451996 ) ) ;
#46768=CARTESIAN_POINT ( 'NONE',  ( 16.13393739769620083, -15.61618894467929941, -32.14999999999999858 ) ) ;
#46770=CARTESIAN_POINT ( 'NONE',  ( 22.98728463840710035, -20.20033033726479843, -37.69532517445340147 ) ) ;
#46779=CARTESIAN_POINT ( 'NONE',  ( 23.04646436867740533, -19.60031334711585416, -35.95899589054670997 ) ) ;
#46790=CARTESIAN_POINT ( 'NONE',  ( 21.40914480240369855, -20.87726119049199980, -55.31691565165660052 ) ) ;
#46797=CARTESIAN_POINT ( 'NONE',  ( 20.29261112856793758, -10.20487222028709695, -74.16115355788735997 ) ) ;
#46798=AXIS2_PLACEMENT_3D ( 'NONE', #5293, #48528, #12634 ) ;
#46799=CARTESIAN_POINT ( 'NONE',  ( 9.146229968232489682, -16.61861051933619748, -81.23899999999999011 ) ) ;
#46804=ORIENTED_EDGE ( 'NONE', *, *, #11383, .T. ) ;
#46806=CARTESIAN_POINT ( 'NONE',  ( 23.35918962205809990, -13.17756933140159958, -81.23899999999999011 ) ) ;
#46812=CARTESIAN_POINT ( 'NONE',  ( 12.14980047455250833, -8.703668882721308009, -52.84100284372439660 ) ) ;
#46813=EDGE_LOOP ( 'NONE', ( #17009, #4496, #18556, #10324 ) ) ;
#46819=VECTOR ( 'NONE', #19144, 1000.000000000000000 ) ;
#46831=CARTESIAN_POINT ( 'NONE',  ( 17.43302574698969920, -23.35564096946199797, -51.73456986325390261 ) ) ;
#46839=CARTESIAN_POINT ( 'NONE',  ( 22.04234237985629719, -11.89659550907480146, -32.14999999999999858 ) ) ;
#46840=CARTESIAN_POINT ( 'NONE',  ( 22.90080846266944548, -15.61618871746016879, -44.84718732428002852 ) ) ;
#46845=CARTESIAN_POINT ( 'NONE',  ( 23.04645369194869886, -19.60033335300210666, -45.95903034818195465 ) ) ;
#46848=CARTESIAN_POINT ( 'NONE',  ( 19.32514136844950059, -21.90576575011689897, -69.19772247832989365 ) ) ;
#46849=ORIENTED_EDGE ( 'NONE', *, *, #812, .T. ) ;
#46866=CARTESIAN_POINT ( 'NONE',  ( 9.807714802521521946, -10.75458453011491500, -39.00066019740137335 ) ) ;
#46873=ORIENTED_EDGE ( 'NONE', *, *, #44355, .F. ) ;
#46874=CARTESIAN_POINT ( 'NONE',  ( 24.04493739861623780, -15.61807028455928936, -55.50774772363322285 ) ) ;
#46876=CARTESIAN_POINT ( 'NONE',  ( 13.80275570120679340, -9.247983252851710745, -45.84118090379607935 ) ) ;
#46879=ORIENTED_EDGE ( 'NONE', *, *, #28669, .T. ) ;
#46880=CARTESIAN_POINT ( 'NONE',  ( 24.00414318207540987, -14.78277253604543162, -33.75875707254959934 ) ) ;
#46881=CARTESIAN_POINT ( 'NONE',  ( 9.367491665984019278, -15.61623476897930018, -53.45282021618999124 ) ) ;
#46885=CARTESIAN_POINT ( 'NONE',  ( 12.57046430646940038, -22.60821348122700059, -48.66252544231259236 ) ) ;
#46893=CARTESIAN_POINT ( 'NONE',  ( 21.72984300404249680, -19.90902013391950121, -43.05547522733549926 ) ) ;
#46918=CARTESIAN_POINT ( 'NONE',  ( 18.46354428964319894, -22.27317703432000329, -50.84566773101410320 ) ) ;
#46924=CARTESIAN_POINT ( 'NONE',  ( 17.48707020955630043, -23.34637521513419856, -35.73234578840269648 ) ) ;
#46947=DIRECTION ( 'NONE',  ( 1.000000000000000000, 0.000000000000000000, 0.000000000000000000 ) ) ;
#46949=CARTESIAN_POINT ( 'NONE',  ( 11.84381659772448359, -20.90316959714175482, -33.16995766164247783 ) ) ;
#46952=AXIS2_PLACEMENT_3D ( 'NONE', #50416, #14246, #30472 ) ;
#46954=CARTESIAN_POINT ( 'NONE',  ( 7.996487269003661247, -16.94458100238550102, -58.74082357793219700 ) ) ;
#46958=EDGE_CURVE ( 'NONE', #30218, #25861, #49459, .T. ) ;
#46961=CARTESIAN_POINT ( 'NONE',  ( 9.100096492641728929, -13.16022153293940100, -59.33958724536140039 ) ) ;
#46963=CARTESIAN_POINT ( 'NONE',  ( 11.29194847953979952, -21.71414834165970120, -32.14999999999999858 ) ) ;
#46964=LINE ( 'NONE', #50876, #19811 ) ;
#46971=CARTESIAN_POINT ( 'NONE',  ( 10.48770214978459947, -9.607632692615419856, -58.76756083737620173 ) ) ;
#46972=CARTESIAN_POINT ( 'NONE',  ( 22.24965316085219769, -20.21082810026819843, -32.14999999999999858 ) ) ;
#46975=CARTESIAN_POINT ( 'NONE',  ( 10.72251786782789829, -11.45764625195264763, -59.66113601203608141 ) ) ;
#46983=CARTESIAN_POINT ( 'NONE',  ( 16.13393739769620083, -15.61618894467929941, -28.45282021618999835 ) ) ;
#47009=CARTESIAN_POINT ( 'NONE',  ( 21.67357473421246183, -21.26394646704419600, -77.76073867017645114 ) ) ;
#47016=CARTESIAN_POINT ( 'NONE',  ( 22.90741988437979515, -20.31753503473960265, -37.98546363926389802 ) ) ;
#47031=CARTESIAN_POINT ( 'NONE',  ( 21.23527585712999866, -9.138607094074950865, -37.22001158807159271 ) ) ;
#47043=CARTESIAN_POINT ( 'NONE',  ( 8.223528471986069732, -15.61608932669300032, -46.79233150823699816 ) ) ;
#47051=AXIS2_PLACEMENT_3D ( 'NONE', #8285, #35554, #51793 ) ;
#47052=CARTESIAN_POINT ( 'NONE',  ( 22.26809483981789839, -19.84452275524870046, -69.25944751885360517 ) ) ;
#47059=CARTESIAN_POINT ( 'NONE',  ( 19.54197251953754133, -9.703303650694202531, -74.11948689072868035 ) ) ;
#47066=ORIENTED_EDGE ( 'NONE', *, *, #7531, .T. ) ;
#47068=CARTESIAN_POINT ( 'NONE',  ( 23.59606912666399836, -14.83744389001519970, -81.23899999999999011 ) ) ;
#47086=CARTESIAN_POINT ( 'NONE',  ( 9.366359996283680545, -15.61618532483699973, -43.84717978381009118 ) ) ;
#47087=CARTESIAN_POINT ( 'NONE',  ( 15.00841818149010010, -23.38278116244979898, -49.83331551772699441 ) ) ;
#47088=ORIENTED_EDGE ( 'NONE', *, *, #20137, .T. ) ;
#47098=CARTESIAN_POINT ( 'NONE',  ( 12.71325777259860068, -22.74941205225429997, -32.14999999999999858 ) ) ;
#47101=CARTESIAN_POINT ( 'NONE',  ( 18.38973105523400164, -21.99613282959019500, -81.23899999999999011 ) ) ;
#47103=CARTESIAN_POINT ( 'NONE',  ( 15.09834328865568942, -7.705194580850375452, -71.25065062966832841 ) ) ;
#47104=ORIENTED_EDGE ( 'NONE', *, *, #49527, .T. ) ;
#47105=CARTESIAN_POINT ( 'NONE',  ( 10.65555890294879937, -10.56702432004940029, -36.30437219638799462 ) ) ;
#47107=EDGE_LOOP ( 'NONE', ( #45541, #38283, #44195, #3021 ) ) ;
#47109=CARTESIAN_POINT ( 'NONE',  ( 24.04525281611314824, -15.61618915252426376, -57.50766930885080086 ) ) ;
#47113=CARTESIAN_POINT ( 'NONE',  ( 9.367334447929739127, -15.61631861598680082, -57.84717978380999170 ) ) ;
#47114=FACE_OUTER_BOUND ( 'NONE', #24299, .T. ) ;
#47115=CARTESIAN_POINT ( 'NONE',  ( 14.06332941558105176, -23.32130738014068427, -42.09100129603611151 ) ) ;
#47118=ORIENTED_EDGE ( 'NONE', *, *, #18128, .F. ) ;
#47133=CARTESIAN_POINT ( 'NONE',  ( 18.20216584027211226, -9.151158977368147873, -46.05145469637805888 ) ) ;
#47139=CARTESIAN_POINT ( 'NONE',  ( 14.36277846218990994, -9.025292797381190724, -51.86948580630411954 ) ) ;
#47141=CARTESIAN_POINT ( 'NONE',  ( 23.57355577660240087, -13.11842475088059956, -43.90938957849549951 ) ) ;
#47148=CARTESIAN_POINT ( 'NONE',  ( 14.72053854714299881, -22.52595470508729747, -39.41140439840899745 ) ) ;
#47161=CARTESIAN_POINT ( 'NONE',  ( 21.21190018575672198, -9.527978319518107142, -65.22899277009032915 ) ) ;
#47164=CARTESIAN_POINT ( 'NONE',  ( 8.639346811003365545, -18.23486530003722805, -32.68527743787428363 ) ) ;
#47165=CARTESIAN_POINT ( 'NONE',  ( 8.222937397696199469, -15.61618894467929941, -32.14999999999999858 ) ) ;
#47174=CARTESIAN_POINT ( 'NONE',  ( 21.04132893801929782, -20.68176561141629932, -56.70786862972200026 ) ) ;
#47181=CARTESIAN_POINT ( 'NONE',  ( 19.78225038875690345, -22.56432254316750274, -37.63360013392959758 ) ) ;
#47195=EDGE_LOOP ( 'NONE', ( #13746, #51244, #32337, #25789 ) ) ;
#47198=CARTESIAN_POINT ( 'NONE',  ( 21.75943287738522969, -10.02997240260718392, -49.25881891216832287 ) ) ;
#47200=ORIENTED_EDGE ( 'NONE', *, *, #32159, .F. ) ;
#47202=CARTESIAN_POINT ( 'NONE',  ( 20.99561534953419439, -21.94235425079530089, -35.79933301742941865 ) ) ;
#47205=CARTESIAN_POINT ( 'NONE',  ( 17.16945288656774693, -7.705184376242745437, -69.33399987328904501 ) ) ;
#47206=CARTESIAN_POINT ( 'NONE',  ( 24.24467483768560072, -17.09897626438820240, -59.84988861282279515 ) ) ;
#47210=VERTEX_POINT ( 'NONE', #19475 ) ;
#47211=VERTEX_POINT ( 'NONE', #3243 ) ;
#47213=CARTESIAN_POINT ( 'NONE',  ( 14.78897567340050045, -8.288312597105930379, -49.67487765559970114 ) ) ;
#47220=CARTESIAN_POINT ( 'NONE',  ( 24.04463300525956981, -15.61618495692933273, -55.50767188603018809 ) ) ;
#47222=CARTESIAN_POINT ( 'NONE',  ( 24.20737599035849996, -13.94217878954719936, -71.44258980755520838 ) ) ;
#47223=CARTESIAN_POINT ( 'NONE',  ( 21.03039687228480048, -21.66520938706709742, -32.14999999999999858 ) ) ;
#47226=CARTESIAN_POINT ( 'NONE',  ( 10.22096080473554558, -12.20830889007442721, -59.61947214002722006 ) ) ;
#47229=VECTOR ( 'NONE', #40501, 1000.000000000000000 ) ;
#47233=CARTESIAN_POINT ( 'NONE',  ( 8.330546865915890109, -14.12868128525956202, -64.85222125236775526 ) ) ;
#47236=CARTESIAN_POINT ( 'NONE',  ( 9.707462416632068880, -11.84695651314819997, -77.40150352786659482 ) ) ;
#47243=EDGE_CURVE ( 'NONE', #44797, #26214, #24206, .T. ) ;
#47244=CARTESIAN_POINT ( 'NONE',  ( 24.02040458163389047, -16.29250541910551320, -61.53487776366242201 ) ) ;
#47245=CARTESIAN_POINT ( 'NONE',  ( 23.04645858955461435, -11.63205371370243313, -37.62566744954315112 ) ) ;
#47258=ORIENTED_EDGE ( 'NONE', *, *, #46177, .T. ) ;
#47260=CARTESIAN_POINT ( 'NONE',  ( 12.14977014199372007, -22.52869264618974299, -78.17430626959000506 ) ) ;
#47263=EDGE_LOOP ( 'NONE', ( #29067, #8771, #16624, #6574 ) ) ;
#47272=CARTESIAN_POINT ( 'NONE',  ( 8.222920351416638240, -16.35567762970788408, -50.76256645574265747 ) ) ;
#47275=CARTESIAN_POINT ( 'NONE',  ( 15.24817818853745699, -8.849184231705592651, -63.91115456625989566 ) ) ;
#47277=CARTESIAN_POINT ( 'NONE',  ( 8.475754741739530473, -13.90184186731750060, -79.08259497074239164 ) ) ;
#47278=CARTESIAN_POINT ( 'NONE',  ( 20.29258223004187656, -21.02752873420811852, -36.74448494115042507 ) ) ;
#47280=ADVANCED_FACE ( 'NONE', ( #35199 ), #35462, .T. ) ;
#47286=CARTESIAN_POINT ( 'NONE',  ( 21.82199750194000032, -10.20939643101050009, -81.04557435679289767 ) ) ;
#47305=CARTESIAN_POINT ( 'NONE',  ( 9.367462981151710721, -15.61611677545310073, -63.45282021618999124 ) ) ;
#47309=CARTESIAN_POINT ( 'NONE',  ( 11.39453405654320051, -9.867732603346510700, -64.34787379290919773 ) ) ;
#47317=CARTESIAN_POINT ( 'NONE',  ( 11.29901709724989978, -9.719023915928469037, -81.23899999999999011 ) ) ;
#47323=CARTESIAN_POINT ( 'NONE',  ( 23.54267176174619891, -15.98686785723220005, -81.23899999999999011 ) ) ;
#47328=CARTESIAN_POINT ( 'NONE',  ( 23.04646809146690956, -11.63207151544812668, -63.62566669017797949 ) ) ;
#47329=VECTOR ( 'NONE', #36409, 1000.000000000000000 ) ;
#47342=CARTESIAN_POINT ( 'NONE',  ( 21.74587401173889845, -10.13048792993660108, -49.04112620709079806 ) ) ;
#47356=CARTESIAN_POINT ( 'NONE',  ( 20.99565159046659701, -21.94232532607928476, -37.79933726366152058 ) ) ;
#47359=CARTESIAN_POINT ( 'NONE',  ( 11.71654021571490034, -21.61563036701890184, -33.76936640235209808 ) ) ;
#47368=CARTESIAN_POINT ( 'NONE',  ( 23.04647490150570732, -11.63208424308849409, -67.34099948691266491 ) ) ;
#47373=CARTESIAN_POINT ( 'NONE',  ( 16.13393739769620083, -15.61618894467929941, -40.14999999999999858 ) ) ;
#47381=CARTESIAN_POINT ( 'NONE',  ( 23.64088771302849068, -18.16524997366306593, -55.61181301324595694 ) ) ;
#47385=FACE_OUTER_BOUND ( 'NONE', #43184, .T. ) ;
#47386=LINE ( 'NONE', #22982, #23552 ) ;
#47393=CARTESIAN_POINT ( 'NONE',  ( 22.46012663862139291, -20.47783394216208919, -48.00066642373527515 ) ) ;
#47397=CARTESIAN_POINT ( 'NONE',  ( 23.75919800905029788, -17.47149166944270249, -50.08846620145769890 ) ) ;
#47398=AXIS2_PLACEMENT_3D ( 'NONE', #42811, #35182, #46490 ) ;
#47404=CARTESIAN_POINT ( 'NONE',  ( 22.40972105350460097, -18.83443360286479873, -56.99800709453259628 ) ) ;
#47410=DIRECTION ( 'NONE',  ( 0.000000000000000000, 0.000000000000000000, -1.000000000000000000 ) ) ;
#47414=CIRCLE ( 'NONE', #42388, 12.00000000000000000 ) ;
#47428=CARTESIAN_POINT ( 'NONE',  ( 22.90122612410699077, -15.61618894223031440, -74.45282020639018583 ) ) ;
#47431=CARTESIAN_POINT ( 'NONE',  ( 17.18162999253079803, -22.59077846115649990, -52.90535993866819808 ) ) ;
#47436=CARTESIAN_POINT ( 'NONE',  ( 8.827366647101261066, -18.47988795989260069, -40.16860592796539464 ) ) ;
#47445=CARTESIAN_POINT ( 'NONE',  ( 8.223069265346360623, -15.61598766837350105, -56.50766849176299189 ) ) ;
#47450=CARTESIAN_POINT ( 'NONE',  ( 23.96601493904643476, -16.76745162487207352, -43.83877825466511524 ) ) ;
#47451=CARTESIAN_POINT ( 'NONE',  ( 9.577040858161863568, -11.12070122226039892, -76.69910475397914240 ) ) ;
#47453=CARTESIAN_POINT ( 'NONE',  ( 17.75165935666287353, -7.846201640880932082, -49.07295956893727151 ) ) ;
#47455=CARTESIAN_POINT ( 'NONE',  ( 8.223606718150689332, -15.61618413875730127, -36.50766849176289952 ) ) ;
#47459=CARTESIAN_POINT ( 'NONE',  ( 23.83903407973103228, -13.54549564773435222, -69.70900104909422623 ) ) ;
#47460=CARTESIAN_POINT ( 'NONE',  ( 19.74175079524499665, -8.202255943660620829, -77.43649130894638688 ) ) ;
#47462=CARTESIAN_POINT ( 'NONE',  ( 16.13393739769620083, -15.61618894467929941, -28.45282021618999835 ) ) ;
#47466=CARTESIAN_POINT ( 'NONE',  ( 23.56515851745149703, -15.08360423362579894, -52.20988344963559769 ) ) ;
#47477=CARTESIAN_POINT ( 'NONE',  ( 8.322288761255229872, -12.97784357498919938, -74.61134705009999379 ) ) ;
#47478=CARTESIAN_POINT ( 'NONE',  ( 20.09253040080429997, -22.41528281924199817, -32.14999999999999858 ) ) ;
#47489=CARTESIAN_POINT ( 'NONE',  ( 20.18579949284930208, -21.86831717169179967, -74.54962200957619700 ) ) ;
#47492=CARTESIAN_POINT ( 'NONE',  ( 24.04490452168148451, -15.61618923948461557, -69.79232899952297942 ) ) ;
#47495=CARTESIAN_POINT ( 'NONE',  ( 16.37276388111695624, -23.52373572102649746, -61.99806274663424688 ) ) ;
#47496=CARTESIAN_POINT ( 'NONE',  ( 17.16946792601238059, -7.705186524535062809, -37.33399987008601073 ) ) ;
#47497=CARTESIAN_POINT ( 'NONE',  ( 9.366426063424411197, -15.61626247110940113, -71.45282021618990598 ) ) ;
#47509=CARTESIAN_POINT ( 'NONE',  ( 9.543101276256674481, -17.38757133593738047, -59.36948685926856939 ) ) ;
#47512=CARTESIAN_POINT ( 'NONE',  ( 8.222923464767577073, -16.65163797661076472, -78.46599076961739172 ) ) ;
#47515=CARTESIAN_POINT ( 'NONE',  ( 17.94759653393067467, -22.18343915517746723, -80.86687695485406380 ) ) ;
#47520=CARTESIAN_POINT ( 'NONE',  ( 17.73895862251804800, -23.38184506017118380, -50.22737503043536123 ) ) ;
#47521=CARTESIAN_POINT ( 'NONE',  ( 22.55207325930935625, -17.84354922411136357, -50.55919571307475735 ) ) ;
#47523=CARTESIAN_POINT ( 'NONE',  ( 22.72481167109963351, -13.84494687364363408, -64.36948891632977166 ) ) ;
#47525=CARTESIAN_POINT ( 'NONE',  ( 8.380091037990700542, -16.82640141431589953, -74.96321055543440082 ) ) ;
#47533=CARTESIAN_POINT ( 'NONE',  ( 13.96167471279819949, -23.57005564816219945, -46.09253186719709561 ) ) ;
#47534=VERTEX_POINT ( 'NONE', #50617 ) ;
#47552=CARTESIAN_POINT ( 'NONE',  ( 9.366927950383001189, -16.50191825106599808, -63.41115275078119851 ) ) ;
#47555=CARTESIAN_POINT ( 'NONE',  ( 10.40593262108130013, -10.85208823022969860, -62.28818158525499626 ) ) ;
#47556=CARTESIAN_POINT ( 'NONE',  ( 18.20466015165334639, -7.911101059566782112, -77.37566301139611369 ) ) ;
#47563=FACE_OUTER_BOUND ( 'NONE', #16108, .T. ) ;
#47564=CARTESIAN_POINT ( 'NONE',  ( 8.985990923957119847, -15.50133730118559861, -81.23899999999999011 ) ) ;
#47571=CARTESIAN_POINT ( 'NONE',  ( 23.46520187981169769, -13.64785293624529849, -81.23899999999999011 ) ) ;
#47573=EDGE_CURVE ( 'NONE', #39379, #27118, #46706, .T. ) ;
#47578=CARTESIAN_POINT ( 'NONE',  ( 15.78285172300917694, -8.812156430328993650, -79.93657430706403488 ) ) ;
#47592=CARTESIAN_POINT ( 'NONE',  ( 8.337315010399510840, -16.51029605967550040, -64.25116097130579362 ) ) ;
#47595=CARTESIAN_POINT ( 'NONE',  ( 9.366365918819754555, -15.58120503557203484, -75.84882408509788831 ) ) ;
#47604=CARTESIAN_POINT ( 'NONE',  ( 24.04493292379381231, -15.60707448483026738, -45.50730927894573341 ) ) ;
#47607=ORIENTED_EDGE ( 'NONE', *, *, #12523, .T. ) ;
#47608=CARTESIAN_POINT ( 'NONE',  ( 18.38973105523419704, -21.99613282959019500, -81.23899999999999011 ) ) ;
#47609=CARTESIAN_POINT ( 'NONE',  ( 15.24809864170513052, -22.38318404622074098, -76.99450079008921932 ) ) ;
#47610=VERTEX_POINT ( 'NONE', #40618 ) ;
#47624=CARTESIAN_POINT ( 'NONE',  ( 8.428810482305360452, -13.54560713631422963, -38.87566260121617034 ) ) ;
#47628=ORIENTED_EDGE ( 'NONE', *, *, #17574, .T. ) ;
#47632=CARTESIAN_POINT ( 'NONE',  ( 22.89540641129645948, -15.32079363685985030, -46.43893137664500870 ) ) ;
#47638=CARTESIAN_POINT ( 'NONE',  ( 23.04647732774926183, -19.60028910769844757, -47.95899984034043939 ) ) ;
#47641=CARTESIAN_POINT ( 'NONE',  ( 8.222476383702659319, -15.61632876086509825, -54.50766849176299900 ) ) ;
#47644=CARTESIAN_POINT ( 'NONE',  ( 21.94814240175420039, -20.88703022120900243, -50.24690406358499217 ) ) ;
#47651=LINE ( 'NONE', #3887, #19560 ) ;
#47652=CARTESIAN_POINT ( 'NONE',  ( 22.91931868946720030, -13.69234906055819856, -48.75923826391610305 ) ) ;
#47657=CARTESIAN_POINT ( 'NONE',  ( 8.223606718150689332, -15.61618413875730127, -36.50766849176289952 ) ) ;
#47660=CARTESIAN_POINT ( 'NONE',  ( 8.222476383702659319, -15.61632876086509825, -54.50766849176299900 ) ) ;
#47667=CARTESIAN_POINT ( 'NONE',  ( 14.06335050055401936, -23.32131284038766950, -58.37566472363047154 ) ) ;
#47678=CARTESIAN_POINT ( 'NONE',  ( 21.54530251441495992, -19.77479970165442325, -74.66115355887134797 ) ) ;
#47680=CYLINDRICAL_SURFACE ( 'NONE', #29031, 7.910999999999997812 ) ;
#47681=CARTESIAN_POINT ( 'NONE',  ( 21.89967498990359829, -19.67806396915169742, -54.64817642206789827 ) ) ;
#47686=CARTESIAN_POINT ( 'NONE',  ( 10.06545220148790065, -10.64022314831530025, -46.50612041305500099 ) ) ;
#47695=ORIENTED_EDGE ( 'NONE', *, *, #20164, .F. ) ;
#47704=CARTESIAN_POINT ( 'NONE',  ( 17.08918660137072720, -7.732233853712758176, -49.04612841921350963 ) ) ;
#47708=CARTESIAN_POINT ( 'NONE',  ( 8.223069265346360623, -15.61598766837350105, -56.50766849176299189 ) ) ;
#47709=CARTESIAN_POINT ( 'NONE',  ( 10.63467927709140071, -9.472828286302069856, -75.05992337703769124 ) ) ;
#47715=CARTESIAN_POINT ( 'NONE',  ( 19.77582419784589973, -9.116700169395430819, -67.89523180023219595 ) ) ;
#47716=VECTOR ( 'NONE', #14747, 1000.000000000000000 ) ;
#47719=CARTESIAN_POINT ( 'NONE',  ( 12.40813258608080005, -22.56902654875089809, -32.14999999999999858 ) ) ;
#47720=AXIS2_PLACEMENT_3D ( 'NONE', #29037, #29547, #5211 ) ;
#47725=CARTESIAN_POINT ( 'NONE',  ( 13.58396071722250120, -7.775248973093270344, -68.90758401351938289 ) ) ;
#47726=CARTESIAN_POINT ( 'NONE',  ( 23.43844683284619990, -16.50873768209440229, -32.14999999999999858 ) ) ;
#47730=CARTESIAN_POINT ( 'NONE',  ( 22.90093741614429135, -14.73038836730692580, -60.41114393275640282 ) ) ;
#47738=CARTESIAN_POINT ( 'NONE',  ( 14.06314509805251411, -23.32125965905213150, -72.37568720284336621 ) ) ;
#47740=CARTESIAN_POINT ( 'NONE',  ( 15.79570006403920068, -23.05878857862889930, -70.74711331852249430 ) ) ;
#47743=CARTESIAN_POINT ( 'NONE',  ( 12.14985788165700420, -22.52874148118596054, -70.45899922006387328 ) ) ;
#47767=CARTESIAN_POINT ( 'NONE',  ( 16.47165959384855682, -23.52718952250380369, -77.99408671543044136 ) ) ;
#47771=CARTESIAN_POINT ( 'NONE',  ( 12.14989278840985598, -8.703616661238887886, -34.84100081756681533 ) ) ;
#47772=CARTESIAN_POINT ( 'NONE',  ( 21.91218854648699832, -21.49790074630919889, -40.04515584691789343 ) ) ;
#47773=CARTESIAN_POINT ( 'NONE',  ( 20.11807550982419102, -22.52870806245297786, -67.84099995454940313 ) ) ;
#47774=CARTESIAN_POINT ( 'NONE',  ( 24.04493642151950539, -15.62074925824641980, -49.79251394409821785 ) ) ;
#47778=CARTESIAN_POINT ( 'NONE',  ( 17.24979877144579987, -7.848203483545518999, -79.55790855712419329 ) ) ;
#47786=CARTESIAN_POINT ( 'NONE',  ( 20.40418685453369818, -8.562984688076911155, -41.18095814125259579 ) ) ;
#47793=CARTESIAN_POINT ( 'NONE',  ( 22.90092413496008561, -15.63002623182754824, -56.45347593842252110 ) ) ;
#47802=CARTESIAN_POINT ( 'NONE',  ( 24.04487853986463008, -15.61618860033810030, -61.79233400586811342 ) ) ;
#47805=CARTESIAN_POINT ( 'NONE',  ( 23.94343461585225086, -14.32673262226892064, -75.74025377681455495 ) ) ;
#47806=CARTESIAN_POINT ( 'NONE',  ( 17.01970573595322378, -22.38319328302324251, -62.91115104534193847 ) ) ;
#47810=CARTESIAN_POINT ( 'NONE',  ( 9.225026380130959325, -12.82806360859640016, -64.18943593078189735 ) ) ;
#47813=ORIENTED_EDGE ( 'NONE', *, *, #48872, .T. ) ;
#47818=CARTESIAN_POINT ( 'NONE',  ( 9.002563573228689719, -15.69178742396579906, -81.23899999999999011 ) ) ;
#47820=EDGE_CURVE ( 'NONE', #42604, #49152, #1818, .T. ) ;
#47826=CARTESIAN_POINT ( 'NONE',  ( 23.60004879085900242, -15.23558838188970022, -81.23899999999999011 ) ) ;
#47827=CARTESIAN_POINT ( 'NONE',  ( 24.04527493495583457, -15.61618894149694192, -73.79233149842438877 ) ) ;
#47831=CARTESIAN_POINT ( 'NONE',  ( 11.27225130591669178, -9.290029843429451262, -52.79933604972921302 ) ) ;
#47844=CARTESIAN_POINT ( 'NONE',  ( 22.70037966282230002, -11.31867987988980140, -67.10304248959599249 ) ) ;
#47848=CARTESIAN_POINT ( 'NONE',  ( 9.367334447929739127, -15.61631861598680082, -57.84717978380999170 ) ) ;
#47866=CARTESIAN_POINT ( 'NONE',  ( 9.612189680941000347, -12.93116213325089880, -79.97149710298209868 ) ) ;
#47876=CARTESIAN_POINT ( 'NONE',  ( 8.222959511069191763, -14.58047957805684902, -66.54933504152046453 ) ) ;
#47895=EDGE_LOOP ( 'NONE', ( #50463, #22912, #41697, #23430 ) ) ;
#47897=CIRCLE ( 'NONE', #38699, 7.910999999999997812 ) ;
#47899=DIRECTION ( 'NONE',  ( 1.071169953407190059E-15, 3.740764114965449782E-16, -1.000000000000000000 ) ) ;
#47901=CARTESIAN_POINT ( 'NONE',  ( 22.17654210678049864, -10.60882677270349994, -55.79222923803829559 ) ) ;
#47903=LINE ( 'NONE', #20875, #11285 ) ;
#47904=CARTESIAN_POINT ( 'NONE',  ( 11.64736116878922800, -10.17438842308481561, -64.12771089026477966 ) ) ;
#47907=CARTESIAN_POINT ( 'NONE',  ( 17.90522632298731764, -22.20705046304115626, -38.86948870843807669 ) ) ;
#47908=CARTESIAN_POINT ( 'NONE',  ( 9.727227354358010558, -18.56519311474089662, -49.70986543667950031 ) ) ;
#47909=CARTESIAN_POINT ( 'NONE',  ( 11.97521819796847886, -10.20490511463765593, -43.74446124033270422 ) ) ;
#47915=CARTESIAN_POINT ( 'NONE',  ( 8.222938026844484938, -14.58063686431121120, -36.54933528226675321 ) ) ;
#47916=EDGE_CURVE ( 'NONE', #3482, #31302, #38776, .T. ) ;
#47918=EDGE_CURVE ( 'NONE', #25861, #35823, #30580, .T. ) ;
#47919=DIRECTION ( 'NONE',  ( 0.000000000000000000, 0.000000000000000000, -1.000000000000000000 ) ) ;
#47923=CARTESIAN_POINT ( 'NONE',  ( 19.90518632087238515, -8.638643742139599624, -65.16544870160124958 ) ) ;
#47932=ORIENTED_EDGE ( 'NONE', *, *, #11059, .F. ) ;
#47934=CARTESIAN_POINT ( 'NONE',  ( 12.72604000439749505, -21.52915361658608617, -75.11948688679269992 ) ) ;
#47937=CARTESIAN_POINT ( 'NONE',  ( 9.507110174141249814, -18.03025597891349818, -57.34162007823109519 ) ) ;
#47941=VERTEX_POINT ( 'NONE', #30051 ) ;
#47942=CARTESIAN_POINT ( 'NONE',  ( 22.91038278696110098, -11.65809141310010055, -41.11923310072890558 ) ) ;
#47954=AXIS2_PLACEMENT_3D ( 'NONE', #21200, #33256, #17295 ) ;
#47957=CARTESIAN_POINT ( 'NONE',  ( 8.222937397696199469, -15.61618894467929941, -32.14999999999999858 ) ) ;
#47960=CARTESIAN_POINT ( 'NONE',  ( 8.412057011451022248, -13.65889379580994145, -48.58652191394980946 ) ) ;
#47962=CARTESIAN_POINT ( 'NONE',  ( 17.16948262820418236, -23.52718926469356120, -35.96600018786083552 ) ) ;
#47964=CARTESIAN_POINT ( 'NONE',  ( 9.366715917462860475, -15.61603296970410071, -51.45282021618999835 ) ) ;
#47967=CARTESIAN_POINT ( 'NONE',  ( 19.25379761885410446, -7.984073100670400436, -71.41585254811130312 ) ) ;
#47972=CARTESIAN_POINT ( 'NONE',  ( 9.936147368269889313, -11.48168866577140079, -67.41991821385050798 ) ) ;
#47975=CARTESIAN_POINT ( 'NONE',  ( 9.944491257508540016, -20.09032267960250095, -32.14999999999999858 ) ) ;
#47981=CARTESIAN_POINT ( 'NONE',  ( 20.73645074902539776, -22.45721164306379691, -73.81915773946390402 ) ) ;
#47985=B_SPLINE_CURVE_WITH_KNOTS ( 'NONE', 3,
 ( #48173, #36892, #32672, #44236, #20631, #4404, #48700, #20372, #16456, #16200, #51848, #36361, #9119, #992, #15952, #25069, #43982, #32410 ),
 .UNSPECIFIED., .F., .F.,
 ( 4, 2, 2, 2, 2, 2, 2, 2, 4 ),
 ( 0.4999996453781777039, 0.5624996897059054701, 0.6249997340336331808, 0.6874997783613608915, 0.7499998226890887132, 0.8124998670168164239, 0.8749999113445443566, 0.9374999556722721783, 1.000000000000000000 ),
 .UNSPECIFIED. ) ;
#47987=CARTESIAN_POINT ( 'NONE',  ( 22.72480800315950233, -13.84492856927137794, -60.36947377164519679 ) ) ;
#47991=ORIENTED_EDGE ( 'NONE', *, *, #24833, .T. ) ;
#47994=CARTESIAN_POINT ( 'NONE',  ( 17.37335237021048684, -23.49782243706750862, -66.24288056328899188 ) ) ;
#47996=CARTESIAN_POINT ( 'NONE',  ( 20.18929396301779988, -9.366326791539540508, -73.91587056106729392 ) ) ;
#48002=DIRECTION ( 'NONE',  ( 0.000000000000000000, 0.000000000000000000, -1.000000000000000000 ) ) ;
#48005=CARTESIAN_POINT ( 'NONE',  ( 9.367580626013266354, -15.02763158364818352, -67.87485971631076609 ) ) ;
#48014=ORIENTED_EDGE ( 'NONE', *, *, #35749, .T. ) ;
#48015=EDGE_LOOP ( 'NONE', ( #30414, #21096, #35248, #49757 ) ) ;
#48019=CARTESIAN_POINT ( 'NONE',  ( 20.11802340169658265, -8.703638663582415447, -59.17429998693496884 ) ) ;
#48020=CARTESIAN_POINT ( 'NONE',  ( 15.69633972878563632, -8.840832517840322424, -49.93237391020534943 ) ) ;
#48024=CARTESIAN_POINT ( 'NONE',  ( 22.46011990848845130, -10.75453471358487434, -35.29933276554705657 ) ) ;
#48026=CARTESIAN_POINT ( 'NONE',  ( 8.005967485763431313, -17.00140559439540056, -42.73859950308099798 ) ) ;
#48036=CARTESIAN_POINT ( 'NONE',  ( 8.929533209956950657, -12.50435150369649939, -81.14228717839660021 ) ) ;
#48042=CARTESIAN_POINT ( 'NONE',  ( 16.13393739769620083, -15.61618894467929941, -32.14999999999999858 ) ) ;
#48043=CARTESIAN_POINT ( 'NONE',  ( 7.905295319356000050, -16.13788833661330102, -38.48751448508949835 ) ) ;
#48048=CARTESIAN_POINT ( 'NONE',  ( 18.08024390712562024, -23.31108359709902800, -39.92886493447741714 ) ) ;
#48049=CARTESIAN_POINT ( 'NONE',  ( 20.11812365984145146, -22.52867927707677254, -64.12566632045644610 ) ) ;
#48050=CARTESIAN_POINT ( 'NONE',  ( 22.87920530775617323, -16.16928024828671084, -56.47886066825785178 ) ) ;
#48053=DIRECTION ( 'NONE',  ( 0.000000000000000000, 0.000000000000000000, 1.000000000000000000 ) ) ;
#48059=DIRECTION ( 'NONE',  ( 0.000000000000000000, 0.000000000000000000, -1.000000000000000000 ) ) ;
#48066=CARTESIAN_POINT ( 'NONE',  ( 20.11812447700029693, -8.703699102511096797, -73.17433468560057008 ) ) ;
#48072=CARTESIAN_POINT ( 'NONE',  ( 12.06548384426220011, -9.083113220787328856, -81.23899999999999011 ) ) ;
#48079=CARTESIAN_POINT ( 'NONE',  ( 23.40109865623389851, -16.77414853570180142, -81.23899999999999011 ) ) ;
#48081=CARTESIAN_POINT ( 'NONE',  ( 18.62287818089072644, -13.80786761600151102, -22.14999999999999858 ) ) ;
#48083=CARTESIAN_POINT ( 'NONE',  ( 13.88552899772848015, -22.30103889375535431, -35.45045784522820753 ) ) ;
#48092=CARTESIAN_POINT ( 'NONE',  ( 14.89345596857563869, -8.902066654702450066, -39.89498197283463554 ) ) ;
#48098=CARTESIAN_POINT ( 'NONE',  ( 22.40813251518540028, -10.90224963547539971, -61.08240372876090163 ) ) ;
#48105=EDGE_CURVE ( 'NONE', #34841, #51612, #40197, .T. ) ;
#48116=CARTESIAN_POINT ( 'NONE',  ( 11.31465934174710064, -9.934475242017009933, -32.34342564320699864 ) ) ;
#48121=LINE ( 'NONE', #40257, #2812 ) ;
#48124=CARTESIAN_POINT ( 'NONE',  ( 18.20459725043313526, -23.32129460736597082, -78.20899634472944228 ) ) ;
#48126=CARTESIAN_POINT ( 'NONE',  ( 23.04646243352704005, -19.60031697277015539, -51.67433271905296976 ) ) ;
#48132=FACE_OUTER_BOUND ( 'NONE', #43001, .T. ) ;
#48150=DIRECTION ( 'NONE',  ( 0.000000000000000000, 0.000000000000000000, -1.000000000000000000 ) ) ;
#48151=CARTESIAN_POINT ( 'NONE',  ( 14.37574545305890084, -23.26442460248919986, -56.58441854867449905 ) ) ;
#48158=CARTESIAN_POINT ( 'NONE',  ( 10.98133074358459993, -10.80025665254149914, -52.08643336858800410 ) ) ;
#48160=CARTESIAN_POINT ( 'NONE',  ( 23.83903855266338923, -13.54551783030957779, -41.70899764726264891 ) ) ;
#48166=CARTESIAN_POINT ( 'NONE',  ( 17.90517255728681434, -9.025312231919581762, -38.03615537510474809 ) ) ;
#48168=CARTESIAN_POINT ( 'NONE',  ( 20.75744454082159862, -20.94213870710139958, -77.11961558469170086 ) ) ;
#48170=CARTESIAN_POINT ( 'NONE',  ( 10.22095790285375294, -12.20831385113555889, -75.61947464293628229 ) ) ;
#48173=CARTESIAN_POINT ( 'NONE',  ( 24.04526354826459666, -15.61618910718878794, -73.50766907743336276 ) ) ;
#48177=ORIENTED_EDGE ( 'NONE', *, *, #49527, .F. ) ;
#48184=CARTESIAN_POINT ( 'NONE',  ( 23.07179105164740207, -16.88455221006540086, -60.51037732077569586 ) ) ;
#48190=CARTESIAN_POINT ( 'NONE',  ( 12.71275554691149878, -8.553451307824580852, -40.64391951434709682 ) ) ;
#48191=ORIENTED_EDGE ( 'NONE', *, *, #8979, .F. ) ;
#48205=EDGE_LOOP ( 'NONE', ( #48389, #8213, #19253, #25430 ) ) ;
#48209=CARTESIAN_POINT ( 'NONE',  ( 18.97410177224724137, -8.205170569095422195, -49.12422271383822903 ) ) ;
#48217=CARTESIAN_POINT ( 'NONE',  ( 18.29630866101669895, -7.659627465277500491, -75.37679910129210725 ) ) ;
#48222=CARTESIAN_POINT ( 'NONE',  ( 17.61790714432060057, -8.315193971646580806, -69.79648614575899046 ) ) ;
#48235=CARTESIAN_POINT ( 'NONE',  ( 15.90134539241399736, -23.85807111248870171, -70.01664904841000237 ) ) ;
#48249=CARTESIAN_POINT ( 'NONE',  ( 18.08784342482760010, -8.426686525020091523, -75.81712490659408843 ) ) ;
#48258=CARTESIAN_POINT ( 'NONE',  ( 20.57457857590170036, -10.13683997779680013, -68.56397102982089109 ) ) ;
#48259=CARTESIAN_POINT ( 'NONE',  ( 14.36273137698815461, -22.20707289941944040, -71.03615485597320856 ) ) ;
#48270=CARTESIAN_POINT ( 'NONE',  ( 9.367243689500000414, -15.61633989587210003, -59.45282021618999835 ) ) ;
#48279=CARTESIAN_POINT ( 'NONE',  ( 16.07824235657712109, -23.60611652474380762, -66.00953593440993927 ) ) ;
#48281=CARTESIAN_POINT ( 'NONE',  ( 14.12315431978420044, -7.619972872716400225, -43.21391308946279963 ) ) ;
#48286=ORIENTED_EDGE ( 'NONE', *, *, #1027, .T. ) ;
#48288=CARTESIAN_POINT ( 'NONE',  ( 11.28980945888330112, -9.441723080053581185, -81.30072504052380111 ) ) ;
#48291=CARTESIAN_POINT ( 'NONE',  ( 24.04181170281000135, -15.85636501970542867, -59.80198823605401515 ) ) ;
#48295=CARTESIAN_POINT ( 'NONE',  ( 24.37435181540019613, -15.89599411523789918, -47.51847262634210267 ) ) ;
#48300=CARTESIAN_POINT ( 'NONE',  ( 19.54188187493409146, -21.52912850391220090, -56.78610451874590836 ) ) ;
#48306=EDGE_CURVE ( 'NONE', #32526, #41688, #41549, .T. ) ;
#48312=CARTESIAN_POINT ( 'NONE',  ( 9.807807174049782972, -10.75446600372985628, -61.00066419533776241 ) ) ;
#48319=EDGE_CURVE ( 'NONE', #49834, #43383, #6192, .T. ) ;
#48326=CARTESIAN_POINT ( 'NONE',  ( 9.667674752789849890, -11.97066205877570155, -81.23899999999999011 ) ) ;
#48333=CARTESIAN_POINT ( 'NONE',  ( 20.99657455844219811, -20.65612899709289962, -81.23899999999999011 ) ) ;
#48337=CARTESIAN_POINT ( 'NONE',  ( 9.366504787982940172, -15.61629640169840094, -69.84717978381009118 ) ) ;
#48341=VERTEX_POINT ( 'NONE', #37889 ) ;
#48342=CARTESIAN_POINT ( 'NONE',  ( 9.367812230547961860, -14.91300876115404606, -41.88025658668828299 ) ) ;
#48352=CARTESIAN_POINT ( 'NONE',  ( 12.14984841769559765, -22.52873612623772104, -68.45899737382208627 ) ) ;
#48356=CARTESIAN_POINT ( 'NONE',  ( 23.69882969085709945, -13.52833052609389952, -65.20178814406908430 ) ) ;
#48357=VERTEX_POINT ( 'NONE', #6437 ) ;
#48363=CARTESIAN_POINT ( 'NONE',  ( 9.807791109152047326, -20.47789127149569310, -36.58399760381443144 ) ) ;
#48369=CARTESIAN_POINT ( 'NONE',  ( 24.04493739769619864, -15.61618894467929941, -32.14999999999999858 ) ) ;
#48370=DIRECTION ( 'NONE',  ( 0.000000000000000000, 0.000000000000000000, -1.000000000000000000 ) ) ;
#48373=CARTESIAN_POINT ( 'NONE',  ( 23.14732642514769978, -18.12996472783180124, -45.17689247551339804 ) ) ;
#48374=CARTESIAN_POINT ( 'NONE',  ( 22.04684393501796080, -19.02418972032391764, -76.61949155326421135 ) ) ;
#48389=ORIENTED_EDGE ( 'NONE', *, *, #1110, .T. ) ;
#48391=CARTESIAN_POINT ( 'NONE',  ( 11.27229735085614593, -9.289995009674603565, -79.08399885391317241 ) ) ;
#48394=ORIENTED_EDGE ( 'NONE', *, *, #48306, .F. ) ;
#48404=ORIENTED_EDGE ( 'NONE', *, *, #18180, .T. ) ;
#48409=CARTESIAN_POINT ( 'NONE',  ( 10.93745414090779988, -21.49694649396669988, -56.74285641080179943 ) ) ;
#48411=B_SPLINE_CURVE_WITH_KNOTS ( 'NONE', 3,
 ( #26248, #46460, #26504, #7385, #38588, #42520, #38320, #23334, #42255, #18390 ),
 .UNSPECIFIED., .F., .F.,
 ( 4, 2, 2, 2, 4 ),
 ( 0.5000000023607420463, 0.6250000017705563682, 0.7500000011803709121, 0.8750000005901854561, 1.000000000000000000 ),
 .UNSPECIFIED. ) ;
#48418=CARTESIAN_POINT ( 'NONE',  ( 13.90590011285059902, -8.924521810714191261, -52.24487123071539685 ) ) ;
#48426=CARTESIAN_POINT ( 'NONE',  ( 23.04646185301237438, -11.63205982887159173, -37.34100430183969621 ) ) ;
#48431=LINE ( 'NONE', #16712, #4719 ) ;
#48433=EDGE_CURVE ( 'NONE', #29027, #3978, #35168, .T. ) ;
#48442=FACE_OUTER_BOUND ( 'NONE', #5083, .T. ) ;
#48445=CARTESIAN_POINT ( 'NONE',  ( 22.12488360164890011, -19.33789853544120163, -64.62976173608399222 ) ) ;
#48464=EDGE_CURVE ( 'NONE', #33306, #5521, #50969, .T. ) ;
#48465=LINE ( 'NONE', #25103, #13303 ) ;
#48467=CARTESIAN_POINT ( 'NONE',  ( 22.46010119316818887, -20.47786885658587153, -43.71601729080407495 ) ) ;
#48469=ORIENTED_EDGE ( 'NONE', *, *, #1942, .F. ) ;
#48470=CARTESIAN_POINT ( 'NONE',  ( 9.366958635467167227, -14.73023523842327265, -67.49448678272128177 ) ) ;
#48474=CARTESIAN_POINT ( 'NONE',  ( 9.585777066488809339, -10.60576817065870081, -73.00023116938359635 ) ) ;
#48476=PLANE ( 'NONE',  #12492 ) ;
#48480=CARTESIAN_POINT ( 'NONE',  ( 15.36594091644890092, -23.02678104045260099, -60.76552800450640035 ) ) ;
#48492=CYLINDRICAL_SURFACE ( 'NONE', #38174, 6.766999999999998572 ) ;
#48497=EDGE_CURVE ( 'NONE', #45497, #14613, #42379, .T. ) ;
#48498=VERTEX_POINT ( 'NONE', #13725 ) ;
#48502=CARTESIAN_POINT ( 'NONE',  ( 24.04493741894995296, -16.65173984875949031, -71.83400671401952309 ) ) ;
#48504=CARTESIAN_POINT ( 'NONE',  ( 11.53513604979039897, -9.754423462944890488, -81.52088794317478460 ) ) ;
#48510=FACE_OUTER_BOUND ( 'NONE', #5156, .T. ) ;
#48520=CARTESIAN_POINT ( 'NONE',  ( 18.20454996519679725, -23.32130808853898074, -71.92427505145974465 ) ) ;
#48528=DIRECTION ( 'NONE',  ( 0.000000000000000000, 0.000000000000000000, -1.000000000000000000 ) ) ;
#48535=CARTESIAN_POINT ( 'NONE',  ( 16.97480724641878425, -8.843458757663720249, -71.99243736330308252 ) ) ;
#48538=CARTESIAN_POINT ( 'NONE',  ( 23.16791630292550153, -19.91803283035480021, -47.96704895327989959 ) ) ;
#48542=B_SPLINE_CURVE_WITH_KNOTS ( 'NONE', 3,
 ( #7956, #6938, #51470, #19744, #27859, #15814, #22891, #43098, #23656, #7189, #101, #11386, #43353, #10866, #7446, #43609, #3255, #23145 ),
 .UNSPECIFIED., .F., .F.,
 ( 4, 2, 2, 2, 2, 2, 2, 2, 4 ),
 ( 0.000000000000000000, 0.06249980440203799226, 0.1249996088040759845, 0.1874994132061139629, 0.2499992176081519690, 0.3124990220101899752, 0.3749988264122279258, 0.4374986308142659319, 0.4999984352163039381 ),
 .UNSPECIFIED. ) ;
#48544=B_SPLINE_CURVE_WITH_KNOTS ( 'NONE', 3,
 ( #23603, #39622, #44575, #20708, #800, #3725, #19698, #35689, #51674, #34512, #6236, #9901, #41874, #46342, #30052, #38729, #2563, #50518, #10428, #22192, #30318, #17762, #46081, #26380, #2825, #12880, #33733, #6494, #30576 ),
 .UNSPECIFIED., .F., .F.,
 ( 4, 2, 1, 1, 1, 1, 1, 2, 2, 2, 2, 2, 2, 2, 2, 2, 4 ),
 ( 0.5000036335122389763, 0.5002477723630629480, 0.5004919112138870307, 0.5009801889155351962, 0.5019567443188316380, 0.5039098551254245217, 0.5078160767386101782, 0.5156285199649813800, 0.5312534064177240056, 0.5625031793232091459, 0.6250027251341792045, 0.6875022709451493741, 0.7500018167561195437, 0.8125013625670896023, 0.8750009083780597718, 0.9375004541890299414, 1.000000000000000000 ),
 .UNSPECIFIED. ) ;
#48545=CARTESIAN_POINT ( 'NONE',  ( 22.90093739769620029, -15.61618894467913243, -28.45282021618999835 ) ) ;
#48546=CARTESIAN_POINT ( 'NONE',  ( 19.96627852001369874, -22.46453588084860087, -80.35009786776049623 ) ) ;
#48548=CARTESIAN_POINT ( 'NONE',  ( 16.13393739769620083, -15.61618894467929941, -22.14999999999999858 ) ) ;
#48552=CARTESIAN_POINT ( 'NONE',  ( 23.83903845189011150, -13.54551734412039465, -57.70899791543581614 ) ) ;
#48553=CARTESIAN_POINT ( 'NONE',  ( 24.37516582201759974, -15.36148368927210051, -41.49783386550709707 ) ) ;
#48557=CARTESIAN_POINT ( 'NONE',  ( 17.16957436647078694, -23.52717616726175720, -64.25066604316528185 ) ) ;
#48576=CARTESIAN_POINT ( 'NONE',  ( 9.366959236597619309, -16.50214705144793470, -65.41115364195393056 ) ) ;
#48579=CARTESIAN_POINT ( 'NONE',  ( 23.79191343808687620, -13.56498988170000608, -75.70900991007390246 ) ) ;
#48580=CARTESIAN_POINT ( 'NONE',  ( 9.367786036389057713, -14.73543740969510374, -79.88861889020083140 ) ) ;
#48583=CARTESIAN_POINT ( 'NONE',  ( 16.22164304676950408, -22.66849390760810223, -80.94886153518950778 ) ) ;
#48597=CARTESIAN_POINT ( 'NONE',  ( 23.06214062797170072, -27.61618894467930119, -32.14999999999999858 ) ) ;
#48598=CARTESIAN_POINT ( 'NONE',  ( 22.35028251693639945, -19.17153531005600087, -81.23899999999999011 ) ) ;
#48603=CARTESIAN_POINT ( 'NONE',  ( 9.651154978174693255, -13.08642360888446987, -41.96614601027561520 ) ) ;
#48607=AXIS2_PLACEMENT_3D ( 'NONE', #46983, #39360, #38851 ) ;
#48611=VECTOR ( 'NONE', #31808, 1000.000000000000000 ) ;
#48613=EDGE_CURVE ( 'NONE', #50703, #37063, #30718, .T. ) ;
#48617=B_SPLINE_CURVE_WITH_KNOTS ( 'NONE', 3,
 ( #21160, #17251, #27360, #19244, #46072, #43623, #2033, #18013, #10421, #43367, #2292, #34233, #31277, #10159, #23669, #35751, #39686, #46335 ),
 .UNSPECIFIED., .F., .F.,
 ( 4, 2, 2, 2, 2, 2, 2, 2, 4 ),
 ( 0.000000000000000000, 0.06249992064097868727, 0.1249998412819573745, 0.1874997619229360479, 0.2499996825639147491, 0.3124996032048934502, 0.3749995238458720959, 0.4374994444868507970, 0.4999993651278294982 ),
 .UNSPECIFIED. ) ;
#48620=CARTESIAN_POINT ( 'NONE',  ( 22.90067702240739322, -15.61618873416334807, -54.84718332859007006 ) ) ;
#48622=CARTESIAN_POINT ( 'NONE',  ( 15.45935907336719950, -23.43486480875809974, -59.81490083174309547 ) ) ;
#48624=CYLINDRICAL_SURFACE ( 'NONE', #5433, 6.766999999999998572 ) ;
#48630=CARTESIAN_POINT ( 'NONE',  ( 15.09840986696447729, -23.52719135345972390, -36.33399691850734570 ) ) ;
#48631=EDGE_CURVE ( 'NONE', #20276, #13824, #27424, .T. ) ;
#48635=CARTESIAN_POINT ( 'NONE',  ( 18.57796361324281520, -23.17930195404681015, -33.90807609102002829 ) ) ;
#48638=EDGE_LOOP ( 'NONE', ( #42659, #33921, #17022, #9806 ) ) ;
#48639=CARTESIAN_POINT ( 'NONE',  ( 19.97308036710279922, -22.00114592173070349, -47.39502254529469383 ) ) ;
#48645=CARTESIAN_POINT ( 'NONE',  ( 9.903866441572990453, -10.68225490921047971, -81.00563702421779055 ) ) ;
#48654=ORIENTED_EDGE ( 'NONE', *, *, #23115, .F. ) ;
#48675=CARTESIAN_POINT ( 'NONE',  ( 16.23592030529090025, -7.769129171863720096, -67.51663103545399736 ) ) ;
#48677=CARTESIAN_POINT ( 'NONE',  ( 14.04950511168917515, -17.13061764721083335, -40.14999999999999858 ) ) ;
#48679=DIRECTION ( 'NONE',  ( 0.000000000000000000, 0.000000000000000000, 1.000000000000000000 ) ) ;
#48689=ORIENTED_EDGE ( 'NONE', *, *, #9567, .T. ) ;
#48692=CARTESIAN_POINT ( 'NONE',  ( 17.16948702526555337, -7.705189252755917373, -37.04933676831282696 ) ) ;
#48695=CARTESIAN_POINT ( 'NONE',  ( 22.12600828401099662, -12.01106615515799980, -32.14999999999999858 ) ) ;
#48696=CARTESIAN_POINT ( 'NONE',  ( 8.223247527389670353, -15.61637340300369914, -74.79233150823711185 ) ) ;
#48700=CARTESIAN_POINT ( 'NONE',  ( 20.11811409522369587, -22.52868499068620167, -73.84100135226722728 ) ) ;
#48704=CARTESIAN_POINT ( 'NONE',  ( 18.25866816536740345, -8.891006542739390284, -64.44458661451268711 ) ) ;
#48711=CARTESIAN_POINT ( 'NONE',  ( 10.26677323880680071, -11.70224675945619985, -67.64008111650149146 ) ) ;
#48720=AXIS2_PLACEMENT_3D ( 'NONE', #6500, #9906, #25864 ) ;
#48725=CARTESIAN_POINT ( 'NONE',  ( 23.04644875934005555, -11.63203529592211893, -75.34097925061534795 ) ) ;
#48731=ORIENTED_EDGE ( 'NONE', *, *, #5712, .T. ) ;
#48737=CARTESIAN_POINT ( 'NONE',  ( 14.81467456660999993, -7.815966731016759539, -81.23899999999999011 ) ) ;
#48745=CARTESIAN_POINT ( 'NONE',  ( 9.681283356623689329, -11.89195081703809898, -61.39927945301539580 ) ) ;
#48755=CARTESIAN_POINT ( 'NONE',  ( 24.04490452168148451, -15.61618923948461557, -69.79232899952297942 ) ) ;
#48757=CYLINDRICAL_SURFACE ( 'NONE', #23579, 7.910999999999997812 ) ;
#48767=DIRECTION ( 'NONE',  ( 0.000000000000000000, 0.000000000000000000, -1.000000000000000000 ) ) ;
#48769=CARTESIAN_POINT ( 'NONE',  ( 10.09870140130719918, -19.26563892577449977, -39.27970379572569470 ) ) ;
#48776=CYLINDRICAL_SURFACE ( 'NONE', #4377, 7.910999999999997812 ) ;
#48777=CARTESIAN_POINT ( 'NONE',  ( 9.865947636674368582, -11.58890714499520058, -66.24912813843610593 ) ) ;
#48787=ORIENTED_EDGE ( 'NONE', *, *, #20785, .T. ) ;
#48789=CARTESIAN_POINT ( 'NONE',  ( 18.20458331782904793, -7.911079347056140243, -55.37565539348986476 ) ) ;
#48791=ORIENTED_EDGE ( 'NONE', *, *, #30363, .T. ) ;
#48793=CARTESIAN_POINT ( 'NONE',  ( 17.90516122990442227, -9.025309029999688093, -70.03615537855314699 ) ) ;
#48794=CARTESIAN_POINT ( 'NONE',  ( 19.08568541577971800, -9.510811376752775104, -50.09616398158074446 ) ) ;
#48800=CARTESIAN_POINT ( 'NONE',  ( 21.52719323332197732, -11.43332263511563518, -72.24312383686958583 ) ) ;
#48801=CARTESIAN_POINT ( 'NONE',  ( 24.03335507664926141, -16.05328977305849136, -65.52525647391593111 ) ) ;
#48802=CARTESIAN_POINT ( 'NONE',  ( 20.96782168322129891, -8.936646836863200605, -47.49173536689819741 ) ) ;
#48804=DIRECTION ( 'NONE',  ( 1.000000000000000000, 2.460964292799963328E-14, 0.000000000000000000 ) ) ;
#48809=CARTESIAN_POINT ( 'NONE',  ( 18.40131669078889942, -8.519310590983641518, -33.83109144287589487 ) ) ;
#48810=CARTESIAN_POINT ( 'NONE',  ( 11.57646884939659948, -10.52741891998659973, -32.14999999999999858 ) ) ;
#48815=CARTESIAN_POINT ( 'NONE',  ( 13.52923768432050089, -7.793257261984160245, -52.90535993866839704 ) ) ;
#48819=CARTESIAN_POINT ( 'NONE',  ( 24.04493739427486076, -15.63665726277926460, -39.50849474849957232 ) ) ;
#48822=CARTESIAN_POINT ( 'NONE',  ( 22.90011000694050480, -14.71637116526028422, -52.80484287475383809 ) ) ;
#48828=VECTOR ( 'NONE', #30722, 1000.000000000000000 ) ;
#48835=CARTESIAN_POINT ( 'NONE',  ( 9.221442873511705329, -11.63200860059268393, -60.95899765791760672 ) ) ;
#48838=CARTESIAN_POINT ( 'NONE',  ( 9.752391369101644614, -17.94198506269301774, -67.34148719073695588 ) ) ;
#48844=ORIENTED_EDGE ( 'NONE', *, *, #25101, .F. ) ;
#48848=CARTESIAN_POINT ( 'NONE',  ( 13.34706694256989756, -8.327013639518519028, -81.23899999999999011 ) ) ;
#48851=VERTEX_POINT ( 'NONE', #17334 ) ;
#48857=CARTESIAN_POINT ( 'NONE',  ( 20.43018706615270119, -21.07797482358570207, -81.23899999999999011 ) ) ;
#48871=ORIENTED_EDGE ( 'NONE', *, *, #25566, .T. ) ;
#48872=EDGE_CURVE ( 'NONE', #25645, #6190, #22410, .T. ) ;
#48879=CARTESIAN_POINT ( 'NONE',  ( 18.20465300147069243, -23.32127884851029620, -68.20899677301083841 ) ) ;
#48884=CARTESIAN_POINT ( 'NONE',  ( 12.19403623553569993, -22.40323005370389708, -69.95492400788630505 ) ) ;
#48890=PRODUCT_DEFINITION_CONTEXT ( 'detailed design', #33465, 'design' ) ;
#48893=CIRCLE ( 'NONE', #43871, 12.00000000000000000 ) ;
#48895=CARTESIAN_POINT ( 'NONE',  ( 9.367509130462650546, -15.61619940421079988, -51.84717978381009118 ) ) ;
#48902=CARTESIAN_POINT ( 'NONE',  ( 23.14749236991919901, -19.39874071289914781, -33.66528814357884158 ) ) ;
#48907=CARTESIAN_POINT ( 'NONE',  ( 9.582260743677990078, -19.16333249400659966, -43.90938957849540003 ) ) ;
#48908=B_SPLINE_CURVE_WITH_KNOTS ( 'NONE', 3,
 ( #25302, #29503, #10380, #17718, #33941, #18494, #42348, #37377, #45249, #33686, #38156, #34464, #50474, #49704, #26080, #41307, #5416, #1479, #17974, #49958, #13543, #30008, #10124, #17464, #49449, #9606, #25559, #6191 ),
 .UNSPECIFIED., .F., .F.,
 ( 4, 2, 1, 1, 1, 1, 2, 2, 2, 2, 2, 2, 2, 2, 2, 4 ),
 ( 0.5000038014739186520, 0.5004920790115416906, 0.5009803565491648403, 0.5019569116244110285, 0.5039100217749037380, 0.5078162420758888240, 0.5156286826778588850, 0.5312535638817990069, 0.5625033262896789177, 0.6250028511054390723, 0.6875023759211991159, 0.7500019007369591595, 0.8125014255527194251, 0.8750009503684796908, 0.9375004751842397344, 1.000000000000000000 ),
 .UNSPECIFIED. ) ;
#48911=CARTESIAN_POINT ( 'NONE',  ( 22.90100569266936148, -15.61618883250986300, -34.84718217067427304 ) ) ;
#48916=CARTESIAN_POINT ( 'NONE',  ( 20.11804734517991022, -22.52872490663017757, -78.12566274994264859 ) ) ;
#48918=CARTESIAN_POINT ( 'NONE',  ( 21.77263034913930184, -11.37971624043620089, -60.64207792345899151 ) ) ;
#48920=ORIENTED_EDGE ( 'NONE', *, *, #30622, .T. ) ;
#48926=CARTESIAN_POINT ( 'NONE',  ( 8.223571189834400386, -15.61612039429540033, -78.79233150823698395 ) ) ;
#48929=ORIENTED_EDGE ( 'NONE', *, *, #2459, .F. ) ;
#48930=ORIENTED_EDGE ( 'NONE', *, *, #32314, .T. ) ;
#48931=CARTESIAN_POINT ( 'NONE',  ( 15.09828469353879044, -23.52717631300025403, -56.04926988608728067 ) ) ;
#48932=CARTESIAN_POINT ( 'NONE',  ( 23.51915272595648432, -12.68635589971720457, -77.38738348931531164 ) ) ;
#48935=CARTESIAN_POINT ( 'NONE',  ( 19.54197002857337040, -9.703302158787252552, -36.11948505536842191 ) ) ;
#48943=EDGE_CURVE ( 'NONE', #9734, #27459, #40654, .T. ) ;
#48944=CARTESIAN_POINT ( 'NONE',  ( 21.87691169841230021, -10.26782529091599905, -65.77381455205440375 ) ) ;
#48947=VECTOR ( 'NONE', #42049, 1000.000000000000000 ) ;
#48958=CYLINDRICAL_SURFACE ( 'NONE', #28048, 7.910999999999997812 ) ;
#48960=CARTESIAN_POINT ( 'NONE',  ( 24.04463300525956981, -15.61618495692933273, -55.50767188603018809 ) ) ;
#48961=CARTESIAN_POINT ( 'NONE',  ( 23.37822663296399739, -17.15971063053670065, -32.14999999999999858 ) ) ;
#48967=CARTESIAN_POINT ( 'NONE',  ( 9.366365007129969555, -15.61616877484880028, -59.84717978381009118 ) ) ;
#48971=CARTESIAN_POINT ( 'NONE',  ( 19.72595728692159867, -21.68578137661910077, -63.17708371749489515 ) ) ;
#48978=CARTESIAN_POINT ( 'NONE',  ( 20.66817066224499655, -10.21403313433049931, -70.17508691053730274 ) ) ;
#48983=ADVANCED_FACE ( 'NONE', ( #50073 ), #18347, .T. ) ;
#48986=EDGE_CURVE ( 'NONE', #31691, #50433, #12393, .T. ) ;
#48992=ORIENTED_EDGE ( 'NONE', *, *, #46320, .T. ) ;
#48993=CARTESIAN_POINT ( 'NONE',  ( 24.04466642925503095, -15.61618863334376250, -55.79233649161735542 ) ) ;
#49002=ORIENTED_EDGE ( 'NONE', *, *, #7118, .F. ) ;
#49006=CARTESIAN_POINT ( 'NONE',  ( 13.52049491622099886, -8.034853201522141219, -81.18618737929101314 ) ) ;
#49015=CARTESIAN_POINT ( 'NONE',  ( 20.16990914961741055, -9.832289637797707371, -46.54110819413472200 ) ) ;
#49025=FACE_OUTER_BOUND ( 'NONE', #50981, .T. ) ;
#49032=CARTESIAN_POINT ( 'NONE',  ( 8.428884743720756134, -17.68704076488086230, -74.70899817588775704 ) ) ;
#49034=CARTESIAN_POINT ( 'NONE',  ( 23.56842915955159867, -16.10099296214760400, -80.25338504615679369 ) ) ;
#49042=CARTESIAN_POINT ( 'NONE',  ( 23.42904929335390207, -14.10356315877740130, -71.00226400225309931 ) ) ;
#49044=EDGE_CURVE ( 'NONE', #49799, #20360, #7396, .T. ) ;
#49047=CARTESIAN_POINT ( 'NONE',  ( 21.93491326470667602, -10.21990321164456006, -49.55383906828567575 ) ) ;
#49053=CARTESIAN_POINT ( 'NONE',  ( 17.16939886808665960, -23.52720133053026075, -71.96594023329781464 ) ) ;
#49059=DIRECTION ( 'NONE',  ( 1.000000000000000000, 2.460964292799963328E-14, 0.000000000000000000 ) ) ;
#49062=FACE_OUTER_BOUND ( 'NONE', #15892, .T. ) ;
#49065=ORIENTED_EDGE ( 'NONE', *, *, #18092, .F. ) ;
#49069=CARTESIAN_POINT ( 'NONE',  ( 8.222598545279129922, -15.61602001634830117, -66.50766849176299900 ) ) ;
#49071=CARTESIAN_POINT ( 'NONE',  ( 18.34740929417809951, -23.55868617284500033, -56.20581778389630045 ) ) ;
#49073=CARTESIAN_POINT ( 'NONE',  ( 19.73841138675414442, -9.822567584297365428, -56.13025822577677815 ) ) ;
#49078=CARTESIAN_POINT ( 'NONE',  ( 9.522216423340641001, -19.05011374909959798, -45.08017965390989445 ) ) ;
#49079=VECTOR ( 'NONE', #6741, 1000.000000000000000 ) ;
#49080=CARTESIAN_POINT ( 'NONE',  ( 9.807704732040047446, -10.75459748142696270, -32.71600059186270215 ) ) ;
#49081=B_SPLINE_CURVE_WITH_KNOTS ( 'NONE', 3,
 ( #3818, #27899, #4064, #7997, #27135, #23184, #15612, #48092, #27391, #31567, #39714, #43393, #43142, #38950, #137, #20031, #32074, #43903, #3295, #7488, #23950, #19277, #19014, #22930, #34989, #36028, #3561, #23700 ),
 .UNSPECIFIED., .F., .F.,
 ( 4, 2, 2, 2, 2, 2, 2, 2, 2, 2, 1, 1, 1, 1, 2, 4 ),
 ( 0.000000000000000000, 0.06250045418902985817, 0.1250009083780597163, 0.1875013625670895467, 0.2500018167561194327, 0.3125022709451493186, 0.3750027251341790935, 0.4375031793232089794, 0.4687534064177240056, 0.4843785199649814355, 0.4921910767386101782, 0.4960973551254245217, 0.4980504943188317490, 0.4990270639155353072, 0.4995153487138871418, 0.5000036335122389763 ),
 .UNSPECIFIED. ) ;
#49085=CARTESIAN_POINT ( 'NONE',  ( 10.78136697721919823, -21.88776853859420157, -56.23255504334029098 ) ) ;
#49105=CARTESIAN_POINT ( 'NONE',  ( 8.222937397696199469, -15.61618894467929941, -32.14999999999999858 ) ) ;
#49108=CARTESIAN_POINT ( 'NONE',  ( 22.74532932033418930, -17.09449615818190082, -66.52281770332464816 ) ) ;
#49111=CARTESIAN_POINT ( 'NONE',  ( 20.29256129770259776, -21.02754544282699456, -60.74449963404457264 ) ) ;
#49112=CARTESIAN_POINT ( 'NONE',  ( 10.72263364360945737, -11.45749769863363809, -47.66115396588360653 ) ) ;
#49116=FACE_OUTER_BOUND ( 'NONE', #16087, .T. ) ;
#49117=AXIS2_PLACEMENT_3D ( 'NONE', #38383, #41337, #45278 ) ;
#49128=CARTESIAN_POINT ( 'NONE',  ( 19.62200085763610247, -21.54020370181870092, -81.23899999999999011 ) ) ;
#49134=ORIENTED_EDGE ( 'NONE', *, *, #47918, .T. ) ;
#49137=CARTESIAN_POINT ( 'NONE',  ( 23.86187795847609650, -17.34972413055976403, -33.86254089651572485 ) ) ;
#49139=CARTESIAN_POINT ( 'NONE',  ( 15.12242003932687062, -22.59611672426211015, -49.39298971242588721 ) ) ;
#49146=CARTESIAN_POINT ( 'NONE',  ( 24.04493737374410145, -16.65173368866850367, -67.83399587179394530 ) ) ;
#49149=VECTOR ( 'NONE', #34246, 1000.000000000000000 ) ;
#49151=CARTESIAN_POINT ( 'NONE',  ( 15.91255700721379895, -23.46078829110179953, -69.79648614575910415 ) ) ;
#49152=VERTEX_POINT ( 'NONE', #17460 ) ;
#49157=CARTESIAN_POINT ( 'NONE',  ( 17.16950173226367582, -23.52718653585607100, -36.25066335673832185 ) ) ;
#49159=CARTESIAN_POINT ( 'NONE',  ( 21.54527565159127533, -19.77483657756496171, -78.66115106571606930 ) ) ;
#49164=CARTESIAN_POINT ( 'NONE',  ( 12.48460695861928649, -22.65913801891631607, -34.15979310000165015 ) ) ;
#49166=DIRECTION ( 'NONE',  ( 0.000000000000000000, 0.000000000000000000, -1.000000000000000000 ) ) ;
#49169=CARTESIAN_POINT ( 'NONE',  ( 16.96290023960060367, -8.212168756627189481, -46.60283323465849747 ) ) ;
#49172=ORIENTED_EDGE ( 'NONE', *, *, #28559, .F. ) ;
#49194=CARTESIAN_POINT ( 'NONE',  ( 9.412768094977693067, -14.16268697616711059, -65.91555746443309260 ) ) ;
#49195=CARTESIAN_POINT ( 'NONE',  ( 15.24821961686016714, -8.849179223346602896, -35.91115229312517698 ) ) ;
#49200=CARTESIAN_POINT ( 'NONE',  ( 18.66534361887244486, -21.90748510045777664, -46.83103359700395174 ) ) ;
#49202=CARTESIAN_POINT ( 'NONE',  ( 8.318366073613649547, -14.90654645034790171, -67.04131744907229518 ) ) ;
#49210=CARTESIAN_POINT ( 'NONE',  ( 20.99566151349429077, -9.290060484552283171, -41.50066443384773862 ) ) ;
#49219=CARTESIAN_POINT ( 'NONE',  ( 22.39105762524350141, -12.40667166394900178, -32.14999999999999858 ) ) ;
#49223=CARTESIAN_POINT ( 'NONE',  ( 8.320255473221708442, -14.14592437889882071, -44.56677848951485998 ) ) ;
#49228=CARTESIAN_POINT ( 'NONE',  ( 18.53141933435519917, -22.24903445304479987, -65.23677592514899004 ) ) ;
#49235=CARTESIAN_POINT ( 'NONE',  ( 14.11179025357979988, -22.37292481521379983, -63.04538311481158530 ) ) ;
#49244=CARTESIAN_POINT ( 'NONE',  ( 21.93112139786197190, -10.15704698707457254, -39.26711392836666192 ) ) ;
#49253=ADVANCED_FACE ( 'NONE', ( #2250 ), #3286, .T. ) ;
#49255=CARTESIAN_POINT ( 'NONE',  ( 17.16948286040633320, -23.52718923084113101, -43.96602994729640557 ) ) ;
#49260=CARTESIAN_POINT ( 'NONE',  ( 8.428826428148642691, -13.54554915206019672, -52.87566510375268791 ) ) ;
#49263=CARTESIAN_POINT ( 'NONE',  ( 12.38031658575100025, -8.724376527540918858, -35.35374502362449789 ) ) ;
#49272=CARTESIAN_POINT ( 'NONE',  ( 19.41271919554129965, -21.86055833610469890, -37.19327432862769456 ) ) ;
#49273=FACE_OUTER_BOUND ( 'NONE', #1985, .T. ) ;
#49281=LINE ( 'NONE', #45340, #18329 ) ;
#49294=CARTESIAN_POINT ( 'NONE',  ( 17.44202617202429906, -8.685715479244029424, -38.01220089870779617 ) ) ;
#49304=CARTESIAN_POINT ( 'NONE',  ( 11.77695353238810050, -9.572730833979290921, -70.36851255374429570 ) ) ;
#49313=CARTESIAN_POINT ( 'NONE',  ( 23.64088795765827200, -18.16524924148145814, -71.61181469969464786 ) ) ;
#49314=VERTEX_POINT ( 'NONE', #18225 ) ;
#49320=CYLINDRICAL_SURFACE ( 'NONE', #46798, 7.910999999999997812 ) ;
#49322=CARTESIAN_POINT ( 'NONE',  ( 21.96868942811769898, -19.57828787301799878, -53.03706054135149373 ) ) ;
#49328=CARTESIAN_POINT ( 'NONE',  ( 17.71973881293279973, -7.524961971755559809, -53.35393626560600211 ) ) ;
#49329=CARTESIAN_POINT ( 'NONE',  ( 22.70316795904539120, -13.93762338909561826, -56.37318659548496669 ) ) ;
#49333=CARTESIAN_POINT ( 'NONE',  ( 13.44640934693589962, -8.667528154172808641, -47.61518544794569863 ) ) ;
#49336=CARTESIAN_POINT ( 'NONE',  ( 10.81129653165480065, -11.20976454154149948, -32.14999999999999858 ) ) ;
#49344=CARTESIAN_POINT ( 'NONE',  ( 12.04442768316860146, -22.77570226639050333, -54.17286283568609662 ) ) ;
#49349=CARTESIAN_POINT ( 'NONE',  ( 22.90068744318051586, -15.61618870719606278, -70.84718393407784731 ) ) ;
#49358=FACE_OUTER_BOUND ( 'NONE', #26857, .T. ) ;
#49365=AXIS2_PLACEMENT_3D ( 'NONE', #40310, #15692, #20122 ) ;
#49385=FACE_OUTER_BOUND ( 'NONE', #1697, .T. ) ;
#49400=VECTOR ( 'NONE', #29529, 1000.000000000000000 ) ;
#49408=CARTESIAN_POINT ( 'NONE',  ( 12.81178300798239889, -8.506333925476139868, -72.64836766404940249 ) ) ;
#49410=ORIENTED_EDGE ( 'NONE', *, *, #3242, .F. ) ;
#49418=EDGE_CURVE ( 'NONE', #4493, #16548, #51748, .T. ) ;
#49420=CARTESIAN_POINT ( 'NONE',  ( 23.04644654094820311, -19.60034674646418296, -55.95901133476449019 ) ) ;
#49423=DIRECTION ( 'NONE',  ( 0.000000000000000000, 0.000000000000000000, -1.000000000000000000 ) ) ;
#49425=CARTESIAN_POINT ( 'NONE',  ( 11.35448481870250070, -9.900987514852682025, -48.34564971805809819 ) ) ;
#49427=ORIENTED_EDGE ( 'NONE', *, *, #50427, .F. ) ;
#49444=VERTEX_POINT ( 'NONE', #48081 ) ;
#49449=CARTESIAN_POINT ( 'NONE',  ( 10.22095815093987881, -19.02406446778493176, -73.28612399903180119 ) ) ;
#49450=CARTESIAN_POINT ( 'NONE',  ( 9.367379825797401693, -15.61607429561870042, -45.84717978380999881 ) ) ;
#49452=CARTESIAN_POINT ( 'NONE',  ( 19.54194020638888318, -21.52909355783877032, -52.78615182703926223 ) ) ;
#49458=CARTESIAN_POINT ( 'NONE',  ( 21.91117268576520161, -20.92752587786970153, -66.24912813843610593 ) ) ;
#49459=B_SPLINE_CURVE_WITH_KNOTS ( 'NONE', 3,
 ( #21070, #40743, #37072, #36800, #910, #4573, #48352, #16905, #12445, #9312, #48879, #8521, #24468, #28934, #1170, #17166, #49146, #13243 ),
 .UNSPECIFIED., .F., .F.,
 ( 4, 2, 2, 2, 2, 2, 2, 2, 4 ),
 ( 0.000000000000000000, 0.06250015020281043943, 0.1250003004056208789, 0.1875004506084313183, 0.2500006008112417577, 0.3125007510140521694, 0.3750009012168626366, 0.4375010514196731037, 0.5000012016224835154 ),
 .UNSPECIFIED. ) ;
#49462=EDGE_CURVE ( 'NONE', #1665, #22570, #19907, .T. ) ;
#49465=CARTESIAN_POINT ( 'NONE',  ( 26.52624224310950396, -9.616188944679349149, -22.14999999999999858 ) ) ;
#49470=ORIENTED_EDGE ( 'NONE', *, *, #1221, .F. ) ;
#49479=CARTESIAN_POINT ( 'NONE',  ( 22.81054832899980056, -19.17189294434900049, -32.14999999999999858 ) ) ;
#49480=CARTESIAN_POINT ( 'NONE',  ( 24.04472027134544021, -15.61619704117925522, -43.79232540400376905 ) ) ;
#49487=CARTESIAN_POINT ( 'NONE',  ( 22.46358420153250179, -12.50521955988370060, -62.70177013111300113 ) ) ;
#49494=CARTESIAN_POINT ( 'NONE',  ( 15.35791178160290116, -22.62620627274549889, -76.98791498200870365 ) ) ;
#49497=CARTESIAN_POINT ( 'NONE',  ( 8.222961568625748896, -16.65191337441482489, -80.75066493857167416 ) ) ;
#49520=CARTESIAN_POINT ( 'NONE',  ( 8.865981372670939109, -12.65585574203520025, -33.13561495384320210 ) ) ;
#49521=CARTESIAN_POINT ( 'NONE',  ( 22.90049624866714950, -16.13163838386897453, -64.87141853339200281 ) ) ;
#49527=EDGE_CURVE ( 'NONE', #19003, #40749, #2092, .T. ) ;
#49530=CARTESIAN_POINT ( 'NONE',  ( 15.17121401173930018, -22.60301372889670191, -33.39076563757389948 ) ) ;
#49539=CARTESIAN_POINT ( 'NONE',  ( 23.55887781140449633, -12.03108354813719849, -79.36448291391718612 ) ) ;
#49545=CARTESIAN_POINT ( 'NONE',  ( 17.16947147975978183, -7.705187032170163874, -69.04933684442744379 ) ) ;
#49546=EDGE_CURVE ( 'NONE', #44209, #47941, #33269, .T. ) ;
#49553=ORIENTED_EDGE ( 'NONE', *, *, #20785, .F. ) ;
#49555=CARTESIAN_POINT ( 'NONE',  ( 23.86302254292488101, -17.34441396915490685, -65.86232905850448560 ) ) ;
#49558=CARTESIAN_POINT ( 'NONE',  ( 19.30482607911089943, -21.91603209087760007, -38.80439020934399252 ) ) ;
#49561=CARTESIAN_POINT ( 'NONE',  ( 9.221477657806792294, -19.60042875044780786, -58.34100165946446737 ) ) ;
#49563=B_SPLINE_CURVE_WITH_KNOTS ( 'NONE', 3,
 ( #10385, #33945, #38160, #26341, #46035, #41829, #41569, #5683, #26602, #33692, #6196, #37904, #6454, #1998, #17978, #10127, #26085, #50219, #14309, #30278, #38417, #2515, #50478, #18498, #27895, #23696, #31818, #3036, #11424, #15086, #39711, #19529, #43138, #15859 ),
 .UNSPECIFIED., .F., .F.,
 ( 4, 2, 1, 1, 1, 1, 1, 1, 2, 2, 2, 2, 2, 2, 2, 2, 2, 2, 2, 4 ),
 ( 0.4999954466933561603, 0.5001175181175031570, 0.5002395895416501537, 0.5004837323899442580, 0.5009720180865326888, 0.5019485894797097725, 0.5039017322660637177, 0.5078080178387720522, 0.5156205889841884993, 0.5312457312750212823, 0.5624960158566866264, 0.6249965850200170925, 0.6874971541833474475, 0.7499977233466779136, 0.8124982925100083797, 0.8749988616733388458, 0.9062491462550041899, 0.9374994308366694229, 0.9687497154183346559, 1.000000000000000000 ),
 .UNSPECIFIED. ) ;
#49565=CARTESIAN_POINT ( 'NONE',  ( 10.90317266407199881, -20.92144997887719882, -77.81509207372450021 ) ) ;
#49568=CARTESIAN_POINT ( 'NONE',  ( 23.97848197093998834, -14.55973312613292592, -49.74973267396308074 ) ) ;
#49570=B_SPLINE_CURVE_WITH_KNOTS ( 'NONE', 3,
 ( #35842, #12518, #15933, #11756, #28485, #11499, #27714, #47907, #31888, #3630, #7560, #8324, #32141, #24276, #39529, #43715, #19602, #43966 ),
 .UNSPECIFIED., .F., .F.,
 ( 4, 2, 2, 2, 2, 2, 2, 2, 4 ),
 ( 0.5000015647840699851, 0.5625013691860611953, 0.6250011735880525165, 0.6875009779900437268, 0.7500007823920349370, 0.8125005867940262583, 0.8750003911960174685, 0.9375001955980086787, 1.000000000000000000 ),
 .UNSPECIFIED. ) ;
#49574=CARTESIAN_POINT ( 'NONE',  ( 23.04646553001205334, -11.63206671227860944, -45.62564837832152875 ) ) ;
#49576=CARTESIAN_POINT ( 'NONE',  ( 8.426478244294473896, -17.64473173899449066, -46.42595012760061479 ) ) ;
#49583=CARTESIAN_POINT ( 'NONE',  ( 22.90128585160542585, -15.83904648336577381, -52.85765549546293585 ) ) ;
#49588=CARTESIAN_POINT ( 'NONE',  ( 24.04215783492454150, -15.38969022549373022, -43.78321255858008243 ) ) ;
#49589=CARTESIAN_POINT ( 'NONE',  ( 23.64151217820790052, -19.02486038249190159, -51.92799550646089557 ) ) ;
#49596=CARTESIAN_POINT ( 'NONE',  ( 14.04776077600850037, -22.76843061483210207, -46.82299613730950227 ) ) ;
#49604=CARTESIAN_POINT ( 'NONE',  ( 20.83574943972819682, -9.224047739598423945, -61.20962266139596863 ) ) ;
#49605=CARTESIAN_POINT ( 'NONE',  ( 7.959636065010880834, -14.53752382916180075, -56.54943076759479936 ) ) ;
#49627=CARTESIAN_POINT ( 'NONE',  ( 9.543085168726568313, -13.84486511917021367, -47.53615371606744588 ) ) ;
#49629=CARTESIAN_POINT ( 'NONE',  ( 16.79927617522759675, -22.63757652019199895, -73.31710689363809763 ) ) ;
#49637=EDGE_CURVE ( 'NONE', #41326, #1162, #27967, .T. ) ;
#49644=EDGE_CURVE ( 'NONE', #31407, #25645, #21108, .T. ) ;
#49645=CARTESIAN_POINT ( 'NONE',  ( 17.16954007596327969, -7.705196829635915456, -63.04933605003357400 ) ) ;
#49652=CARTESIAN_POINT ( 'NONE',  ( 9.973725646770976283, -20.62007079165992707, -34.57520601010690342 ) ) ;
#49656=LINE ( 'NONE', #33894, #20794 ) ;
#49666=CARTESIAN_POINT ( 'NONE',  ( 23.93780514016240346, -16.44467940405539608, -69.32117255937750144 ) ) ;
#49673=CARTESIAN_POINT ( 'NONE',  ( 8.428805360677591452, -13.54562575312001727, -42.59098949349206009 ) ) ;
#49674=CARTESIAN_POINT ( 'NONE',  ( 8.428796441877244305, -13.54565802726606272, -58.87567998479666187 ) ) ;
#49676=CARTESIAN_POINT ( 'NONE',  ( 22.46007819155687812, -20.47790044386577790, -56.00067946053424350 ) ) ;
#49677=CARTESIAN_POINT ( 'NONE',  ( 22.90093739854874144, -15.61802774535847504, -62.45291482988292842 ) ) ;
#49680=ORIENTED_EDGE ( 'NONE', *, *, #34132, .T. ) ;
#49681=CARTESIAN_POINT ( 'NONE',  ( 16.88857569320390084, -23.02815328493989711, -57.53504572143789630 ) ) ;
#49686=CARTESIAN_POINT ( 'NONE',  ( 20.76113993473645891, -22.05978133672951458, -61.80939319232501816 ) ) ;
#49688=CARTESIAN_POINT ( 'NONE',  ( 20.11811741000025577, -8.703694875967890709, -35.45899634741810047 ) ) ;
#49704=CARTESIAN_POINT ( 'NONE',  ( 22.04683771704192452, -19.02420141048479962, -72.61946099805257404 ) ) ;
#49705=CARTESIAN_POINT ( 'NONE',  ( 20.29258548203541679, -21.02752613792475245, -52.74448505271735144 ) ) ;
#49706=CARTESIAN_POINT ( 'NONE',  ( 17.90516683090147865, -9.025310613233809676, -54.03615538479979818 ) ) ;
#49711=CARTESIAN_POINT ( 'NONE',  ( 17.19549608311789868, -7.840596314597150673, -63.55568448227298717 ) ) ;
#49716=ADVANCED_FACE ( 'NONE', ( #39797 ), #8089, .F. ) ;
#49721=CARTESIAN_POINT ( 'NONE',  ( 9.367400418259169470, -16.60470970061016516, -33.80066697648281604 ) ) ;
#49728=CARTESIAN_POINT ( 'NONE',  ( 20.40033783584950200, -10.32204753240149842, -32.14999999999999858 ) ) ;
#49731=CARTESIAN_POINT ( 'NONE',  ( 22.40487833862019684, -10.75395050048665446, -45.29781307381240651 ) ) ;
#49735=ORIENTED_EDGE ( 'NONE', *, *, #3562, .F. ) ;
#49736=CARTESIAN_POINT ( 'NONE',  ( 11.34022645397350004, -10.44290231406579927, -74.10929620427420161 ) ) ;
#49743=CARTESIAN_POINT ( 'NONE',  ( 22.33004736977609994, -18.98528079716979988, -74.61134705009999379 ) ) ;
#49751=ORIENTED_EDGE ( 'NONE', *, *, #33034, .F. ) ;
#49754=CARTESIAN_POINT ( 'NONE',  ( 8.222524523195870572, -15.61634168869099959, -38.50766849176289952 ) ) ;
#49755=CARTESIAN_POINT ( 'NONE',  ( 15.24818679882209693, -22.38319469959796848, -54.99448832485959571 ) ) ;
#49757=ORIENTED_EDGE ( 'NONE', *, *, #5665, .F. ) ;
#49766=DIRECTION ( 'NONE',  ( 0.000000000000000000, 0.000000000000000000, -1.000000000000000000 ) ) ;
#49771=CARTESIAN_POINT ( 'NONE',  ( 20.16036405916679897, -22.81136437679689877, -80.12993496510939906 ) ) ;
#49778=CARTESIAN_POINT ( 'NONE',  ( 22.41342994594504390, -12.46412855248205531, -78.69890846647390958 ) ) ;
#49781=CARTESIAN_POINT ( 'NONE',  ( 22.61356707982760028, -12.83105728587160144, -36.71796074224590001 ) ) ;
#49799=VERTEX_POINT ( 'NONE', #51849 ) ;
#49803=CARTESIAN_POINT ( 'NONE',  ( 19.66377316389889529, -21.72215472907910083, -48.78597552336009358 ) ) ;
#49811=CARTESIAN_POINT ( 'NONE',  ( 9.643579408486090188, -11.95805451436680045, -76.23071345245209329 ) ) ;
#49821=CARTESIAN_POINT ( 'NONE',  ( 19.83705332263880194, -9.918041006030941631, -62.13619471124365390 ) ) ;
#49822=CARTESIAN_POINT ( 'NONE',  ( 10.22109417245393637, -12.20808089752747527, -57.61948683568049745 ) ) ;
#49829=ORIENTED_EDGE ( 'NONE', *, *, #3562, .T. ) ;
#49832=CARTESIAN_POINT ( 'NONE',  ( 20.11810349957197985, -22.52869132921505724, -69.84100390017049165 ) ) ;
#49834=VERTEX_POINT ( 'NONE', #48967 ) ;
#49837=CARTESIAN_POINT ( 'NONE',  ( 22.90115736359569354, -15.61618877121331295, -78.84717825834033533 ) ) ;
#49838=CARTESIAN_POINT ( 'NONE',  ( 13.66418357337590095, -7.749611791737230249, -53.19549840347870173 ) ) ;
#49845=CARTESIAN_POINT ( 'NONE',  ( 13.00183092915110095, -8.856262696942298618, -41.59454668711060066 ) ) ;
#49847=CARTESIAN_POINT ( 'NONE',  ( 8.842772715000620565, -15.57939790529679946, -32.14999999999999858 ) ) ;
#49852=CARTESIAN_POINT ( 'NONE',  ( 23.31002121937839178, -12.21984004604830076, -61.36704460802273786 ) ) ;
#49855=CARTESIAN_POINT ( 'NONE',  ( 23.00121520682850118, -11.05294270968670034, -51.32098131739589775 ) ) ;
#49856=EDGE_LOOP ( 'NONE', ( #36065, #65, #46236, #13212 ) ) ;
#49874=CARTESIAN_POINT ( 'NONE',  ( 22.90092024398637349, -15.63379323775387242, -66.45364811189233478 ) ) ;
#49894=CARTESIAN_POINT ( 'NONE',  ( 24.04493739695976018, -15.61630955180015334, -77.50768068703865765 ) ) ;
#49901=CARTESIAN_POINT ( 'NONE',  ( 20.23496625000258220, -22.44645670734013621, -34.12034017523288298 ) ) ;
#49908=CARTESIAN_POINT ( 'NONE',  ( 24.04504587474531263, -15.61618895646369687, -51.50767080737492165 ) ) ;
#49914=CARTESIAN_POINT ( 'NONE',  ( 9.181218999323579766, -19.25575692125479677, -76.13400063084870339 ) ) ;
#49925=AXIS2_PLACEMENT_3D ( 'NONE', #40822, #31904, #40563 ) ;
#49931=CARTESIAN_POINT ( 'NONE',  ( 8.222903922732800908, -15.61639209420869889, -32.79233150823699816 ) ) ;
#49936=CARTESIAN_POINT ( 'NONE',  ( 14.58992756899499987, -22.90472295277830028, -55.63379137591109469 ) ) ;
#49941=CARTESIAN_POINT ( 'NONE',  ( 18.91091419587250044, -22.09931774463699838, -75.21836123916489214 ) ) ;
#49944=CARTESIAN_POINT ( 'NONE',  ( 9.221486982277522060, -11.63193319550961036, -34.95899771803228617 ) ) ;
#49945=CARTESIAN_POINT ( 'NONE',  ( 9.618998415436749383, -18.02038534747480014, -81.23899999999999011 ) ) ;
#49951=VERTEX_POINT ( 'NONE', #6478 ) ;
#49958=CARTESIAN_POINT ( 'NONE',  ( 15.24805423083535594, -22.38317868667326493, -72.99443523961514302 ) ) ;
#49961=ORIENTED_EDGE ( 'NONE', *, *, #16301, .T. ) ;
#49966=CARTESIAN_POINT ( 'NONE',  ( 10.53189742092200021, -10.12038184378820027, -69.25944751885370465 ) ) ;
#49970=CARTESIAN_POINT ( 'NONE',  ( 29.99034385824719706, -15.61618894467929941, -24.14999999999999858 ) ) ;
#49973=CARTESIAN_POINT ( 'NONE',  ( 15.17121401173929485, -22.60301372889673388, -33.39076563757389948 ) ) ;
#49988=CARTESIAN_POINT ( 'NONE',  ( 17.65356943138449708, -22.50337107214560106, -77.27805344681910071 ) ) ;
#49997=CARTESIAN_POINT ( 'NONE',  ( 11.09655785439759867, -20.55252016947139992, -79.20604505178991417 ) ) ;
#49998=CARTESIAN_POINT ( 'NONE',  ( 9.366633833501754935, -15.85814187007113851, -79.83580626949178338 ) ) ;
#50001=ORIENTED_EDGE ( 'NONE', *, *, #12422, .F. ) ;
#50004=EDGE_CURVE ( 'NONE', #37063, #3350, #11150, .T. ) ;
#50007=LINE ( 'NONE', #30324, #49149 ) ;
#50010=ORIENTED_EDGE ( 'NONE', *, *, #16319, .T. ) ;
#50011=ORIENTED_EDGE ( 'NONE', *, *, #24110, .T. ) ;
#50019=CARTESIAN_POINT ( 'NONE',  ( 24.04315726994194335, -15.44410872182987582, -33.78540739674929938 ) ) ;
#50022=CARTESIAN_POINT ( 'NONE',  ( 15.09849901009799211, -7.705175762525661831, -56.96600136960869776 ) ) ;
#50024=CARTESIAN_POINT ( 'NONE',  ( 23.08008446722849882, -19.26828265651219851, -42.16657309509579932 ) ) ;
#50030=FACE_OUTER_BOUND ( 'NONE', #14683, .T. ) ;
#50031=CARTESIAN_POINT ( 'NONE',  ( 22.90118952179220813, -15.61618876469732875, -46.84717865327674247 ) ) ;
#50033=CARTESIAN_POINT ( 'NONE',  ( 10.40182605014470063, -11.50699697134410115, -40.04515584691789343 ) ) ;
#50047=CARTESIAN_POINT ( 'NONE',  ( 8.486156673604268619, -13.29521644607133801, -70.60117058448025773 ) ) ;
#50051=B_SPLINE_CURVE_WITH_KNOTS ( 'NONE', 3,
 ( #39719, #27652, #22682, #35265, #34735, #19796, #30800, #26879, #23188, #11437 ),
 .UNSPECIFIED., .F., .F.,
 ( 4, 1, 1, 1, 1, 1, 1, 4 ),
 ( 0.5000014761122578699, 0.5444555141086205863, 0.6236744451722389115, 0.7028933762358566817, 0.7821123072994755621, 0.8613312383630933322, 0.9405501694267122126, 1.000000000000000000 ),
 .UNSPECIFIED. ) ;
#50056=CARTESIAN_POINT ( 'NONE',  ( 11.16602909665550136, -20.62242963097040160, -47.20159690208769376 ) ) ;
#50062=ORIENTED_EDGE ( 'NONE', *, *, #35261, .T. ) ;
#50063=CARTESIAN_POINT ( 'NONE',  ( 22.61907617509890045, -11.94880985653349903, -72.90351834778009277 ) ) ;
#50064=ADVANCED_FACE ( 'NONE', ( #39485 ), #43412, .T. ) ;
#50066=CARTESIAN_POINT ( 'NONE',  ( 24.04460491192063998, -15.61619351124008404, -49.79233069347445451 ) ) ;
#50070=CARTESIAN_POINT ( 'NONE',  ( 8.222342146248220018, -15.61610160653870061, -76.79233150823698395 ) ) ;
#50073=FACE_OUTER_BOUND ( 'NONE', #35654, .T. ) ;
#50077=CARTESIAN_POINT ( 'NONE',  ( 24.04518460902906085, -15.61618869790763675, -47.79232989768991757 ) ) ;
#50081=CARTESIAN_POINT ( 'NONE',  ( 8.222431652840050731, -15.61631456792169992, -70.50766849176299900 ) ) ;
#50087=CARTESIAN_POINT ( 'NONE',  ( 24.04424255568759961, -15.50293698162811040, -43.78776901094543206 ) ) ;
#50088=CARTESIAN_POINT ( 'NONE',  ( 22.87440586111459950, -20.36474714160580035, -53.98768771411489098 ) ) ;
#50089=CARTESIAN_POINT ( 'NONE',  ( 20.99566323537737134, -21.94231603232962513, -47.79933614068776393 ) ) ;
#50093=CARTESIAN_POINT ( 'NONE',  ( 23.57447716569279805, -15.99705869407809899, -48.24893689645459460 ) ) ;
#50095=CARTESIAN_POINT ( 'NONE',  ( 9.970633004574349201, -12.25822725531089930, -32.14999999999999858 ) ) ;
#50096=EDGE_CURVE ( 'NONE', #19315, #21614, #36818, .T. ) ;
#50098=B_SPLINE_CURVE_WITH_KNOTS ( 'NONE', 3,
 ( #27501, #7606, #23554, #8115, #20400, #24061, #36142, #16745, #32698, #4432, #9148, #16481, #40082, #40588, #48725, #12827, #243, #1 ),
 .UNSPECIFIED., .F., .F.,
 ( 4, 2, 2, 2, 2, 2, 2, 2, 4 ),
 ( 0.000000000000000000, 0.06250000040564351877, 0.1250000008112870375, 0.1875000012169305563, 0.2500000016225740751, 0.3125000020282175939, 0.3750000024338611126, 0.4375000028395046314, 0.5000000032451481502 ),
 .UNSPECIFIED. ) ;
#50100=CARTESIAN_POINT ( 'NONE',  ( 9.807862442681825499, -10.75439508610775974, -51.00066430329498957 ) ) ;
#50103=CARTESIAN_POINT ( 'NONE',  ( 24.04360322966152452, -15.45924965371268556, -61.50136194718664484 ) ) ;
#50106=CARTESIAN_POINT ( 'NONE',  ( 14.89443207003930070, -23.76765183496380018, -66.05570249522899928 ) ) ;
#50136=CARTESIAN_POINT ( 'NONE',  ( 9.903862192720572111, -10.68226006460541555, -80.72097351600584147 ) ) ;
#50147=CARTESIAN_POINT ( 'NONE',  ( 9.367442997458502063, -15.61610373232760018, -47.45282021618999835 ) ) ;
#50151=VECTOR ( 'NONE', #46444, 1000.000000000000000 ) ;
#50152=AXIS2_PLACEMENT_3D ( 'NONE', #20467, #36455, #16549 ) ;
#50158=CARTESIAN_POINT ( 'NONE',  ( 22.68269334052732944, -17.37751627684776068, -46.53645479080106639 ) ) ;
#50170=CARTESIAN_POINT ( 'NONE',  ( 8.138816769778330240, -13.60105449406839995, -36.58626013956259726 ) ) ;
#50174=CARTESIAN_POINT ( 'NONE',  ( 8.222937397696199469, -15.61618894467929941, -32.14999999999999858 ) ) ;
#50181=CARTESIAN_POINT ( 'NONE',  ( 23.17687047303220638, -11.91936411872809920, -65.35394111064542244 ) ) ;
#50193=CARTESIAN_POINT ( 'NONE',  ( 16.05054682600030347, -8.166374158331009880, -50.56377978783940108 ) ) ;
#50201=CARTESIAN_POINT ( 'NONE',  ( 9.402037793986869119, -17.49569968449790025, -81.23899999999999011 ) ) ;
#50204=ORIENTED_EDGE ( 'NONE', *, *, #7176, .F. ) ;
#50205=B_SPLINE_CURVE_WITH_KNOTS ( 'NONE', 3,
 ( #41630, #30079, #33755, #37966, #41898, #46103, #7551, #30598, #6779, #19073, #3106, #39010, #35046, #47393, #47638, #42683, #51055, #27446 ),
 .UNSPECIFIED., .F., .F.,
 ( 4, 2, 2, 2, 2, 2, 2, 2, 4 ),
 ( 0.000000000000000000, 0.06249987509224218946, 0.1249997501844843789, 0.1874996252767265614, 0.2499995003689687578, 0.3124993754612109265, 0.3749992505534531229, 0.4374991256456953193, 0.4999990007379375156 ),
 .UNSPECIFIED. ) ;
#50209=EDGE_CURVE ( 'NONE', #44209, #7516, #25444, .T. ) ;
#50210=ORIENTED_EDGE ( 'NONE', *, *, #38640, .T. ) ;
#50214=CARTESIAN_POINT ( 'NONE',  ( 12.72597450771867145, -21.52911656548743480, -53.11948602161462674 ) ) ;
#50218=ORIENTED_EDGE ( 'NONE', *, *, #11186, .F. ) ;
#50219=CARTESIAN_POINT ( 'NONE',  ( 22.02211878048609961, -20.97478655844351891, -49.74279633225222597 ) ) ;
#50224=CARTESIAN_POINT ( 'NONE',  ( 18.18784219828660298, -23.19037026424729930, -72.42820476139849006 ) ) ;
#50233=DIRECTION ( 'NONE',  ( -0.7071067811865470176, 0.000000000000000000, 0.7071067811865480168 ) ) ;
#50241=CARTESIAN_POINT ( 'NONE',  ( 22.08340413664989654, -11.95206882129740045, -32.14999999999999858 ) ) ;
#50244=CARTESIAN_POINT ( 'NONE',  ( 19.43172305940224831, -9.381835016295289265, -50.50205474733376576 ) ) ;
#50246=CARTESIAN_POINT ( 'NONE',  ( 17.16943926069780701, -23.52719545942989754, -46.25071487151191008 ) ) ;
#50251=CARTESIAN_POINT ( 'NONE',  ( 10.74314122376619984, -11.06845590621349906, -78.07024275745519049 ) ) ;
#50260=CARTESIAN_POINT ( 'NONE',  ( 17.13677513945059872, -8.635009040899712218, -79.99823436242620289 ) ) ;
#50263=CARTESIAN_POINT ( 'NONE',  ( 24.04523903120960782, -15.61618918343368101, -41.50766953063602926 ) ) ;
#50264=DIRECTION ( 'NONE',  ( 0.000000000000000000, 0.000000000000000000, -1.000000000000000000 ) ) ;
#50270=CYLINDRICAL_SURFACE ( 'NONE', #48720, 7.910999999999997812 ) ;
#50271=CARTESIAN_POINT ( 'NONE',  ( 10.50324867407785767, -10.02729031740725674, -38.75656930020886648 ) ) ;
#50272=CARTESIAN_POINT ( 'NONE',  ( 9.543085836910789155, -17.38751520322140820, -55.36948714503900959 ) ) ;
#50279=EDGE_CURVE ( 'NONE', #35817, #16605, #39916, .T. ) ;
#50280=CARTESIAN_POINT ( 'NONE',  ( 9.404870085045700989, -14.72357982206546900, -45.49475439789830489 ) ) ;
#50286=CARTESIAN_POINT ( 'NONE',  ( 16.15665784884619782, -7.677406726810557913, -33.29332427056172605 ) ) ;
#50290=CARTESIAN_POINT ( 'NONE',  ( 20.11810762141488595, -22.52868886509989821, -53.84100386235245139 ) ) ;
#50291=CARTESIAN_POINT ( 'NONE',  ( 13.03098752936530147, -22.82440992535179802, -42.64188668147749439 ) ) ;
#50296=CARTESIAN_POINT ( 'NONE',  ( 22.72481174712088858, -13.84494720633589360, -78.36948400686931393 ) ) ;
#50299=CARTESIAN_POINT ( 'NONE',  ( 17.74966129736979781, -22.48146355349690140, -45.27360529711679504 ) ) ;
#50303=VERTEX_POINT ( 'NONE', #4037 ) ;
#50310=CARTESIAN_POINT ( 'NONE',  ( 22.90120720387987774, -15.61618909956830770, -56.84718059981966576 ) ) ;
#50314=CARTESIAN_POINT ( 'NONE',  ( 17.96991432777422304, -7.851816221580103949, -71.08187692902760091 ) ) ;
#50316=ORIENTED_EDGE ( 'NONE', *, *, #24867, .T. ) ;
#50320=CARTESIAN_POINT ( 'NONE',  ( 22.90121965235462653, -15.61618904849089340, -42.45282069170939110 ) ) ;
#50323=CARTESIAN_POINT ( 'NONE',  ( 19.88990749180780071, -9.646662384828470493, -42.13158531401599305 ) ) ;
#50329=CARTESIAN_POINT ( 'NONE',  ( 13.60282763607719936, -8.187849186844388782, -36.68297296116619322 ) ) ;
#50335=CARTESIAN_POINT ( 'NONE',  ( 22.46789922215001312, -18.61594777151466218, -66.98826990121492031 ) ) ;
#50336=CARTESIAN_POINT ( 'NONE',  ( 19.30814099325047906, -9.610988906536928056, -62.10768522194346986 ) ) ;
#50339=CARTESIAN_POINT ( 'NONE',  ( 22.72481324571542061, -13.84495462270172261, -58.36948662338765104 ) ) ;
#50355=CARTESIAN_POINT ( 'NONE',  ( 8.349645199064468670, -12.89819059621470210, -58.89926144005930553 ) ) ;
#50360=CARTESIAN_POINT ( 'NONE',  ( 10.24628260800490054, -20.18151641185739820, -59.02271152110689911 ) ) ;
#50362=CARTESIAN_POINT ( 'NONE',  ( 9.088130602754668885, -18.12643738272649685, -32.14999999999999858 ) ) ;
#50371=CARTESIAN_POINT ( 'NONE',  ( 8.222939282903173108, -14.98363466968944024, -60.53312594118477108 ) ) ;
#50373=CARTESIAN_POINT ( 'NONE',  ( 8.620230944888110258, -19.01132311728650137, -66.37257821948348635 ) ) ;
#50382=CARTESIAN_POINT ( 'NONE',  ( 16.13393739769620083, -15.61618894467929941, -28.45282021618999835 ) ) ;
#50384=CARTESIAN_POINT ( 'NONE',  ( 9.019466863379530963, -12.08793898035315451, -64.93882274181090963 ) ) ;
#50402=ORIENTED_EDGE ( 'NONE', *, *, #36828, .T. ) ;
#50416=CARTESIAN_POINT ( 'NONE',  ( 16.13393739769620083, -15.61618894467929941, -32.14999999999999858 ) ) ;
#50420=CARTESIAN_POINT ( 'NONE',  ( 10.16807496446329928, -9.924861728319630316, -37.03483646650040129 ) ) ;
#50422=CARTESIAN_POINT ( 'NONE',  ( 9.366922816393266515, -16.24874389531281693, -51.42305503118727472 ) ) ;
#50427=EDGE_CURVE ( 'NONE', #23870, #8412, #6386, .T. ) ;
#50432=CARTESIAN_POINT ( 'NONE',  ( 7.903303049004190228, -15.12692539678219994, -34.52656793190860185 ) ) ;
#50433=VERTEX_POINT ( 'NONE', #18244 ) ;
#50453=CARTESIAN_POINT ( 'NONE',  ( 20.33583072231489908, -21.76848825687689981, -57.37660785931080198 ) ) ;
#50455=EDGE_LOOP ( 'NONE', ( #22125, #39823, #20834, #33940 ) ) ;
#50460=CARTESIAN_POINT ( 'NONE',  ( 9.151707502888131174, -16.64276093509979759, -81.23899999999999011 ) ) ;
#50463=ORIENTED_EDGE ( 'NONE', *, *, #20544, .T. ) ;
#50465=ORIENTED_EDGE ( 'NONE', *, *, #10177, .F. ) ;
#50474=CARTESIAN_POINT ( 'NONE',  ( 22.55531542943956680, -17.79663745630361049, -72.55697149734855600 ) ) ;
#50478=CARTESIAN_POINT ( 'NONE',  ( 15.70135240704478186, -23.59237159327061306, -50.02457256032881361 ) ) ;
#50485=CARTESIAN_POINT ( 'NONE',  ( 23.04647744410513255, -19.60028888980541240, -79.67433673434211983 ) ) ;
#50490=CARTESIAN_POINT ( 'NONE',  ( 11.09952124908870097, -9.596105703907399587, -48.56581262070909588 ) ) ;
#50501=CARTESIAN_POINT ( 'NONE',  ( 22.57793705737757506, -13.54241025272627219, -80.74806968844832511 ) ) ;
#50507=CARTESIAN_POINT ( 'NONE',  ( 9.532113884515599267, -18.09781854541880364, -71.73272827236579019 ) ) ;
#50515=CARTESIAN_POINT ( 'NONE',  ( 9.830109632710200884, -18.77914866715480358, -77.30479070626310545 ) ) ;
#50518=CARTESIAN_POINT ( 'NONE',  ( 19.54188305415121008, -21.52912787978993947, -40.78610065424740583 ) ) ;
#50522=VERTEX_POINT ( 'NONE', #14579 ) ;
#50543=CARTESIAN_POINT ( 'NONE',  ( 10.60612691485259873, -21.18665201854900104, -46.76127109678569838 ) ) ;
#50551=CARTESIAN_POINT ( 'NONE',  ( 20.16990914961739989, -9.832289637797728687, -46.54110819413470068 ) ) ;
#50557=CARTESIAN_POINT ( 'NONE',  ( 22.46012548327199454, -10.75454236778581318, -57.58399795081778194 ) ) ;
#50560=CARTESIAN_POINT ( 'NONE',  ( 4.133937397696199945, -15.61618894467930652, -22.14999999999999858 ) ) ;
#50567=CARTESIAN_POINT ( 'NONE',  ( 10.14686910709649936, -10.32892520170320338, -70.73769537184530520 ) ) ;
#50574=CARTESIAN_POINT ( 'NONE',  ( 22.04686314924591883, -12.20822412868739981, -42.28615306984772815 ) ) ;
#50576=FACE_OUTER_BOUND ( 'NONE', #1726, .T. ) ;
#50577=CARTESIAN_POINT ( 'NONE',  ( 22.82000994230530111, -13.37141888410519996, -44.34971538379739542 ) ) ;
#50582=ORIENTED_EDGE ( 'NONE', *, *, #33421, .T. ) ;
#50584=CARTESIAN_POINT ( 'NONE',  ( 8.300043692618718438, -15.15050933049450066, -34.30640502925760416 ) ) ;
#50590=CARTESIAN_POINT ( 'NONE',  ( 24.01934093808031179, -16.26519669879829166, -75.81845923383386321 ) ) ;
#50591=CARTESIAN_POINT ( 'NONE',  ( 13.18974571921978978, -9.507163701089766050, -61.80991948917802148 ) ) ;
#50594=ADVANCED_FACE ( 'NONE', ( #5865 ), #29948, .T. ) ;
#50606=CARTESIAN_POINT ( 'NONE',  ( 15.09835210727568011, -7.705193513269825267, -69.25066627866567615 ) ) ;
#50607=CARTESIAN_POINT ( 'NONE',  ( 24.36192440164969852, -15.08425857451129914, -67.77178171918468763 ) ) ;
#50608=CIRCLE ( 'NONE', #33827, 2.999999999999960920 ) ;
#50609=CARTESIAN_POINT ( 'NONE',  ( 22.90088705258820667, -15.61618575905976414, -62.45282818884277276 ) ) ;
#50613=CARTESIAN_POINT ( 'NONE',  ( 23.58405125408460279, -15.56621563185109913, -58.23052221047069565 ) ) ;
#50614=CARTESIAN_POINT ( 'NONE',  ( 10.18216224808260151, -11.95184640257830111, -32.14999999999999858 ) ) ;
#50617=CARTESIAN_POINT ( 'NONE',  ( 26.52624224310950041, -21.61618894467929763, -22.14999999999999858 ) ) ;
#50620=CARTESIAN_POINT ( 'NONE',  ( 8.674532686402148585, -12.88142895660771359, -60.61962948924526273 ) ) ;
#50621=CARTESIAN_POINT ( 'NONE',  ( 13.90615343176800067, -23.55468372077690020, -62.09475594204819515 ) ) ;
#50638=CARTESIAN_POINT ( 'NONE',  ( 9.367334447929739127, -15.61631861598680082, -57.84717978380999170 ) ) ;
#50645=CARTESIAN_POINT ( 'NONE',  ( 23.83903461665352097, -13.54549833210122856, -37.70900104367377281 ) ) ;
#50647=CARTESIAN_POINT ( 'NONE',  ( 8.222281512103441159, -15.61614627842319969, -76.50766849176299900 ) ) ;
#50656=CARTESIAN_POINT ( 'NONE',  ( 22.84151302485214075, -17.15290527753463934, -36.91946906410927198 ) ) ;
#50663=CARTESIAN_POINT ( 'NONE',  ( 21.61927372987474172, -21.31691565204681638, -77.76379145751687361 ) ) ;
#50665=VERTEX_POINT ( 'NONE', #9294 ) ;
#50670=CARTESIAN_POINT ( 'NONE',  ( 7.912936474371079498, -14.98542442814910025, -34.81670639671899892 ) ) ;
#50673=CARTESIAN_POINT ( 'NONE',  ( 16.16386221864532047, -22.38313233367915345, -46.95141631609453015 ) ) ;
#50681=CARTESIAN_POINT ( 'NONE',  ( 19.93821446653229756, -8.301122528535961109, -35.16031938041749783 ) ) ;
#50683=ORIENTED_EDGE ( 'NONE', *, *, #913, .F. ) ;
#50703=VERTEX_POINT ( 'NONE', #33101 ) ;
#50704=CARTESIAN_POINT ( 'NONE',  ( 15.97580875125819944, -23.06479214726149962, -53.57409916825699270 ) ) ;
#50712=CARTESIAN_POINT ( 'NONE',  ( 9.544598273871880423, -17.84714125077449864, -81.23899999999999011 ) ) ;
#50742=CARTESIAN_POINT ( 'NONE',  ( 8.343752523778771746, -16.56474986173779840, -48.24893689645469408 ) ) ;
#50755=CARTESIAN_POINT ( 'NONE',  ( 22.10482594698319758, -11.98148934663060139, -32.14999999999999858 ) ) ;
#50759=CARTESIAN_POINT ( 'NONE',  ( 24.04493739769670313, -15.61618198714410610, -45.50767582953553614 ) ) ;
#50761=CARTESIAN_POINT ( 'NONE',  ( 22.46009103554561293, -10.75449509031862938, -71.58399138287670382 ) ) ;
#50763=CARTESIAN_POINT ( 'NONE',  ( 9.778345137114559549, -12.55857448374969998, -69.98991178896608290 ) ) ;
#50773=CARTESIAN_POINT ( 'NONE',  ( 14.34415610061919821, -8.794221333858748935, -58.26550999155039534 ) ) ;
#50776=DIRECTION ( 'NONE',  ( 1.000000000000000000, 2.460964292799963328E-14, 0.000000000000000000 ) ) ;
#50800=CARTESIAN_POINT ( 'NONE',  ( 9.366908763506170743, -15.61636271700460021, -33.45282021618999835 ) ) ;
#50802=ADVANCED_FACE ( 'NONE', ( #10580 ), #25901, .T. ) ;
#50803=CARTESIAN_POINT ( 'NONE',  ( 19.20059249649200339, -22.83992579596429806, -44.38470316487709511 ) ) ;
#50809=CARTESIAN_POINT ( 'NONE',  ( 9.081105072284950452, -15.60544817723029887, -43.84766453797169561 ) ) ;
#50817=CARTESIAN_POINT ( 'NONE',  ( 14.06332624887442861, -7.911071329197555180, -46.92433573622849252 ) ) ;
#50834=CARTESIAN_POINT ( 'NONE',  ( 23.16873431782460102, -15.11201537419210084, -52.43004635228659538 ) ) ;
#50839=CARTESIAN_POINT ( 'NONE',  ( 23.94572442901580089, -14.86603458648409948, -35.25703220202099430 ) ) ;
#50853=CARTESIAN_POINT ( 'NONE',  ( 12.14986582965795670, -8.703631913686264099, -47.12566550774506169 ) ) ;
#50858=VERTEX_POINT ( 'NONE', #23813 ) ;
#50866=CARTESIAN_POINT ( 'NONE',  ( 10.99908320461310041, -9.165143101429379158, -65.07833806302170387 ) ) ;
#50868=CARTESIAN_POINT ( 'NONE',  ( 22.46012711993053657, -20.47783328051634300, -47.71600292291422107 ) ) ;
#50871=ORIENTED_EDGE ( 'NONE', *, *, #6446, .T. ) ;
#50874=CARTESIAN_POINT ( 'NONE',  ( 20.22938470947429934, -21.83985387152069890, -58.54739793472509746 ) ) ;
#50875=CARTESIAN_POINT ( 'NONE',  ( 16.13393739769620083, -15.61618894467929941, -28.45282021618999835 ) ) ;
#50876=CARTESIAN_POINT ( 'NONE',  ( 9.366937397696199596, -15.61618894467949836, -28.45282021618999835 ) ) ;
#50881=CARTESIAN_POINT ( 'NONE',  ( 13.08127967867459951, -7.956946060459409331, -62.88694525268430624 ) ) ;
#50883=CARTESIAN_POINT ( 'NONE',  ( 21.65241842836849884, -21.01139045118939919, -32.14999999999999858 ) ) ;
#50889=ORIENTED_EDGE ( 'NONE', *, *, #28034, .F. ) ;
#50899=CARTESIAN_POINT ( 'NONE',  ( 20.11809198619220140, -22.52869821230809677, -70.12566693189073419 ) ) ;
#50902=CARTESIAN_POINT ( 'NONE',  ( 16.13393739769620083, -15.61618894467929941, -28.45282021618999835 ) ) ;
#50926=CARTESIAN_POINT ( 'NONE',  ( 8.609312831402940347, -18.98705607306339971, -34.65826853459189749 ) ) ;
#50930=CARTESIAN_POINT ( 'NONE',  ( 10.99043526536265958, -20.04924589561327153, -51.22642174526011871 ) ) ;
#50939=CARTESIAN_POINT ( 'NONE',  ( 22.84203745199910074, -19.68904318595090075, -79.46119573552050497 ) ) ;
#50940=ADVANCED_FACE ( 'NONE', ( #16685 ), #25039, .T. ) ;
#50956=CARTESIAN_POINT ( 'NONE',  ( 16.13393739769620083, -15.61618894467929941, -22.64999999999999858 ) ) ;
#50960=CARTESIAN_POINT ( 'NONE',  ( 17.49210479782680139, -8.290748640399698388, -68.62569607034470209 ) ) ;
#50964=CARTESIAN_POINT ( 'NONE',  ( 22.90117443638819239, -15.61618876209028528, -62.84717844892357164 ) ) ;
#50967=CARTESIAN_POINT ( 'NONE',  ( 9.366957987891332493, -14.73023998519778743, -73.49448688334868507 ) ) ;
#50969=LINE ( 'NONE', #31034, #24249 ) ;
#50973=VERTEX_POINT ( 'NONE', #189 ) ;
#50976=CARTESIAN_POINT ( 'NONE',  ( 22.92703987217370099, -11.95345884179289975, -81.23899999999999011 ) ) ;
#50981=EDGE_LOOP ( 'NONE', ( #23923, #11299, #1176, #19189 ) ) ;
#50991=DIRECTION ( 'NONE',  ( 1.000000000000000000, 0.000000000000000000, 0.000000000000000000 ) ) ;
#51001=CARTESIAN_POINT ( 'NONE',  ( 20.24515493355339757, -8.931531993418198923, -56.96301931345279712 ) ) ;
#51012=CARTESIAN_POINT ( 'NONE',  ( 8.423931095146343750, -17.63235750399038082, -40.42643503837953745 ) ) ;
#51015=CARTESIAN_POINT ( 'NONE',  ( 9.366376358913971245, -15.61615244833809868, -75.84717978381000592 ) ) ;
#51017=CARTESIAN_POINT ( 'NONE',  ( 20.11804220191760351, -8.703649910996523076, -71.45898685654994154 ) ) ;
#51019=CARTESIAN_POINT ( 'NONE',  ( 17.41854199065469899, -22.95488674316110078, -35.51218288575179827 ) ) ;
#51027=CARTESIAN_POINT ( 'NONE',  ( 9.366881967297588929, -15.61636073738300112, -79.84717978380999170 ) ) ;
#51028=CARTESIAN_POINT ( 'NONE',  ( 8.428873746072833129, -17.68700077691279660, -42.42433505261755045 ) ) ;
#51031=DIRECTION ( 'NONE',  ( 0.000000000000000000, 0.000000000000000000, -1.000000000000000000 ) ) ;
#51032=EDGE_LOOP ( 'NONE', ( #34102, #11798, #32353 ) ) ;
#51036=CARTESIAN_POINT ( 'NONE',  ( 18.20457692116078263, -7.911077539172547191, -39.37565924810114382 ) ) ;
#51049=CARTESIAN_POINT ( 'NONE',  ( 9.366956826296663152, -14.73024848268338438, -35.49448676863867291 ) ) ;
#51055=CARTESIAN_POINT ( 'NONE',  ( 24.04493742333003325, -16.65172792896177967, -47.83400009015595344 ) ) ;
#51056=CARTESIAN_POINT ( 'NONE',  ( 11.97538872468891391, -10.20477610388419265, -51.74448612926989455 ) ) ;
#51058=CARTESIAN_POINT ( 'NONE',  ( 23.63916941805720029, -17.90927418342020161, -40.10688088744169733 ) ) ;
#51065=CARTESIAN_POINT ( 'NONE',  ( 23.10043867740759893, -16.71637942556440137, -42.89703736520819888 ) ) ;
#51066=CARTESIAN_POINT ( 'NONE',  ( 9.366918674202366901, -14.73052779765556686, -43.49448186140821093 ) ) ;
#51083=ORIENTED_EDGE ( 'NONE', *, *, #20791, .F. ) ;
#51090=CARTESIAN_POINT ( 'NONE',  ( 22.55585100403209964, -18.53193658968969970, -52.58848421441379628 ) ) ;
#51095=CARTESIAN_POINT ( 'NONE',  ( 17.45659250951840136, -7.880729576396868552, -36.84141082329339412 ) ) ;
#51101=CARTESIAN_POINT ( 'NONE',  ( 20.11801055182510112, -22.52874690906305233, -40.12567795478347676 ) ) ;
#51105=ORIENTED_EDGE ( 'NONE', *, *, #2428, .F. ) ;
#51108=EDGE_CURVE ( 'NONE', #14302, #48357, #30384, .T. ) ;
#51111=CARTESIAN_POINT ( 'NONE',  ( 22.83754687068412892, -19.96581757452138106, -43.97580730608837740 ) ) ;
#51115=CARTESIAN_POINT ( 'NONE',  ( 23.94726892773138260, -14.25686971664534575, -49.45287839032192778 ) ) ;
#51116=VECTOR ( 'NONE', #48767, 1000.000000000000000 ) ;
#51118=ADVANCED_FACE ( 'NONE', ( #46031 ), #10904, .T. ) ;
#51119=CARTESIAN_POINT ( 'NONE',  ( 12.14980481010722890, -22.52871145908785877, -36.17433415090009419 ) ) ;
#51127=CARTESIAN_POINT ( 'NONE',  ( 20.21053605544689802, -22.78306158478949683, -64.12771089025820004 ) ) ;
#51134=CARTESIAN_POINT ( 'NONE',  ( 13.90228228614060058, -8.507995836145079593, -53.63582420878069001 ) ) ;
#51143=CARTESIAN_POINT ( 'NONE',  ( 12.46522631496400102, -23.00017700672360021, -64.15444814970220477 ) ) ;
#51144=CARTESIAN_POINT ( 'NONE',  ( 22.40560713194629727, -19.95407936107560332, -32.14999999999999858 ) ) ;
#51154=VECTOR ( 'NONE', #4557, 1000.000000000000000 ) ;
#51161=CARTESIAN_POINT ( 'NONE',  ( 21.90359465038130082, -10.90261821839509970, -72.01461621554048520 ) ) ;
#51164=CARTESIAN_POINT ( 'NONE',  ( 15.09843646001806761, -23.52719456774363138, -70.33399961199894790 ) ) ;
#51178=VERTEX_POINT ( 'NONE', #6194 ) ;
#51179=DIRECTION ( 'NONE',  ( 1.000000000000000000, 0.000000000000000000, 0.000000000000000000 ) ) ;
#51183=CARTESIAN_POINT ( 'NONE',  ( 20.70919841900760261, -22.07818802934547264, -77.81157068189432380 ) ) ;
#51186=CARTESIAN_POINT ( 'NONE',  ( 10.83684432477319959, -19.82762902495380075, -81.23899999999999011 ) ) ;
#51187=B_SPLINE_CURVE_WITH_KNOTS ( 'NONE', 3,
 ( #34376, #25993, #26255, #18397, #45938, #2687, #41736, #21545, #13965, #50638 ),
 .UNSPECIFIED., .F., .F.,
 ( 4, 1, 1, 1, 1, 1, 1, 4 ),
 ( 0.5000013100879009409, 0.5754136553612179128, 0.6546325864248377924, 0.7338515174884554515, 0.8130704485520910962, 0.8922893796157064239, 0.9715083106793263035, 1.000000000000000000 ),
 .UNSPECIFIED. ) ;
#51194=CARTESIAN_POINT ( 'NONE',  ( 24.04526736911255469, -15.61618908158827068, -41.79233198438217300 ) ) ;
#51197=CARTESIAN_POINT ( 'NONE',  ( 22.90093737620393100, -14.73039356599736749, -64.41115567542702536 ) ) ;
#51199=CARTESIAN_POINT ( 'NONE',  ( 8.290267814922380296, -15.86836957012680038, -71.00226400225328405 ) ) ;
#51207=CARTESIAN_POINT ( 'NONE',  ( 17.55559842845789831, -23.73786368710720041, -35.95250869105369418 ) ) ;
#51212=B_SPLINE_CURVE_WITH_KNOTS ( 'NONE', 3,
 ( #19319, #35300, #27938, #15394, #27429, #11726, #8039, #7533, #19830, #23992 ),
 .UNSPECIFIED., .F., .F.,
 ( 4, 1, 1, 1, 1, 1, 1, 4 ),
 ( 0.4999964962326966522, 0.5260408281246501394, 0.6052597591882703520, 0.6844786902518882332, 0.7636976213155060034, 0.8429165523791239956, 0.9221354834427439862, 1.000000000000000000 ),
 .UNSPECIFIED. ) ;
#51231=CARTESIAN_POINT ( 'NONE',  ( 17.01461248871479981, -8.218141518337640505, -62.60505730950960412 ) ) ;
#51237=CARTESIAN_POINT ( 'NONE',  ( 22.87787853217752598, -16.19320691800228929, -34.47998061787313873 ) ) ;
#51240=CARTESIAN_POINT ( 'NONE',  ( 9.157169031609750931, -13.44670018174929993, -81.23899999999999011 ) ) ;
#51242=ORIENTED_EDGE ( 'NONE', *, *, #44975, .F. ) ;
#51244=ORIENTED_EDGE ( 'NONE', *, *, #24047, .T. ) ;
#51253=CARTESIAN_POINT ( 'NONE',  ( 23.83903661103793326, -13.54550828489940706, -63.70900020837209610 ) ) ;
#51264=CARTESIAN_POINT ( 'NONE',  ( 22.90079931266048874, -15.61618915558698184, -42.84717230777439312 ) ) ;
#51265=CARTESIAN_POINT ( 'NONE',  ( 14.58466807763749884, -7.922911830399110400, -48.72425048283629678 ) ) ;
#51273=CARTESIAN_POINT ( 'NONE',  ( 8.327683877742938279, -17.09775678691067213, -32.44805707646908388 ) ) ;
#51276=CARTESIAN_POINT ( 'NONE',  ( 24.01793456853353703, -14.94176252685236683, -45.48051509102815970 ) ) ;
#51278=CARTESIAN_POINT ( 'NONE',  ( 9.205734167420699166, -27.61618894467930119, -24.14999999999999858 ) ) ;
#51282=CARTESIAN_POINT ( 'NONE',  ( 23.41350660572370046, -17.20193020699759856, -33.13561495384320210 ) ) ;
#51285=CARTESIAN_POINT ( 'NONE',  ( 23.83903775132751335, -17.68686396165632146, -57.59100091412105371 ) ) ;
#51309=CARTESIAN_POINT ( 'NONE',  ( 22.90059226164785500, -15.54233919852935664, -46.44935462124129799 ) ) ;
#51317=CARTESIAN_POINT ( 'NONE',  ( 22.90066504558609850, -15.61618132107965984, -48.84717678326153845 ) ) ;
#51319=CARTESIAN_POINT ( 'NONE',  ( 8.949779341734769744, -18.77445122298149727, -50.88065551209399473 ) ) ;
#51323=CARTESIAN_POINT ( 'NONE',  ( 22.66931125956381976, -13.27800589393286401, -64.73722150501926365 ) ) ;
#51327=CARTESIAN_POINT ( 'NONE',  ( 23.15902141439090300, -14.99108596689769968, -50.81893047157019794 ) ) ;
#51328=CARTESIAN_POINT ( 'NONE',  ( 22.90065123677362635, -15.61618748955864433, -66.45281999012681240 ) ) ;
#51332=CARTESIAN_POINT ( 'NONE',  ( 17.16955733179256782, -7.705199290335150053, -51.04933357283481143 ) ) ;
#51334=FACE_OUTER_BOUND ( 'NONE', #44914, .T. ) ;
#51339=CARTESIAN_POINT ( 'NONE',  ( 8.222930619450961487, -15.61639179890759976, -64.50766849176299900 ) ) ;
#51342=EDGE_CURVE ( 'NONE', #3035, #39880, #30532, .T. ) ;
#51352=CARTESIAN_POINT ( 'NONE',  ( 19.93152537058130136, -9.673051365519301115, -58.13380938886719917 ) ) ;
#51357=ORIENTED_EDGE ( 'NONE', *, *, #30069, .T. ) ;
#51358=CARTESIAN_POINT ( 'NONE',  ( 14.56124311489510070, -23.30471161656020129, -39.85173020371090047 ) ) ;
#51363=CARTESIAN_POINT ( 'NONE',  ( 24.04465145034966156, -15.61618865458276595, -39.79233592887338489 ) ) ;
#51372=CARTESIAN_POINT ( 'NONE',  ( 9.031253978508082980, -19.22508473272204554, -44.64247938458763798 ) ) ;
#51373=CARTESIAN_POINT ( 'NONE',  ( 15.85768616877558657, -7.688762805127981714, -76.99657294770088356 ) ) ;
#51378=CARTESIAN_POINT ( 'NONE',  ( 8.222926353263792620, -16.65165556482179099, -62.75066471232383947 ) ) ;
#51379=CYLINDRICAL_SURFACE ( 'NONE', #15015, 7.910999999999997812 ) ;
#51382=CARTESIAN_POINT ( 'NONE',  ( 8.992839782551710570, -11.49460612895030032, -60.95895364771349989 ) ) ;
#51384=CARTESIAN_POINT ( 'NONE',  ( 22.90093739769620029, -15.61618894467913243, -28.45282021618999835 ) ) ;
#51389=CARTESIAN_POINT ( 'NONE',  ( 18.13401765809539867, -22.79298298917490229, -56.64614358919829584 ) ) ;
#51397=CARTESIAN_POINT ( 'NONE',  ( 21.72942902755440286, -9.560349272993629910, -75.24509849860889688 ) ) ;
#51409=ORIENTED_EDGE ( 'NONE', *, *, #38697, .T. ) ;
#51414=CARTESIAN_POINT ( 'NONE',  ( 15.09829039507263992, -23.52717692012846129, -72.33402119296106036 ) ) ;
#51416=CARTESIAN_POINT ( 'NONE',  ( 14.41409580431940185, -22.86524672475230346, -72.80680552617650392 ) ) ;
#51420=CARTESIAN_POINT ( 'NONE',  ( 11.27230730455335461, -21.94239041139972457, -70.50066575608552455 ) ) ;
#51423=CARTESIAN_POINT ( 'NONE',  ( 16.15735268940072444, -23.52715647658576614, -62.00672901155839156 ) ) ;
#51425=CARTESIAN_POINT ( 'NONE',  ( 8.222937397696199469, -15.61618894467929941, -32.14999999999999858 ) ) ;
#51431=CARTESIAN_POINT ( 'NONE',  ( 22.90065123677362635, -15.61618748955864433, -66.45281999012681240 ) ) ;
#51442=CARTESIAN_POINT ( 'NONE',  ( 22.88844470591842750, -16.50768533441256380, -80.49475390970813748 ) ) ;
#51445=AXIS2_PLACEMENT_3D ( 'NONE', #31639, #30872, #39789 ) ;
#51447=CARTESIAN_POINT ( 'NONE',  ( 16.12586798055579962, -7.371029459282210539, -35.29201998310079347 ) ) ;
#51448=CARTESIAN_POINT ( 'NONE',  ( 17.16949817664738376, -23.52718704373073066, -67.96600030527693548 ) ) ;
#51450=CARTESIAN_POINT ( 'NONE',  ( 10.12088335912352477, -20.79866362218473341, -50.56593387224838665 ) ) ;
#51452=CARTESIAN_POINT ( 'NONE',  ( 17.01976861749745140, -8.849193657844582006, -63.99448808445440307 ) ) ;
#51454=CARTESIAN_POINT ( 'NONE',  ( 8.743127158028750401, -12.97750146928379955, -75.12164841756138856 ) ) ;
#51461=CARTESIAN_POINT ( 'NONE',  ( 24.28204518499680020, -14.35481659857889980, -45.45878041868809305 ) ) ;
#51464=VECTOR ( 'NONE', #970, 1000.000000000000000 ) ;
#51470=CARTESIAN_POINT ( 'NONE',  ( 8.428868622292895907, -17.68698215233624893, -38.70899843570095555 ) ) ;
#51471=CARTESIAN_POINT ( 'NONE',  ( 10.22109734872648978, -19.02430242310299136, -49.28615388261155772 ) ) ;
#51478=DIRECTION ( 'NONE',  ( 0.000000000000000000, 0.000000000000000000, 1.000000000000000000 ) ) ;
#51483=CARTESIAN_POINT ( 'NONE',  ( 23.01915031812909973, -12.77004464428880048, -68.94257179459910390 ) ) ;
#51484=CARTESIAN_POINT ( 'NONE',  ( 24.04490680206547992, -15.61618865440000192, -77.79233401716611240 ) ) ;
#51488=CARTESIAN_POINT ( 'NONE',  ( 22.89185590794151892, -15.97420724114682855, -34.46966105702839656 ) ) ;
#51490=CARTESIAN_POINT ( 'NONE',  ( 13.55743739769619971, -15.61618894467929941, -22.64999999999999858 ) ) ;
#51491=CARTESIAN_POINT ( 'NONE',  ( 8.977138400209929259, -15.31030486894329989, -81.23899999999999011 ) ) ;
#51494=ORIENTED_EDGE ( 'NONE', *, *, #32990, .F. ) ;
#51498=CARTESIAN_POINT ( 'NONE',  ( 23.22105033138630148, -12.70121737134209994, -81.23899999999999011 ) ) ;
#51500=CARTESIAN_POINT ( 'NONE',  ( 8.223251455316621161, -15.61600507739779786, -72.79233150823699816 ) ) ;
#51502=CARTESIAN_POINT ( 'NONE',  ( 18.89412612953066883, -9.387266263190900517, -80.08542171964066370 ) ) ;
#51519=CARTESIAN_POINT ( 'NONE',  ( 20.17788239820569984, -22.34175635687860151, -47.61518544794569863 ) ) ;
#51526=EDGE_CURVE ( 'NONE', #50522, #22194, #24460, .T. ) ;
#51529=CARTESIAN_POINT ( 'NONE',  ( 22.90095859539430379, -15.61618916398383661, -38.45281773784812174 ) ) ;
#51534=CARTESIAN_POINT ( 'NONE',  ( 23.93801254160047165, -14.27752776017385727, -45.45360011000054357 ) ) ;
#51538=CARTESIAN_POINT ( 'NONE',  ( 19.59748479214910333, -22.21244043963609727, -37.41343723127859278 ) ) ;
#51544=CARTESIAN_POINT ( 'NONE',  ( 9.366428224829499882, -15.61611423639980067, -77.45282021618989177 ) ) ;
#51545=CARTESIAN_POINT ( 'NONE',  ( 9.367832377137357724, -14.89726563169283935, -57.88099794497199468 ) ) ;
#51553=CARTESIAN_POINT ( 'NONE',  ( 9.367167526866026606, -15.17380814805779821, -61.86798012936559132 ) ) ;
#51558=CARTESIAN_POINT ( 'NONE',  ( 22.41898323842375262, -18.19086658339881524, -32.97087606503488644 ) ) ;
#51560=CARTESIAN_POINT ( 'NONE',  ( 17.16857899493826523, -8.907709375196542823, -46.00150713458933183 ) ) ;
#51570=CARTESIAN_POINT ( 'NONE',  ( 11.60978911814099845, -9.203792361795480659, -55.31691565165669289 ) ) ;
#51580=CARTESIAN_POINT ( 'NONE',  ( 21.12773481075129922, -20.59660524975009821, -55.09675274900569519 ) ) ;
#51585=CARTESIAN_POINT ( 'NONE',  ( 8.222958075229072961, -14.58049008954063730, -50.54933503646082471 ) ) ;
#51587=CARTESIAN_POINT ( 'NONE',  ( 24.04523214473702097, -15.61618869705131729, -47.50766735973101618 ) ) ;
#51594=CYLINDRICAL_SURFACE ( 'NONE', #492, 6.766999999999998572 ) ;
#51595=CARTESIAN_POINT ( 'NONE',  ( 8.222960500461509170, -16.65190554600032158, -58.75066482977644000 ) ) ;
#51604=CARTESIAN_POINT ( 'NONE',  ( 9.083937397696097094, -15.61618894467929941, -20.75000000000000711 ) ) ;
#51607=CARTESIAN_POINT ( 'NONE',  ( 22.35343623859719742, -18.94190583952410023, -58.60912297524879477 ) ) ;
#51612=VERTEX_POINT ( 'NONE', #28662 ) ;
#51613=CARTESIAN_POINT ( 'NONE',  ( 8.664468393074560737, -13.20916153058959885, -42.38673599774679701 ) ) ;
#51614=ORIENTED_EDGE ( 'NONE', *, *, #29950, .F. ) ;
#51618=CARTESIAN_POINT ( 'NONE',  ( 23.83903199042086740, -17.68689264766797464, -39.87567244413330769 ) ) ;
#51626=ORIENTED_EDGE ( 'NONE', *, *, #41038, .F. ) ;
#51631=CARTESIAN_POINT ( 'NONE',  ( 24.04493740548085867, -16.65173988180983855, -61.83399520223390056 ) ) ;
#51633=AXIS2_PLACEMENT_3D ( 'NONE', #34161, #10862, #46519 ) ;
#51634=FACE_OUTER_BOUND ( 'NONE', #47195, .T. ) ;
#51636=CARTESIAN_POINT ( 'NONE',  ( 7.987404321646320859, -16.88769155842430081, -74.74304765278330365 ) ) ;
#51643=CARTESIAN_POINT ( 'NONE',  ( 8.983156071820218358, -17.70736570302589996, -63.14209593641499652 ) ) ;
#51647=CARTESIAN_POINT ( 'NONE',  ( 10.58587177825300074, -20.98084142191969903, -32.14999999999999858 ) ) ;
#51652=CARTESIAN_POINT ( 'NONE',  ( 23.85596303094300197, -18.50635171318529970, -77.62166643051759252 ) ) ;
#51660=EDGE_CURVE ( 'NONE', #1081, #47211, #14158, .T. ) ;
#51666=CARTESIAN_POINT ( 'NONE',  ( 11.34449012104014898, -21.94230794375442883, -66.49862320159839157 ) ) ;
#51668=CARTESIAN_POINT ( 'NONE',  ( 20.92368333918920342, -9.909611369538689374, -69.95492400788640452 ) ) ;
#51674=CARTESIAN_POINT ( 'NONE',  ( 22.89142746321374844, -16.00358779221829408, -40.47104892312902535 ) ) ;
#51677=CARTESIAN_POINT ( 'NONE',  ( 22.90090927591486292, -15.61618926791037687, -70.45281771081829447 ) ) ;
#51691=CARTESIAN_POINT ( 'NONE',  ( 16.85486949525910205, -23.50587475634130641, -77.97868939198153271 ) ) ;
#51695=CARTESIAN_POINT ( 'NONE',  ( 9.807844417311496699, -10.75441821519198804, -34.71600119539038332 ) ) ;
#51696=CARTESIAN_POINT ( 'NONE',  ( 8.964216265994560118, -11.54460215946079948, -44.95672957286240035 ) ) ;
#51699=CARTESIAN_POINT ( 'NONE',  ( 24.04492332548655753, -15.63231832970819823, -49.79297929963119174 ) ) ;
#51704=CARTESIAN_POINT ( 'NONE',  ( 12.08163306161019968, -8.895654951072430094, -77.33977848734279803 ) ) ;
#51705=CARTESIAN_POINT ( 'NONE',  ( 11.97531774029090812, -21.02754808119717822, -37.16115274999724249 ) ) ;
#51710=CARTESIAN_POINT ( 'NONE',  ( 24.04493740378650557, -14.58064945420081848, -57.75066457030849421 ) ) ;
#51711=CARTESIAN_POINT ( 'NONE',  ( 20.85221322589909931, -8.854488424989650497, -47.20159690208759429 ) ) ;
#51715=CARTESIAN_POINT ( 'NONE',  ( 23.06315139208389908, -19.45320742824282689, -39.66865486300337551 ) ) ;
#51722=CARTESIAN_POINT ( 'NONE',  ( 22.72481340201672850, -17.38742253237608182, -48.53615538150855002 ) ) ;
#51729=CARTESIAN_POINT ( 'NONE',  ( 16.13393739769620083, -15.61618894467929941, -32.14999999999999858 ) ) ;
#51730=CARTESIAN_POINT ( 'NONE',  ( 14.36265068495626451, -22.20705206307993862, -63.03615020535895042 ) ) ;
#51732=CARTESIAN_POINT ( 'NONE',  ( 23.57797937038209923, -15.92103882122889935, -63.08037089589128499 ) ) ;
#51737=CARTESIAN_POINT ( 'NONE',  ( 14.32416091673447944, -22.20785798411766976, -35.03836990857198685 ) ) ;
#51740=B_SPLINE_CURVE_WITH_KNOTS ( 'NONE', 3,
 ( #23001, #51066, #31892, #3632, #27965, #47909, #6793, #15427, #27199, #43212, #35329, #22746, #31124, #38764, #27458, #7303, #23255, #2859 ),
 .UNSPECIFIED., .F., .F.,
 ( 4, 2, 2, 2, 2, 2, 2, 2, 4 ),
 ( 0.000000000000000000, 0.06250000041077040380, 0.1250000008215408076, 0.1875000012323111975, 0.2500000016430816152, 0.3125000020538520329, 0.3750000024646223951, 0.4375000028753928127, 0.5000000032861632304 ),
 .UNSPECIFIED. ) ;
#51741=CARTESIAN_POINT ( 'NONE',  ( 10.03800373361939968, -11.28597919796850135, -81.23899999999999011 ) ) ;
#51747=CARTESIAN_POINT ( 'NONE',  ( 22.47177368144460274, -11.09078156707060003, -81.23899999999999011 ) ) ;
#51748=LINE ( 'NONE', #35766, #48611 ) ;
#51760=CARTESIAN_POINT ( 'NONE',  ( 29.99034385824719706, -15.61618894467929941, -24.15000000000000213 ) ) ;
#51769=CARTESIAN_POINT ( 'NONE',  ( 17.87834122126339764, -23.26758120253060369, -61.71615517726989708 ) ) ;
#51771=DIRECTION ( 'NONE',  ( 0.000000000000000000, 0.000000000000000000, -1.000000000000000000 ) ) ;
#51778=CARTESIAN_POINT ( 'NONE',  ( 16.13393739769620083, -15.61618894467929941, -40.14999999999999858 ) ) ;
#51779=CARTESIAN_POINT ( 'NONE',  ( 22.57344131301335466, -18.29224899765534929, -44.97302808468992907 ) ) ;
#51785=CARTESIAN_POINT ( 'NONE',  ( 23.83903376137553565, -13.54549413143066516, -71.70899800185173945 ) ) ;
#51787=CARTESIAN_POINT ( 'NONE',  ( 13.73101345958830066, -8.564050908167290643, -36.46281005851519552 ) ) ;
#51788=CARTESIAN_POINT ( 'NONE',  ( 21.54527357617396532, -19.77483941921981980, -76.66116015834198549 ) ) ;
#51789=ORIENTED_EDGE ( 'NONE', *, *, #41621, .T. ) ;
#51792=DIRECTION ( 'NONE',  ( 0.000000000000000000, 0.000000000000000000, 1.000000000000000000 ) ) ;
#51793=DIRECTION ( 'NONE',  ( 1.000000000000000000, 0.000000000000000000, 0.000000000000000000 ) ) ;
#51798=CARTESIAN_POINT ( 'NONE',  ( 8.428880937703265630, -13.54535095895175623, -66.59100159127797269 ) ) ;
#51801=ORIENTED_EDGE ( 'NONE', *, *, #18180, .F. ) ;
#51812=CARTESIAN_POINT ( 'NONE',  ( 21.07716222532573624, -10.95738292575066808, -46.21233756114791191 ) ) ;
#51820=CARTESIAN_POINT ( 'NONE',  ( 22.69443958732917821, -13.86771010790146086, -34.36998131010714985 ) ) ;
#51822=CARTESIAN_POINT ( 'NONE',  ( 12.14988939796288214, -22.52875931012240684, -54.17433617705772519 ) ) ;
#51826=CARTESIAN_POINT ( 'NONE',  ( 14.87499325793340077, -23.36227229334909694, -50.56377978783950056 ) ) ;
#51835=CARTESIAN_POINT ( 'NONE',  ( 21.17745084236759823, -10.68612491792770136, -48.60080040178890215 ) ) ;
#51837=ORIENTED_EDGE ( 'NONE', *, *, #46100, .F. ) ;
#51841=CARTESIAN_POINT ( 'NONE',  ( 12.14981042511106146, -8.703663254087580015, -36.84100281579361535 ) ) ;
#51842=CYLINDRICAL_SURFACE ( 'NONE', #51445, 7.910999999999997812 ) ;
#51846=CARTESIAN_POINT ( 'NONE',  ( 15.08314606030777760, -7.746415292052812873, -64.96536708472149257 ) ) ;
#51847=CARTESIAN_POINT ( 'NONE',  ( 26.52624224310950041, -9.616188944679349149, -22.14999999999999858 ) ) ;
#51848=CARTESIAN_POINT ( 'NONE',  ( 14.06334253594054573, -23.32131077769746597, -74.09100152957813634 ) ) ;
#51849=CARTESIAN_POINT ( 'NONE',  ( 9.367163129351689932, -15.61602587752549809, -57.45282021618999835 ) ) ;
#51858=CARTESIAN_POINT ( 'NONE',  ( 15.24822463963293373, -22.38319927160165790, -74.99448688826869613 ) ) ;
#51862=CARTESIAN_POINT ( 'NONE',  ( 9.105706864571400772, -15.02751733004349965, -51.47941917952310575 ) ) ;
#51867=EDGE_CURVE ( 'NONE', #14876, #630, #5444, .T. ) ;
#51869=CARTESIAN_POINT ( 'NONE',  ( 14.06638412633730084, -23.18665601437029977, -45.87236896454599844 ) ) ;
ENDSEC;
END-ISO-10303-21;
